ISO-10303-21;
HEADER;
/* Generated by software containing ST-Developer
 * from STEP Tools, Inc. (www.steptools.com) 
 */

FILE_DESCRIPTION(
/* description */ ('STEP AP214'),
/* implementation_level */ '2;1');

FILE_NAME(
/* name */ 'Adjustment Screw.step',
/* time_stamp */ '2026-10-06T11:11:25-07:00',
/* author */ (''),
/* organization */ (''),
/* preprocessor_version */ 'ST-DEVELOPER v20.2',
/* originating_system */ 'Autodesk Translation Framework v15.15.0.0',
/* authorisation */ '');

FILE_SCHEMA (('AUTOMOTIVE_DESIGN { 1 0 10303 214 3 1 1 }'));
ENDSEC;

DATA;
#10=MECHANICAL_DESIGN_GEOMETRIC_PRESENTATION_REPRESENTATION('',(#702),#47717);
#88=(
BOUNDED_CURVE()
B_SPLINE_CURVE(2,(#38802,#38803,#38804,#38805,#38806,#38807,#38808,#38809,
#38810,#38811,#38812,#38813,#38814,#38815,#38816,#38817,#38818,#38819,#38820,
#38821,#38822,#38823,#38824,#38825,#38826,#38827,#38828,#38829,#38830,#38831,
#38832,#38833,#38834,#38835,#38836,#38837,#38838,#38839,#38840,#38841,#38842,
#38843,#38844,#38845,#38846,#38847,#38848,#38849,#38850,#38851,#38852,#38853,
#38854,#38855,#38856,#38857,#38858,#38859,#38860,#38861,#38862,#38863,#38864,
#38865,#38866,#38867,#38868,#38869,#38870,#38871,#38872,#38873,#38874,#38875,
#38876,#38877,#38878,#38879,#38880,#38881,#38882,#38883,#38884,#38885,#38886,
#38887,#38888,#38889,#38890,#38891,#38892,#38893,#38894,#38895,#38896,#38897,
#38898,#38899,#38900,#38901,#38902,#38903,#38904,#38905,#38906,#38907,#38908,
#38909,#38910,#38911,#38912,#38913,#38914,#38915,#38916,#38917,#38918,#38919,
#38920,#38921,#38922,#38923,#38924,#38925,#38926,#38927,#38928,#38929,#38930,
#38931,#38932,#38933,#38934,#38935,#38936,#38937,#38938,#38939,#38940,#38941,
#38942,#38943,#38944,#38945,#38946,#38947,#38948,#38949,#38950,#38951,#38952,
#38953,#38954,#38955,#38956,#38957,#38958,#38959,#38960,#38961,#38962,#38963,
#38964,#38965,#38966,#38967,#38968,#38969,#38970,#38971,#38972,#38973,#38974,
#38975,#38976,#38977,#38978,#38979,#38980,#38981,#38982,#38983,#38984,#38985,
#38986,#38987,#38988,#38989,#38990,#38991,#38992,#38993,#38994,#38995,#38996,
#38997,#38998,#38999,#39000,#39001,#39002,#39003,#39004,#39005,#39006,#39007,
#39008,#39009,#39010,#39011,#39012,#39013,#39014,#39015,#39016,#39017,#39018,
#39019,#39020,#39021,#39022,#39023,#39024,#39025,#39026,#39027,#39028,#39029,
#39030,#39031,#39032,#39033,#39034,#39035,#39036,#39037,#39038,#39039,#39040,
#39041,#39042,#39043,#39044,#39045,#39046,#39047,#39048,#39049,#39050,#39051,
#39052,#39053,#39054,#39055,#39056,#39057,#39058,#39059,#39060,#39061,#39062,
#39063,#39064,#39065,#39066,#39067,#39068,#39069,#39070,#39071,#39072,#39073,
#39074,#39075,#39076,#39077,#39078,#39079,#39080,#39081,#39082,#39083,#39084,
#39085,#39086,#39087,#39088,#39089,#39090,#39091,#39092,#39093,#39094,#39095,
#39096,#39097,#39098,#39099,#39100,#39101,#39102,#39103,#39104,#39105,#39106,
#39107,#39108,#39109,#39110,#39111,#39112,#39113,#39114,#39115,#39116,#39117,
#39118,#39119,#39120,#39121,#39122,#39123,#39124,#39125,#39126,#39127,#39128,
#39129,#39130,#39131,#39132,#39133,#39134,#39135,#39136,#39137,#39138,#39139,
#39140,#39141,#39142,#39143,#39144,#39145,#39146,#39147,#39148,#39149,#39150,
#39151,#39152,#39153,#39154,#39155,#39156,#39157,#39158,#39159,#39160,#39161,
#39162,#39163,#39164,#39165,#39166,#39167,#39168,#39169,#39170,#39171,#39172,
#39173,#39174,#39175,#39176,#39177,#39178,#39179,#39180,#39181,#39182,#39183,
#39184,#39185,#39186,#39187,#39188,#39189,#39190,#39191,#39192,#39193,#39194,
#39195,#39196,#39197,#39198,#39199,#39200,#39201,#39202,#39203,#39204,#39205,
#39206,#39207,#39208,#39209,#39210,#39211,#39212,#39213,#39214,#39215,#39216,
#39217,#39218,#39219,#39220,#39221,#39222,#39223,#39224,#39225,#39226,#39227,
#39228,#39229,#39230,#39231,#39232,#39233,#39234,#39235,#39236,#39237,#39238,
#39239,#39240,#39241,#39242,#39243,#39244,#39245,#39246,#39247,#39248,#39249,
#39250,#39251,#39252,#39253,#39254,#39255,#39256,#39257,#39258,#39259,#39260,
#39261,#39262,#39263,#39264,#39265,#39266,#39267,#39268,#39269,#39270,#39271,
#39272,#39273,#39274,#39275,#39276,#39277,#39278,#39279,#39280,#39281,#39282,
#39283,#39284,#39285,#39286,#39287,#39288,#39289,#39290,#39291,#39292,#39293,
#39294,#39295,#39296,#39297,#39298,#39299,#39300,#39301,#39302,#39303,#39304,
#39305,#39306,#39307,#39308,#39309,#39310,#39311,#39312,#39313,#39314,#39315,
#39316,#39317,#39318,#39319,#39320,#39321,#39322,#39323,#39324,#39325,#39326,
#39327,#39328,#39329,#39330,#39331,#39332,#39333,#39334,#39335,#39336,#39337,
#39338,#39339,#39340,#39341,#39342,#39343,#39344,#39345,#39346,#39347,#39348,
#39349,#39350,#39351,#39352,#39353,#39354,#39355,#39356,#39357,#39358,#39359,
#39360,#39361,#39362,#39363,#39364,#39365,#39366,#39367,#39368,#39369,#39370,
#39371,#39372,#39373,#39374,#39375,#39376,#39377,#39378,#39379,#39380,#39381,
#39382,#39383,#39384,#39385,#39386,#39387,#39388,#39389,#39390,#39391,#39392,
#39393,#39394,#39395,#39396,#39397,#39398,#39399,#39400,#39401,#39402,#39403,
#39404,#39405,#39406,#39407,#39408,#39409,#39410,#39411,#39412,#39413,#39414,
#39415,#39416,#39417,#39418,#39419,#39420,#39421,#39422,#39423,#39424,#39425,
#39426,#39427,#39428,#39429,#39430,#39431,#39432,#39433,#39434,#39435,#39436,
#39437,#39438,#39439,#39440,#39441,#39442,#39443,#39444),.UNSPECIFIED.,
 .F.,.F.)
B_SPLINE_CURVE_WITH_KNOTS((3,2,2,2,2,2,2,2,2,2,2,2,2,2,2,2,2,2,2,2,2,2,
2,2,2,2,2,2,2,2,2,2,2,2,2,2,2,2,2,2,2,2,2,2,2,2,2,2,2,2,2,2,2,2,2,2,2,2,
2,2,2,2,2,2,2,2,2,2,2,2,2,2,2,2,2,2,2,2,2,2,2,2,2,2,2,2,2,2,2,2,2,2,2,2,
2,2,2,2,2,2,2,2,2,2,2,2,2,2,2,2,2,2,2,2,2,2,2,2,2,2,2,2,2,2,2,2,2,2,2,2,
2,2,2,2,2,2,2,2,2,2,2,2,2,2,2,2,2,2,2,2,2,2,2,2,2,2,2,2,2,2,2,2,2,2,2,2,
2,2,2,2,2,2,2,2,2,2,2,2,2,2,2,2,2,2,2,2,2,2,2,2,2,2,2,2,2,2,2,2,2,2,2,2,
2,2,2,2,2,2,2,2,2,2,2,2,2,2,2,2,2,2,2,2,2,2,2,2,2,2,2,2,2,2,2,2,2,2,2,2,
2,2,2,2,2,2,2,2,2,2,2,2,2,2,2,2,2,2,2,2,2,2,2,2,2,2,2,2,2,2,2,2,2,2,2,2,
2,2,2,2,2,2,2,2,2,2,2,2,2,2,2,2,2,2,2,2,2,2,2,2,2,2,2,2,2,2,2,2,2,2,2,2,
2,2,2,2,2,2,2,2,2,2,2,3),(0.0125164708018431,0.0144231574970549,0.0173077889964661,
0.0201924204958774,0.0230770519952887,0.0259616834947,0.0288463149941112,
0.0317309464935225,0.0346155779929338,0.037500209492345,0.0403848409917563,
0.0432694724911676,0.0461541039905789,0.0490387354899901,0.0519233669894014,
0.0548079984888127,0.057692629988224,0.0605772614876352,0.0634618929870465,
0.0663465244864578,0.069231155985869,0.0721157874852803,0.0750004189846916,
0.0778850504841029,0.0807696819835141,0.0836543134829254,0.0865389449823367,
0.089423576481748,0.0923082079811592,0.0951928394805705,0.0980774709799818,
0.100962102479393,0.103846733978804,0.106731365478216,0.109615996977627,
0.112500628477038,0.115385259976449,0.118269891475861,0.121154522975272,
0.124039154474683,0.126923785974095,0.129808417473506,0.132693048972917,
0.135577680472328,0.13846231197174,0.141346943471151,0.144231574970562,
0.147116206469973,0.150000837969385,0.152885469468796,0.155770100968207,
0.158654732467619,0.16153936396703,0.164423995466441,0.167308626965852,
0.170193258465264,0.173077889964675,0.175962521464086,0.178847152963497,
0.181731784462909,0.18461641596232,0.187501047461731,0.190385678961143,
0.193270310460554,0.196154941959965,0.199039573459376,0.201924204958788,
0.204808836458199,0.20769346795761,0.210578099457021,0.213462730956433,
0.216347362455844,0.219231993955255,0.222116625454667,0.225001256954078,
0.227885888453489,0.2307705199529,0.233655151452312,0.236539782951723,0.239424414451134,
0.242309045950545,0.245193677449957,0.248078308949368,0.250962940448779,
0.253847571948191,0.256732203447602,0.259616834947013,0.262501466446424,
0.265386097945836,0.268270729445247,0.271155360944658,0.274039992444069,
0.276924623943481,0.279809255442892,0.282693886942303,0.285578518441715,
0.288463149941126,0.291347781440537,0.294232412939948,0.29711704443936,
0.300001675938771,0.302886307438182,0.305770938937593,0.308655570437005,
0.311540201936416,0.314424833435827,0.317309464935239,0.32019409643465,
0.323078727934061,0.325963359433472,0.328847990932884,0.331732622432295,
0.334617253931706,0.337501885431117,0.340386516930529,0.34327114842994,
0.346155779929351,0.349040411428763,0.351925042928174,0.354809674427585,
0.357694305926996,0.360578937426408,0.363463568925819,0.36634820042523,
0.369232831924641,0.372117463424053,0.375002094923464,0.377886726422875,
0.380771357922287,0.383655989421698,0.386540620921109,0.38942525242052,
0.392309883919932,0.395194515419343,0.398079146918754,0.400963778418165,
0.403848409917577,0.406733041416988,0.409617672916399,0.412502304415811,
0.415386935915222,0.418271567414633,0.421156198914044,0.424040830413456,
0.426925461912867,0.429810093412278,0.432694724911689,0.435579356411101,
0.438463987910512,0.441348619409923,0.444233250909335,0.447117882408746,
0.450002513908157,0.452887145407568,0.45577177690698,0.458656408406391,
0.461541039905802,0.464425671405213,0.467310302904625,0.470194934404036,
0.473079565903447,0.475964197402859,0.47884882890227,0.481733460401681,
0.484618091901092,0.487502723400504,0.490387354899915,0.493271986399326,
0.496156617898737,0.499041249398149,0.50192588089756,0.504810512396971,
0.507695143896382,0.510579775395794,0.513464406895205,0.516349038394616,
0.519233669894028,0.522118301393439,0.52500293289285,0.527887564392261,
0.530772195891673,0.533656827391084,0.536541458890495,0.539426090389907,
0.542310721889318,0.545195353388729,0.54807998488814,0.550964616387552,
0.553849247886963,0.556733879386374,0.559618510885786,0.562503142385197,
0.565387773884608,0.568272405384019,0.571157036883431,0.574041668382842,
0.576926299882253,0.579810931381664,0.582695562881076,0.585580194380487,
0.588464825879898,0.591349457379309,0.594234088878721,0.597118720378132,
0.600003351877543,0.602887983376955,0.605772614876366,0.608657246375777,
0.611541877875188,0.6144265093746,0.617311140874011,0.620195772373422,0.623080403872833,
0.625965035372245,0.628849666871656,0.631734298371067,0.634618929870479,
0.63750356136989,0.640388192869301,0.643272824368712,0.646157455868124,
0.649042087367535,0.651926718866946,0.654811350366358,0.657695981865769,
0.66058061336518,0.663465244864591,0.666349876364003,0.669234507863414,
0.672119139362825,0.675003770862236,0.677888402361648,0.680773033861059,
0.68365766536047,0.686542296859882,0.689426928359293,0.692311559858704,
0.695196191358115,0.698080822857527,0.700965454356938,0.703850085856349,
0.70673471735576,0.709619348855172,0.712503980354583,0.715388611853994,
0.718273243353405,0.721157874852817,0.724042506352228,0.726927137851639,
0.729811769351051,0.732696400850462,0.735581032349873,0.738465663849284,
0.741350295348696,0.744234926848107,0.747119558347518,0.75000418984693,
0.752888821346341,0.755773452845752,0.758658084345163,0.761542715844575,
0.764427347343986,0.767311978843397,0.770196610342808,0.77308124184222,
0.775965873341631,0.778850504841042,0.781735136340453,0.784619767839865,
0.787504399339276,0.790389030838687,0.793273662338098,0.79615829383751,
0.799042925336921,0.801927556836332,0.804812188335744,0.807696819835155,
0.810581451334566,0.813466082833978,0.816350714333389,0.8192353458328,0.822119977332211,
0.825004608831623,0.827889240331034,0.830773871830445,0.833658503329856,
0.836543134829268,0.839427766328679,0.84231239782809,0.845197029327502,
0.848081660826913,0.850966292326324,0.853850923825735,0.856735555325147,
0.859620186824558,0.862504818323969,0.86538944982338,0.868274081322792,
0.871158712822203,0.874043344321614,0.876927975821026,0.879812607320437,
0.882697238819848,0.885581870319259,0.888466501818671,0.891351133318082,
0.894235764817493,0.897120396316904,0.900005027816316,0.902889659315727,
0.905774290815138,0.908658922314549,0.911543553813961,0.914428185313372,
0.917312816812783,0.920197448312195,0.923082079811606,0.925966711311017,
0.928851342810428,0.93173597430984,0.934620605809251,0.935598550613399),
 .UNSPECIFIED.)
CURVE()
GEOMETRIC_REPRESENTATION_ITEM()
RATIONAL_B_SPLINE_CURVE((0.965885073571149,0.949685815112381,1.,0.923879532511287,
1.,0.923879532511287,1.,0.923879532511287,1.,0.923879532511287,1.,0.923879532511287,
1.,0.923879532511287,1.,0.923879532511287,1.,0.923879532511287,1.,0.923879532511287,
1.,0.923879532511287,1.,0.923879532511287,1.,0.923879532511287,1.,0.923879532511287,
1.,0.923879532511287,1.,0.923879532511287,1.,0.923879532511287,1.,0.923879532511287,
1.,0.923879532511287,1.,0.923879532511287,1.,0.923879532511287,1.,0.923879532511287,
1.,0.923879532511287,1.,0.923879532511287,1.,0.923879532511287,1.,0.923879532511287,
1.,0.923879532511287,1.,0.923879532511287,1.,0.923879532511287,1.,0.923879532511287,
1.,0.923879532511287,1.,0.923879532511287,1.,0.923879532511287,1.,0.923879532511287,
1.,0.923879532511287,1.,0.923879532511287,1.,0.923879532511287,1.,0.923879532511287,
1.,0.923879532511287,1.,0.923879532511287,1.,0.923879532511287,1.,0.923879532511287,
1.,0.923879532511287,1.,0.923879532511287,1.,0.923879532511287,1.,0.923879532511287,
1.,0.923879532511287,1.,0.923879532511287,1.,0.923879532511287,1.,0.923879532511287,
1.,0.923879532511287,1.,0.923879532511287,1.,0.923879532511287,1.,0.923879532511287,
1.,0.923879532511287,1.,0.923879532511287,1.,0.923879532511287,1.,0.923879532511287,
1.,0.923879532511287,1.,0.923879532511287,1.,0.923879532511287,1.,0.923879532511287,
1.,0.923879532511287,1.,0.923879532511287,1.,0.923879532511287,1.,0.923879532511287,
1.,0.923879532511287,1.,0.923879532511287,1.,0.923879532511287,1.,0.923879532511287,
1.,0.923879532511287,1.,0.923879532511287,1.,0.923879532511287,1.,0.923879532511287,
1.,0.923879532511287,1.,0.923879532511287,1.,0.923879532511287,1.,0.923879532511287,
1.,0.923879532511287,1.,0.923879532511287,1.,0.923879532511287,1.,0.923879532511287,
1.,0.923879532511287,1.,0.923879532511287,1.,0.923879532511287,1.,0.923879532511287,
1.,0.923879532511287,1.,0.923879532511287,1.,0.923879532511287,1.,0.923879532511287,
1.,0.923879532511287,1.,0.923879532511287,1.,0.923879532511287,1.,0.923879532511287,
1.,0.923879532511287,1.,0.923879532511287,1.,0.923879532511287,1.,0.923879532511287,
1.,0.923879532511287,1.,0.923879532511287,1.,0.923879532511287,1.,0.923879532511287,
1.,0.923879532511287,1.,0.923879532511287,1.,0.923879532511287,1.,0.923879532511287,
1.,0.923879532511287,1.,0.923879532511287,1.,0.923879532511287,1.,0.923879532511287,
1.,0.923879532511287,1.,0.923879532511287,1.,0.923879532511287,1.,0.923879532511287,
1.,0.923879532511287,1.,0.923879532511287,1.,0.923879532511287,1.,0.923879532511287,
1.,0.923879532511287,1.,0.923879532511287,1.,0.923879532511287,1.,0.923879532511287,
1.,0.923879532511287,1.,0.923879532511287,1.,0.923879532511287,1.,0.923879532511287,
1.,0.923879532511287,1.,0.923879532511287,1.,0.923879532511287,1.,0.923879532511287,
1.,0.923879532511287,1.,0.923879532511287,1.,0.923879532511287,1.,0.923879532511287,
1.,0.923879532511287,1.,0.923879532511287,1.,0.923879532511287,1.,0.923879532511287,
1.,0.923879532511287,1.,0.923879532511287,1.,0.923879532511287,1.,0.923879532511287,
1.,0.923879532511287,1.,0.923879532511287,1.,0.923879532511287,1.,0.923879532511287,
1.,0.923879532511287,1.,0.923879532511287,1.,0.923879532511287,1.,0.923879532511287,
1.,0.923879532511287,1.,0.923879532511287,1.,0.923879532511287,1.,0.923879532511287,
1.,0.923879532511287,1.,0.923879532511287,1.,0.923879532511287,1.,0.923879532511287,
1.,0.923879532511287,1.,0.923879532511287,1.,0.923879532511287,1.,0.923879532511287,
1.,0.923879532511287,1.,0.923879532511287,1.,0.923879532511287,1.,0.923879532511287,
1.,0.923879532511287,1.,0.923879532511287,1.,0.923879532511287,1.,0.923879532511287,
1.,0.923879532511287,1.,0.923879532511287,1.,0.923879532511287,1.,0.923879532511287,
1.,0.923879532511287,1.,0.923879532511287,1.,0.923879532511287,1.,0.923879532511287,
1.,0.923879532511287,1.,0.923879532511287,1.,0.923879532511287,1.,0.923879532511287,
1.,0.923879532511287,1.,0.923879532511287,1.,0.923879532511287,1.,0.923879532511287,
1.,0.923879532511287,1.,0.923879532511287,1.,0.923879532511287,1.,0.923879532511287,
1.,0.923879532511287,1.,0.923879532511287,1.,0.923879532511287,1.,0.923879532511287,
1.,0.923879532511287,1.,0.923879532511287,1.,0.923879532511287,1.,0.923879532511287,
1.,0.923879532511287,1.,0.923879532511287,1.,0.923879532511287,1.,0.923879532511287,
1.,0.923879532511287,1.,0.923879532511287,1.,0.923879532511287,1.,0.923879532511287,
1.,0.923879532511287,1.,0.923879532511287,1.,0.923879532511287,1.,0.923879532511287,
1.,0.923879532511287,1.,0.923879532511287,1.,0.923879532511287,1.,0.923879532511287,
1.,0.923879532511287,1.,0.923879532511287,1.,0.923879532511287,1.,0.923879532511287,
1.,0.923879532511287,1.,0.923879532511287,1.,0.923879532511287,1.,0.923879532511287,
1.,0.923879532511287,1.,0.923879532511287,1.,0.923879532511287,1.,0.923879532511287,
1.,0.923879532511287,1.,0.923879532511287,1.,0.923879532511287,1.,0.923879532511287,
1.,0.923879532511287,1.,0.923879532511287,1.,0.923879532511287,1.,0.923879532511287,
1.,0.923879532511287,1.,0.923879532511287,1.,0.923879532511287,1.,0.923879532511287,
1.,0.923879532511287,1.,0.923879532511287,1.,0.923879532511287,1.,0.923879532511287,
1.,0.923879532511287,1.,0.923879532511287,1.,0.923879532511287,1.,0.923879532511287,
1.,0.923879532511287,1.,0.923879532511287,1.,0.923879532511287,1.,0.923879532511287,
1.,0.923879532511287,1.,0.923879532511287,1.,0.923879532511287,1.,0.923879532511287,
1.,0.923879532511287,1.,0.923879532511287,1.,0.923879532511287,1.,0.923879532511287,
1.,0.923879532511287,1.,0.923879532511287,1.,0.923879532511287,1.,0.923879532511287,
1.,0.923879532511287,1.,0.923879532511287,1.,0.923879532511287,1.,0.923879532511287,
1.,0.923879532511287,1.,0.923879532511287,1.,0.923879532511287,1.,0.923879532511287,
1.,0.923879532511287,1.,0.923879532511287,1.,0.923879532511287,1.,0.923879532511287,
1.,0.923879532511287,1.,0.923879532511287,1.,0.923879532511287,1.,0.923879532511287,
1.,0.923879532511287,1.,0.923879532511287,1.,0.923879532511287,1.,0.923879532511287,
1.,0.923879532511287,1.,0.923879532511287,1.,0.923879532511287,1.,0.923879532511287,
1.,0.923879532511287,1.,0.923879532511287,1.,0.923879532511287,1.,0.923879532511287,
1.,0.923879532511287,1.,0.923879532511287,1.,0.923879532511287,1.,0.923879532511287,
1.,0.923879532511287,1.,0.923879532511287,1.,0.923879532511287,1.,0.923879532511287,
1.,0.923879532511287,1.,0.923879532511287,1.,0.923879532511287,1.,0.923879532511287,
1.,0.923879532511287,1.,0.923879532511287,1.,0.923879532511287,1.,0.923879532511287,
1.,0.923879532511287,1.,0.923879532511287,1.,0.923879532511287,1.,0.923879532511287,
1.,0.923879532511287,1.,0.923879532511287,1.,0.923879532511287,1.,0.923879532511287,
1.,0.923879532511287,1.,0.923879532511287,1.,0.923879532511287,1.,0.923879532511287,
1.,0.923879532511287,1.,0.923879532511287,1.,0.974193717400275,0.965885073572031))
REPRESENTATION_ITEM('')
);
#89=(
BOUNDED_CURVE()
B_SPLINE_CURVE(2,(#40835,#40836,#40837,#40838,#40839,#40840,#40841,#40842,
#40843,#40844,#40845,#40846,#40847,#40848,#40849,#40850,#40851,#40852,#40853,
#40854,#40855,#40856,#40857,#40858,#40859,#40860,#40861,#40862,#40863,#40864,
#40865,#40866,#40867,#40868,#40869,#40870,#40871,#40872,#40873,#40874,#40875,
#40876,#40877,#40878,#40879,#40880,#40881,#40882,#40883,#40884,#40885,#40886,
#40887,#40888,#40889,#40890,#40891,#40892,#40893,#40894,#40895,#40896,#40897,
#40898,#40899,#40900,#40901,#40902,#40903,#40904,#40905,#40906,#40907,#40908,
#40909,#40910,#40911,#40912,#40913,#40914,#40915,#40916,#40917,#40918,#40919,
#40920,#40921,#40922,#40923,#40924,#40925,#40926,#40927,#40928,#40929,#40930,
#40931,#40932,#40933,#40934,#40935,#40936,#40937,#40938,#40939,#40940,#40941,
#40942,#40943,#40944,#40945,#40946,#40947,#40948,#40949,#40950,#40951,#40952,
#40953,#40954,#40955,#40956,#40957,#40958,#40959,#40960,#40961,#40962,#40963,
#40964,#40965,#40966,#40967,#40968,#40969,#40970,#40971,#40972,#40973,#40974,
#40975,#40976,#40977,#40978,#40979,#40980,#40981,#40982,#40983,#40984,#40985,
#40986,#40987,#40988,#40989,#40990,#40991,#40992,#40993,#40994,#40995,#40996,
#40997,#40998,#40999,#41000,#41001,#41002,#41003,#41004,#41005,#41006,#41007,
#41008,#41009,#41010,#41011,#41012,#41013,#41014,#41015,#41016,#41017,#41018,
#41019,#41020,#41021,#41022,#41023,#41024,#41025,#41026,#41027,#41028,#41029,
#41030,#41031,#41032,#41033,#41034,#41035,#41036,#41037,#41038,#41039,#41040,
#41041,#41042,#41043,#41044,#41045,#41046,#41047,#41048,#41049,#41050,#41051,
#41052,#41053,#41054,#41055,#41056,#41057,#41058,#41059,#41060,#41061,#41062,
#41063,#41064,#41065,#41066,#41067,#41068,#41069,#41070,#41071,#41072,#41073,
#41074,#41075,#41076,#41077,#41078,#41079,#41080,#41081,#41082,#41083,#41084,
#41085,#41086,#41087,#41088,#41089,#41090,#41091,#41092,#41093,#41094,#41095,
#41096,#41097,#41098,#41099,#41100,#41101,#41102,#41103,#41104,#41105,#41106,
#41107,#41108,#41109,#41110,#41111,#41112,#41113,#41114,#41115,#41116,#41117,
#41118,#41119,#41120,#41121,#41122,#41123,#41124,#41125,#41126,#41127,#41128,
#41129,#41130,#41131,#41132,#41133,#41134,#41135,#41136,#41137,#41138,#41139,
#41140,#41141,#41142,#41143,#41144,#41145,#41146,#41147,#41148,#41149,#41150,
#41151,#41152,#41153,#41154,#41155,#41156,#41157,#41158,#41159,#41160,#41161,
#41162,#41163,#41164,#41165,#41166,#41167,#41168,#41169,#41170,#41171,#41172,
#41173,#41174,#41175,#41176,#41177,#41178,#41179,#41180,#41181,#41182,#41183,
#41184,#41185,#41186,#41187,#41188,#41189,#41190,#41191,#41192,#41193,#41194,
#41195,#41196,#41197,#41198,#41199,#41200,#41201,#41202,#41203,#41204,#41205,
#41206,#41207,#41208,#41209,#41210,#41211,#41212,#41213,#41214,#41215,#41216,
#41217,#41218,#41219,#41220,#41221,#41222,#41223,#41224,#41225,#41226,#41227,
#41228,#41229,#41230,#41231,#41232,#41233,#41234,#41235,#41236,#41237,#41238,
#41239,#41240,#41241,#41242,#41243,#41244,#41245,#41246,#41247,#41248,#41249,
#41250,#41251,#41252,#41253,#41254,#41255,#41256,#41257,#41258,#41259,#41260,
#41261,#41262,#41263,#41264,#41265,#41266,#41267,#41268,#41269,#41270,#41271,
#41272,#41273,#41274,#41275,#41276,#41277,#41278,#41279,#41280,#41281,#41282,
#41283,#41284,#41285,#41286,#41287,#41288,#41289,#41290,#41291,#41292,#41293,
#41294,#41295,#41296,#41297,#41298,#41299,#41300,#41301,#41302,#41303,#41304,
#41305,#41306,#41307,#41308,#41309,#41310,#41311,#41312,#41313,#41314,#41315,
#41316,#41317,#41318,#41319,#41320,#41321,#41322,#41323,#41324,#41325,#41326,
#41327,#41328,#41329,#41330,#41331,#41332,#41333,#41334,#41335,#41336,#41337,
#41338,#41339,#41340,#41341,#41342,#41343,#41344,#41345,#41346,#41347,#41348,
#41349,#41350,#41351,#41352,#41353,#41354,#41355,#41356,#41357,#41358,#41359,
#41360,#41361,#41362,#41363,#41364,#41365,#41366,#41367,#41368,#41369,#41370,
#41371,#41372,#41373,#41374,#41375,#41376,#41377,#41378,#41379,#41380,#41381,
#41382,#41383,#41384,#41385,#41386,#41387,#41388,#41389,#41390,#41391,#41392,
#41393,#41394,#41395,#41396,#41397,#41398,#41399,#41400,#41401,#41402,#41403,
#41404,#41405,#41406,#41407,#41408,#41409,#41410,#41411,#41412,#41413,#41414,
#41415,#41416,#41417,#41418,#41419,#41420,#41421,#41422,#41423,#41424,#41425,
#41426,#41427,#41428,#41429,#41430,#41431,#41432,#41433,#41434,#41435,#41436,
#41437,#41438,#41439,#41440,#41441,#41442,#41443,#41444,#41445,#41446,#41447,
#41448,#41449,#41450,#41451,#41452,#41453,#41454,#41455,#41456,#41457,#41458,
#41459,#41460,#41461,#41462,#41463,#41464,#41465,#41466,#41467,#41468,#41469,
#41470,#41471,#41472,#41473,#41474,#41475,#41476,#41477),.UNSPECIFIED.,
 .F.,.F.)
B_SPLINE_CURVE_WITH_KNOTS((3,2,2,2,2,2,2,2,2,2,2,2,2,2,2,2,2,2,2,2,2,2,
2,2,2,2,2,2,2,2,2,2,2,2,2,2,2,2,2,2,2,2,2,2,2,2,2,2,2,2,2,2,2,2,2,2,2,2,
2,2,2,2,2,2,2,2,2,2,2,2,2,2,2,2,2,2,2,2,2,2,2,2,2,2,2,2,2,2,2,2,2,2,2,2,
2,2,2,2,2,2,2,2,2,2,2,2,2,2,2,2,2,2,2,2,2,2,2,2,2,2,2,2,2,2,2,2,2,2,2,2,
2,2,2,2,2,2,2,2,2,2,2,2,2,2,2,2,2,2,2,2,2,2,2,2,2,2,2,2,2,2,2,2,2,2,2,2,
2,2,2,2,2,2,2,2,2,2,2,2,2,2,2,2,2,2,2,2,2,2,2,2,2,2,2,2,2,2,2,2,2,2,2,2,
2,2,2,2,2,2,2,2,2,2,2,2,2,2,2,2,2,2,2,2,2,2,2,2,2,2,2,2,2,2,2,2,2,2,2,2,
2,2,2,2,2,2,2,2,2,2,2,2,2,2,2,2,2,2,2,2,2,2,2,2,2,2,2,2,2,2,2,2,2,2,2,2,
2,2,2,2,2,2,2,2,2,2,2,2,2,2,2,2,2,2,2,2,2,2,2,2,2,2,2,2,2,2,2,2,2,2,2,2,
2,2,2,2,2,2,2,2,2,2,2,3),(0.0047186950560118,0.00568181818181818,0.00852272727272727,
0.0113636363636364,0.0142045454545455,0.0170454545454545,0.0198863636363636,
0.0227272727272727,0.0255681818181818,0.0284090909090909,0.03125,0.0340909090909091,
0.0369318181818182,0.0397727272727273,0.0426136363636364,0.0454545454545455,
0.0482954545454545,0.0511363636363636,0.0539772727272727,0.0568181818181818,
0.0596590909090909,0.0625,0.0653409090909091,0.0681818181818182,0.0710227272727273,
0.0738636363636364,0.0767045454545455,0.0795454545454545,0.0823863636363636,
0.0852272727272727,0.0880681818181818,0.0909090909090909,0.09375,0.0965909090909091,
0.0994318181818182,0.102272727272727,0.105113636363636,0.107954545454545,
0.110795454545455,0.113636363636364,0.116477272727273,0.119318181818182,
0.122159090909091,0.125,0.127840909090909,0.130681818181818,0.133522727272727,
0.136363636363636,0.139204545454545,0.142045454545455,0.144886363636364,
0.147727272727273,0.150568181818182,0.153409090909091,0.15625,0.159090909090909,
0.161931818181818,0.164772727272727,0.167613636363636,0.170454545454545,
0.173295454545455,0.176136363636364,0.178977272727273,0.181818181818182,
0.184659090909091,0.1875,0.190340909090909,0.193181818181818,0.196022727272727,
0.198863636363636,0.201704545454545,0.204545454545455,0.207386363636364,
0.210227272727273,0.213068181818182,0.215909090909091,0.21875,0.221590909090909,
0.224431818181818,0.227272727272727,0.230113636363636,0.232954545454545,
0.235795454545455,0.238636363636364,0.241477272727273,0.244318181818182,
0.247159090909091,0.25,0.252840909090909,0.255681818181818,0.258522727272727,
0.261363636363636,0.264204545454545,0.267045454545455,0.269886363636364,
0.272727272727273,0.275568181818182,0.278409090909091,0.28125,0.284090909090909,
0.286931818181818,0.289772727272727,0.292613636363636,0.295454545454545,
0.298295454545455,0.301136363636364,0.303977272727273,0.306818181818182,
0.309659090909091,0.3125,0.315340909090909,0.318181818181818,0.321022727272727,
0.323863636363636,0.326704545454545,0.329545454545455,0.332386363636364,
0.335227272727273,0.338068181818182,0.340909090909091,0.34375,0.346590909090909,
0.349431818181818,0.352272727272727,0.355113636363636,0.357954545454545,
0.360795454545455,0.363636363636364,0.366477272727273,0.369318181818182,
0.372159090909091,0.375,0.377840909090909,0.380681818181818,0.383522727272727,
0.386363636363636,0.389204545454546,0.392045454545455,0.394886363636364,
0.397727272727273,0.400568181818182,0.403409090909091,0.40625,0.409090909090909,
0.411931818181818,0.414772727272727,0.417613636363636,0.420454545454545,
0.423295454545455,0.426136363636364,0.428977272727273,0.431818181818182,
0.434659090909091,0.4375,0.440340909090909,0.443181818181818,0.446022727272727,
0.448863636363636,0.451704545454545,0.454545454545455,0.457386363636364,
0.460227272727273,0.463068181818182,0.465909090909091,0.46875,0.471590909090909,
0.474431818181818,0.477272727272727,0.480113636363636,0.482954545454545,
0.485795454545455,0.488636363636364,0.491477272727273,0.494318181818182,
0.497159090909091,0.5,0.502840909090909,0.505681818181818,0.508522727272727,
0.511363636363636,0.514204545454545,0.517045454545455,0.519886363636364,
0.522727272727273,0.525568181818182,0.528409090909091,0.53125,0.534090909090909,
0.536931818181818,0.539772727272727,0.542613636363636,0.545454545454545,
0.548295454545455,0.551136363636364,0.553977272727273,0.556818181818182,
0.559659090909091,0.5625,0.565340909090909,0.568181818181818,0.571022727272727,
0.573863636363636,0.576704545454545,0.579545454545455,0.582386363636364,
0.585227272727273,0.588068181818182,0.590909090909091,0.59375,0.596590909090909,
0.599431818181818,0.602272727272727,0.605113636363636,0.607954545454545,
0.610795454545455,0.613636363636364,0.616477272727273,0.619318181818182,
0.622159090909091,0.625,0.627840909090909,0.630681818181818,0.633522727272727,
0.636363636363636,0.639204545454545,0.642045454545455,0.644886363636364,
0.647727272727273,0.650568181818182,0.653409090909091,0.65625,0.659090909090909,
0.661931818181818,0.664772727272727,0.667613636363636,0.670454545454546,
0.673295454545455,0.676136363636364,0.678977272727273,0.681818181818182,
0.684659090909091,0.6875,0.690340909090909,0.693181818181818,0.696022727272727,
0.698863636363636,0.701704545454545,0.704545454545455,0.707386363636364,
0.710227272727273,0.713068181818182,0.715909090909091,0.71875,0.721590909090909,
0.724431818181818,0.727272727272727,0.730113636363636,0.732954545454545,
0.735795454545455,0.738636363636364,0.741477272727273,0.744318181818182,
0.747159090909091,0.75,0.752840909090909,0.755681818181818,0.758522727272727,
0.761363636363636,0.764204545454545,0.767045454545455,0.769886363636364,
0.772727272727273,0.775568181818182,0.778409090909091,0.78125,0.784090909090909,
0.786931818181818,0.789772727272727,0.792613636363636,0.795454545454545,
0.798295454545455,0.801136363636364,0.803977272727273,0.806818181818182,
0.809659090909091,0.8125,0.815340909090909,0.818181818181818,0.821022727272727,
0.823863636363636,0.826704545454546,0.829545454545455,0.832386363636364,
0.835227272727273,0.838068181818182,0.840909090909091,0.84375,0.846590909090909,
0.849431818181818,0.852272727272727,0.855113636363636,0.857954545454545,
0.860795454545455,0.863636363636364,0.866477272727273,0.869318181818182,
0.872159090909091,0.875,0.877840909090909,0.880681818181818,0.883522727272727,
0.886363636363636,0.889204545454545,0.892045454545455,0.894886363636364,
0.897727272727273,0.900568181818182,0.903409090909091,0.90625,0.909090909090909,
0.911931818181818,0.913809604147033),.UNSPECIFIED.)
CURVE()
GEOMETRIC_REPRESENTATION_ITEM()
RATIONAL_B_SPLINE_CURVE((0.965885055496846,0.974193689329879,1.,0.923879532511287,
1.,0.923879532511287,1.,0.923879532511287,1.,0.923879532511287,1.,0.923879532511287,
1.,0.923879532511287,1.,0.923879532511287,1.,0.923879532511287,1.,0.923879532511287,
1.,0.923879532511287,1.,0.923879532511287,1.,0.923879532511287,1.,0.923879532511287,
1.,0.923879532511287,1.,0.923879532511287,1.,0.923879532511287,1.,0.923879532511287,
1.,0.923879532511287,1.,0.923879532511287,1.,0.923879532511287,1.,0.923879532511287,
1.,0.923879532511287,1.,0.923879532511287,1.,0.923879532511287,1.,0.923879532511287,
1.,0.923879532511287,1.,0.923879532511287,1.,0.923879532511287,1.,0.923879532511287,
1.,0.923879532511287,1.,0.923879532511287,1.,0.923879532511287,1.,0.923879532511287,
1.,0.923879532511287,1.,0.923879532511287,1.,0.923879532511287,1.,0.923879532511287,
1.,0.923879532511287,1.,0.923879532511287,1.,0.923879532511287,1.,0.923879532511287,
1.,0.923879532511287,1.,0.923879532511287,1.,0.923879532511287,1.,0.923879532511287,
1.,0.923879532511287,1.,0.923879532511287,1.,0.923879532511287,1.,0.923879532511287,
1.,0.923879532511287,1.,0.923879532511287,1.,0.923879532511287,1.,0.923879532511287,
1.,0.923879532511287,1.,0.923879532511287,1.,0.923879532511287,1.,0.923879532511287,
1.,0.923879532511287,1.,0.923879532511287,1.,0.923879532511287,1.,0.923879532511287,
1.,0.923879532511287,1.,0.923879532511287,1.,0.923879532511287,1.,0.923879532511287,
1.,0.923879532511287,1.,0.923879532511287,1.,0.923879532511287,1.,0.923879532511287,
1.,0.923879532511287,1.,0.923879532511287,1.,0.923879532511287,1.,0.923879532511287,
1.,0.923879532511287,1.,0.923879532511287,1.,0.923879532511287,1.,0.923879532511287,
1.,0.923879532511287,1.,0.923879532511287,1.,0.923879532511287,1.,0.923879532511287,
1.,0.923879532511287,1.,0.923879532511287,1.,0.923879532511287,1.,0.923879532511287,
1.,0.923879532511287,1.,0.923879532511287,1.,0.923879532511287,1.,0.923879532511287,
1.,0.923879532511287,1.,0.923879532511287,1.,0.923879532511287,1.,0.923879532511287,
1.,0.923879532511287,1.,0.923879532511287,1.,0.923879532511287,1.,0.923879532511287,
1.,0.923879532511287,1.,0.923879532511287,1.,0.923879532511287,1.,0.923879532511287,
1.,0.923879532511287,1.,0.923879532511287,1.,0.923879532511287,1.,0.923879532511287,
1.,0.923879532511287,1.,0.923879532511287,1.,0.923879532511287,1.,0.923879532511287,
1.,0.923879532511287,1.,0.923879532511287,1.,0.923879532511287,1.,0.923879532511287,
1.,0.923879532511287,1.,0.923879532511287,1.,0.923879532511287,1.,0.923879532511287,
1.,0.923879532511287,1.,0.923879532511287,1.,0.923879532511287,1.,0.923879532511287,
1.,0.923879532511287,1.,0.923879532511287,1.,0.923879532511287,1.,0.923879532511287,
1.,0.923879532511287,1.,0.923879532511287,1.,0.923879532511287,1.,0.923879532511287,
1.,0.923879532511287,1.,0.923879532511287,1.,0.923879532511287,1.,0.923879532511287,
1.,0.923879532511287,1.,0.923879532511287,1.,0.923879532511287,1.,0.923879532511287,
1.,0.923879532511287,1.,0.923879532511287,1.,0.923879532511287,1.,0.923879532511287,
1.,0.923879532511287,1.,0.923879532511287,1.,0.923879532511287,1.,0.923879532511287,
1.,0.923879532511287,1.,0.923879532511287,1.,0.923879532511287,1.,0.923879532511287,
1.,0.923879532511287,1.,0.923879532511287,1.,0.923879532511287,1.,0.923879532511287,
1.,0.923879532511287,1.,0.923879532511287,1.,0.923879532511287,1.,0.923879532511287,
1.,0.923879532511287,1.,0.923879532511287,1.,0.923879532511287,1.,0.923879532511287,
1.,0.923879532511287,1.,0.923879532511287,1.,0.923879532511287,1.,0.923879532511287,
1.,0.923879532511287,1.,0.923879532511287,1.,0.923879532511287,1.,0.923879532511287,
1.,0.923879532511287,1.,0.923879532511287,1.,0.923879532511287,1.,0.923879532511287,
1.,0.923879532511287,1.,0.923879532511287,1.,0.923879532511287,1.,0.923879532511287,
1.,0.923879532511287,1.,0.923879532511287,1.,0.923879532511287,1.,0.923879532511287,
1.,0.923879532511287,1.,0.923879532511287,1.,0.923879532511287,1.,0.923879532511287,
1.,0.923879532511287,1.,0.923879532511287,1.,0.923879532511287,1.,0.923879532511287,
1.,0.923879532511287,1.,0.923879532511287,1.,0.923879532511287,1.,0.923879532511287,
1.,0.923879532511287,1.,0.923879532511287,1.,0.923879532511287,1.,0.923879532511287,
1.,0.923879532511287,1.,0.923879532511287,1.,0.923879532511287,1.,0.923879532511287,
1.,0.923879532511287,1.,0.923879532511287,1.,0.923879532511287,1.,0.923879532511287,
1.,0.923879532511287,1.,0.923879532511287,1.,0.923879532511287,1.,0.923879532511287,
1.,0.923879532511287,1.,0.923879532511287,1.,0.923879532511287,1.,0.923879532511287,
1.,0.923879532511287,1.,0.923879532511287,1.,0.923879532511287,1.,0.923879532511287,
1.,0.923879532511287,1.,0.923879532511287,1.,0.923879532511287,1.,0.923879532511287,
1.,0.923879532511287,1.,0.923879532511287,1.,0.923879532511287,1.,0.923879532511287,
1.,0.923879532511287,1.,0.923879532511287,1.,0.923879532511287,1.,0.923879532511287,
1.,0.923879532511287,1.,0.923879532511287,1.,0.923879532511287,1.,0.923879532511287,
1.,0.923879532511287,1.,0.923879532511287,1.,0.923879532511287,1.,0.923879532511287,
1.,0.923879532511287,1.,0.923879532511287,1.,0.923879532511287,1.,0.923879532511287,
1.,0.923879532511287,1.,0.923879532511287,1.,0.923879532511287,1.,0.923879532511287,
1.,0.923879532511287,1.,0.923879532511287,1.,0.923879532511287,1.,0.923879532511287,
1.,0.923879532511287,1.,0.923879532511287,1.,0.923879532511287,1.,0.923879532511287,
1.,0.923879532511287,1.,0.923879532511287,1.,0.923879532511287,1.,0.923879532511287,
1.,0.923879532511287,1.,0.923879532511287,1.,0.923879532511287,1.,0.923879532511287,
1.,0.923879532511287,1.,0.923879532511287,1.,0.923879532511287,1.,0.923879532511287,
1.,0.923879532511287,1.,0.923879532511287,1.,0.923879532511287,1.,0.923879532511287,
1.,0.923879532511287,1.,0.923879532511287,1.,0.923879532511287,1.,0.923879532511287,
1.,0.923879532511287,1.,0.923879532511287,1.,0.923879532511287,1.,0.923879532511287,
1.,0.923879532511287,1.,0.923879532511287,1.,0.923879532511287,1.,0.923879532511287,
1.,0.923879532511287,1.,0.923879532511287,1.,0.923879532511287,1.,0.923879532511287,
1.,0.923879532511287,1.,0.923879532511287,1.,0.923879532511287,1.,0.923879532511287,
1.,0.923879532511287,1.,0.923879532511287,1.,0.923879532511287,1.,0.923879532511287,
1.,0.923879532511287,1.,0.923879532511287,1.,0.923879532511287,1.,0.923879532511287,
1.,0.923879532511287,1.,0.923879532511287,1.,0.923879532511287,1.,0.923879532511287,
1.,0.923879532511287,1.,0.923879532511287,1.,0.923879532511287,1.,0.923879532511287,
1.,0.923879532511287,1.,0.923879532511287,1.,0.923879532511287,1.,0.923879532511287,
1.,0.923879532511287,1.,0.923879532511287,1.,0.923879532511287,1.,0.923879532511287,
1.,0.923879532511287,1.,0.923879532511287,1.,0.923879532511287,1.,0.923879532511287,
1.,0.923879532511287,1.,0.923879532511287,1.,0.949685843178392,0.965885055498788))
REPRESENTATION_ITEM('')
);
#141=CONICAL_SURFACE('',#9390,2.99999999999999,0.78539816339745);
#310=B_SPLINE_CURVE_WITH_KNOTS('',3,(#32348,#32349,#32350,#32351,#32352,
#32353,#32354,#32355,#32356,#32357),.UNSPECIFIED.,.F.,.F.,(4,2,2,2,4),(-0.317022884646079,
-0.305729538758937,-0.18510534189066,-0.0921237868962644,-1.00000008007584E-6),
 .UNSPECIFIED.);
#311=B_SPLINE_CURVE_WITH_KNOTS('',3,(#32363,#32364,#32365,#32366,#32367,
#32368,#32369,#32370,#32371,#32372,#32373,#32374,#32375,#32376,#32377,#32378,
#32379,#32380,#32381,#32382,#32383,#32384,#32385,#32386,#32387,#32388,#32389,
#32390,#32391,#32392,#32393,#32394,#32395,#32396,#32397,#32398),
 .UNSPECIFIED.,.F.,.F.,(4,2,2,2,2,2,2,2,2,2,2,2,2,2,2,2,2,4),(-2.20877752486386,
-2.1921017198068,-2.0724399317334,-1.95706912003883,-1.83729284877479,-1.72182784454118,
-1.60193535202522,-1.48637284172353,-1.36636241511554,-1.25069926792504,
-1.13056922486976,-1.01480248488051,-0.894551178068988,-0.778678056364855,
-0.658303877405628,-0.54232174411607,-0.421823126741146,-0.317022884646079),
 .UNSPECIFIED.);
#312=B_SPLINE_CURVE_WITH_KNOTS('',3,(#32401,#32402,#32403,#32404,#32405,
#32406,#32407,#32408,#32409,#32410,#32411,#32412,#32413,#32414,#32415,#32416,
#32417,#32418,#32419,#32420,#32421,#32422,#32423,#32424,#32425,#32426,#32427,
#32428,#32429,#32430,#32431,#32432),.UNSPECIFIED.,.F.,.F.,(4,2,2,2,2,2,
2,2,2,2,2,2,2,2,2,4),(-56.1018496897495,-56.020261169572,-55.9400137990114,
-55.8174844812794,-55.6902240350637,-55.5678472298567,-55.4407451859001,
-55.3185207025299,-55.1915768628461,-55.0695045107994,-54.9427186775888,
-54.8207982665224,-54.6941702421669,-54.5724015819026,-54.4459311689611,
-54.4423592036668),.UNSPECIFIED.);
#313=B_SPLINE_CURVE_WITH_KNOTS('',3,(#32437,#32438,#32439,#32440,#32441,
#32442,#32443,#32444,#32445,#32446,#32447,#32448,#32449,#32450,#32451,#32452,
#32453,#32454,#32455,#32456,#32457,#32458,#32459,#32460,#32461,#32462,#32463,
#32464,#32465,#32466,#32467,#32468,#32469,#32470,#32471,#32472),
 .UNSPECIFIED.,.F.,.F.,(4,2,2,2,2,2,2,2,2,2,2,2,2,2,2,2,2,4),(-4.09054085430461,
-4.06552527473558,-3.94671600483119,-3.83195524526434,-3.71304546474063,
-3.59822439924299,-3.4792124302724,-3.36432605817047,-3.24521018614115,
-3.13025373205913,-3.01103221426206,-2.89600112622998,-2.77667220060433,
-2.66156214681765,-2.54212404054857,-2.42693090497668,-2.30738184277471,
-2.20877752486386),.UNSPECIFIED.);
#314=B_SPLINE_CURVE_WITH_KNOTS('',3,(#32473,#32474,#32475,#32476,#32477,
#32478,#32479,#32480,#32481,#32482,#32483,#32484,#32485,#32486,#32487,#32488,
#32489,#32490,#32491,#32492,#32493,#32494,#32495,#32496,#32497,#32498,#32499,
#32500,#32501,#32502,#32503,#32504,#32505,#32506,#32507,#32508),
 .UNSPECIFIED.,.F.,.F.,(4,2,2,2,2,2,2,2,2,2,2,2,2,2,2,2,2,4),(-54.4423592036668,
-54.3243140694799,-54.198001070683,-54.0765353421194,-53.9503795603631,
-53.8290650129986,-53.7030662513386,-53.5819026955948,-53.4560607572401,
-53.3350480036717,-53.2093626919771,-53.0885005512639,-52.9629716697227,
-52.8422599526612,-52.7168873048974,-52.5963258223919,-52.4711092121511,
-52.4675692868415),.UNSPECIFIED.);
#315=B_SPLINE_CURVE_WITH_KNOTS('',3,(#32513,#32514,#32515,#32516,#32517,
#32518,#32519,#32520,#32521,#32522,#32523,#32524,#32525,#32526,#32527,#32528,
#32529,#32530,#32531,#32532,#32533,#32534,#32535,#32536,#32537,#32538,#32539,
#32540,#32541,#32542,#32543,#32544,#32545,#32546,#32547,#32548),
 .UNSPECIFIED.,.F.,.F.,(4,2,2,2,2,2,2,2,2,2,2,2,2,2,2,2,2,4),(-5.96600277725799,
-5.92915238724561,-5.81109356976484,-5.6966089801729,-5.57846094519294,
-5.46396379271469,-5.34572536991432,-5.23120900895501,-5.11287895829174,
-4.99833691252241,-4.87991392178187,-4.76533989948019,-4.64682258434647,
-4.53221049115057,-4.41359739749494,-4.29894134662589,-4.18023095468391,
-4.09054085430461),.UNSPECIFIED.);
#316=B_SPLINE_CURVE_WITH_KNOTS('',3,(#32549,#32550,#32551,#32552,#32553,
#32554,#32555,#32556,#32557,#32558,#32559,#32560,#32561,#32562,#32563,#32564,
#32565,#32566,#32567,#32568,#32569,#32570,#32571,#32572,#32573,#32574,#32575,
#32576,#32577,#32578,#32579,#32580,#32581,#32582,#32583,#32584),
 .UNSPECIFIED.,.F.,.F.,(4,2,2,2,2,2,2,2,2,2,2,2,2,2,2,2,2,4),(-52.4675692868415,
-52.350697775204,-52.2256370063445,-52.1053754260461,-51.980470302529,-51.8603583900464,
-51.7356087159248,-51.6156462824901,-51.4910518618977,-51.3712387187952,
-51.2467993559344,-51.1271353144871,-51.0028508136156,-50.8833356851705,
-50.7592058505875,-50.6398394464999,-50.5158640825307,-50.5123532699249),
 .UNSPECIFIED.);
#317=B_SPLINE_CURVE_WITH_KNOTS('',3,(#32589,#32590,#32591,#32592,#32593,
#32594,#32595,#32596,#32597,#32598,#32599,#32600,#32601,#32602,#32603,#32604,
#32605,#32606,#32607,#32608,#32609,#32610,#32611,#32612,#32613,#32614,#32615,
#32616,#32617,#32618,#32619,#32620,#32621,#32622,#32623,#32624),
 .UNSPECIFIED.,.F.,.F.,(4,2,2,2,2,2,2,2,2,2,2,2,2,2,2,2,2,4),(-7.83850150145777,
-7.78679682633793,-7.6694148644393,-7.55477823480178,-7.4373151677535,-7.32272259398481,
-7.20517736951867,-7.09062168679696,-6.97299330726751,-6.85846731695973,
-6.74075481453558,-6.62625131506633,-6.508453728985,-6.39396554585313,-6.27608190217634,
-6.16160191669192,-6.04363121088209,-5.96600277725799),.UNSPECIFIED.);
#318=B_SPLINE_CURVE_WITH_KNOTS('',3,(#32625,#32626,#32627,#32628,#32629,
#32630,#32631,#32632,#32633,#32634,#32635,#32636,#32637,#32638,#32639,#32640,
#32641,#32642,#32643,#32644,#32645,#32646,#32647,#32648,#32649,#32650,#32651,
#32652,#32653,#32654,#32655,#32656,#32657,#32658,#32659,#32660),
 .UNSPECIFIED.,.F.,.F.,(4,2,2,2,2,2,2,2,2,2,2,2,2,2,2,2,2,4),(-50.5123532699249,
-50.3966462141476,-50.2728251251281,-50.1537556037699,-50.0300885940287,
-49.9111672309698,-49.7876541048099,-49.6688807112583,-49.5455212729371,
-49.4268956600118,-49.3036897137199,-49.1852116924269,-49.0621590422651,
-48.9438284234721,-48.8209288734267,-48.7027454678352,-48.5799988217518,
-48.5765122072365),.UNSPECIFIED.);
#319=B_SPLINE_CURVE_WITH_KNOTS('',3,(#32665,#32666,#32667,#32668,#32669,
#32670,#32671,#32672,#32673,#32674,#32675,#32676,#32677,#32678,#32679,#32680,
#32681,#32682,#32683,#32684,#32685,#32686,#32687,#32688,#32689,#32690,#32691,
#32692,#32693,#32694,#32695,#32696,#32697,#32698,#32699,#32700),
 .UNSPECIFIED.,.F.,.F.,(4,2,2,2,2,2,2,2,2,2,2,2,2,2,2,2,2,4),(-9.71034922447295,
-9.64303824023506,-9.52555324115343,-9.41092911859412,-9.29352551362348,
-9.17885213083062,-9.06152881110041,-8.94679913569492,-8.82955489151035,
-8.71476200974326,-8.59759550315609,-8.48271269177544,-8.36556678591869,
-8.25075580545369,-8.13353254602213,-8.01878660157305,-7.90148461160325,
-7.83850150145777),.UNSPECIFIED.);
#320=B_SPLINE_CURVE_WITH_KNOTS('',3,(#32701,#32702,#32703,#32704,#32705,
#32706,#32707,#32708,#32709,#32710,#32711,#32712,#32713,#32714,#32715,#32716,
#32717,#32718,#32719,#32720,#32721,#32722,#32723,#32724,#32725,#32726,#32727,
#32728,#32729,#32730,#32731,#32732,#32733,#32734,#32735,#32736),
 .UNSPECIFIED.,.F.,.F.,(4,2,2,2,2,2,2,2,2,2,2,2,2,2,2,2,2,4),(-48.5765122072365,
-48.4619624398676,-48.3393685014224,-48.2214789535238,-48.099037526194,
-47.9812946222979,-47.8590055093283,-47.7414090591536,-47.6192720635222,
-47.5018218764501,-47.3798368008302,-47.2625326858626,-47.1406993325827,
-47.0235410982965,-46.9018592692971,-46.7848467237956,-46.6633162205828,
-46.6598453653102),.UNSPECIFIED.);
#321=B_SPLINE_CURVE_WITH_KNOTS('',3,(#32741,#32742,#32743,#32744,#32745,
#32746,#32747,#32748,#32749,#32750,#32751,#32752,#32753,#32754,#32755,#32756,
#32757,#32758,#32759,#32760,#32761,#32762,#32763,#32764,#32765,#32766,#32767,
#32768,#32769,#32770,#32771,#32772,#32773,#32774,#32775,#32776),
 .UNSPECIFIED.,.F.,.F.,(4,2,2,2,2,2,2,2,2,2,2,2,2,2,2,2,2,4),(-11.5834064169039,
-11.5020464607245,-11.383874304121,-11.2693870023825,-11.1513043704658,
-11.0368246707749,-10.9188304411037,-10.8043514485982,-10.6864445575209,
-10.5719592629818,-10.4541386951801,-10.339639999561,-10.2219047744793,
-10.1073855154856,-9.98973467070285,-9.87518765111858,-9.75762022283361,
-9.71034922447295),.UNSPECIFIED.);
#322=B_SPLINE_CURVE_WITH_KNOTS('',3,(#32777,#32778,#32779,#32780,#32781,
#32782,#32783,#32784,#32785,#32786,#32787,#32788,#32789,#32790,#32791,#32792,
#32793,#32794,#32795,#32796,#32797,#32798,#32799,#32800,#32801,#32802,#32803,
#32804,#32805,#32806,#32807,#32808,#32809,#32810,#32811,#32812),
 .UNSPECIFIED.,.F.,.F.,(4,2,2,2,2,2,2,2,2,2,2,2,2,2,2,2,2,4),(-46.6598453653102,
-46.5464491714436,-46.4250697950394,-46.3083480492585,-46.1871196001471,
-46.0705429640784,-45.9494652421493,-45.8330335214402,-45.7121063259267,
-45.5958193254485,-45.4750424548615,-45.3588999786348,-45.2382732306923,
-45.1222750818075,-45.0017982533583,-44.8859442338891,-44.765617120832,
-44.7621473413414),.UNSPECIFIED.);
#323=B_SPLINE_CURVE_WITH_KNOTS('',3,(#32817,#32818,#32819,#32820,#32821,
#32822,#32823,#32824,#32825,#32826,#32827,#32828,#32829,#32830,#32831,#32832,
#32833,#32834,#32835,#32836,#32837,#32838,#32839,#32840,#32841,#32842,#32843,
#32844,#32845,#32846,#32847,#32848,#32849,#32850,#32851,#32852),
 .UNSPECIFIED.,.F.,.F.,(4,2,2,2,2,2,2,2,2,2,2,2,2,2,2,2,2,4),(-13.4602816584202,
-13.3677504690497,-13.2488134515995,-13.1340370217358,-13.0152009606675,
-12.9004810337686,-12.7817442835188,-12.6670754689181,-12.5484364348836,
-12.4338131199453,-12.3152702656808,-12.200686620704,-12.0822384740026,
-11.9676884593812,-11.8493336169002,-11.7348109926818,-11.6165481227706,
-11.5834064169039),.UNSPECIFIED.);
#324=B_SPLINE_CURVE_WITH_KNOTS('',3,(#32853,#32854,#32855,#32856,#32857,
#32858,#32859,#32860,#32861,#32862,#32863,#32864,#32865,#32866,#32867,#32868,
#32869,#32870,#32871,#32872,#32873,#32874,#32875,#32876,#32877,#32878,#32879,
#32880,#32881,#32882,#32883,#32884,#32885,#32886,#32887,#32888),
 .UNSPECIFIED.,.F.,.F.,(4,2,2,2,2,2,2,2,2,2,2,2,2,2,2,2,2,4),(-44.7621473413414,
-44.6499070317433,-44.5297294289392,-44.414163069988,-44.2941347711661,
-44.1787119407951,-44.058832738453,-43.9435532336761,-43.8238229189713,
-43.7086865352514,-43.5891048978864,-43.4741114290031,-43.3546782571008,
-43.239827495009,-43.1205425749804,-43.0058343096585,-42.8866974260598,
-42.8832029855023),.UNSPECIFIED.);
#325=B_SPLINE_CURVE_WITH_KNOTS('',3,(#32893,#32894,#32895,#32896,#32897,
#32898,#32899,#32900,#32901,#32902,#32903,#32904,#32905,#32906,#32907,#32908,
#32909,#32910,#32911,#32912,#32913,#32914,#32915,#32916,#32917,#32918,#32919,
#32920,#32921,#32922,#32923,#32924,#32925,#32926,#32927,#32928),
 .UNSPECIFIED.,.F.,.F.,(4,2,2,2,2,2,2,2,2,2,2,2,2,2,2,2,2,4),(-15.3445125192805,
-15.2439072626969,-15.1240999953518,-15.0087042601519,-14.8890119441516,
-14.773707856193,-14.6541287387574,-14.5389126503526,-14.4194449642385,
-14.3043130251781,-14.1849549957844,-14.0699031470151,-13.9506530000678,
-13.8356769681113,-13.716532937833,-13.601628230118,-13.4825885677557,-13.4602816584202),
 .UNSPECIFIED.);
#326=B_SPLINE_CURVE_WITH_KNOTS('',3,(#32929,#32930,#32931,#32932,#32933,
#32934,#32935,#32936,#32937,#32938,#32939,#32940,#32941,#32942,#32943,#32944,
#32945,#32946,#32947,#32948,#32949,#32950,#32951,#32952,#32953,#32954,#32955,
#32956,#32957,#32958,#32959,#32960,#32961,#32962,#32963,#32964),
 .UNSPECIFIED.,.F.,.F.,(4,2,2,2,2,2,2,2,2,2,2,2,2,2,2,2,2,4),(-42.8832029855023,
-42.7721314453461,-42.6531423807262,-42.5387184701442,-42.4198770048811,
-42.3055949474507,-42.1869008595761,-42.072760435612,-41.9542135006233,
-41.8402144875176,-41.7218144781773,-41.6079566501668,-41.4897033362861,
-41.3759864642018,-41.2578796124106,-41.1443034634091,-41.026342836909,
-41.0227784649616),.UNSPECIFIED.);
#327=B_SPLINE_CURVE_WITH_KNOTS('',3,(#32969,#32970,#32971,#32972,#32973,
#32974,#32975,#32976,#32977,#32978,#32979,#32980,#32981,#32982,#32983,#32984,
#32985,#32986,#32987,#32988,#32989,#32990,#32991,#32992,#32993,#32994,#32995,
#32996,#32997,#32998,#32999,#33000,#33001,#33002,#33003,#33004),
 .UNSPECIFIED.,.F.,.F.,(4,2,2,2,2,2,2,2,2,2,2,2,2,2,2,2,2,4),(-17.239659277801,
-17.1263645119701,-17.012759266358,-16.8965209759557,-16.7758624329729,
-16.6597385709917,-16.5392063880205,-16.4231946561967,-16.3027873240138,
-16.1868852828097,-16.066601246905,-15.9508063077464,-15.8306439707352,
-15.7149533881291,-15.594911112786,-15.4793219763771,-15.3593980893255,
-15.3445125192805),.UNSPECIFIED.);
#328=B_SPLINE_CURVE_WITH_KNOTS('',3,(#33005,#33006,#33007,#33008,#33009,
#33010,#33011,#33012,#33013,#33014,#33015,#33016,#33017,#33018,#33019,#33020,
#33021,#33022,#33023,#33024,#33025,#33026,#33027,#33028,#33029,#33030,#33031,
#33032,#33033,#33034,#33035,#33036,#33037,#33038,#33039,#33040),
 .UNSPECIFIED.,.F.,.F.,(4,2,2,2,2,2,2,2,2,2,2,2,2,2,2,2,2,4),(-41.0227784649616,
-40.912907174184,-40.7950925324838,-40.6817971149564,-40.5641282135893,
-40.4509727955753,-40.333449385797,-40.2204337166497,-40.1030555451148,
-39.9901793688419,-39.8729461772583,-39.7602092321103,-39.6431207568703,
-39.5305227748983,-39.4135787466845,-39.3011194532662,-39.1843195966306,
-39.1806055994443),.UNSPECIFIED.);
#329=B_SPLINE_CURVE_WITH_KNOTS('',3,(#33045,#33046,#33047,#33048,#33049,
#33050,#33051,#33052,#33053,#33054,#33055,#33056,#33057,#33058,#33059,#33060,
#33061,#33062,#33063,#33064,#33065,#33066,#33067,#33068,#33069,#33070,#33071,
#33072,#33073,#33074,#33075,#33076,#33077,#33078,#33079,#33080),
 .UNSPECIFIED.,.F.,.F.,(4,2,2,2,2,2,2,2,2,2,2,2,2,2,2,2,2,4),(-1.8864038091393,
-1.88297644722096,-1.76336400027372,-1.64819816326404,-1.52843681680261,
-1.41312762991872,-1.29321718601239,-1.17776445769835,-1.05770471902055,
-0.942108258372344,-0.821899028143226,-0.706158644847652,-0.585799726779994,
-0.469915231058453,-0.349406429307703,-0.233377631863377,-0.116663456726142,
-1.00000007918766E-6),.UNSPECIFIED.);
#330=B_SPLINE_CURVE_WITH_KNOTS('',3,(#33081,#33082,#33083,#33084,#33085,
#33086,#33087,#33088,#33089,#33090,#33091,#33092,#33093,#33094,#33095,#33096,
#33097,#33098,#33099,#33100,#33101,#33102,#33103,#33104,#33105,#33106,#33107,
#33108,#33109,#33110,#33111,#33112,#33113,#33114,#33115,#33116),
 .UNSPECIFIED.,.F.,.F.,(4,2,2,2,2,2,2,2,2,2,2,2,2,2,2,2,2,4),(-39.1806055994443,
-39.0719987099611,-38.9553427428763,-38.8431599734215,-38.726647606802,
-38.6146026567122,-38.4982335939045,-38.3863261563847,-38.2701000926236,
-38.1583298512582,-38.0422464730891,-37.9306131011166,-37.8146720857803,
-37.7031752453158,-37.5873762600955,-37.4760156012962,-37.360358302823,
-37.3563546200977),.UNSPECIFIED.);
#331=B_SPLINE_CURVE_WITH_KNOTS('',3,(#33121,#33122,#33123,#33124,#33125,
#33126,#33127,#33128,#33129,#33130,#33131,#33132,#33133,#33134,#33135,#33136,
#33137,#33138,#33139,#33140,#33141,#33142,#33143,#33144,#33145,#33146,#33147,
#33148,#33149,#33150,#33151,#33152,#33153,#33154,#33155,#33156),
 .UNSPECIFIED.,.F.,.F.,(4,2,2,2,2,2,2,2,2,2,2,2,2,2,2,2,2,4),(-3.75416502035407,
-3.75072999190081,-3.6323014575776,-3.51827536100683,-3.39969954076099,
-3.28553165907193,-3.16680834748475,-3.05249848111017,-2.93362747400919,
-2.81917542471142,-2.70015651906918,-2.58556208983264,-2.46639508367228,
-2.35165807860358,-2.23234277091081,-2.11746299514582,-1.99799918578683,
-1.8864038091393),.UNSPECIFIED.);
#332=B_SPLINE_CURVE_WITH_KNOTS('',3,(#33157,#33158,#33159,#33160,#33161,
#33162,#33163,#33164,#33165,#33166,#33167,#33168,#33169,#33170,#33171,#33172,
#33173,#33174,#33175,#33176,#33177,#33178,#33179,#33180,#33181,#33182,#33183,
#33184,#33185,#33186,#33187,#33188,#33189,#33190,#33191,#33192),
 .UNSPECIFIED.,.F.,.F.,(4,2,2,2,2,2,2,2,2,2,2,2,2,2,2,2,2,4),(-37.3563546200977,
-37.249133462993,-37.1336174965104,-37.0225280991403,-36.9071530977245,
-36.796198751462,-36.6809643351962,-36.5701446327417,-36.4550504078441,
-36.3443649247666,-36.2294104826689,-36.1188587761375,-36.0040436925138,
-35.8936252999371,-35.7789491336822,-35.6686635712511,-35.554125863407,
-35.5495875005638),.UNSPECIFIED.);
#333=B_SPLINE_CURVE_WITH_KNOTS('',3,(#33197,#33198,#33199,#33200,#33201,
#33202,#33203,#33204,#33205,#33206,#33207,#33208,#33209,#33210,#33211,#33212,
#33213,#33214,#33215,#33216,#33217,#33218,#33219,#33220,#33221,#33222,#33223,
#33224,#33225,#33226,#33227,#33228,#33229,#33230,#33231,#33232),
 .UNSPECIFIED.,.F.,.F.,(4,2,2,2,2,2,2,2,2,2,2,2,2,2,2,2,2,4),(-5.60348486335477,
-5.60001012322833,-5.48275229191451,-5.3698530900914,-5.2524496759028,-5.1394103491365,
-5.02186113203936,-4.90868146518021,-4.79098622750961,-4.67766600793584,
-4.55982453421918,-4.44636355164717,-4.32837562843943,-4.21477367474718,
-4.09663909047685,-3.98289595953924,-3.86461450436494,-3.75416502035407),
 .UNSPECIFIED.);
#334=B_SPLINE_CURVE_WITH_KNOTS('',3,(#33233,#33234,#33235,#33236,#33237,
#33238,#33239,#33240,#33241,#33242,#33243,#33244,#33245,#33246,#33247,#33248,
#33249,#33250,#33251,#33252,#33253,#33254,#33255,#33256,#33257,#33258,#33259,
#33260,#33261,#33262,#33263,#33264,#33265,#33266,#33267,#33268),
 .UNSPECIFIED.,.F.,.F.,(4,2,2,2,2,2,2,2,2,2,2,2,2,2,2,2,2,4),(-35.5495875005638,
-35.4439726245336,-35.3295728971633,-35.2195514508088,-35.1052892058185,
-34.9953989947032,-34.8812737126131,-34.7715141513007,-34.6575252899646,
-34.5478957628118,-34.4340427560889,-34.3245426150538,-34.2108248714336,
-34.1014534337317,-33.9878703349176,-33.8786268805186,-33.765177779973,
-33.7596801984378),.UNSPECIFIED.);
#335=B_SPLINE_CURVE_WITH_KNOTS('',3,(#33273,#33274,#33275,#33276,#33277,
#33278,#33279,#33280,#33281,#33282,#33283,#33284,#33285,#33286,#33287,#33288,
#33289,#33290,#33291,#33292,#33293,#33294,#33295,#33296,#33297,#33298,#33299,
#33300,#33301,#33302,#33303,#33304,#33305,#33306,#33307,#33308),
 .UNSPECIFIED.,.F.,.F.,(4,2,2,2,2,2,2,2,2,2,2,2,2,2,2,2,2,4),(-7.43460594093514,
-7.43103508403617,-7.31493364113757,-7.20314731541428,-7.08690216096382,
-6.97497755039835,-6.85858843734785,-6.74652529782059,-6.62999198343581,
-6.51779007547386,-6.40111232103036,-6.28877140947195,-6.17194897996997,
-6.05946883365251,-5.94250149755131,-5.82988188902049,-5.71276941798947,
-5.60348486335477),.UNSPECIFIED.);
#336=B_SPLINE_CURVE_WITH_KNOTS('',3,(#33309,#33310,#33311,#33312,#33313,
#33314,#33315,#33316,#33317,#33318,#33319,#33320,#33321,#33322,#33323,#33324,
#33325,#33326,#33327,#33328,#33329,#33330,#33331,#33332,#33333,#33334,#33335,
#33336,#33337,#33338,#33339,#33340,#33341,#33342,#33343,#33344),
 .UNSPECIFIED.,.F.,.F.,(4,2,2,2,2,2,2,2,2,2,2,2,2,2,2,2,2,4),(-33.7596801984378,
-33.6560615489264,-33.5427457703844,-33.4337559599665,-33.3205727959264,
-33.2117085575971,-33.0986572677943,-32.9899177039548,-32.8769975138331,
-32.7683816743734,-32.6555917735641,-32.5470986521904,-32.4344381930159,
-32.3260667233496,-32.2135348193684,-32.1052838708055,-31.9928795954187,
-31.9856997234716),.UNSPECIFIED.);
#337=B_SPLINE_CURVE_WITH_KNOTS('',3,(#33349,#33350,#33351,#33352,#33353,
#33354,#33355,#33356,#33357,#33358,#33359,#33360,#33361,#33362,#33363,#33364,
#33365,#33366,#33367,#33368,#33369,#33370,#33371,#33372,#33373,#33374,#33375,
#33376,#33377,#33378,#33379,#33380,#33381,#33382,#33383,#33384),
 .UNSPECIFIED.,.F.,.F.,(4,2,2,2,2,2,2,2,2,2,2,2,2,2,2,2,2,4),(-9.24781408327546,
-9.24404785059257,-9.12908657031949,-9.01839704548918,-8.90329422945898,
-8.79246858929011,-8.67722394216834,-8.56626188992463,-8.45087512400147,
-8.33977637133277,-8.22424720601036,-8.11301147236165,-7.99733963367234,
-7.88596664573283,-7.77015186588773,-7.65864135707772,-7.54268337404331,
-7.43460594093514),.UNSPECIFIED.);
#338=B_SPLINE_CURVE_WITH_KNOTS('',3,(#33385,#33386,#33387,#33388,#33389,
#33390,#33391,#33392,#33393,#33394,#33395,#33396,#33397,#33398,#33399,#33400,
#33401,#33402,#33403,#33404,#33405,#33406,#33407,#33408,#33409,#33410,#33411,
#33412,#33413,#33414,#33415,#33416,#33417,#33418,#33419,#33420),
 .UNSPECIFIED.,.F.,.F.,(4,2,2,2,2,2,2,2,2,2,2,2,2,2,2,2,2,4),(-31.9856997234716,
-31.8847479687416,-31.7724703538844,-31.6644567766188,-31.5523048115627,
-31.4444079330731,-31.3323805633673,-31.224598949686,-31.1126950762707,
-31.0050272046579,-30.8932456831846,-30.7856899364194,-30.6740295768158,
-30.5665842372219,-30.4550438035427,-30.3477070467546,-30.2362852573616,
-30.2262289907375),.UNSPECIFIED.);
#339=B_SPLINE_CURVE_WITH_KNOTS('',3,(#33425,#33426,#33427,#33428,#33429,
#33430,#33431,#33432,#33433,#33434,#33435,#33436,#33437,#33438,#33439,#33440,
#33441,#33442,#33443,#33444,#33445,#33446,#33447,#33448,#33449,#33450,#33451,
#33452,#33453,#33454,#33455,#33456,#33457,#33458,#33459,#33460),
 .UNSPECIFIED.,.F.,.F.,(4,2,2,2,2,2,2,2,2,2,2,2,2,2,2,2,2,4),(-11.0434719915356,
-11.0393361985858,-10.9254954600852,-10.8158829367058,-10.7019033729697,
-10.5921574968065,-10.4780387286715,-10.3681591087133,-10.2539007700906,
-10.1438870302894,-10.0294887673364,-9.91934054557108,-9.8048020159083,
-9.69451896301604,-9.5798398349881,-9.46942161386276,-9.35460156584121,
-9.24781408327546),.UNSPECIFIED.);
#340=B_SPLINE_CURVE_WITH_KNOTS('',3,(#33461,#33462,#33463,#33464,#33465,
#33466,#33467,#33468,#33469,#33470,#33471,#33472,#33473,#33474,#33475,#33476,
#33477,#33478,#33479,#33480,#33481,#33482,#33483,#33484,#33485,#33486,#33487,
#33488,#33489,#33490,#33491,#33492,#33493,#33494,#33495,#33496),
 .UNSPECIFIED.,.F.,.F.,(4,2,2,2,2,2,2,2,2,2,2,2,2,2,2,2,2,4),(-30.2262289907375,
-30.1290551458449,-30.0177506739607,-29.9106251503024,-29.799436624984,
-29.6924135049774,-29.5813395125561,-29.474416478111,-29.3634555641427,
-29.2566301560602,-29.1457808278288,-29.0390504384916,-28.9283111681011,
-28.8216730341374,-28.7110422622252,-28.6044934572187,-28.4939695973085,
-28.4791693611398),.UNSPECIFIED.);
#341=B_SPLINE_CURVE_WITH_KNOTS('',3,(#33501,#33502,#33503,#33504,#33505,
#33506,#33507,#33508,#33509,#33510,#33511,#33512,#33513,#33514,#33515,#33516,
#33517,#33518,#33519,#33520,#33521,#33522,#33523,#33524,#33525,#33526,#33527,
#33528,#33529,#33530,#33531,#33532,#33533,#33534,#33535,#33536),
 .UNSPECIFIED.,.F.,.F.,(4,2,2,2,2,2,2,2,2,2,2,2,2,2,2,2,2,4),(-12.8220763382543,
-12.8172672572996,-12.7045215901235,-12.5959596100703,-12.4830787371158,
-12.3743872228875,-12.2613706246955,-12.1525490180385,-12.0393961966312,
-11.9304439657368,-11.8171544433878,-11.7080710810895,-11.5946443991462,
-11.4854294212359,-11.3718651389923,-11.2625180826477,-11.1488157762692,
-11.0434719915356),.UNSPECIFIED.);
#342=B_SPLINE_CURVE_WITH_KNOTS('',3,(#33537,#33538,#33539,#33540,#33541,
#33542,#33543,#33544,#33545,#33546,#33547,#33548,#33549,#33550,#33551,#33552,
#33553,#33554,#33555,#33556,#33557,#33558,#33559,#33560,#33561,#33562,#33563,
#33564,#33565,#33566,#33567,#33568,#33569,#33570,#33571,#33572),
 .UNSPECIFIED.,.F.,.F.,(4,2,2,2,2,2,2,2,2,2,2,2,2,2,2,2,2,4),(-28.4791693611398,
-28.3875070246388,-28.2770884681434,-28.1707088540541,-28.0603939759199,
-27.9540938629274,-27.8438810278951,-27.7376567686623,-27.6275443380962,
-27.5213920899141,-27.4113784291267,-27.3052941491546,-27.19790732132,-27.0895249674442,
-26.9821403317088,-26.8738980863906,-26.7665104947947,-26.7416213224891),
 .UNSPECIFIED.);
#343=B_SPLINE_CURVE_WITH_KNOTS('',3,(#33577,#33578,#33579,#33580,#33581,
#33582,#33583,#33584,#33585,#33586,#33587,#33588,#33589,#33590,#33591,#33592,
#33593,#33594,#33595,#33596,#33597,#33598,#33599,#33600,#33601,#33602,#33603,
#33604,#33605,#33606,#33607,#33608,#33609,#33610,#33611,#33612),
 .UNSPECIFIED.,.F.,.F.,(4,2,2,2,2,2,2,2,2,2,2,2,2,2,2,2,2,4),(-14.5843512552458,
-14.5783456507132,-14.4666599094173,-14.3591102293336,-14.2472943736648,
-14.1396208394509,-14.0276741285958,-13.9198758885642,-13.8077976145064,
-13.6998738631166,-13.5876633491269,-13.4796133239238,-13.3672699230625,
-13.259092901806,-13.1466159954471,-13.0383112934215,-12.9257002898058,
-12.8220763382543),.UNSPECIFIED.);
#344=B_SPLINE_CURVE_WITH_KNOTS('',3,(#33613,#33614,#33615,#33616,#33617,
#33618,#33619,#33620,#33621,#33622,#33623,#33624,#33625,#33626,#33627,#33628,
#33629,#33630,#33631,#33632,#33633,#33634,#33635,#33636,#33637,#33638,#33639,
#33640,#33641,#33642,#33643,#33644,#33645,#33646,#33647,#33648),
 .UNSPECIFIED.,.F.,.F.,(4,2,2,2,2,2,2,2,2,2,2,2,2,2,2,2,2,4),(-26.7416213224891,
-26.6584069731989,-26.5510113186852,-26.4430449411355,-26.3356361819669,
-26.227805159592,-26.1203783441819,-26.0126806650304,-25.905230956766,-25.7976643726548,
-25.6901870742437,-25.5827490886205,-25.4752396654594,-25.3679275225695,
-25.2603816246109,-25.1531923002647,-25.0456057818525,-25.0095548405133),
 .UNSPECIFIED.);
#345=B_SPLINE_CURVE_WITH_KNOTS('',3,(#33653,#33654,#33655,#33656,#33657,
#33658,#33659,#33660,#33661,#33662,#33663,#33664,#33665,#33666,#33667,#33668,
#33669,#33670,#33671,#33672,#33673,#33674,#33675,#33676,#33677,#33678,#33679,
#33680,#33681,#33682,#33683,#33684,#33685,#33686,#33687,#33688),
 .UNSPECIFIED.,.F.,.F.,(4,2,2,2,2,2,2,2,2,2,2,2,2,2,2,2,2,4),(-16.3313912073472,
-16.3233072623272,-16.2126313466116,-16.1060351236341,-15.9952363748485,
-15.8885252103429,-15.7776025742812,-15.6707751111625,-15.5597275770881,
-15.4527825369049,-15.3416091365489,-15.234545314564,-15.1232451209766,
-15.0160613815074,-14.9046335077918,-14.7973287798048,-14.6857723777617,
-14.5843512552458),.UNSPECIFIED.);
#346=B_SPLINE_CURVE_WITH_KNOTS('',3,(#33689,#33690,#33691,#33692,#33693,
#33694,#33695,#33696,#33697,#33698,#33699,#33700,#33701,#33702,#33703,#33704,
#33705,#33706,#33707,#33708,#33709,#33710,#33711,#33712,#33713,#33714,#33715,
#33716,#33717,#33718,#33719,#33720,#33721,#33722,#33723,#33724),
 .UNSPECIFIED.,.F.,.F.,(4,2,2,2,2,2,2,2,2,2,2,2,2,2,2,2,2,4),(-25.0095548405133,
-24.9385359760839,-24.8309049132433,-24.7239510451331,-24.6162717498346,
-24.5094299547549,-24.4016989857275,-24.2949651152216,-24.1871792849693,
-24.0805489094451,-23.9727052872149,-23.866173701574,-23.7582696121387,
-23.6518318444031,-23.5438648626452,-23.4375156855802,-23.3294836269944,
-23.279856360261),.UNSPECIFIED.);
#347=B_SPLINE_CURVE_WITH_KNOTS('',3,(#33729,#33730,#33731,#33732,#33733,
#33734,#33735,#33736,#33737,#33738,#33739,#33740,#33741,#33742,#33743,#33744,
#33745,#33746,#33747,#33748,#33749,#33750,#33751,#33752,#33753,#33754,#33755,
#33756,#33757,#33758,#33759,#33760,#33761,#33762,#33763,#33764),
 .UNSPECIFIED.,.F.,.F.,(4,2,2,2,2,2,2,2,2,2,2,2,2,2,2,2,2,4),(-18.0648505045038,
-18.0532589064653,-17.9435223335512,-17.8377855197036,-17.7279361558219,
-17.6220987648756,-17.5121352015826,-17.4061950390038,-17.2961159095967,
-17.1900709080828,-17.0798748891579,-16.973723101753,-16.8634089142914,
-16.7571485076961,-16.6467149177216,-16.5403441658243,-16.4297899846795,
-16.3313912073472),.UNSPECIFIED.);
#348=B_SPLINE_CURVE_WITH_KNOTS('',3,(#33765,#33766,#33767,#33768,#33769,
#33770,#33771,#33772,#33773,#33774,#33775,#33776,#33777,#33778,#33779,#33780,
#33781,#33782,#33783,#33784,#33785,#33786,#33787,#33788,#33789,#33790,#33791,
#33792,#33793,#33794,#33795,#33796,#33797,#33798,#33799,#33800),
 .UNSPECIFIED.,.F.,.F.,(4,2,2,2,2,2,2,2,2,2,2,2,2,2,2,2,2,4),(-23.279856360261,
-23.2232175726558,-23.1151184800197,-23.008929857083,-22.9007619836687,
-22.7946448568816,-22.6864066321872,-22.5803544617475,-22.4720444874161,
-22.3660510309762,-22.2576680642617,-22.1517269410299,-22.0432698589546,
-21.9373745771184,-21.8288423511376,-21.7229863362235,-21.6143780072058,
-21.5505504016126),.UNSPECIFIED.);
#349=B_SPLINE_CURVE_WITH_KNOTS('',3,(#33805,#33806,#33807,#33808,#33809,
#33810,#33811,#33812,#33813,#33814,#33815,#33816,#33817,#33818,#33819,#33820,
#33821,#33822,#33823,#33824,#33825,#33826,#33827,#33828,#33829,#33830,#33831,
#33832,#33833,#33834,#33835,#33836,#33837,#33838,#33839,#33840),
 .UNSPECIFIED.,.F.,.F.,(4,2,2,2,2,2,2,2,2,2,2,2,2,2,2,2,2,4),(-19.78711920009,
-19.7698563339641,-19.6609673312242,-19.5559385091401,-19.4469491127778,
-19.3418427059215,-19.2327512982833,-19.1275638383411,-19.0183688100397,
-18.9130970119967,-18.8037967682599,-18.6984375240007,-18.5890304904218,
-18.4835808619618,-18.374065489621,-18.2685227020834,-18.1588974720274,
-18.0648505045038),.UNSPECIFIED.);
#350=B_SPLINE_CURVE_WITH_KNOTS('',3,(#33841,#33842,#33843,#33844,#33845,
#33846,#33847,#33848,#33849,#33850,#33851,#33852,#33853,#33854,#33855,#33856,
#33857,#33858,#33859,#33860,#33861,#33862,#33863,#33864,#33865,#33866,#33867,
#33868,#33869,#33870,#33871,#33872,#33873,#33874,#33875,#33876),
 .UNSPECIFIED.,.F.,.F.,(4,2,2,2,2,2,2,2,2,2,2,2,2,2,2,2,2,4),(-21.5505504016126,
-21.5085546309099,-21.3998692850715,-21.2940718940921,-21.1853086404519,
-21.0795305848717,-20.9706885347095,-20.8649231955014,-20.7560014442002,
-20.6502422594702,-20.5412398710138,-20.4354803606454,-20.326396354935,
-20.2206301433518,-20.1114634864004,-20.0056843232298,-19.8964339201928,
-19.8198937274011),.UNSPECIFIED.);
#351=B_SPLINE_CURVE_WITH_KNOTS('',3,(#33881,#33882,#33883,#33884,#33885,
#33886,#33887,#33888,#33889,#33890,#33891,#33892,#33893,#33894,#33895,#33896,
#33897,#33898,#33899,#33900,#33901,#33902,#33903,#33904,#33905,#33906,#33907,
#33908,#33909,#33910,#33911,#33912,#33913,#33914,#33915,#33916),
 .UNSPECIFIED.,.F.,.F.,(4,2,2,2,2,2,2,2,2,2,2,2,2,2,2,2,2,4),(-21.5013063400995,
-21.4754634098236,-21.3673207575314,-21.2627641819231,-21.1545334840107,
-21.0499342013519,-20.9416140435757,-20.8369669813094,-20.7285558978255,
-20.6238561866133,-20.5153526667363,-20.4105956426116,-20.3019981382347,
-20.1971793430677,-20.0884862764785,-19.983601456934,-19.8748112287902,
-19.78711920009),.UNSPECIFIED.);
#352=B_SPLINE_CURVE_WITH_KNOTS('',3,(#33917,#33918,#33919,#33920,#33921,
#33922,#33923,#33924,#33925,#33926,#33927,#33928,#33929,#33930,#33931,#33932,
#33933,#33934,#33935,#33936,#33937,#33938,#33939,#33940,#33941,#33942,#33943,
#33944,#33945,#33946,#33947,#33948,#33949,#33950,#33951,#33952),
 .UNSPECIFIED.,.F.,.F.,(4,2,2,2,2,2,2,2,2,2,2,2,2,2,2,2,2,4),(-19.8198937274011,
-19.790635698669,-19.6813003895888,-19.5754771626003,-19.4660557206704,
-19.3602017144112,-19.2506928465104,-19.1448024717488,-19.0352048209613,
-18.9292726819867,-18.8195848317987,-18.7136057331458,-18.6038262130013,
-18.4977951640837,-18.3879224559889,-18.2818346737982,-18.171867219676,
-18.0853560917774),.UNSPECIFIED.);
#353=B_SPLINE_CURVE_WITH_KNOTS('',3,(#33957,#33958,#33959,#33960,#33961,
#33962,#33963,#33964,#33965,#33966,#33967,#33968,#33969,#33970,#33971,#33972,
#33973,#33974,#33975,#33976,#33977,#33978,#33979,#33980,#33981,#33982,#33983,
#33984,#33985,#33986,#33987,#33988,#33989,#33990,#33991,#33992),
 .UNSPECIFIED.,.F.,.F.,(4,2,2,2,2,2,2,2,2,2,2,2,2,2,2,2,2,4),(-23.2107745567376,
-23.1731702436624,-23.0656884326081,-22.9612688279359,-22.8537080700236,
-22.7492927201854,-22.6416520801072,-22.5372346143341,-22.4295131102289,
-22.3250872669613,-22.2172838615344,-22.1128435082049,-22.0049571026223,
-21.9004962531731,-21.7925256835865,-21.6880385136444,-21.5799825501392,
-21.5013063400995),.UNSPECIFIED.);
#354=B_SPLINE_CURVE_WITH_KNOTS('',3,(#33993,#33994,#33995,#33996,#33997,
#33998,#33999,#34000,#34001,#34002,#34003,#34004,#34005,#34006,#34007,#34008,
#34009,#34010,#34011,#34012,#34013,#34014,#34015,#34016,#34017,#34018,#34019,
#34020,#34021,#34022,#34023,#34024,#34025,#34026,#34027,#34028),
 .UNSPECIFIED.,.F.,.F.,(4,2,2,2,2,2,2,2,2,2,2,2,2,2,2,2,2,4),(-18.0853560917774,
-18.0657181297179,-17.9556543392361,-17.849439574889,-17.739277833515,-17.6329932339954,
-17.5227319110613,-17.4163735181846,-17.3060109747783,-17.1995750286937,
-17.0891096252262,-16.9825925592995,-16.8720226626297,-16.7654210976342,
-16.6547450876619,-16.5480558254253,-16.437272101092,-16.343613120543),
 .UNSPECIFIED.);
#355=B_SPLINE_CURVE_WITH_KNOTS('',3,(#34033,#34034,#34035,#34036,#34037,
#34038,#34039,#34040,#34041,#34042,#34043,#34044,#34045,#34046,#34047,#34048,
#34049,#34050,#34051,#34052,#34053,#34054,#34055,#34056,#34057,#34058,#34059,
#34060,#34061,#34062,#34063,#34064,#34065,#34066,#34067,#34068),
 .UNSPECIFIED.,.F.,.F.,(4,2,2,2,2,2,2,2,2,2,2,2,2,2,2,2,2,4),(-24.9183017004615,
-24.8665828889058,-24.759699498358,-24.655011382145,-24.5480567922721,-24.4434248725477,
-24.3363978924142,-24.2318158355854,-24.1247153854245,-24.0201767561447,
-23.9130018423663,-23.8085001317139,-23.7012498224075,-23.5967784763971,
-23.4894518779437,-23.3850043259115,-23.2776005612417,-23.2107745567376),
 .UNSPECIFIED.);
#356=B_SPLINE_CURVE_WITH_KNOTS('',3,(#34069,#34070,#34071,#34072,#34073,
#34074,#34075,#34076,#34077,#34078,#34079,#34080,#34081,#34082,#34083,#34084,
#34085,#34086,#34087,#34088,#34089,#34090,#34091,#34092,#34093,#34094,#34095,
#34096,#34097,#34098,#34099,#34100,#34101,#34102,#34103,#34104),
 .UNSPECIFIED.,.F.,.F.,(4,2,2,2,2,2,2,2,2,2,2,2,2,2,2,2,2,4),(-16.343613120543,
-16.3304921177346,-16.2195991023927,-16.1127255412756,-16.0017216874107,
-15.8947518519012,-15.7836356452055,-15.67656699135,-15.5653369541634,-15.4581670833479,
-15.34682177749,-15.2395484291535,-15.128086458181,-15.020707502638,-14.9091275135678,
-14.8016409449841,-14.6899416295231,-14.5913702832229),.UNSPECIFIED.);
#357=B_SPLINE_CURVE_WITH_KNOTS('',3,(#34109,#34110,#34111,#34112,#34113,
#34114,#34115,#34116,#34117,#34118,#34119,#34120,#34121,#34122,#34123,#34124,
#34125,#34126,#34127,#34128,#34129,#34130,#34131,#34132,#34133,#34134,#34135,
#34136,#34137,#34138,#34139,#34140,#34141,#34142,#34143,#34144),
 .UNSPECIFIED.,.F.,.F.,(4,2,2,2,2,2,2,2,2,2,2,2,2,2,2,2,2,4),(-26.6257527730801,
-26.5595330341774,-26.4531553556633,-26.3478065454012,-26.241373857084,
-26.136125938725,-26.0296354188406,-25.9244836714166,-25.817932749385,-25.71287219139,
-25.6062585413088,-25.5012839430023,-25.3946054731675,-25.289711371732,
-25.1829662104685,-25.0781469278626,-24.9713334060639,-24.9183017004615),
 .UNSPECIFIED.);
#358=B_SPLINE_CURVE_WITH_KNOTS('',3,(#34145,#34146,#34147,#34148,#34149,
#34150,#34151,#34152,#34153,#34154,#34155,#34156,#34157,#34158,#34159,#34160,
#34161,#34162,#34163,#34164,#34165,#34166,#34167,#34168,#34169,#34170,#34171,
#34172,#34173,#34174,#34175,#34176,#34177,#34178,#34179,#34180),
 .UNSPECIFIED.,.F.,.F.,(4,2,2,2,2,2,2,2,2,2,2,2,2,2,2,2,2,4),(-14.5913702832229,
-14.5823455590806,-14.4705256544105,-14.36281830369,-14.2508765928518,-14.1430562874532,
-14.0309915993766,-13.9230567627926,-13.8108679720163,-13.7028171197676,
-13.5905031458913,-13.4823348799311,-13.3698946868393,-13.2616076902261,
-13.1490402851216,-13.0406333169609,-12.9279377492393,-12.8259818435135),
 .UNSPECIFIED.);
#359=B_SPLINE_CURVE_WITH_KNOTS('',3,(#34185,#34186,#34187,#34188,#34189,
#34190,#34191,#34192,#34193,#34194,#34195,#34196,#34197,#34198,#34199,#34200,
#34201,#34202,#34203,#34204,#34205,#34206,#34207,#34208,#34209,#34210,#34211,
#34212,#34213,#34214,#34215,#34216,#34217,#34218,#34219,#34220),
 .UNSPECIFIED.,.F.,.F.,(4,2,2,2,2,2,2,2,2,2,2,2,2,2,2,2,2,4),(-28.3349853381226,
-28.2567214667917,-28.1486990903277,-28.0442274779986,-27.9362901024047,
-27.8318430252495,-27.7239894411045,-27.619561023636,-27.5117900874993,
-27.4073742969973,-27.2996849296331,-27.1952755920485,-27.0876667741569,
-26.98325759234,-26.8757283576048,-26.7713129316046,-26.6649871874145,-26.6257527730801),
 .UNSPECIFIED.);
#360=B_SPLINE_CURVE_WITH_KNOTS('',3,(#34221,#34222,#34223,#34224,#34225,
#34226,#34227,#34228,#34229,#34230,#34231,#34232,#34233,#34234,#34235,#34236,
#34237,#34238,#34239,#34240,#34241,#34242,#34243,#34244,#34245,#34246,#34247,
#34248,#34249,#34250,#34251,#34252,#34253,#34254,#34255,#34256),
 .UNSPECIFIED.,.F.,.F.,(4,2,2,2,2,2,2,2,2,2,2,2,2,2,2,2,2,4),(-12.8259818435135,
-12.8194096398901,-12.7065849998897,-12.5979346464299,-12.4849800640805,
-12.3762064260245,-12.263121069424,-12.1542231646846,-12.0410062386213,
-11.9319831397061,-11.8186338841484,-11.7094847145824,-11.5960024031513,
-11.4867263341141,-11.3731102725527,-11.2637065197223,-11.1499560443741,
-11.0455738233171),.UNSPECIFIED.);
#361=B_SPLINE_CURVE_WITH_KNOTS('',3,(#34261,#34262,#34263,#34264,#34265,
#34266,#34267,#34268,#34269,#34270,#34271,#34272,#34273,#34274,#34275,#34276,
#34277,#34278,#34279,#34280,#34281,#34282,#34283,#34284,#34285,#34286,#34287,
#34288,#34289,#34290,#34291,#34292,#34293,#34294,#34295,#34296),
 .UNSPECIFIED.,.F.,.F.,(4,2,2,2,2,2,2,2,2,2,2,2,2,2,2,2,2,4),(-30.0488168723486,
-29.9614261880733,-29.8526732714368,-29.7478161474901,-29.6391598895154,
-29.5343674916912,-29.4258062989781,-29.3210743110622,-29.2126066143105,
-29.1079305148352,-28.9995547767932,-28.8949298384416,-28.7866445616262,
-28.6820658522004,-28.5738695861414,-28.4693319712739,-28.3612233190107,
-28.3349853381226),.UNSPECIFIED.);
#362=B_SPLINE_CURVE_WITH_KNOTS('',3,(#34297,#34298,#34299,#34300,#34301,
#34302,#34303,#34304,#34305,#34306,#34307,#34308,#34309,#34310,#34311,#34312,
#34313,#34314,#34315,#34316,#34317,#34318,#34319,#34320,#34321,#34322,#34323,
#34324,#34325,#34326,#34327,#34328,#34329,#34330,#34331,#34332),
 .UNSPECIFIED.,.F.,.F.,(4,2,2,2,2,2,2,2,2,2,2,2,2,2,2,2,2,4),(-11.0455738233171,
-11.0404238649656,-10.926538341273,-10.8168770312622,-10.7028558522917,
-10.5930647438152,-10.4789073288171,-10.3689857877375,-10.2546915807464,
-10.1446390043743,-10.0302074728524,-9.92002328781561,-9.80545392134402,
-9.6951375815958,-9.58042989061549,-9.46998087557298,-9.35513439017667,
-9.24889674820361),.UNSPECIFIED.);
#363=B_SPLINE_CURVE_WITH_KNOTS('',3,(#34337,#34338,#34339,#34340,#34341,
#34342,#34343,#34344,#34345,#34346,#34347,#34348,#34349,#34350,#34351,#34352,
#34353,#34354,#34355,#34356,#34357,#34358,#34359,#34360,#34361,#34362,#34363,
#34364,#34365,#34366,#34367,#34368,#34369,#34370,#34371,#34372),
 .UNSPECIFIED.,.F.,.F.,(4,2,2,2,2,2,2,2,2,2,2,2,2,2,2,2,2,4),(-31.7705993303663,
-31.6767622191949,-31.5671782708775,-31.4616714603343,-31.3521968961548,
-31.2467823972444,-31.137415688639,-31.0320906769712,-30.9228302667284,
-30.8175917526226,-30.7084360595614,-30.6032808810914,-30.4942283053797,
-30.3891531217064,-30.2802020507996,-30.175203335912,-30.0663521510776,
-30.0488168723486),.UNSPECIFIED.);
#364=B_SPLINE_CURVE_WITH_KNOTS('',3,(#34373,#34374,#34375,#34376,#34377,
#34378,#34379,#34380,#34381,#34382,#34383,#34384,#34385,#34386,#34387,#34388,
#34389,#34390,#34391,#34392,#34393,#34394,#34395,#34396,#34397,#34398,#34399,
#34400,#34401,#34402,#34403,#34404,#34405,#34406,#34407,#34408),
 .UNSPECIFIED.,.F.,.F.,(4,2,2,2,2,2,2,2,2,2,2,2,2,2,2,2,2,4),(-9.24889674820361,
-9.24455220298207,-9.129566471758,-9.01885063765458,-8.90372522658263,-8.79287529139848,
-8.67760978279836,-8.56662531153122,-8.45121930306199,-8.34009987855865,
-8.22455298226888,-8.11329820399297,-7.99761004542018,-7.88621952830298,
-7.77038974562149,-7.65886311898992,-7.54289136220465,-7.4351272610323),
 .UNSPECIFIED.);
#365=B_SPLINE_CURVE_WITH_KNOTS('',3,(#34413,#34414,#34415,#34416,#34417,
#34418,#34419,#34420,#34421,#34422,#34423,#34424,#34425,#34426,#34427,#34428,
#34429,#34430,#34431,#34432,#34433,#34434,#34435,#34436,#34437,#34438,#34439,
#34440,#34441,#34442,#34443,#34444,#34445,#34446,#34447,#34448),
 .UNSPECIFIED.,.F.,.F.,(4,2,2,2,2,2,2,2,2,2,2,2,2,2,2,2,2,4),(-33.5034635227188,
-33.4052107333307,-33.2947011786237,-33.1883716652711,-33.0779823310297,
-32.9717626329138,-32.8614923165309,-32.7553806751721,-32.6452281287722,
-32.539222676534,-32.4291866073623,-32.3232853609123,-32.2133644321201,
-32.1075652856769,-31.9977581175486,-31.8920588359429,-31.7823640076096,
-31.7705993303663),.UNSPECIFIED.);
#366=B_SPLINE_CURVE_WITH_KNOTS('',3,(#34449,#34450,#34451,#34452,#34453,
#34454,#34455,#34456,#34457,#34458,#34459,#34460,#34461,#34462,#34463,#34464,
#34465,#34466,#34467,#34468,#34469,#34470,#34471,#34472,#34473,#34474,#34475,
#34476,#34477,#34478,#34479,#34480,#34481,#34482,#34483,#34484),
 .UNSPECIFIED.,.F.,.F.,(4,2,2,2,2,2,2,2,2,2,2,2,2,2,2,2,2,4),(-7.4351272610323,
-7.43122826878166,-7.3151141989672,-7.20331429393996,-7.08705758252279,
-6.97512053267358,-6.85872086075526,-6.74664634365187,-6.63010340137265,
-6.51789110461339,-6.40120459055263,-6.28885421106297,-6.1720238316763,
-6.05953507505318,-5.94256054414322,-5.82993312404414,-5.71281416226422,
-5.60370818057896),.UNSPECIFIED.);
#367=B_SPLINE_CURVE_WITH_KNOTS('',3,(#34489,#34490,#34491,#34492,#34493,
#34494,#34495,#34496,#34497,#34498,#34499,#34500,#34501,#34502,#34503,#34504,
#34505,#34506,#34507,#34508,#34509,#34510,#34511,#34512,#34513,#34514,#34515,
#34516,#34517,#34518,#34519,#34520,#34521,#34522,#34523,#34524),
 .UNSPECIFIED.,.F.,.F.,(4,2,2,2,2,2,2,2,2,2,2,2,2,2,2,2,2,4),(-35.249829569753,
-35.1485139120437,-35.037004621044,-34.92974441726,-34.8183633878881,-34.7112238400841,
-34.5999702123749,-34.4929502300442,-34.3818231049099,-34.2749215315651,
-34.1639199694648,-34.0571355781546,-33.9462585978623,-33.8395900864318,
-33.7288366639292,-33.62228265002,-33.5116517175468,-33.5034635227188),
 .UNSPECIFIED.);
#368=B_SPLINE_CURVE_WITH_KNOTS('',3,(#34525,#34526,#34527,#34528,#34529,
#34530,#34531,#34532,#34533,#34534,#34535,#34536,#34537,#34538,#34539,#34540,
#34541,#34542,#34543,#34544,#34545,#34546,#34547,#34548,#34549,#34550,#34551,
#34552,#34553,#34554,#34555,#34556,#34557,#34558,#34559,#34560),
 .UNSPECIFIED.,.F.,.F.,(4,2,2,2,2,2,2,2,2,2,2,2,2,2,2,2,2,4),(-5.60370818057896,
-5.60004779983838,-5.48278413422669,-5.36987855758419,-5.25246992112663,
-5.13942486484497,-5.02187099606657,-4.90868620073017,-4.79098684331131,
-4.67766205508293,-4.55981695750053,-4.44635192772174,-4.32836084291342,
-4.21475532773292,-4.09661801278269,-3.98287177280955,-3.86458798865395,
-3.75424064676522),.UNSPECIFIED.);
#369=B_SPLINE_CURVE_WITH_KNOTS('',3,(#34565,#34566,#34567,#34568,#34569,
#34570,#34571,#34572,#34573,#34574,#34575,#34576,#34577,#34578,#34579,#34580,
#34581,#34582,#34583,#34584,#34585,#34586,#34587,#34588,#34589,#34590,#34591,
#34592,#34593,#34594,#34595,#34596,#34597,#34598,#34599,#34600),
 .UNSPECIFIED.,.F.,.F.,(4,2,2,2,2,2,2,2,2,2,2,2,2,2,2,2,2,4),(-37.0113773411355,
-36.9078345617278,-36.7952724338226,-36.6870143515743,-36.5745861319252,
-36.4664555141774,-36.3541606029054,-36.2461567536563,-36.1339945235731,
-36.0261167084853,-35.9140865036374,-35.8063339472929,-35.6944350814774,
-35.5868069644492,-35.4750387197121,-35.3675341754426,-35.2558958005675,
-35.249829569753),.UNSPECIFIED.);
#370=B_SPLINE_CURVE_WITH_KNOTS('',3,(#34601,#34602,#34603,#34604,#34605,
#34606,#34607,#34608,#34609,#34610,#34611,#34612,#34613,#34614,#34615,#34616,
#34617,#34618,#34619,#34620,#34621,#34622,#34623,#34624,#34625,#34626,#34627,
#34628,#34629,#34630,#34631,#34632,#34633,#34634,#34635,#34636),
 .UNSPECIFIED.,.F.,.F.,(4,2,2,2,2,2,2,2,2,2,2,2,2,2,2,2,2,4),(-3.75424064676522,
-3.7507007886352,-3.63227029978869,-3.51824190830858,-3.39966448260667,
-3.28549467180693,-3.16677008016633,-3.05245862548541,-2.9335866416799,
-2.81913332161029,-2.70011372206143,-2.58551831792344,-2.4663508815052,
-2.35161317723662,-2.23229768509284,-2.11741746705273,-1.99795370242702,
-1.88641723413452),.UNSPECIFIED.);
#371=B_SPLINE_CURVE_WITH_KNOTS('',3,(#34641,#34642,#34643,#34644,#34645,
#34646,#34647,#34648,#34649,#34650,#34651,#34652,#34653,#34654,#34655,#34656,
#34657,#34658,#34659,#34660,#34661,#34662,#34663,#34664,#34665,#34666,#34667,
#34668,#34669,#34670,#34671,#34672,#34673,#34674,#34675,#34676),
 .UNSPECIFIED.,.F.,.F.,(4,2,2,2,2,2,2,2,2,2,2,2,2,2,2,2,2,4),(-38.7892191392797,
-38.6839424852085,-38.5702903229789,-38.4609912918716,-38.3474770154212,
-38.2383099131738,-38.1249330935883,-38.0158974509548,-37.9026576421227,
-37.7937529679977,-37.6806497055188,-37.5718754853313,-37.4589082853741,
-37.350263979368,-37.2374323374757,-37.1289173788685,-37.0162207687146,
-37.0113773411355),.UNSPECIFIED.);
#372=B_SPLINE_CURVE_WITH_KNOTS('',3,(#34677,#34678,#34679,#34680,#34681,
#34682,#34683,#34684,#34685,#34686,#34687,#34688,#34689,#34690,#34691,#34692,
#34693,#34694,#34695,#34696,#34697,#34698,#34699,#34700,#34701,#34702,#34703,
#34704,#34705,#34706,#34707,#34708,#34709,#34710,#34711,#34712),
 .UNSPECIFIED.,.F.,.F.,(4,2,2,2,2,2,2,2,2,2,2,2,2,2,2,2,2,4),(-1.88641723413452,
-1.88293076106139,-1.7633185725453,-1.6481527558743,-1.52839186711642,-1.41308290859082,
-1.29317310822235,-1.17772080218214,-1.0576618803597,-0.942066022770442,
-0.821857771055554,-0.706118159380599,-0.585760370627368,-0.469876803708684,
-0.349369271959349,-0.2333415499069,-0.116644727036975,-1.00000007829948E-6),
 .UNSPECIFIED.);
#373=B_SPLINE_CURVE_WITH_KNOTS('',3,(#34717,#34718,#34719,#34720,#34721,
#34722,#34723,#34724,#34725,#34726,#34727,#34728,#34729,#34730,#34731,#34732,
#34733,#34734,#34735,#34736,#34737,#34738,#34739,#34740,#34741,#34742,#34743,
#34744,#34745,#34746,#34747,#34748,#34749,#34750,#34751,#34752),
 .UNSPECIFIED.,.F.,.F.,(4,2,2,2,2,2,2,2,2,2,2,2,2,2,2,2,2,4),(-40.5840903660244,
-40.4773621269581,-40.362593181144,-40.2522239979018,-40.1375958644443,
-40.0273617375903,-39.9128740918523,-39.8027746806653,-39.6884271877721,
-39.578462139203,-39.4642544533322,-39.3544234010816,-39.2403551647114,
-39.1306577282415,-39.0167285713529,-38.9071643548272,-38.793373894062,
-38.7892191392797),.UNSPECIFIED.);
#374=B_SPLINE_CURVE_WITH_KNOTS('',3,(#34753,#34754,#34755,#34756,#34757,
#34758,#34759,#34760,#34761,#34762,#34763,#34764,#34765,#34766,#34767,#34768,
#34769,#34770,#34771,#34772,#34773,#34774,#34775,#34776,#34777,#34778,#34779,
#34780,#34781,#34782,#34783,#34784,#34785,#34786,#34787,#34788),
 .UNSPECIFIED.,.F.,.F.,(4,2,2,2,2,2,2,2,2,2,2,2,2,2,2,2,2,4),(-7.49403777883289,
-7.41673253643292,-7.33806391100879,-7.22291817343654,-7.10721789492446,
-6.9919436003314,-6.87628697708284,-6.7608805786065,-6.64526315078516,-6.52972139809384,
-6.41413848618954,-6.2984584175721,-6.18290514374928,-6.06708407617364,
-5.95155538779921,-5.83559090525242,-5.72008160003587,-5.63205117539197),
 .UNSPECIFIED.);
#375=B_SPLINE_CURVE_WITH_KNOTS('',3,(#34793,#34794,#34795,#34796,#34797,
#34798,#34799,#34800,#34801,#34802,#34803,#34804,#34805,#34806,#34807,#34808,
#34809,#34810,#34811,#34812,#34813,#34814,#34815,#34816,#34817,#34818,#34819,
#34820,#34821,#34822,#34823,#34824,#34825,#34826,#34827,#34828),
 .UNSPECIFIED.,.F.,.F.,(4,2,2,2,2,2,2,2,2,2,2,2,2,2,2,2,2,4),(-42.3964944372798,
-42.2884719551661,-42.1725658485947,-42.0611051693233,-41.9453421761501,
-41.834018927021,-41.7183987834928,-41.6072126959141,-41.4917351323945,
-41.3806859308888,-41.2653506714268,-41.1544380731067,-41.0392448349755,
-40.9284685489806,-40.8134170421869,-40.7027767690798,-40.5878666958406,
-40.5840903660244),.UNSPECIFIED.);
#376=B_SPLINE_CURVE_WITH_KNOTS('',3,(#34829,#34830,#34831,#34832,#34833,
#34834,#34835,#34836,#34837,#34838,#34839,#34840,#34841,#34842,#34843,#34844,
#34845,#34846,#34847,#34848,#34849,#34850,#34851,#34852,#34853,#34854,#34855,
#34856,#34857,#34858,#34859,#34860,#34861,#34862,#34863,#34864),
 .UNSPECIFIED.,.F.,.F.,(4,2,2,2,2,2,2,2,2,2,2,2,2,2,2,2,2,4),(-5.63205117539197,
-5.60397154046265,-5.48847629264442,-5.37221873379735,-5.25673212084505,
-5.14032536534831,-5.02484189465898,-4.90828445456914,-4.79279858972369,
-4.67608917084805,-4.56059535702089,-4.44373284322738,-4.32822553141539,
-4.21120896913925,-4.09280065613099,-3.97853814728176,-3.86002416031382,
-3.76459284001855),.UNSPECIFIED.);
#377=B_SPLINE_CURVE_WITH_KNOTS('',3,(#34869,#34870,#34871,#34872,#34873,
#34874,#34875,#34876,#34877,#34878,#34879,#34880,#34881,#34882,#34883,#34884,
#34885,#34886,#34887,#34888,#34889,#34890,#34891,#34892,#34893,#34894,#34895,
#34896,#34897,#34898,#34899,#34900,#34901,#34902,#34903,#34904),
 .UNSPECIFIED.,.F.,.F.,(4,2,2,2,2,2,2,2,2,2,2,2,2,2,2,2,2,4),(-44.2267979604378,
-44.1175661329609,-44.0005062076739,-43.8879370974253,-43.7710222273151,
-43.6585925002181,-43.5418224560014,-43.4295318834992,-43.3129064326076,
-43.2007547823476,-43.0842736886739,-42.9722607242104,-42.8559237478365,
-42.7440492283116,-42.6278561252182,-42.5161198050192,-42.4000703267746,
-42.3964944372798),.UNSPECIFIED.);
#378=B_SPLINE_CURVE_WITH_KNOTS('',3,(#34905,#34906,#34907,#34908,#34909,
#34910,#34911,#34912,#34913,#34914,#34915,#34916,#34917,#34918,#34919,#34920,
#34921,#34922,#34923,#34924,#34925,#34926,#34927,#34928,#34929,#34930,#34931,
#34932,#34933,#34934,#34935,#34936,#34937,#34938,#34939,#34940),
 .UNSPECIFIED.,.F.,.F.,(4,2,2,2,2,2,2,2,2,2,2,2,2,2,2,2,2,4),(-3.76459284001855,
-3.74568575401325,-3.62706433685894,-3.51264581413931,-3.39391520319397,
-3.27941255749952,-3.16057098984337,-3.04598042137986,-2.927026142345,-2.81234405171484,
-2.69327532186702,-2.57849830314693,-2.45931340462086,-2.34443823802314,
-2.22513548017335,-2.11015912441778,-1.99073684877269,-1.88834843134424),
 .UNSPECIFIED.);
#379=B_SPLINE_CURVE_WITH_KNOTS('',3,(#34945,#34946,#34947,#34948,#34949,
#34950,#34951,#34952,#34953,#34954,#34955,#34956,#34957,#34958,#34959,#34960,
#34961,#34962,#34963,#34964,#34965,#34966,#34967,#34968,#34969,#34970,#34971,
#34972,#34973,#34974,#34975,#34976,#34977,#34978,#34979,#34980),
 .UNSPECIFIED.,.F.,.F.,(4,2,2,2,2,2,2,2,2,2,2,2,2,2,2,2,2,4),(-46.0752889773848,
-45.964891178069,-45.8466628798698,-45.7329708487168,-45.6148893471227,
-45.5013384204638,-45.3834035051267,-45.2699934762495,-45.1522049350479,
-45.0389355951934,-44.9212932140859,-44.8081643522802,-44.6906679151483,
-44.5776793180225,-44.460328606502,-44.347480058098,-44.2302748513988,-44.2267979604378),
 .UNSPECIFIED.);
#380=B_SPLINE_CURVE_WITH_KNOTS('',3,(#34981,#34982,#34983,#34984,#34985,
#34986,#34987,#34988,#34989,#34990,#34991,#34992,#34993,#34994,#34995,#34996,
#34997,#34998,#34999,#35000,#35001,#35002,#35003,#35004,#35005,#35006,#35007,
#35008,#35009,#35010,#35011,#35012,#35013,#35014,#35015,#35016),
 .UNSPECIFIED.,.F.,.F.,(4,2,2,2,2,2,2,2,2,2,2,2,2,2,2,2,2,4),(-1.88834843134424,
-1.87565643327968,-1.7561130177999,-1.64092583480119,-1.52125969746077,
-1.40596319410974,-1.28617279582862,-1.17076456637983,-1.05084841334602,
-0.935326191460909,-0.815282836884644,-0.699644488109694,-0.579472533457261,
-0.4637160479124,-0.343414143669268,-0.227537628973816,-0.113637758694294,
0.),.UNSPECIFIED.);
#381=B_SPLINE_CURVE_WITH_KNOTS('',3,(#35021,#35022,#35023,#35024,#35025,
#35026,#35027,#35028,#35029,#35030,#35031,#35032,#35033,#35034,#35035,#35036,
#35037,#35038,#35039,#35040,#35041,#35042,#35043,#35044,#35045,#35046,#35047,
#35048,#35049,#35050,#35051,#35052,#35053,#35054,#35055,#35056),
 .UNSPECIFIED.,.F.,.F.,(4,2,2,2,2,2,2,2,2,2,2,2,2,2,2,2,2,4),(-47.9422113160818,
-47.8306672541019,-47.7112571821755,-47.5964290719752,-47.4771674302257,
-47.3624820212509,-47.2433686092934,-47.1288257063837,-47.0098603229286,
-46.8954597298667,-46.7766421726348,-46.6623836920508,-46.5437137576842,
-46.429597190954,-46.3110746749191,-46.1970998220542,-46.0787245185386,
-46.0752889773848),.UNSPECIFIED.);
#382=B_SPLINE_CURVE_WITH_KNOTS('',3,(#35057,#35058,#35059,#35060,#35061,
#35062,#35063,#35064,#35065,#35066,#35067,#35068,#35069,#35070,#35071,#35072,
#35073,#35074,#35075,#35076,#35077,#35078,#35079,#35080,#35081,#35082,#35083,
#35084,#35085,#35086,#35087,#35088,#35089,#35090,#35091,#35092),
 .UNSPECIFIED.,.F.,.F.,(4,2,2,2,2,2,2,2,2,2,2,2,2,2,2,2,2,4),(-9.73841549569248,
-9.64066589843865,-9.54184328358783,-9.42684071170168,-9.30840307871922,
-9.19339350762375,-9.07504249845454,-8.96001878949922,-8.84175342158102,
-8.72670837518871,-8.60852768245023,-8.49345406672159,-8.37535707971806,
-8.26024766039142,-8.14223338386421,-8.0270809552092,-7.90914834348772,
-7.85755307378671),.UNSPECIFIED.);
#383=B_SPLINE_CURVE_WITH_KNOTS('',3,(#35097,#35098,#35099,#35100,#35101,
#35102,#35103,#35104,#35105,#35106,#35107,#35108,#35109,#35110,#35111,#35112,
#35113,#35114,#35115,#35116,#35117,#35118,#35119,#35120,#35121,#35122,#35123,
#35124,#35125,#35126,#35127,#35128,#35129,#35130,#35131,#35132),
 .UNSPECIFIED.,.F.,.F.,(4,2,2,2,2,2,2,2,2,2,2,2,2,2,2,2,2,4),(-49.8277844545049,
-49.7151003815012,-49.5944957394318,-49.4785190939317,-49.3580644608813,
-49.242232049276,-49.1219272296907,-49.0062388625519,-48.8860836604681,
-48.77053914787,-48.6505333668662,-48.5351325183314,-48.4152759614772,-48.300018585919,
-48.18031105572,-48.0651969613802,-47.9456382597193,-47.9422113160818),
 .UNSPECIFIED.);
#384=B_SPLINE_CURVE_WITH_KNOTS('',3,(#35133,#35134,#35135,#35136,#35137,
#35138,#35139,#35140,#35141,#35142,#35143,#35144,#35145,#35146,#35147,#35148,
#35149,#35150,#35151,#35152,#35153,#35154,#35155,#35156,#35157,#35158,#35159,
#35160,#35161,#35162,#35163,#35164,#35165,#35166,#35167,#35168),
 .UNSPECIFIED.,.F.,.F.,(4,2,2,2,2,2,2,2,2,2,2,2,2,2,2,2,2,4),(-7.85755307378671,
-7.79394575966839,-7.67609369044231,-7.56083389685531,-7.44306114393897,
-7.32773720801898,-7.21004241380288,-7.09464755478704,-6.97702919010705,
-6.86155628126466,-6.74401263106893,-6.62845525109629,-6.51098440652207,
-6.39533637675224,-6.27793619918513,-6.16219158472876,-6.04485968769943,
-5.97715388014199),.UNSPECIFIED.);
#385=B_SPLINE_CURVE_WITH_KNOTS('',3,(#35173,#35174,#35175,#35176,#35177,
#35178,#35179,#35180,#35181,#35182,#35183,#35184,#35185,#35186,#35187,#35188,
#35189,#35190,#35191,#35192,#35193,#35194,#35195,#35196,#35197,#35198,#35199,
#35200,#35201,#35202,#35203,#35204,#35205,#35206,#35207,#35208),
 .UNSPECIFIED.,.F.,.F.,(4,2,2,2,2,2,2,2,2,2,2,2,2,2,2,2,2,4),(-51.7322148856786,
-51.6183893945336,-51.4965776761934,-51.3794403848007,-51.2577802299048,
-51.14078867526,-51.0192798901623,-50.9024338852763,-50.7810762762027,-50.6643756339059,
-50.5431690069267,-50.4266135398375,-50.3055577008387,-50.1891472213314,
-50.0682419759833,-49.9519762961531,-49.8312214498766,-49.8277844545049),
 .UNSPECIFIED.);
#386=B_SPLINE_CURVE_WITH_KNOTS('',3,(#35209,#35210,#35211,#35212,#35213,
#35214,#35215,#35216,#35217,#35218,#35219,#35220,#35221,#35222,#35223,#35224,
#35225,#35226,#35227,#35228,#35229,#35230,#35231,#35232,#35233,#35234,#35235,
#35236,#35237,#35238,#35239,#35240,#35241,#35242,#35243,#35244),
 .UNSPECIFIED.,.F.,.F.,(4,2,2,2,2,2,2,2,2,2,2,2,2,2,2,2,2,4),(-5.97715388014199,
-5.92901281616251,-5.811746551025,-5.69579202819225,-5.57858847398357,-5.46252119631723,
-5.34537715406377,-5.2291923179436,-5.11210430953573,-4.99579741723946,
-4.87876168885324,-4.76377104513167,-4.64521911964579,-4.53022541977396,
-4.41158432394141,-4.29658068603151,-4.17784927068626,-4.09558903017493),
 .UNSPECIFIED.);
#387=B_SPLINE_CURVE_WITH_KNOTS('',3,(#35249,#35250,#35251,#35252,#35253,
#35254,#35255,#35256,#35257,#35258,#35259,#35260,#35261,#35262,#35263,#35264,
#35265,#35266,#35267,#35268,#35269,#35270,#35271,#35272,#35273,#35274,#35275,
#35276,#35277,#35278,#35279,#35280,#35281,#35282,#35283,#35284),
 .UNSPECIFIED.,.F.,.F.,(4,2,2,2,2,2,2,2,2,2,2,2,2,2,2,2,2,4),(-53.6557025845032,
-53.5407298928425,-53.4176987034498,-53.2993887996668,-53.1765107209798,
-53.0583480463698,-52.9356228849868,-52.8176072531345,-52.6950348156857,
-52.5771660401742,-52.4547461333068,-52.3370240277007,-52.2147564580623,
-52.0971808358888,-51.9750654101091,-51.8576360848382,-51.7356726095103,
-51.7322148856786),.UNSPECIFIED.);
#388=B_SPLINE_CURVE_WITH_KNOTS('',3,(#35285,#35286,#35287,#35288,#35289,
#35290,#35291,#35292,#35293,#35294,#35295,#35296,#35297,#35298,#35299,#35300,
#35301,#35302,#35303,#35304,#35305,#35306,#35307,#35308,#35309,#35310,#35311,
#35312,#35313,#35314,#35315,#35316,#35317,#35318,#35319,#35320),
 .UNSPECIFIED.,.F.,.F.,(4,2,2,2,2,2,2,2,2,2,2,2,2,2,2,2,2,4),(-4.09558903017493,
-4.06282895703941,-3.9440060047118,-3.82896244084379,-3.71004666222381,
-3.59497345330519,-3.47596348634699,-3.360854431037,-3.24174884241533,-3.1265979441254,
-3.00739523272272,-2.8921967083926,-2.77289531047598,-2.65764359698508,
-2.53824189272868,-2.42293165109723,-2.30342797211658,-2.21008111793747),
 .UNSPECIFIED.);
#389=B_SPLINE_CURVE_WITH_KNOTS('',3,(#35327,#35328,#35329,#35330,#35331,
#35332,#35333,#35334,#35335,#35336,#35337,#35338,#35339,#35340,#35341,#35342,
#35343,#35344,#35345,#35346,#35347,#35348,#35349,#35350,#35351,#35352,#35353,
#35354,#35355,#35356,#35357,#35358),.UNSPECIFIED.,.F.,.F.,(4,2,2,2,2,2,
2,2,2,2,2,2,2,2,2,4),(-55.2720782428214,-55.1926108670175,-55.1144496740328,
-54.9951040192258,-54.8711501794093,-54.7519530597782,-54.6281534924038,
-54.5091047211471,-54.3854592323477,-54.266558622755,-54.1430670187691,
-54.0243143842106,-53.9009764713722,-53.7823716252871,-53.6591872100146,
-53.6557025845032),.UNSPECIFIED.);
#390=B_SPLINE_CURVE_WITH_KNOTS('',3,(#35359,#35360,#35361,#35362,#35363,
#35364,#35365,#35366,#35367,#35368,#35369,#35370,#35371,#35372,#35373,#35374,
#35375,#35376,#35377,#35378,#35379,#35380,#35381,#35382,#35383,#35384,#35385,
#35386,#35387,#35388,#35389,#35390,#35391,#35392,#35393,#35394),
 .UNSPECIFIED.,.F.,.F.,(4,2,2,2,2,2,2,2,2,2,2,2,2,2,2,2,2,4),(-2.21008111793747,
-2.18805408967434,-2.0684467272563,-1.9530043179717,-1.83329153171217,-1.71777593488302,
-1.59795596147469,-1.48236273898472,-1.36243380093483,-1.24675873327631,
-1.12671904736753,-1.0109581286233,-0.890805913968434,-0.774955345935989,
-0.654688831510368,-0.538745017138309,-0.418362448705376,-0.317026523413959),
 .UNSPECIFIED.);
#391=B_SPLINE_CURVE_WITH_KNOTS('',3,(#35405,#35406,#35407,#35408,#35409,
#35410,#35411,#35412,#35413,#35414,#35415,#35416,#35417,#35418,#35419,#35420,
#35421,#35422,#35423,#35424,#35425,#35426,#35427,#35428,#35429,#35430,#35431,
#35432,#35433,#35434,#35435,#35436),.UNSPECIFIED.,.F.,.F.,(4,2,2,2,2,2,
2,2,2,2,2,2,2,2,2,4),(0.,0.0392663678244995,0.0704169284194691,0.0927548217162514,
0.110721970139896,0.123565722758962,0.128289439509511,0.131295508607438,
0.134067308634044,0.137660564724108,0.145063726347613,0.161462983996547,
0.177979987307193,0.198867571223351,0.226369846271957,0.257489265746057),
 .UNSPECIFIED.);
#392=B_SPLINE_CURVE_WITH_KNOTS('',3,(#35440,#35441,#35442,#35443,#35444,
#35445,#35446,#35447,#35448,#35449,#35450,#35451,#35452,#35453,#35454,#35455,
#35456,#35457,#35458,#35459,#35460,#35461,#35462,#35463,#35464,#35465,#35466,
#35467,#35468,#35469,#35470,#35471),.UNSPECIFIED.,.F.,.F.,(4,2,2,2,2,2,
2,2,2,2,2,2,2,2,2,4),(0.,0.0392663678249377,0.0704169284194495,0.0927548217152616,
0.110721970138253,0.123565722756902,0.12828943950701,0.131295508605003,
0.134067308631639,0.137660564721307,0.145063726344776,0.161462983993541,
0.177979987304027,0.198867571220078,0.226369846268986,0.257489265743641),
 .UNSPECIFIED.);
#393=B_SPLINE_CURVE_WITH_KNOTS('',3,(#35476,#35477,#35478,#35479,#35480,
#35481,#35482,#35483,#35484,#35485,#35486,#35487,#35488,#35489,#35490,#35491,
#35492,#35493,#35494,#35495,#35496,#35497,#35498,#35499,#35500,#35501,#35502,
#35503,#35504,#35505,#35506,#35507),.UNSPECIFIED.,.F.,.F.,(4,2,2,2,2,2,
2,2,2,2,2,2,2,2,2,4),(0.,0.039266367824589,0.0704169284199113,0.092754821717152,
0.110721970141282,0.123565722760872,0.128289439511348,0.131295508609272,
0.134067308635804,0.137660564725569,0.145063726349089,0.161462983998042,
0.177979987308742,0.198867571225001,0.22636984627417,0.257489265748717),
 .UNSPECIFIED.);
#394=B_SPLINE_CURVE_WITH_KNOTS('',3,(#35511,#35512,#35513,#35514,#35515,
#35516,#35517,#35518,#35519,#35520,#35521,#35522,#35523,#35524,#35525,#35526,
#35527,#35528,#35529,#35530,#35531,#35532,#35533,#35534,#35535,#35536,#35537,
#35538,#35539,#35540,#35541,#35542),.UNSPECIFIED.,.F.,.F.,(4,2,2,2,2,2,
2,2,2,2,2,2,2,2,2,4),(0.,0.0392663678249047,0.0704169284198803,0.0927548217163086,
0.110721970139767,0.123565722758766,0.128289439509206,0.13129550860702,
0.134067308633502,0.137660564723442,0.145063726347079,0.161462983996174,
0.177979987306964,0.198867571223311,0.226369846272921,0.257489265748311),
 .UNSPECIFIED.);
#395=B_SPLINE_CURVE_WITH_KNOTS('',3,(#35547,#35548,#35549,#35550,#35551,
#35552,#35553,#35554,#35555,#35556,#35557,#35558,#35559,#35560,#35561,#35562,
#35563,#35564,#35565,#35566,#35567,#35568,#35569,#35570,#35571,#35572,#35573,
#35574,#35575,#35576,#35577,#35578),.UNSPECIFIED.,.F.,.F.,(4,2,2,2,2,2,
2,2,2,2,2,2,2,2,2,4),(0.,0.0392663678248331,0.0704169284201615,0.0927548217171289,
0.110721970141034,0.123565722760465,0.128289439510992,0.131295508609155,
0.134067308635896,0.137660564725619,0.145063726348897,0.161462983997348,
0.177979987307562,0.198867571223244,0.226369846271105,0.257489265744014),
 .UNSPECIFIED.);
#396=B_SPLINE_CURVE_WITH_KNOTS('',3,(#35582,#35583,#35584,#35585,#35586,
#35587,#35588,#35589,#35590,#35591,#35592,#35593,#35594,#35595,#35596,#35597,
#35598,#35599,#35600,#35601,#35602,#35603,#35604,#35605,#35606,#35607,#35608,
#35609,#35610,#35611,#35612,#35613),.UNSPECIFIED.,.F.,.F.,(4,2,2,2,2,2,
2,2,2,2,2,2,2,2,2,4),(0.,0.0392663678247495,0.070416928419445,0.0927548217155992,
0.110721970138876,0.123565722757605,0.128289439508189,0.131295508606264,
0.134067308632887,0.137660564722685,0.145063726346118,0.161462983994792,
0.177979987305081,0.198867571220603,0.226369846268855,0.257489265742627),
 .UNSPECIFIED.);
#397=B_SPLINE_CURVE_WITH_KNOTS('',3,(#35618,#35619,#35620,#35621,#35622,
#35623,#35624,#35625,#35626,#35627,#35628,#35629,#35630,#35631,#35632,#35633,
#35634,#35635,#35636,#35637,#35638,#35639,#35640,#35641,#35642,#35643,#35644,
#35645,#35646,#35647,#35648,#35649),.UNSPECIFIED.,.F.,.F.,(4,2,2,2,2,2,
2,2,2,2,2,2,2,2,2,4),(0.,0.0392663678249739,0.0704169284201815,0.0927548217168303,
0.110721970140497,0.123565722759709,0.12828943951013,0.131295508608142,
0.134067308634776,0.137660564724678,0.145063726348717,0.161462983998648,
0.17797998731033,0.198867571227874,0.22636984627903,0.257489265756248),
 .UNSPECIFIED.);
#398=B_SPLINE_CURVE_WITH_KNOTS('',3,(#35653,#35654,#35655,#35656,#35657,
#35658,#35659,#35660,#35661,#35662,#35663,#35664,#35665,#35666,#35667,#35668,
#35669,#35670,#35671,#35672,#35673,#35674,#35675,#35676,#35677,#35678,#35679,
#35680,#35681,#35682,#35683,#35684),.UNSPECIFIED.,.F.,.F.,(4,2,2,2,2,2,
2,2,2,2,2,2,2,2,2,4),(0.,0.0392663678247806,0.0704169284192398,0.0927548217150881,
0.110721970138062,0.123565722756726,0.128289439506608,0.131295508604434,
0.134067308631067,0.137660564720986,0.145063726344604,0.161462983993715,
0.177979987304472,0.198867571220671,0.2263698462694,0.257489265743336),
 .UNSPECIFIED.);
#399=B_SPLINE_CURVE_WITH_KNOTS('',3,(#35689,#35690,#35691,#35692,#35693,
#35694,#35695,#35696,#35697,#35698,#35699,#35700,#35701,#35702,#35703,#35704,
#35705,#35706,#35707,#35708,#35709,#35710,#35711,#35712,#35713,#35714,#35715,
#35716,#35717,#35718,#35719,#35720),.UNSPECIFIED.,.F.,.F.,(4,2,2,2,2,2,
2,2,2,2,2,2,2,2,2,4),(0.,0.0392663678244778,0.0704169284194323,0.0927548217161555,
0.110721970139643,0.123565722758622,0.128289439508742,0.131295508606697,
0.134067308633816,0.137660564725199,0.145063726351016,0.161462984005015,
0.177979987320616,0.198867571242853,0.226369846299339,0.257489265781862),
 .UNSPECIFIED.);
#400=B_SPLINE_CURVE_WITH_KNOTS('',3,(#35724,#35725,#35726,#35727,#35728,
#35729,#35730,#35731,#35732,#35733,#35734,#35735,#35736,#35737,#35738,#35739,
#35740,#35741,#35742,#35743,#35744,#35745,#35746,#35747,#35748,#35749,#35750,
#35751,#35752,#35753,#35754,#35755),.UNSPECIFIED.,.F.,.F.,(4,2,2,2,2,2,
2,2,2,2,2,2,2,2,2,4),(0.,0.0392663678248244,0.0704169284195352,0.0927548217156887,
0.110721970139069,0.123565722757938,0.128289439508065,0.131295508606377,
0.134067308633623,0.137660564724286,0.145063726348926,0.161462984000236,
0.177979987313331,0.198867571232472,0.226369846285091,0.257489265763111),
 .UNSPECIFIED.);
#401=B_SPLINE_CURVE_WITH_KNOTS('',3,(#35760,#35761,#35762,#35763,#35764,
#35765,#35766,#35767,#35768,#35769,#35770,#35771,#35772,#35773,#35774,#35775,
#35776,#35777,#35778,#35779,#35780,#35781,#35782,#35783,#35784,#35785,#35786,
#35787,#35788,#35789,#35790,#35791),.UNSPECIFIED.,.F.,.F.,(4,2,2,2,2,2,
2,2,2,2,2,2,2,2,2,4),(0.,0.0392663678249251,0.070416928419892,0.0927548217161836,
0.110721970139611,0.123565722758602,0.128289439508551,0.131295508606161,
0.13406730863253,0.137660564722374,0.145063726346409,0.161462983995986,
0.177979987307282,0.198867571224163,0.226369846273867,0.257489265749124),
 .UNSPECIFIED.);
#402=B_SPLINE_CURVE_WITH_KNOTS('',3,(#35795,#35796,#35797,#35798,#35799,
#35800,#35801,#35802,#35803,#35804,#35805,#35806,#35807,#35808,#35809,#35810,
#35811,#35812,#35813,#35814,#35815,#35816,#35817,#35818,#35819,#35820,#35821,
#35822,#35823,#35824,#35825,#35826),.UNSPECIFIED.,.F.,.F.,(4,2,2,2,2,2,
2,2,2,2,2,2,2,2,2,4),(0.,0.0392663678246274,0.0704169284197599,0.0927548217167053,
0.110721970140675,0.123565722759913,0.128289439510793,0.131295508608582,
0.134067308634807,0.137660564724331,0.145063726347116,0.161462983994171,
0.177979987302965,0.198867571216829,0.226369846262802,0.257489265733735),
 .UNSPECIFIED.);
#403=B_SPLINE_CURVE_WITH_KNOTS('',3,(#35831,#35832,#35833,#35834,#35835,
#35836,#35837,#35838,#35839,#35840,#35841,#35842,#35843,#35844,#35845,#35846,
#35847,#35848,#35849,#35850,#35851,#35852,#35853,#35854,#35855,#35856,#35857,
#35858,#35859,#35860,#35861,#35862),.UNSPECIFIED.,.F.,.F.,(4,2,2,2,2,2,
2,2,2,2,2,2,2,2,2,4),(0.,0.0392663678247802,0.070416928419353,0.0927548217152033,
0.110721970137883,0.123565722756308,0.128289439505835,0.131295508603904,
0.134067308631161,0.137660564722251,0.14506372634802,0.161462984001055,
0.177979987315666,0.198867571236657,0.226369846291255,0.257489265771073),
 .UNSPECIFIED.);
#404=B_SPLINE_CURVE_WITH_KNOTS('',3,(#35866,#35867,#35868,#35869,#35870,
#35871,#35872,#35873,#35874,#35875,#35876,#35877,#35878,#35879,#35880,#35881,
#35882,#35883,#35884,#35885,#35886,#35887,#35888,#35889,#35890,#35891,#35892,
#35893,#35894,#35895,#35896,#35897),.UNSPECIFIED.,.F.,.F.,(4,2,2,2,2,2,
2,2,2,2,2,2,2,2,2,4),(0.,0.0392663678245154,0.0704169284191378,0.0927548217152303,
0.110721970138229,0.123565722756741,0.128289439506368,0.131295508603649,
0.134067308629744,0.137660564719498,0.145063726343503,0.161462983992689,
0.177979987303389,0.198867571219121,0.226369846267092,0.257489265740257),
 .UNSPECIFIED.);
#405=B_SPLINE_CURVE_WITH_KNOTS('',3,(#35902,#35903,#35904,#35905,#35906,
#35907,#35908,#35909,#35910,#35911,#35912,#35913,#35914,#35915,#35916,#35917,
#35918,#35919,#35920,#35921,#35922,#35923,#35924,#35925,#35926,#35927,#35928,
#35929,#35930,#35931,#35932,#35933),.UNSPECIFIED.,.F.,.F.,(4,2,2,2,2,2,
2,2,2,2,2,2,2,2,2,4),(0.,0.0392663678246403,0.0704169284196593,0.0927548217162621,
0.110721970139792,0.123565722758691,0.128289439509469,0.131295508607455,
0.134067308634163,0.137660564724622,0.145063726348764,0.161462983999486,
0.177979987311735,0.198867571229894,0.226369846281758,0.25748926576032),
 .UNSPECIFIED.);
#406=B_SPLINE_CURVE_WITH_KNOTS('',3,(#35937,#35938,#35939,#35940,#35941,
#35942,#35943,#35944,#35945,#35946,#35947,#35948,#35949,#35950,#35951,#35952,
#35953,#35954,#35955,#35956,#35957,#35958,#35959,#35960,#35961,#35962,#35963,
#35964,#35965,#35966,#35967,#35968),.UNSPECIFIED.,.F.,.F.,(4,2,2,2,2,2,
2,2,2,2,2,2,2,2,2,4),(0.,0.0392663678247903,0.070416928419749,0.0927548217163387,
0.110721970139937,0.123565722758935,0.128289439509696,0.131295508608072,
0.134067308634654,0.137660564723633,0.145063726346522,0.161462983994072,
0.177979987303378,0.198867571217868,0.226369846264756,0.257489265736797),
 .UNSPECIFIED.);
#407=B_SPLINE_CURVE_WITH_KNOTS('',3,(#35973,#35974,#35975,#35976,#35977,
#35978,#35979,#35980,#35981,#35982,#35983,#35984,#35985,#35986,#35987,#35988,
#35989,#35990,#35991,#35992,#35993,#35994,#35995,#35996,#35997,#35998,#35999,
#36000,#36001,#36002,#36003,#36004),.UNSPECIFIED.,.F.,.F.,(4,2,2,2,2,2,
2,2,2,2,2,2,2,2,2,4),(0.,0.0392663678247125,0.0704169284195073,0.0927548217158198,
0.110721970139137,0.123565722757943,0.128289439508104,0.131295508606656,
0.134067308633928,0.137660564724143,0.145063726348696,0.161462983999483,
0.17797998731199,0.198867571230429,0.226369846281902,0.257489265758881),
 .UNSPECIFIED.);
#408=B_SPLINE_CURVE_WITH_KNOTS('',3,(#36008,#36009,#36010,#36011,#36012,
#36013,#36014,#36015,#36016,#36017,#36018,#36019,#36020,#36021,#36022,#36023,
#36024,#36025,#36026,#36027,#36028,#36029,#36030,#36031,#36032,#36033,#36034,
#36035,#36036,#36037,#36038,#36039),.UNSPECIFIED.,.F.,.F.,(4,2,2,2,2,2,
2,2,2,2,2,2,2,2,2,4),(0.,0.0392663678246693,0.0704169284192301,0.0927548217150732,
0.110721970137704,0.123565722755857,0.128289439505946,0.131295508603737,
0.134067308630246,0.13766056472024,0.145063726344291,0.161462983993872,
0.177979987304981,0.198867571221343,0.226369846269783,0.257489265742993),
 .UNSPECIFIED.);
#409=B_SPLINE_CURVE_WITH_KNOTS('',3,(#36044,#36045,#36046,#36047,#36048,
#36049,#36050,#36051,#36052,#36053,#36054,#36055,#36056,#36057,#36058,#36059,
#36060,#36061,#36062,#36063,#36064,#36065,#36066,#36067,#36068,#36069,#36070,
#36071,#36072,#36073,#36074,#36075),.UNSPECIFIED.,.F.,.F.,(4,2,2,2,2,2,
2,2,2,2,2,2,2,2,2,4),(0.,0.0392663678249069,0.0704169284199938,0.0927548217165904,
0.110721970140226,0.123565722759382,0.128289439509785,0.131295508607764,
0.13406730863429,0.137660564723914,0.145063726347582,0.161462983996786,
0.177979987307717,0.198867571224335,0.226369846273865,0.257489265748956),
 .UNSPECIFIED.);
#410=B_SPLINE_CURVE_WITH_KNOTS('',3,(#36079,#36080,#36081,#36082,#36083,
#36084,#36085,#36086,#36087,#36088,#36089,#36090,#36091,#36092,#36093,#36094,
#36095,#36096,#36097,#36098,#36099,#36100,#36101,#36102,#36103,#36104,#36105,
#36106,#36107,#36108,#36109,#36110),.UNSPECIFIED.,.F.,.F.,(4,2,2,2,2,2,
2,2,2,2,2,2,2,2,2,4),(0.,0.039266367824699,0.0704169284194923,0.0927548217158646,
0.11072197013936,0.123565722758493,0.128289439508746,0.131295508606819,
0.134067308633445,0.13766056472298,0.145063726346669,0.161462983996177,
0.177979987307315,0.198867571224074,0.226369846273922,0.257489265749371),
 .UNSPECIFIED.);
#411=B_SPLINE_CURVE_WITH_KNOTS('',3,(#36120,#36121,#36122,#36123,#36124,
#36125,#36126,#36127,#36128,#36129,#36130,#36131,#36132,#36133,#36134,#36135,
#36136,#36137,#36138,#36139,#36140,#36141,#36142,#36143,#36144,#36145,#36146,
#36147,#36148,#36149,#36150,#36151),.UNSPECIFIED.,.F.,.F.,(4,2,2,2,2,2,
2,2,2,2,2,2,2,2,2,4),(-1.76634793841595E-15,0.0392663678245224,0.0704169284190363,
0.0927548217151552,0.110721970138219,0.123565722756832,0.128289439506975,
0.131295508604955,0.134067308631658,0.137660564721908,0.145063726347255,
0.161462983999379,0.177979987313175,0.198867571232894,0.226369846286481,
0.257489265765706),.UNSPECIFIED.);
#412=B_SPLINE_CURVE_WITH_KNOTS('',3,(#36155,#36156,#36157,#36158,#36159,
#36160,#36161,#36162,#36163,#36164,#36165,#36166,#36167,#36168,#36169,#36170,
#36171,#36172,#36173,#36174,#36175,#36176,#36177,#36178,#36179,#36180,#36181,
#36182,#36183,#36184,#36185,#36186),.UNSPECIFIED.,.F.,.F.,(4,2,2,2,2,2,
2,2,2,2,2,2,2,2,2,4),(-3.43854363132254E-15,0.0392663678246992,0.0704169284198385,
0.0927548217167047,0.110721970140455,0.123565722759784,0.128289439510127,
0.131295508608258,0.134067308635215,0.137660564725771,0.145063726350863,
0.16146298400288,0.177979987316548,0.198867571236671,0.226369846290545,
0.257489265770492),.UNSPECIFIED.);
#413=B_SPLINE_CURVE_WITH_KNOTS('',3,(#36190,#36191,#36192,#36193,#36194,
#36195,#36196,#36197,#36198,#36199,#36200,#36201,#36202,#36203,#36204,#36205,
#36206,#36207,#36208,#36209,#36210,#36211,#36212,#36213,#36214,#36215,#36216,
#36217,#36218,#36219,#36220,#36221),.UNSPECIFIED.,.F.,.F.,(4,2,2,2,2,2,
2,2,2,2,2,2,2,2,2,4),(-3.34439138581297E-15,0.0392663678246232,0.0704169284196317,
0.0927548217162855,0.110721970139993,0.123565722759132,0.128289439510069,
0.13129550860811,0.134067308634763,0.137660564724976,0.1450637263486,0.161462983997844,
0.177979987308744,0.198867571225209,0.226369846274388,0.257489265749007),
 .UNSPECIFIED.);
#414=B_SPLINE_CURVE_WITH_KNOTS('',3,(#36225,#36226,#36227,#36228,#36229,
#36230,#36231,#36232,#36233,#36234,#36235,#36236,#36237,#36238,#36239,#36240,
#36241,#36242,#36243,#36244,#36245,#36246,#36247,#36248,#36249,#36250,#36251,
#36252,#36253,#36254,#36255,#36256),.UNSPECIFIED.,.F.,.F.,(4,2,2,2,2,2,
2,2,2,2,2,2,2,2,2,4),(-3.43854363132217E-15,0.0392663678249148,0.0704169284200044,
0.0927548217166559,0.110721970140529,0.123565722759803,0.128289439510254,
0.13129550860835,0.134067308634935,0.137660564724413,0.145063726347793,
0.161462983996495,0.177979987306919,0.198867571222842,0.226369846271352,
0.257489265745074),.UNSPECIFIED.);
#415=B_SPLINE_CURVE_WITH_KNOTS('',3,(#36260,#36261,#36262,#36263,#36264,
#36265,#36266,#36267,#36268,#36269,#36270,#36271,#36272,#36273,#36274,#36275,
#36276,#36277,#36278,#36279,#36280,#36281,#36282,#36283,#36284,#36285,#36286,
#36287,#36288,#36289,#36290,#36291),.UNSPECIFIED.,.F.,.F.,(4,2,2,2,2,2,
2,2,2,2,2,2,2,2,2,4),(-1.76634793841593E-15,0.0392663678246619,0.070416928419432,
0.0927548217157895,0.110721970139278,0.123565722758194,0.128289439508417,
0.131295508606941,0.134067308634171,0.137660564724305,0.1450637263484,0.161462983998334,
0.177979987309968,0.198867571227245,0.226369846278035,0.257489265754873),
 .UNSPECIFIED.);
#416=B_SPLINE_CURVE_WITH_KNOTS('',3,(#36295,#36296,#36297,#36298,#36299,
#36300,#36301,#36302,#36303,#36304,#36305,#36306,#36307,#36308,#36309,#36310,
#36311,#36312,#36313,#36314,#36315,#36316,#36317,#36318,#36319,#36320,#36321,
#36322,#36323,#36324,#36325,#36326),.UNSPECIFIED.,.F.,.F.,(4,2,2,2,2,2,
2,2,2,2,2,2,2,2,2,4),(-3.25023914030354E-15,0.0392663678248276,0.0704169284192996,
0.092754821715151,0.110721970137982,0.123565722756635,0.128289439506694,
0.131295508604321,0.13406730863081,0.137660564720951,0.145063726344476,
0.161462983993191,0.177979987303611,0.198867571219355,0.226369846267676,
0.257489265741455),.UNSPECIFIED.);
#417=B_SPLINE_CURVE_WITH_KNOTS('',3,(#36330,#36331,#36332,#36333,#36334,
#36335,#36336,#36337,#36338,#36339,#36340,#36341,#36342,#36343,#36344,#36345,
#36346,#36347,#36348,#36349,#36350,#36351,#36352,#36353,#36354,#36355,#36356,
#36357,#36358,#36359,#36360,#36361),.UNSPECIFIED.,.F.,.F.,(4,2,2,2,2,2,
2,2,2,2,2,2,2,2,2,4),(-3.43854363132254E-15,0.0392663678247849,0.0704169284203094,
0.0927548217175492,0.110721970141637,0.123565722761111,0.128289439511682,
0.131295508609654,0.134067308636262,0.137660564726202,0.145063726349868,
0.161462983999319,0.17797998731052,0.198867571227385,0.226369846277203,
0.257489265752561),.UNSPECIFIED.);
#418=B_SPLINE_CURVE_WITH_KNOTS('',3,(#36365,#36366,#36367,#36368,#36369,
#36370,#36371,#36372,#36373,#36374,#36375,#36376,#36377,#36378,#36379,#36380,
#36381,#36382,#36383,#36384,#36385,#36386,#36387,#36388,#36389,#36390,#36391,
#36392,#36393,#36394,#36395,#36396),.UNSPECIFIED.,.F.,.F.,(4,2,2,2,2,2,
2,2,2,2,2,2,2,2,2,4),(-3.62684812234152E-15,0.0392663678249345,0.070416928420165,
0.0927548217169184,0.110721970140689,0.12356572276004,0.128289439510604,
0.131295508608354,0.134067308634811,0.137660564724923,0.145063726348958,
0.161462983999017,0.177979987310905,0.198867571228708,0.226369846279955,
0.257489265757467),.UNSPECIFIED.);
#419=B_SPLINE_CURVE_WITH_KNOTS('',3,(#36410,#36411,#36412,#36413,#36414,
#36415,#36416,#36417,#36418,#36419,#36420,#36421,#36422,#36423,#36424,#36425,
#36426,#36427,#36428,#36429,#36430,#36431,#36432,#36433,#36434,#36435,#36436,
#36437,#36438,#36439,#36440,#36441),.UNSPECIFIED.,.F.,.F.,(4,2,2,2,2,2,
2,2,2,2,2,2,2,2,2,4),(-3.62684812234151E-15,0.0392663678245326,0.0704169284186608,
0.0927548217142498,0.110721970136877,0.123565722755316,0.128289439504875,
0.131295508602739,0.134067308629719,0.137660564720433,0.145063726345226,
0.161462983996599,0.177979987309569,0.198867571228362,0.226369846280901,
0.257489265759448),.UNSPECIFIED.);
#420=B_SPLINE_CURVE_WITH_KNOTS('',3,(#36445,#36446,#36447,#36448,#36449,
#36450,#36451,#36452,#36453,#36454,#36455,#36456,#36457,#36458,#36459,#36460,
#36461,#36462,#36463,#36464,#36465,#36466,#36467,#36468,#36469,#36470,#36471,
#36472,#36473,#36474,#36475,#36476),.UNSPECIFIED.,.F.,.F.,(4,2,2,2,2,2,
2,2,2,2,2,2,2,2,2,4),(-5.29904381524748E-15,0.0392663678245013,0.0704169284189458,
0.0927548217149502,0.110721970138046,0.123565722756779,0.128289439506874,
0.131295508604914,0.134067308631792,0.137660564721975,0.145063726345566,
0.161462983994717,0.177979987305542,0.198867571221693,0.226369846270547,
0.257489265744874),.UNSPECIFIED.);
#421=B_SPLINE_CURVE_WITH_KNOTS('',3,(#36480,#36481,#36482,#36483,#36484,
#36485,#36486,#36487,#36488,#36489,#36490,#36491,#36492,#36493,#36494,#36495,
#36496,#36497,#36498,#36499,#36500,#36501,#36502,#36503,#36504,#36505,#36506,
#36507,#36508,#36509,#36510,#36511),.UNSPECIFIED.,.F.,.F.,(4,2,2,2,2,2,
2,2,2,2,2,2,2,2,2,4),(-1.67219569290643E-15,0.0392663678247147,0.0704169284193986,
0.0927548217155684,0.110721970138799,0.123565722757588,0.128289439508,0.131295508606025,
0.134067308632753,0.13766056472281,0.145063726346428,0.161462983995307,
0.177979987305903,0.198867571221865,0.22636984627118,0.257489265746664),
 .UNSPECIFIED.);
#422=B_SPLINE_CURVE_WITH_KNOTS('',3,(#36515,#36516,#36517,#36518,#36519,
#36520,#36521,#36522,#36523,#36524,#36525,#36526,#36527,#36528,#36529,#36530,
#36531,#36532,#36533,#36534,#36535,#36536,#36537,#36538,#36539,#36540,#36541,
#36542,#36543,#36544,#36545,#36546),.UNSPECIFIED.,.F.,.F.,(4,2,2,2,2,2,
2,2,2,2,2,2,2,2,2,4),(-3.53269587683169E-15,0.0392663678247277,0.0704169284193875,
0.0927548217155201,0.11072197013873,0.123565722757556,0.128289439507877,
0.13129550860585,0.134067308632342,0.137660564721825,0.145063726345164,
0.161462983993392,0.17797998730333,0.198867571218531,0.226369846266786,
0.2574892657409),.UNSPECIFIED.);
#423=B_SPLINE_CURVE_WITH_KNOTS('',3,(#36550,#36551,#36552,#36553,#36554,
#36555,#36556,#36557,#36558,#36559,#36560,#36561,#36562,#36563,#36564,#36565,
#36566,#36567,#36568,#36569,#36570,#36571,#36572,#36573,#36574,#36575,#36576,
#36577,#36578,#36579,#36580,#36581),.UNSPECIFIED.,.F.,.F.,(4,2,2,2,2,2,
2,2,2,2,2,2,2,2,2,4),(0.,0.0392663678247719,0.0704169284195709,0.0927548217157682,
0.110721970138893,0.123565722757687,0.128289439507762,0.131295508605502,
0.134067308632007,0.137660564721959,0.145063726345763,0.161462983995323,
0.177979987306524,0.198867571223098,0.226369846272715,0.257489265748122),
 .UNSPECIFIED.);
#424=B_SPLINE_CURVE_WITH_KNOTS('',3,(#36585,#36586,#36587,#36588,#36589,
#36590,#36591,#36592,#36593,#36594,#36595,#36596,#36597,#36598,#36599,#36600,
#36601,#36602,#36603,#36604,#36605,#36606,#36607,#36608,#36609,#36610,#36611,
#36612,#36613,#36614,#36615,#36616),.UNSPECIFIED.,.F.,.F.,(4,2,2,2,2,2,
2,2,2,2,2,2,2,2,2,4),(-1.76634793841592E-15,0.0392663678247361,0.0704169284199132,
0.0927548217167579,0.110721970140471,0.123565722759657,0.128289439510084,
0.131295508608104,0.134067308634866,0.137660564725111,0.145063726349294,
0.16146298399946,0.177979987311368,0.198867571229017,0.226369846280088,
0.25748926575724),.UNSPECIFIED.);
#425=B_SPLINE_CURVE_WITH_KNOTS('',3,(#36620,#36621,#36622,#36623,#36624,
#36625,#36626,#36627,#36628,#36629,#36630,#36631,#36632,#36633,#36634,#36635,
#36636,#36637,#36638,#36639,#36640,#36641,#36642,#36643,#36644,#36645,#36646,
#36647,#36648,#36649,#36650,#36651),.UNSPECIFIED.,.F.,.F.,(4,2,2,2,2,2,
2,2,2,2,2,2,2,2,2,4),(0.,0.0392663678245323,0.0704169284195438,0.0927548217162293,
0.110721970139834,0.12356572275881,0.128289439508994,0.13129550860705,0.134067308633916,
0.13766056472422,0.145063726348449,0.16146298399857,0.177979987310414,0.198867571227846,
0.226369846278175,0.257489265753618),.UNSPECIFIED.);
#426=B_SPLINE_CURVE_WITH_KNOTS('',3,(#36655,#36656,#36657,#36658,#36659,
#36660,#36661,#36662,#36663,#36664,#36665,#36666,#36667,#36668,#36669,#36670,
#36671,#36672,#36673,#36674,#36675,#36676,#36677,#36678,#36679,#36680,#36681,
#36682,#36683,#36684,#36685,#36686),.UNSPECIFIED.,.F.,.F.,(4,2,2,2,2,2,
2,2,2,2,2,2,2,2,2,4),(-1.67219569290647E-15,0.0392663678247851,0.0704169284199364,
0.0927548217166158,0.110721970140177,0.123565722759255,0.128289439509636,
0.13129550860772,0.134067308634613,0.137660564724923,0.145063726348494,
0.161462983997478,0.177979987308109,0.198867571224169,0.226369846273075,
0.257489265747719),.UNSPECIFIED.);
#427=B_SPLINE_CURVE_WITH_KNOTS('',3,(#36701,#36702,#36703,#36704,#36705,
#36706,#36707,#36708,#36709,#36710,#36711,#36712,#36713,#36714,#36715,#36716,
#36717,#36718,#36719,#36720,#36721,#36722,#36723,#36724,#36725,#36726,#36727,
#36728,#36729,#36730,#36731,#36732),.UNSPECIFIED.,.F.,.F.,(4,2,2,2,2,2,
2,2,2,2,2,2,2,2,2,4),(0.,0.0392663678244286,0.0704169284192886,0.0927548217159949,
0.110721970139649,0.123565722758812,0.128289439509101,0.131295508607411,
0.134067308634294,0.137660564723937,0.145063726347504,0.161462983996596,
0.177979987307378,0.198867571223475,0.22636984627213,0.257489265746436),
 .UNSPECIFIED.);
#428=B_SPLINE_CURVE_WITH_KNOTS('',3,(#36736,#36737,#36738,#36739,#36740,
#36741,#36742,#36743,#36744,#36745,#36746,#36747,#36748,#36749,#36750,#36751,
#36752,#36753,#36754,#36755,#36756,#36757,#36758,#36759,#36760,#36761,#36762,
#36763,#36764,#36765,#36766,#36767),.UNSPECIFIED.,.F.,.F.,(4,2,2,2,2,2,
2,2,2,2,2,2,2,2,2,4),(-1.67219569290635E-15,0.0392663678244886,0.0704169284192001,
0.0927548217156716,0.11072197013908,0.123565722758101,0.128289439508155,
0.131295508605815,0.134067308632236,0.13766056472206,0.145063726345475,
0.161462983994193,0.177979987304618,0.19886757122036,0.226369846268546,
0.257489265742088),.UNSPECIFIED.);
#429=B_SPLINE_CURVE_WITH_KNOTS('',3,(#36771,#36772,#36773,#36774,#36775,
#36776,#36777,#36778,#36779,#36780,#36781,#36782,#36783,#36784,#36785,#36786,
#36787,#36788,#36789,#36790,#36791,#36792,#36793,#36794,#36795,#36796,#36797,
#36798,#36799,#36800,#36801,#36802),.UNSPECIFIED.,.F.,.F.,(4,2,2,2,2,2,
2,2,2,2,2,2,2,2,2,4),(-3.43854363132256E-15,0.0392663678247843,0.0704169284198121,
0.0927548217163949,0.110721970139939,0.123565722758948,0.128289439509206,
0.131295508607079,0.134067308633498,0.137660564722997,0.145063726346605,
0.161462983995843,0.177979987306685,0.198867571223128,0.226369846272286,
0.257489265746815),.UNSPECIFIED.);
#430=B_SPLINE_CURVE_WITH_KNOTS('',3,(#36806,#36807,#36808,#36809,#36810,
#36811,#36812,#36813,#36814,#36815,#36816,#36817,#36818,#36819,#36820,#36821,
#36822,#36823,#36824,#36825,#36826,#36827,#36828,#36829,#36830,#36831,#36832,
#36833,#36834,#36835,#36836,#36837),.UNSPECIFIED.,.F.,.F.,(4,2,2,2,2,2,
2,2,2,2,2,2,2,2,2,4),(3.62684812234147E-15,0.0392663678247153,0.0704169284195201,
0.0927548217158921,0.110721970139242,0.12356572275814,0.128289439508467,
0.131295508606043,0.134067308632338,0.137660564722272,0.145063726345893,
0.161462983995342,0.177979987306438,0.198867571223068,0.226369846272216,
0.25748926574638),.UNSPECIFIED.);
#431=B_SPLINE_CURVE_WITH_KNOTS('',3,(#36841,#36842,#36843,#36844,#36845,
#36846,#36847,#36848,#36849,#36850,#36851,#36852,#36853,#36854,#36855,#36856,
#36857,#36858,#36859,#36860,#36861,#36862,#36863,#36864,#36865,#36866,#36867,
#36868,#36869,#36870,#36871,#36872),.UNSPECIFIED.,.F.,.F.,(4,2,2,2,2,2,
2,2,2,2,2,2,2,2,2,4),(1.76634793841596E-15,0.0392663678246221,0.070416928418827,
0.0927548217143397,0.110721970136809,0.123565722754925,0.128289439504577,
0.131295508601993,0.134067308628616,0.137660564719576,0.145063726344241,
0.161462983995214,0.177979987307686,0.198867571225782,0.226369846276743,
0.257489265752939),.UNSPECIFIED.);
#432=B_SPLINE_CURVE_WITH_KNOTS('',3,(#36876,#36877,#36878,#36879,#36880,
#36881,#36882,#36883,#36884,#36885,#36886,#36887,#36888,#36889,#36890,#36891,
#36892,#36893,#36894,#36895,#36896,#36897,#36898,#36899,#36900,#36901,#36902,
#36903,#36904,#36905,#36906,#36907),.UNSPECIFIED.,.F.,.F.,(4,2,2,2,2,2,
2,2,2,2,2,2,2,2,2,4),(1.67219569290649E-15,0.0392663678248474,0.0704169284201005,
0.0927548217170368,0.110721970141041,0.123565722760672,0.128289439511198,
0.131295508609165,0.134067308635788,0.137660564725585,0.145063726348477,
0.161462983996445,0.177979987306176,0.198867571221256,0.226369846269141,
0.257489265742917),.UNSPECIFIED.);
#433=B_SPLINE_CURVE_WITH_KNOTS('',3,(#36911,#36912,#36913,#36914,#36915,
#36916,#36917,#36918,#36919,#36920,#36921,#36922,#36923,#36924,#36925,#36926,
#36927,#36928,#36929,#36930,#36931,#36932,#36933,#36934,#36935,#36936,#36937,
#36938,#36939,#36940,#36941,#36942),.UNSPECIFIED.,.F.,.F.,(4,2,2,2,2,2,
2,2,2,2,2,2,2,2,2,4),(1.57804344739692E-15,0.0392663678243967,0.0704169284187512,
0.0927548217148942,0.110721970138087,0.123565722756915,0.128289439507759,
0.131295508605752,0.134067308632248,0.137660564721969,0.145063726344741,
0.161462983992119,0.177979987301147,0.198867571215294,0.226369846261679,
0.257489265732903),.UNSPECIFIED.);
#434=B_SPLINE_CURVE_WITH_KNOTS('',3,(#36946,#36947,#36948,#36949,#36950,
#36951,#36952,#36953,#36954,#36955,#36956,#36957,#36958,#36959,#36960,#36961,
#36962,#36963,#36964,#36965,#36966,#36967,#36968,#36969,#36970,#36971,#36972,
#36973,#36974,#36975,#36976,#36977),.UNSPECIFIED.,.F.,.F.,(4,2,2,2,2,2,
2,2,2,2,2,2,2,2,2,4),(1.48389120188744E-15,0.0392663678246362,0.0704169284193307,
0.0927548217156513,0.11072197013894,0.123565722757702,0.128289439508219,
0.13129550860668,0.134067308633863,0.137660564724131,0.14506372634765,0.161462983996701,
0.177979987307462,0.198867571223755,0.22636984627265,0.257489265747157),
 .UNSPECIFIED.);
#435=B_SPLINE_CURVE_WITH_KNOTS('',3,(#36981,#36982,#36983,#36984,#36985,
#36986,#36987,#36988,#36989,#36990,#36991,#36992,#36993,#36994,#36995,#36996,
#36997,#36998,#36999,#37000,#37001,#37002,#37003,#37004,#37005,#37006,#37007,
#37008,#37009,#37010,#37011,#37012),.UNSPECIFIED.,.F.,.F.,(4,2,2,2,2,2,
2,2,2,2,2,2,2,2,2,4),(-1.86050018392547E-15,0.0392663678246196,0.070416928419344,
0.0927548217158401,0.110721970139278,0.123565722758188,0.128289439508702,
0.131295508606563,0.134067308633031,0.137660564722894,0.145063726346462,
0.161462983995227,0.177979987305691,0.198867571221603,0.226369846269658,
0.257489265742502),.UNSPECIFIED.);
#436=B_SPLINE_CURVE_WITH_KNOTS('',3,(#37016,#37017,#37018,#37019,#37020,
#37021,#37022,#37023,#37024,#37025,#37026,#37027,#37028,#37029,#37030,#37031,
#37032,#37033,#37034,#37035,#37036,#37037,#37038,#37039,#37040,#37041,#37042,
#37043,#37044,#37045,#37046,#37047),.UNSPECIFIED.,.F.,.F.,(4,2,2,2,2,2,
2,2,2,2,2,2,2,2,2,4),(0.,0.039266367824605,0.0704169284192653,0.0927548217155983,
0.110721970139038,0.123565722758227,0.128289439508356,0.131295508606434,
0.134067308633204,0.137660564722963,0.145063726346308,0.161462983994947,
0.177979987305301,0.198867571221117,0.22636984626943,0.257489265742971),
 .UNSPECIFIED.);
#437=B_SPLINE_CURVE_WITH_KNOTS('',3,(#37051,#37052,#37053,#37054,#37055,
#37056,#37057,#37058,#37059,#37060,#37061,#37062,#37063,#37064,#37065,#37066,
#37067,#37068,#37069,#37070,#37071,#37072,#37073,#37074,#37075,#37076,#37077,
#37078,#37079,#37080,#37081,#37082),.UNSPECIFIED.,.F.,.F.,(4,2,2,2,2,2,
2,2,2,2,2,2,2,2,2,4),(-1.76634793841601E-15,0.0392663678246844,0.0704169284198206,
0.0927548217167689,0.110721970140703,0.123565722760151,0.128289439510863,
0.131295508609073,0.134067308635863,0.137660564725819,0.145063726349486,
0.161462983998877,0.177979987310031,0.198867571226897,0.226369846277016,
0.257489265752877),.UNSPECIFIED.);
#438=B_SPLINE_CURVE_WITH_KNOTS('',3,(#37086,#37087,#37088,#37089,#37090,
#37091,#37092,#37093,#37094,#37095,#37096,#37097,#37098,#37099,#37100,#37101,
#37102,#37103,#37104,#37105,#37106,#37107,#37108,#37109,#37110,#37111,#37112,
#37113,#37114,#37115,#37116,#37117),.UNSPECIFIED.,.F.,.F.,(4,2,2,2,2,2,
2,2,2,2,2,2,2,2,2,4),(-1.76634793841602E-15,0.0392663678249098,0.0704169284202436,
0.0927548217171559,0.110721970140946,0.123565722760192,0.128289439510643,
0.13129550860873,0.134067308635531,0.137660564725647,0.14506372634943,0.161462983998864,
0.17797998731004,0.198867571226972,0.226369846276657,0.257489265751791),
 .UNSPECIFIED.);
#439=B_SPLINE_CURVE_WITH_KNOTS('',3,(#37121,#37122,#37123,#37124,#37125,
#37126,#37127,#37128,#37129,#37130,#37131,#37132,#37133,#37134,#37135,#37136,
#37137,#37138,#37139,#37140,#37141,#37142,#37143,#37144,#37145,#37146,#37147,
#37148,#37149,#37150,#37151,#37152),.UNSPECIFIED.,.F.,.F.,(4,2,2,2,2,2,
2,2,2,2,2,2,2,2,2,4),(1.76634793841582E-15,0.0392663678245818,0.0704169284194132,
0.0927548217159401,0.110721970139461,0.123565722758553,0.128289439508967,
0.131295508606888,0.134067308633461,0.137660564723424,0.14506372634746,
0.161462983997496,0.17797998730928,0.198867571226825,0.226369846276753,
0.257489265751656),.UNSPECIFIED.);
#440=B_SPLINE_CURVE_WITH_KNOTS('',3,(#37156,#37157,#37158,#37159,#37160,
#37161,#37162,#37163,#37164,#37165,#37166,#37167,#37168,#37169,#37170,#37171,
#37172,#37173,#37174,#37175,#37176,#37177,#37178,#37179,#37180,#37181,#37182,
#37183,#37184,#37185,#37186,#37187),.UNSPECIFIED.,.F.,.F.,(4,2,2,2,2,2,
2,2,2,2,2,2,2,2,2,4),(-1.76634793841602E-15,0.0392663678247105,0.0704169284196071,
0.0927548217161623,0.110721970139774,0.123565722758804,0.128289439509258,
0.131295508607385,0.134067308634216,0.137660564724393,0.145063726348231,
0.161462983997576,0.1779799873087,0.198867571225463,0.226369846275158,0.25748926575035),
 .UNSPECIFIED.);
#441=B_SPLINE_CURVE_WITH_KNOTS('',3,(#37191,#37192,#37193,#37194,#37195,
#37196,#37197,#37198,#37199,#37200,#37201,#37202,#37203,#37204,#37205,#37206,
#37207,#37208,#37209,#37210,#37211,#37212,#37213,#37214,#37215,#37216,#37217,
#37218,#37219,#37220,#37221,#37222),.UNSPECIFIED.,.F.,.F.,(4,2,2,2,2,2,
2,2,2,2,2,2,2,2,2,4),(0.,0.039266367824639,0.0704169284196416,0.0927548217164797,
0.110721970140397,0.123565722759903,0.128289439510384,0.131295508608112,
0.134067308634667,0.137660564725083,0.145063726349291,0.16146298399955,
0.177979987311731,0.198867571229869,0.226369846281328,0.257489265758592),
 .UNSPECIFIED.);
#442=B_SPLINE_CURVE_WITH_KNOTS('',3,(#37226,#37227,#37228,#37229,#37230,
#37231,#37232,#37233,#37234,#37235,#37236,#37237,#37238,#37239,#37240,#37241,
#37242,#37243,#37244,#37245,#37246,#37247,#37248,#37249,#37250,#37251,#37252,
#37253,#37254,#37255,#37256,#37257),.UNSPECIFIED.,.F.,.F.,(4,2,2,2,2,2,
2,2,2,2,2,2,2,2,2,4),(-1.76634793841584E-15,0.0392663678248517,0.0704169284197748,
0.0927548217161432,0.110721970139464,0.123565722758405,0.128289439508459,
0.131295508606329,0.134067308633017,0.137660564723293,0.145063726348177,
0.161462983999597,0.177979987312819,0.198867571232171,0.226369846284916,
0.257489265763157),.UNSPECIFIED.);
#443=B_SPLINE_CURVE_WITH_KNOTS('',3,(#37265,#37266,#37267,#37268,#37269,
#37270,#37271,#37272,#37273,#37274),.UNSPECIFIED.,.F.,.F.,(4,2,2,2,4),(-0.317026523413959,
-0.302322031379582,-0.181822057847978,-0.0905311996482953,-9.99999998141377E-7),
 .UNSPECIFIED.);
#444=B_SPLINE_CURVE_WITH_KNOTS('',3,(#37333,#37334,#37335,#37336,#37337,
#37338,#37339,#37340,#37341,#37342,#37343,#37344,#37345,#37346),
 .UNSPECIFIED.,.F.,.F.,(4,2,2,2,2,2,4),(-0.844978516211101,-0.706255465582548,
-0.570455953228873,-0.422452321689898,-0.274454069952361,-0.138687373055613,
0.),.UNSPECIFIED.);
#445=B_SPLINE_CURVE_WITH_KNOTS('',3,(#37347,#37348,#37349,#37350,#37351,
#37352,#37353,#37354,#37355,#37356),.UNSPECIFIED.,.F.,.F.,(4,2,2,2,4),(-0.564860666687477,
-0.387918780397416,-0.216626435797941,-0.0894002839461589,0.),
 .UNSPECIFIED.);
#446=B_SPLINE_CURVE_WITH_KNOTS('',3,(#37357,#37358,#37359,#37360,#37361,
#37362,#37363,#37364,#37365,#37366),.UNSPECIFIED.,.F.,.F.,(4,2,2,2,4),(-0.305777613429687,
-0.25789998327206,-0.189518825213173,-0.0962950640176603,0.),
 .UNSPECIFIED.);
#447=B_SPLINE_CURVE_WITH_KNOTS('',3,(#37373,#37374,#37375,#37376,#37377,
#37378,#37379,#37380,#37381,#37382),.UNSPECIFIED.,.F.,.F.,(4,2,2,2,4),(-0.305777613709471,
-0.257899983501032,-0.189518825369156,-0.0962950640743464,0.),
 .UNSPECIFIED.);
#448=B_SPLINE_CURVE_WITH_KNOTS('',3,(#37384,#37385,#37386,#37387,#37388,
#37389,#37390,#37391,#37392,#37393),.UNSPECIFIED.,.F.,.F.,(4,2,2,2,4),(-0.564860671099225,
-0.387918783323875,-0.216626437248832,-0.0894002842905878,0.),
 .UNSPECIFIED.);
#449=B_SPLINE_CURVE_WITH_KNOTS('',3,(#37394,#37395,#37396,#37397,#37398,
#37399,#37400,#37401,#37402,#37403,#37404,#37405,#37406,#37407),
 .UNSPECIFIED.,.F.,.F.,(4,2,2,2,2,2,4),(-0.844959728295684,-0.706031861511686,
-0.570044179645694,-0.421929648490435,-0.273898821298179,-0.13839817385903,
0.),.UNSPECIFIED.);
#587=(
BOUNDED_SURFACE()
B_SPLINE_SURFACE(1,2,((#37408,#37409,#37410,#37411,#37412,#37413,#37414,
#37415,#37416,#37417,#37418,#37419,#37420,#37421,#37422,#37423,#37424,#37425,
#37426,#37427,#37428,#37429,#37430,#37431,#37432,#37433,#37434,#37435,#37436,
#37437,#37438,#37439,#37440,#37441,#37442,#37443,#37444,#37445,#37446,#37447,
#37448,#37449,#37450,#37451,#37452,#37453,#37454,#37455,#37456,#37457,#37458,
#37459,#37460,#37461,#37462,#37463,#37464,#37465,#37466,#37467,#37468,#37469,
#37470,#37471,#37472,#37473,#37474,#37475,#37476,#37477,#37478,#37479,#37480,
#37481,#37482,#37483,#37484,#37485,#37486,#37487,#37488,#37489,#37490,#37491,
#37492,#37493,#37494,#37495,#37496,#37497,#37498,#37499,#37500,#37501,#37502,
#37503,#37504,#37505,#37506,#37507,#37508,#37509,#37510,#37511,#37512,#37513,
#37514,#37515,#37516,#37517,#37518,#37519,#37520,#37521,#37522,#37523,#37524,
#37525,#37526,#37527,#37528,#37529,#37530,#37531,#37532,#37533,#37534,#37535,
#37536,#37537,#37538,#37539,#37540,#37541,#37542,#37543,#37544,#37545,#37546,
#37547,#37548,#37549,#37550,#37551,#37552,#37553,#37554,#37555,#37556,#37557,
#37558,#37559,#37560,#37561,#37562,#37563,#37564,#37565,#37566,#37567,#37568,
#37569,#37570,#37571,#37572,#37573,#37574,#37575,#37576,#37577,#37578,#37579,
#37580,#37581,#37582,#37583,#37584,#37585,#37586,#37587,#37588,#37589,#37590,
#37591,#37592,#37593,#37594,#37595,#37596,#37597,#37598,#37599,#37600,#37601,
#37602,#37603,#37604,#37605,#37606,#37607,#37608,#37609,#37610,#37611,#37612,
#37613,#37614,#37615,#37616,#37617,#37618,#37619,#37620,#37621,#37622,#37623,
#37624,#37625,#37626,#37627,#37628,#37629,#37630,#37631,#37632,#37633,#37634,
#37635,#37636,#37637,#37638,#37639,#37640,#37641,#37642,#37643,#37644,#37645,
#37646,#37647,#37648,#37649,#37650,#37651,#37652,#37653,#37654,#37655,#37656,
#37657,#37658,#37659,#37660,#37661,#37662,#37663,#37664,#37665,#37666,#37667,
#37668,#37669,#37670,#37671,#37672,#37673,#37674,#37675,#37676,#37677,#37678,
#37679,#37680,#37681,#37682,#37683,#37684,#37685,#37686,#37687,#37688,#37689,
#37690,#37691,#37692,#37693,#37694,#37695,#37696,#37697,#37698,#37699,#37700,
#37701,#37702,#37703,#37704,#37705,#37706,#37707,#37708,#37709,#37710,#37711,
#37712,#37713,#37714,#37715,#37716,#37717,#37718,#37719,#37720,#37721,#37722,
#37723,#37724,#37725,#37726,#37727,#37728,#37729,#37730,#37731,#37732,#37733,
#37734,#37735,#37736,#37737,#37738,#37739,#37740,#37741,#37742,#37743,#37744,
#37745,#37746,#37747,#37748,#37749,#37750,#37751,#37752,#37753,#37754,#37755,
#37756,#37757,#37758,#37759,#37760,#37761,#37762,#37763,#37764,#37765,#37766,
#37767,#37768,#37769,#37770,#37771,#37772,#37773,#37774,#37775,#37776,#37777,
#37778,#37779,#37780,#37781,#37782,#37783,#37784,#37785,#37786,#37787,#37788,
#37789,#37790,#37791,#37792,#37793,#37794,#37795,#37796,#37797,#37798,#37799,
#37800,#37801,#37802,#37803,#37804,#37805,#37806,#37807,#37808,#37809,#37810,
#37811,#37812,#37813,#37814,#37815,#37816,#37817,#37818,#37819,#37820,#37821,
#37822,#37823,#37824,#37825,#37826,#37827,#37828,#37829,#37830,#37831,#37832,
#37833,#37834,#37835,#37836,#37837,#37838,#37839,#37840,#37841,#37842,#37843,
#37844,#37845,#37846,#37847,#37848,#37849,#37850,#37851,#37852,#37853,#37854,
#37855,#37856,#37857,#37858,#37859,#37860,#37861,#37862,#37863,#37864,#37865,
#37866,#37867,#37868,#37869,#37870,#37871,#37872,#37873,#37874,#37875,#37876,
#37877,#37878,#37879,#37880,#37881,#37882,#37883,#37884,#37885,#37886,#37887,
#37888,#37889,#37890,#37891,#37892,#37893,#37894,#37895,#37896,#37897,#37898,
#37899,#37900,#37901,#37902,#37903,#37904,#37905,#37906,#37907,#37908,#37909,
#37910,#37911,#37912,#37913,#37914,#37915,#37916,#37917,#37918,#37919,#37920,
#37921,#37922,#37923,#37924,#37925,#37926,#37927,#37928,#37929,#37930,#37931,
#37932,#37933,#37934,#37935,#37936,#37937,#37938,#37939,#37940,#37941,#37942,
#37943,#37944,#37945,#37946,#37947,#37948,#37949,#37950,#37951,#37952,#37953,
#37954,#37955,#37956,#37957,#37958,#37959,#37960,#37961,#37962,#37963,#37964,
#37965,#37966,#37967,#37968,#37969,#37970,#37971,#37972,#37973,#37974,#37975,
#37976,#37977,#37978,#37979,#37980,#37981,#37982,#37983,#37984,#37985,#37986,
#37987,#37988,#37989,#37990,#37991,#37992,#37993,#37994,#37995,#37996,#37997,
#37998,#37999,#38000,#38001,#38002,#38003,#38004,#38005,#38006,#38007,#38008,
#38009,#38010,#38011,#38012,#38013,#38014,#38015,#38016,#38017,#38018,#38019,
#38020,#38021,#38022,#38023,#38024,#38025,#38026,#38027,#38028,#38029,#38030,
#38031,#38032,#38033,#38034,#38035,#38036,#38037,#38038,#38039,#38040,#38041,
#38042,#38043,#38044,#38045,#38046,#38047,#38048,#38049,#38050,#38051,#38052,
#38053,#38054,#38055,#38056,#38057,#38058,#38059,#38060,#38061,#38062,#38063,
#38064,#38065,#38066,#38067,#38068,#38069,#38070,#38071,#38072,#38073,#38074,
#38075,#38076,#38077,#38078,#38079,#38080,#38081,#38082,#38083,#38084,#38085,
#38086,#38087,#38088,#38089,#38090,#38091,#38092,#38093,#38094,#38095,#38096,
#38097,#38098,#38099,#38100,#38101,#38102,#38103,#38104),(#38105,#38106,
#38107,#38108,#38109,#38110,#38111,#38112,#38113,#38114,#38115,#38116,#38117,
#38118,#38119,#38120,#38121,#38122,#38123,#38124,#38125,#38126,#38127,#38128,
#38129,#38130,#38131,#38132,#38133,#38134,#38135,#38136,#38137,#38138,#38139,
#38140,#38141,#38142,#38143,#38144,#38145,#38146,#38147,#38148,#38149,#38150,
#38151,#38152,#38153,#38154,#38155,#38156,#38157,#38158,#38159,#38160,#38161,
#38162,#38163,#38164,#38165,#38166,#38167,#38168,#38169,#38170,#38171,#38172,
#38173,#38174,#38175,#38176,#38177,#38178,#38179,#38180,#38181,#38182,#38183,
#38184,#38185,#38186,#38187,#38188,#38189,#38190,#38191,#38192,#38193,#38194,
#38195,#38196,#38197,#38198,#38199,#38200,#38201,#38202,#38203,#38204,#38205,
#38206,#38207,#38208,#38209,#38210,#38211,#38212,#38213,#38214,#38215,#38216,
#38217,#38218,#38219,#38220,#38221,#38222,#38223,#38224,#38225,#38226,#38227,
#38228,#38229,#38230,#38231,#38232,#38233,#38234,#38235,#38236,#38237,#38238,
#38239,#38240,#38241,#38242,#38243,#38244,#38245,#38246,#38247,#38248,#38249,
#38250,#38251,#38252,#38253,#38254,#38255,#38256,#38257,#38258,#38259,#38260,
#38261,#38262,#38263,#38264,#38265,#38266,#38267,#38268,#38269,#38270,#38271,
#38272,#38273,#38274,#38275,#38276,#38277,#38278,#38279,#38280,#38281,#38282,
#38283,#38284,#38285,#38286,#38287,#38288,#38289,#38290,#38291,#38292,#38293,
#38294,#38295,#38296,#38297,#38298,#38299,#38300,#38301,#38302,#38303,#38304,
#38305,#38306,#38307,#38308,#38309,#38310,#38311,#38312,#38313,#38314,#38315,
#38316,#38317,#38318,#38319,#38320,#38321,#38322,#38323,#38324,#38325,#38326,
#38327,#38328,#38329,#38330,#38331,#38332,#38333,#38334,#38335,#38336,#38337,
#38338,#38339,#38340,#38341,#38342,#38343,#38344,#38345,#38346,#38347,#38348,
#38349,#38350,#38351,#38352,#38353,#38354,#38355,#38356,#38357,#38358,#38359,
#38360,#38361,#38362,#38363,#38364,#38365,#38366,#38367,#38368,#38369,#38370,
#38371,#38372,#38373,#38374,#38375,#38376,#38377,#38378,#38379,#38380,#38381,
#38382,#38383,#38384,#38385,#38386,#38387,#38388,#38389,#38390,#38391,#38392,
#38393,#38394,#38395,#38396,#38397,#38398,#38399,#38400,#38401,#38402,#38403,
#38404,#38405,#38406,#38407,#38408,#38409,#38410,#38411,#38412,#38413,#38414,
#38415,#38416,#38417,#38418,#38419,#38420,#38421,#38422,#38423,#38424,#38425,
#38426,#38427,#38428,#38429,#38430,#38431,#38432,#38433,#38434,#38435,#38436,
#38437,#38438,#38439,#38440,#38441,#38442,#38443,#38444,#38445,#38446,#38447,
#38448,#38449,#38450,#38451,#38452,#38453,#38454,#38455,#38456,#38457,#38458,
#38459,#38460,#38461,#38462,#38463,#38464,#38465,#38466,#38467,#38468,#38469,
#38470,#38471,#38472,#38473,#38474,#38475,#38476,#38477,#38478,#38479,#38480,
#38481,#38482,#38483,#38484,#38485,#38486,#38487,#38488,#38489,#38490,#38491,
#38492,#38493,#38494,#38495,#38496,#38497,#38498,#38499,#38500,#38501,#38502,
#38503,#38504,#38505,#38506,#38507,#38508,#38509,#38510,#38511,#38512,#38513,
#38514,#38515,#38516,#38517,#38518,#38519,#38520,#38521,#38522,#38523,#38524,
#38525,#38526,#38527,#38528,#38529,#38530,#38531,#38532,#38533,#38534,#38535,
#38536,#38537,#38538,#38539,#38540,#38541,#38542,#38543,#38544,#38545,#38546,
#38547,#38548,#38549,#38550,#38551,#38552,#38553,#38554,#38555,#38556,#38557,
#38558,#38559,#38560,#38561,#38562,#38563,#38564,#38565,#38566,#38567,#38568,
#38569,#38570,#38571,#38572,#38573,#38574,#38575,#38576,#38577,#38578,#38579,
#38580,#38581,#38582,#38583,#38584,#38585,#38586,#38587,#38588,#38589,#38590,
#38591,#38592,#38593,#38594,#38595,#38596,#38597,#38598,#38599,#38600,#38601,
#38602,#38603,#38604,#38605,#38606,#38607,#38608,#38609,#38610,#38611,#38612,
#38613,#38614,#38615,#38616,#38617,#38618,#38619,#38620,#38621,#38622,#38623,
#38624,#38625,#38626,#38627,#38628,#38629,#38630,#38631,#38632,#38633,#38634,
#38635,#38636,#38637,#38638,#38639,#38640,#38641,#38642,#38643,#38644,#38645,
#38646,#38647,#38648,#38649,#38650,#38651,#38652,#38653,#38654,#38655,#38656,
#38657,#38658,#38659,#38660,#38661,#38662,#38663,#38664,#38665,#38666,#38667,
#38668,#38669,#38670,#38671,#38672,#38673,#38674,#38675,#38676,#38677,#38678,
#38679,#38680,#38681,#38682,#38683,#38684,#38685,#38686,#38687,#38688,#38689,
#38690,#38691,#38692,#38693,#38694,#38695,#38696,#38697,#38698,#38699,#38700,
#38701,#38702,#38703,#38704,#38705,#38706,#38707,#38708,#38709,#38710,#38711,
#38712,#38713,#38714,#38715,#38716,#38717,#38718,#38719,#38720,#38721,#38722,
#38723,#38724,#38725,#38726,#38727,#38728,#38729,#38730,#38731,#38732,#38733,
#38734,#38735,#38736,#38737,#38738,#38739,#38740,#38741,#38742,#38743,#38744,
#38745,#38746,#38747,#38748,#38749,#38750,#38751,#38752,#38753,#38754,#38755,
#38756,#38757,#38758,#38759,#38760,#38761,#38762,#38763,#38764,#38765,#38766,
#38767,#38768,#38769,#38770,#38771,#38772,#38773,#38774,#38775,#38776,#38777,
#38778,#38779,#38780,#38781,#38782,#38783,#38784,#38785,#38786,#38787,#38788,
#38789,#38790,#38791,#38792,#38793,#38794,#38795,#38796,#38797,#38798,#38799,
#38800,#38801)),.UNSPECIFIED.,.F.,.F.,.F.)
B_SPLINE_SURFACE_WITH_KNOTS((2,2),(3,2,2,2,2,2,2,2,2,2,2,2,2,2,2,2,2,2,
2,2,2,2,2,2,2,2,2,2,2,2,2,2,2,2,2,2,2,2,2,2,2,2,2,2,2,2,2,2,2,2,2,2,2,2,
2,2,2,2,2,2,2,2,2,2,2,2,2,2,2,2,2,2,2,2,2,2,2,2,2,2,2,2,2,2,2,2,2,2,2,2,
2,2,2,2,2,2,2,2,2,2,2,2,2,2,2,2,2,2,2,2,2,2,2,2,2,2,2,2,2,2,2,2,2,2,2,2,
2,2,2,2,2,2,2,2,2,2,2,2,2,2,2,2,2,2,2,2,2,2,2,2,2,2,2,2,2,2,2,2,2,2,2,2,
2,2,2,2,2,2,2,2,2,2,2,2,2,2,2,2,2,2,2,2,2,2,2,2,2,2,2,2,2,2,2,2,2,2,2,2,
2,2,2,2,2,2,2,2,2,2,2,2,2,2,2,2,2,2,2,2,2,2,2,2,2,2,2,2,2,2,2,2,2,2,2,2,
2,2,2,2,2,2,2,2,2,2,2,2,2,2,2,2,2,2,2,2,2,2,2,2,2,2,2,2,2,2,2,2,2,2,2,2,
2,2,2,2,2,2,2,2,2,2,2,2,2,2,2,2,2,2,2,2,2,2,2,2,2,2,2,2,2,2,2,2,2,2,2,2,
2,2,2,2,2,2,2,2,2,2,2,2,2,2,2,2,2,2,2,2,2,2,2,2,2,2,2,2,2,2,2,2,2,2,2,2,
2,2,2,2,2,2,3),(0.,1.),(0.,0.00284090909090909,0.00568181818181818,0.00852272727272727,
0.0113636363636364,0.0142045454545455,0.0170454545454545,0.0198863636363636,
0.0227272727272727,0.0255681818181818,0.0284090909090909,0.03125,0.0340909090909091,
0.0369318181818182,0.0397727272727273,0.0426136363636364,0.0454545454545455,
0.0482954545454545,0.0511363636363636,0.0539772727272727,0.0568181818181818,
0.0596590909090909,0.0625,0.0653409090909091,0.0681818181818182,0.0710227272727273,
0.0738636363636364,0.0767045454545455,0.0795454545454545,0.0823863636363636,
0.0852272727272727,0.0880681818181818,0.0909090909090909,0.09375,0.0965909090909091,
0.0994318181818182,0.102272727272727,0.105113636363636,0.107954545454545,
0.110795454545455,0.113636363636364,0.116477272727273,0.119318181818182,
0.122159090909091,0.125,0.127840909090909,0.130681818181818,0.133522727272727,
0.136363636363636,0.139204545454545,0.142045454545455,0.144886363636364,
0.147727272727273,0.150568181818182,0.153409090909091,0.15625,0.159090909090909,
0.161931818181818,0.164772727272727,0.167613636363636,0.170454545454545,
0.173295454545455,0.176136363636364,0.178977272727273,0.181818181818182,
0.184659090909091,0.1875,0.190340909090909,0.193181818181818,0.196022727272727,
0.198863636363636,0.201704545454545,0.204545454545455,0.207386363636364,
0.210227272727273,0.213068181818182,0.215909090909091,0.21875,0.221590909090909,
0.224431818181818,0.227272727272727,0.230113636363636,0.232954545454545,
0.235795454545455,0.238636363636364,0.241477272727273,0.244318181818182,
0.247159090909091,0.25,0.252840909090909,0.255681818181818,0.258522727272727,
0.261363636363636,0.264204545454545,0.267045454545455,0.269886363636364,
0.272727272727273,0.275568181818182,0.278409090909091,0.28125,0.284090909090909,
0.286931818181818,0.289772727272727,0.292613636363636,0.295454545454545,
0.298295454545455,0.301136363636364,0.303977272727273,0.306818181818182,
0.309659090909091,0.3125,0.315340909090909,0.318181818181818,0.321022727272727,
0.323863636363636,0.326704545454545,0.329545454545455,0.332386363636364,
0.335227272727273,0.338068181818182,0.340909090909091,0.34375,0.346590909090909,
0.349431818181818,0.352272727272727,0.355113636363636,0.357954545454545,
0.360795454545455,0.363636363636364,0.366477272727273,0.369318181818182,
0.372159090909091,0.375,0.377840909090909,0.380681818181818,0.383522727272727,
0.386363636363636,0.389204545454545,0.392045454545455,0.394886363636364,
0.397727272727273,0.400568181818182,0.403409090909091,0.40625,0.409090909090909,
0.411931818181818,0.414772727272727,0.417613636363636,0.420454545454545,
0.423295454545455,0.426136363636364,0.428977272727273,0.431818181818182,
0.434659090909091,0.4375,0.440340909090909,0.443181818181818,0.446022727272727,
0.448863636363636,0.451704545454545,0.454545454545455,0.457386363636364,
0.460227272727273,0.463068181818182,0.465909090909091,0.46875,0.471590909090909,
0.474431818181818,0.477272727272727,0.480113636363636,0.482954545454545,
0.485795454545455,0.488636363636364,0.491477272727273,0.494318181818182,
0.497159090909091,0.5,0.502840909090909,0.505681818181818,0.508522727272727,
0.511363636363636,0.514204545454545,0.517045454545455,0.519886363636364,
0.522727272727273,0.525568181818182,0.528409090909091,0.53125,0.534090909090909,
0.536931818181818,0.539772727272727,0.542613636363636,0.545454545454545,
0.548295454545455,0.551136363636364,0.553977272727273,0.556818181818182,
0.559659090909091,0.5625,0.565340909090909,0.568181818181818,0.571022727272727,
0.573863636363636,0.576704545454545,0.579545454545455,0.582386363636364,
0.585227272727273,0.588068181818182,0.590909090909091,0.59375,0.596590909090909,
0.599431818181818,0.602272727272727,0.605113636363636,0.607954545454545,
0.610795454545455,0.613636363636364,0.616477272727273,0.619318181818182,
0.622159090909091,0.625,0.627840909090909,0.630681818181818,0.633522727272727,
0.636363636363636,0.639204545454545,0.642045454545455,0.644886363636364,
0.647727272727273,0.650568181818182,0.653409090909091,0.65625,0.659090909090909,
0.661931818181818,0.664772727272727,0.667613636363636,0.670454545454545,
0.673295454545455,0.676136363636364,0.678977272727273,0.681818181818182,
0.684659090909091,0.6875,0.690340909090909,0.693181818181818,0.696022727272727,
0.698863636363636,0.701704545454545,0.704545454545455,0.707386363636364,
0.710227272727273,0.713068181818182,0.715909090909091,0.71875,0.721590909090909,
0.724431818181818,0.727272727272727,0.730113636363636,0.732954545454545,
0.735795454545455,0.738636363636364,0.741477272727273,0.744318181818182,
0.747159090909091,0.75,0.752840909090909,0.755681818181818,0.758522727272727,
0.761363636363636,0.764204545454545,0.767045454545455,0.769886363636364,
0.772727272727273,0.775568181818182,0.778409090909091,0.78125,0.784090909090909,
0.786931818181818,0.789772727272727,0.792613636363636,0.795454545454545,
0.798295454545455,0.801136363636364,0.803977272727273,0.806818181818182,
0.809659090909091,0.8125,0.815340909090909,0.818181818181818,0.821022727272727,
0.823863636363636,0.826704545454545,0.829545454545455,0.832386363636364,
0.835227272727273,0.838068181818182,0.840909090909091,0.84375,0.846590909090909,
0.849431818181818,0.852272727272727,0.855113636363636,0.857954545454545,
0.860795454545455,0.863636363636364,0.866477272727273,0.869318181818182,
0.872159090909091,0.875,0.877840909090909,0.880681818181818,0.883522727272727,
0.886363636363636,0.889204545454545,0.892045454545455,0.894886363636364,
0.897727272727273,0.900568181818182,0.903409090909091,0.90625,0.909090909090909,
0.911931818181818,0.914772727272727,0.917613636363636,0.920454545454545,
0.923295454545455,0.926136363636364,0.928977272727273,0.931818181818182,
0.934659090909091,0.9375,0.940340909090909,0.943181818181818,0.946022727272727,
0.948863636363636,0.951704545454545,0.954545454545455,0.957386363636364,
0.960227272727273,0.963068181818182,0.965909090909091,0.96875,0.971590909090909,
0.974431818181818,0.977272727272727,0.980113636363636,0.982954545454545,
0.984842983060018,0.994691412890618),.UNSPECIFIED.)
GEOMETRIC_REPRESENTATION_ITEM()
RATIONAL_B_SPLINE_SURFACE(((1.,0.923879532511287,1.,0.923879532511287,1.,
0.923879532511287,1.,0.923879532511287,1.,0.923879532511287,1.,0.923879532511287,
1.,0.923879532511287,1.,0.923879532511287,1.,0.923879532511287,1.,0.923879532511287,
1.,0.923879532511287,1.,0.923879532511287,1.,0.923879532511287,1.,0.923879532511287,
1.,0.923879532511287,1.,0.923879532511287,1.,0.923879532511287,1.,0.923879532511287,
1.,0.923879532511287,1.,0.923879532511287,1.,0.923879532511287,1.,0.923879532511287,
1.,0.923879532511287,1.,0.923879532511287,1.,0.923879532511287,1.,0.923879532511287,
1.,0.923879532511287,1.,0.923879532511287,1.,0.923879532511287,1.,0.923879532511287,
1.,0.923879532511287,1.,0.923879532511287,1.,0.923879532511287,1.,0.923879532511287,
1.,0.923879532511287,1.,0.923879532511287,1.,0.923879532511287,1.,0.923879532511287,
1.,0.923879532511287,1.,0.923879532511287,1.,0.923879532511287,1.,0.923879532511287,
1.,0.923879532511287,1.,0.923879532511287,1.,0.923879532511287,1.,0.923879532511287,
1.,0.923879532511287,1.,0.923879532511287,1.,0.923879532511287,1.,0.923879532511287,
1.,0.923879532511287,1.,0.923879532511287,1.,0.923879532511287,1.,0.923879532511287,
1.,0.923879532511287,1.,0.923879532511287,1.,0.923879532511287,1.,0.923879532511287,
1.,0.923879532511287,1.,0.923879532511287,1.,0.923879532511287,1.,0.923879532511287,
1.,0.923879532511287,1.,0.923879532511287,1.,0.923879532511287,1.,0.923879532511287,
1.,0.923879532511287,1.,0.923879532511287,1.,0.923879532511287,1.,0.923879532511287,
1.,0.923879532511287,1.,0.923879532511287,1.,0.923879532511287,1.,0.923879532511287,
1.,0.923879532511287,1.,0.923879532511287,1.,0.923879532511287,1.,0.923879532511287,
1.,0.923879532511287,1.,0.923879532511287,1.,0.923879532511287,1.,0.923879532511287,
1.,0.923879532511287,1.,0.923879532511287,1.,0.923879532511287,1.,0.923879532511287,
1.,0.923879532511287,1.,0.923879532511287,1.,0.923879532511287,1.,0.923879532511287,
1.,0.923879532511287,1.,0.923879532511287,1.,0.923879532511287,1.,0.923879532511287,
1.,0.923879532511287,1.,0.923879532511287,1.,0.923879532511287,1.,0.923879532511287,
1.,0.923879532511287,1.,0.923879532511287,1.,0.923879532511287,1.,0.923879532511287,
1.,0.923879532511287,1.,0.923879532511287,1.,0.923879532511287,1.,0.923879532511287,
1.,0.923879532511287,1.,0.923879532511287,1.,0.923879532511287,1.,0.923879532511287,
1.,0.923879532511287,1.,0.923879532511287,1.,0.923879532511287,1.,0.923879532511287,
1.,0.923879532511287,1.,0.923879532511287,1.,0.923879532511287,1.,0.923879532511287,
1.,0.923879532511287,1.,0.923879532511287,1.,0.923879532511287,1.,0.923879532511287,
1.,0.923879532511287,1.,0.923879532511287,1.,0.923879532511287,1.,0.923879532511287,
1.,0.923879532511287,1.,0.923879532511287,1.,0.923879532511287,1.,0.923879532511287,
1.,0.923879532511287,1.,0.923879532511287,1.,0.923879532511287,1.,0.923879532511287,
1.,0.923879532511287,1.,0.923879532511287,1.,0.923879532511287,1.,0.923879532511287,
1.,0.923879532511287,1.,0.923879532511287,1.,0.923879532511287,1.,0.923879532511287,
1.,0.923879532511287,1.,0.923879532511287,1.,0.923879532511287,1.,0.923879532511287,
1.,0.923879532511287,1.,0.923879532511287,1.,0.923879532511287,1.,0.923879532511287,
1.,0.923879532511287,1.,0.923879532511287,1.,0.923879532511287,1.,0.923879532511287,
1.,0.923879532511287,1.,0.923879532511287,1.,0.923879532511287,1.,0.923879532511287,
1.,0.923879532511287,1.,0.923879532511287,1.,0.923879532511287,1.,0.923879532511287,
1.,0.923879532511287,1.,0.923879532511287,1.,0.923879532511287,1.,0.923879532511287,
1.,0.923879532511287,1.,0.923879532511287,1.,0.923879532511287,1.,0.923879532511287,
1.,0.923879532511287,1.,0.923879532511287,1.,0.923879532511287,1.,0.923879532511287,
1.,0.923879532511287,1.,0.923879532511287,1.,0.923879532511287,1.,0.923879532511287,
1.,0.923879532511287,1.,0.923879532511287,1.,0.923879532511287,1.,0.923879532511287,
1.,0.923879532511287,1.,0.923879532511287,1.,0.923879532511287,1.,0.923879532511287,
1.,0.923879532511287,1.,0.923879532511287,1.,0.923879532511287,1.,0.923879532511287,
1.,0.923879532511287,1.,0.923879532511287,1.,0.923879532511287,1.,0.923879532511287,
1.,0.923879532511287,1.,0.923879532511287,1.,0.923879532511287,1.,0.923879532511287,
1.,0.923879532511287,1.,0.923879532511287,1.,0.923879532511287,1.,0.923879532511287,
1.,0.923879532511287,1.,0.923879532511287,1.,0.923879532511287,1.,0.923879532511287,
1.,0.923879532511287,1.,0.923879532511287,1.,0.923879532511287,1.,0.923879532511287,
1.,0.923879532511287,1.,0.923879532511287,1.,0.923879532511287,1.,0.923879532511287,
1.,0.923879532511287,1.,0.923879532511287,1.,0.923879532511287,1.,0.923879532511287,
1.,0.923879532511287,1.,0.923879532511287,1.,0.923879532511287,1.,0.923879532511287,
1.,0.923879532511287,1.,0.923879532511287,1.,0.923879532511287,1.,0.923879532511287,
1.,0.923879532511287,1.,0.923879532511287,1.,0.923879532511287,1.,0.923879532511287,
1.,0.923879532511287,1.,0.923879532511287,1.,0.923879532511287,1.,0.923879532511287,
1.,0.923879532511287,1.,0.923879532511287,1.,0.923879532511287,1.,0.923879532511287,
1.,0.923879532511287,1.,0.923879532511287,1.,0.923879532511287,1.,0.923879532511287,
1.,0.923879532511287,1.,0.923879532511287,1.,0.923879532511287,1.,0.923879532511287,
1.,0.923879532511287,1.,0.923879532511287,1.,0.923879532511287,1.,0.923879532511287,
1.,0.923879532511287,1.,0.923879532511287,1.,0.923879532511287,1.,0.923879532511287,
1.,0.923879532511287,1.,0.923879532511287,1.,0.923879532511287,1.,0.923879532511287,
1.,0.923879532511287,1.,0.923879532511287,1.,0.923879532511287,1.,0.923879532511287,
1.,0.923879532511287,1.,0.923879532511287,1.,0.923879532511287,1.,0.923879532511287,
1.,0.923879532511287,1.,0.923879532511287,1.,0.923879532511287,1.,0.923879532511287,
1.,0.923879532511287,1.,0.923879532511287,1.,0.923879532511287,1.,0.923879532511287,
1.,0.923879532511287,1.,0.923879532511287,1.,0.923879532511287,1.,0.923879532511287,
1.,0.923879532511287,1.,0.923879532511287,1.,0.923879532511287,1.,0.923879532511287,
1.,0.923879532511287,1.,0.923879532511287,1.,0.923879532511287,1.,0.923879532511287,
1.,0.923879532511287,1.,0.923879532511287,1.,0.923879532511287,1.,0.923879532511287,
1.,0.923879532511287,1.,0.923879532511287,1.,0.923879532511287,1.,0.923879532511287,
1.,0.923879532511287,1.,0.923879532511287,1.,0.923879532511287,1.,0.923879532511287,
1.,0.923879532511287,1.,0.923879532511287,1.,0.923879532511287,1.,0.923879532511287,
1.,0.923879532511287,1.,0.923879532511287,1.,0.923879532511287,1.,0.923879532511287,
1.,0.923879532511287,1.,0.923879532511287,1.,0.923879532511287,1.,0.923879532511287,
1.,0.923879532511287,1.,0.923879532511287,1.,0.923879532511287,1.,0.923879532511287,
1.,0.923879532511287,1.,0.923879532511287,1.,0.923879532511287,1.,0.923879532511287,
1.,0.923879532511287,1.,0.923879532511287,1.,0.923879532511287,1.,0.923879532511287,
1.,0.923879532511287,1.,0.923879532511287,1.,0.923879532511287,1.,0.923879532511287,
1.,0.923879532511287,1.,0.923879532511287,1.,0.923879532511287,1.,0.923879532511287,
1.,0.923879532511287,1.,0.923879532511287,1.,0.923879532511287,1.,0.923879532511287,
1.,0.923879532511287,1.,0.923879532511287,1.,0.923879532511287,1.,0.923879532511287,
1.,0.923879532511287,1.,0.923879532511287,1.,0.923879532511287,1.,0.923879532511287,
1.,0.923879532511287,1.,0.923879532511287,1.,0.923879532511287,1.,0.923879532511287,
1.,0.949400438820153,0.966070974003619,0.966070974003619,0.966070974003619),
(1.,0.923879532511287,1.,0.923879532511287,1.,0.923879532511287,1.,0.923879532511287,
1.,0.923879532511287,1.,0.923879532511287,1.,0.923879532511287,1.,0.923879532511287,
1.,0.923879532511287,1.,0.923879532511287,1.,0.923879532511287,1.,0.923879532511287,
1.,0.923879532511287,1.,0.923879532511287,1.,0.923879532511287,1.,0.923879532511287,
1.,0.923879532511287,1.,0.923879532511287,1.,0.923879532511287,1.,0.923879532511287,
1.,0.923879532511287,1.,0.923879532511287,1.,0.923879532511287,1.,0.923879532511287,
1.,0.923879532511287,1.,0.923879532511287,1.,0.923879532511287,1.,0.923879532511287,
1.,0.923879532511287,1.,0.923879532511287,1.,0.923879532511287,1.,0.923879532511287,
1.,0.923879532511287,1.,0.923879532511287,1.,0.923879532511287,1.,0.923879532511287,
1.,0.923879532511287,1.,0.923879532511287,1.,0.923879532511287,1.,0.923879532511287,
1.,0.923879532511287,1.,0.923879532511287,1.,0.923879532511287,1.,0.923879532511287,
1.,0.923879532511287,1.,0.923879532511287,1.,0.923879532511287,1.,0.923879532511287,
1.,0.923879532511287,1.,0.923879532511287,1.,0.923879532511287,1.,0.923879532511287,
1.,0.923879532511287,1.,0.923879532511287,1.,0.923879532511287,1.,0.923879532511287,
1.,0.923879532511287,1.,0.923879532511287,1.,0.923879532511287,1.,0.923879532511287,
1.,0.923879532511287,1.,0.923879532511287,1.,0.923879532511287,1.,0.923879532511287,
1.,0.923879532511287,1.,0.923879532511287,1.,0.923879532511287,1.,0.923879532511287,
1.,0.923879532511287,1.,0.923879532511287,1.,0.923879532511287,1.,0.923879532511287,
1.,0.923879532511287,1.,0.923879532511287,1.,0.923879532511287,1.,0.923879532511287,
1.,0.923879532511287,1.,0.923879532511287,1.,0.923879532511287,1.,0.923879532511287,
1.,0.923879532511287,1.,0.923879532511287,1.,0.923879532511287,1.,0.923879532511287,
1.,0.923879532511287,1.,0.923879532511287,1.,0.923879532511287,1.,0.923879532511287,
1.,0.923879532511287,1.,0.923879532511287,1.,0.923879532511287,1.,0.923879532511287,
1.,0.923879532511287,1.,0.923879532511287,1.,0.923879532511287,1.,0.923879532511287,
1.,0.923879532511287,1.,0.923879532511287,1.,0.923879532511287,1.,0.923879532511287,
1.,0.923879532511287,1.,0.923879532511287,1.,0.923879532511287,1.,0.923879532511287,
1.,0.923879532511287,1.,0.923879532511287,1.,0.923879532511287,1.,0.923879532511287,
1.,0.923879532511287,1.,0.923879532511287,1.,0.923879532511287,1.,0.923879532511287,
1.,0.923879532511287,1.,0.923879532511287,1.,0.923879532511287,1.,0.923879532511287,
1.,0.923879532511287,1.,0.923879532511287,1.,0.923879532511287,1.,0.923879532511287,
1.,0.923879532511287,1.,0.923879532511287,1.,0.923879532511287,1.,0.923879532511287,
1.,0.923879532511287,1.,0.923879532511287,1.,0.923879532511287,1.,0.923879532511287,
1.,0.923879532511287,1.,0.923879532511287,1.,0.923879532511287,1.,0.923879532511287,
1.,0.923879532511287,1.,0.923879532511287,1.,0.923879532511287,1.,0.923879532511287,
1.,0.923879532511287,1.,0.923879532511287,1.,0.923879532511287,1.,0.923879532511287,
1.,0.923879532511287,1.,0.923879532511287,1.,0.923879532511287,1.,0.923879532511287,
1.,0.923879532511287,1.,0.923879532511287,1.,0.923879532511287,1.,0.923879532511287,
1.,0.923879532511287,1.,0.923879532511287,1.,0.923879532511287,1.,0.923879532511287,
1.,0.923879532511287,1.,0.923879532511287,1.,0.923879532511287,1.,0.923879532511287,
1.,0.923879532511287,1.,0.923879532511287,1.,0.923879532511287,1.,0.923879532511287,
1.,0.923879532511287,1.,0.923879532511287,1.,0.923879532511287,1.,0.923879532511287,
1.,0.923879532511287,1.,0.923879532511287,1.,0.923879532511287,1.,0.923879532511287,
1.,0.923879532511287,1.,0.923879532511287,1.,0.923879532511287,1.,0.923879532511287,
1.,0.923879532511287,1.,0.923879532511287,1.,0.923879532511287,1.,0.923879532511287,
1.,0.923879532511287,1.,0.923879532511287,1.,0.923879532511287,1.,0.923879532511287,
1.,0.923879532511287,1.,0.923879532511287,1.,0.923879532511287,1.,0.923879532511287,
1.,0.923879532511287,1.,0.923879532511287,1.,0.923879532511287,1.,0.923879532511287,
1.,0.923879532511287,1.,0.923879532511287,1.,0.923879532511287,1.,0.923879532511287,
1.,0.923879532511287,1.,0.923879532511287,1.,0.923879532511287,1.,0.923879532511287,
1.,0.923879532511287,1.,0.923879532511287,1.,0.923879532511287,1.,0.923879532511287,
1.,0.923879532511287,1.,0.923879532511287,1.,0.923879532511287,1.,0.923879532511287,
1.,0.923879532511287,1.,0.923879532511287,1.,0.923879532511287,1.,0.923879532511287,
1.,0.923879532511287,1.,0.923879532511287,1.,0.923879532511287,1.,0.923879532511287,
1.,0.923879532511287,1.,0.923879532511287,1.,0.923879532511287,1.,0.923879532511287,
1.,0.923879532511287,1.,0.923879532511287,1.,0.923879532511287,1.,0.923879532511287,
1.,0.923879532511287,1.,0.923879532511287,1.,0.923879532511287,1.,0.923879532511287,
1.,0.923879532511287,1.,0.923879532511287,1.,0.923879532511287,1.,0.923879532511287,
1.,0.923879532511287,1.,0.923879532511287,1.,0.923879532511287,1.,0.923879532511287,
1.,0.923879532511287,1.,0.923879532511287,1.,0.923879532511287,1.,0.923879532511287,
1.,0.923879532511287,1.,0.923879532511287,1.,0.923879532511287,1.,0.923879532511287,
1.,0.923879532511287,1.,0.923879532511287,1.,0.923879532511287,1.,0.923879532511287,
1.,0.923879532511287,1.,0.923879532511287,1.,0.923879532511287,1.,0.923879532511287,
1.,0.923879532511287,1.,0.923879532511287,1.,0.923879532511287,1.,0.923879532511287,
1.,0.923879532511287,1.,0.923879532511287,1.,0.923879532511287,1.,0.923879532511287,
1.,0.923879532511287,1.,0.923879532511287,1.,0.923879532511287,1.,0.923879532511287,
1.,0.923879532511287,1.,0.923879532511287,1.,0.923879532511287,1.,0.923879532511287,
1.,0.923879532511287,1.,0.923879532511287,1.,0.923879532511287,1.,0.923879532511287,
1.,0.923879532511287,1.,0.923879532511287,1.,0.923879532511287,1.,0.923879532511287,
1.,0.923879532511287,1.,0.923879532511287,1.,0.923879532511287,1.,0.923879532511287,
1.,0.923879532511287,1.,0.923879532511287,1.,0.923879532511287,1.,0.923879532511287,
1.,0.923879532511287,1.,0.923879532511287,1.,0.923879532511287,1.,0.923879532511287,
1.,0.923879532511287,1.,0.923879532511287,1.,0.923879532511287,1.,0.923879532511287,
1.,0.923879532511287,1.,0.923879532511287,1.,0.923879532511287,1.,0.923879532511287,
1.,0.923879532511287,1.,0.923879532511287,1.,0.923879532511287,1.,0.923879532511287,
1.,0.923879532511287,1.,0.923879532511287,1.,0.923879532511287,1.,0.923879532511287,
1.,0.923879532511287,1.,0.923879532511287,1.,0.923879532511287,1.,0.923879532511287,
1.,0.923879532511287,1.,0.923879532511287,1.,0.923879532511287,1.,0.923879532511287,
1.,0.923879532511287,1.,0.923879532511287,1.,0.923879532511287,1.,0.923879532511287,
1.,0.923879532511287,1.,0.923879532511287,1.,0.923879532511287,1.,0.923879532511287,
1.,0.923879532511287,1.,0.923879532511287,1.,0.923879532511287,1.,0.923879532511287,
1.,0.923879532511287,1.,0.923879532511287,1.,0.923879532511287,1.,0.923879532511287,
1.,0.923879532511287,1.,0.923879532511287,1.,0.923879532511287,1.,0.923879532511287,
1.,0.923879532511287,1.,0.923879532511287,1.,0.923879532511287,1.,0.923879532511287,
1.,0.923879532511287,1.,0.923879532511287,1.,0.923879532511287,1.,0.923879532511287,
1.,0.923879532511287,1.,0.923879532511287,1.,0.923879532511287,1.,0.923879532511287,
1.,0.923879532511287,1.,0.923879532511287,1.,0.923879532511287,1.,0.923879532511287,
1.,0.923879532511287,1.,0.923879532511287,1.,0.949400438820153,0.966070974003619,
0.966070974003619,0.966070974003619)))
REPRESENTATION_ITEM('')
SURFACE()
);
#588=(
BOUNDED_SURFACE()
B_SPLINE_SURFACE(1,2,((#39445,#39446,#39447,#39448,#39449,#39450,#39451,
#39452,#39453,#39454,#39455,#39456,#39457,#39458,#39459,#39460,#39461,#39462,
#39463,#39464,#39465,#39466,#39467,#39468,#39469,#39470,#39471,#39472,#39473,
#39474,#39475,#39476,#39477,#39478,#39479,#39480,#39481,#39482,#39483,#39484,
#39485,#39486,#39487,#39488,#39489,#39490,#39491,#39492,#39493,#39494,#39495,
#39496,#39497,#39498,#39499,#39500,#39501,#39502,#39503,#39504,#39505,#39506,
#39507,#39508,#39509,#39510,#39511,#39512,#39513,#39514,#39515,#39516,#39517,
#39518,#39519,#39520,#39521,#39522,#39523,#39524,#39525,#39526,#39527,#39528,
#39529,#39530,#39531,#39532,#39533,#39534,#39535,#39536,#39537,#39538,#39539,
#39540,#39541,#39542,#39543,#39544,#39545,#39546,#39547,#39548,#39549,#39550,
#39551,#39552,#39553,#39554,#39555,#39556,#39557,#39558,#39559,#39560,#39561,
#39562,#39563,#39564,#39565,#39566,#39567,#39568,#39569,#39570,#39571,#39572,
#39573,#39574,#39575,#39576,#39577,#39578,#39579,#39580,#39581,#39582,#39583,
#39584,#39585,#39586,#39587,#39588,#39589,#39590,#39591,#39592,#39593,#39594,
#39595,#39596,#39597,#39598,#39599,#39600,#39601,#39602,#39603,#39604,#39605,
#39606,#39607,#39608,#39609,#39610,#39611,#39612,#39613,#39614,#39615,#39616,
#39617,#39618,#39619,#39620,#39621,#39622,#39623,#39624,#39625,#39626,#39627,
#39628,#39629,#39630,#39631,#39632,#39633,#39634,#39635,#39636,#39637,#39638,
#39639,#39640,#39641,#39642,#39643,#39644,#39645,#39646,#39647,#39648,#39649,
#39650,#39651,#39652,#39653,#39654,#39655,#39656,#39657,#39658,#39659,#39660,
#39661,#39662,#39663,#39664,#39665,#39666,#39667,#39668,#39669,#39670,#39671,
#39672,#39673,#39674,#39675,#39676,#39677,#39678,#39679,#39680,#39681,#39682,
#39683,#39684,#39685,#39686,#39687,#39688,#39689,#39690,#39691,#39692,#39693,
#39694,#39695,#39696,#39697,#39698,#39699,#39700,#39701,#39702,#39703,#39704,
#39705,#39706,#39707,#39708,#39709,#39710,#39711,#39712,#39713,#39714,#39715,
#39716,#39717,#39718,#39719,#39720,#39721,#39722,#39723,#39724,#39725,#39726,
#39727,#39728,#39729,#39730,#39731,#39732,#39733,#39734,#39735,#39736,#39737,
#39738,#39739,#39740,#39741,#39742,#39743,#39744,#39745,#39746,#39747,#39748,
#39749,#39750,#39751,#39752,#39753,#39754,#39755,#39756,#39757,#39758,#39759,
#39760,#39761,#39762,#39763,#39764,#39765,#39766,#39767,#39768,#39769,#39770,
#39771,#39772,#39773,#39774,#39775,#39776,#39777,#39778,#39779,#39780,#39781,
#39782,#39783,#39784,#39785,#39786,#39787,#39788,#39789,#39790,#39791,#39792,
#39793,#39794,#39795,#39796,#39797,#39798,#39799,#39800,#39801,#39802,#39803,
#39804,#39805,#39806,#39807,#39808,#39809,#39810,#39811,#39812,#39813,#39814,
#39815,#39816,#39817,#39818,#39819,#39820,#39821,#39822,#39823,#39824,#39825,
#39826,#39827,#39828,#39829,#39830,#39831,#39832,#39833,#39834,#39835,#39836,
#39837,#39838,#39839,#39840,#39841,#39842,#39843,#39844,#39845,#39846,#39847,
#39848,#39849,#39850,#39851,#39852,#39853,#39854,#39855,#39856,#39857,#39858,
#39859,#39860,#39861,#39862,#39863,#39864,#39865,#39866,#39867,#39868,#39869,
#39870,#39871,#39872,#39873,#39874,#39875,#39876,#39877,#39878,#39879,#39880,
#39881,#39882,#39883,#39884,#39885,#39886,#39887,#39888,#39889,#39890,#39891,
#39892,#39893,#39894,#39895,#39896,#39897,#39898,#39899,#39900,#39901,#39902,
#39903,#39904,#39905,#39906,#39907,#39908,#39909,#39910,#39911,#39912,#39913,
#39914,#39915,#39916,#39917,#39918,#39919,#39920,#39921,#39922,#39923,#39924,
#39925,#39926,#39927,#39928,#39929,#39930,#39931,#39932,#39933,#39934,#39935,
#39936,#39937,#39938,#39939,#39940,#39941,#39942,#39943,#39944,#39945,#39946,
#39947,#39948,#39949,#39950,#39951,#39952,#39953,#39954,#39955,#39956,#39957,
#39958,#39959,#39960,#39961,#39962,#39963,#39964,#39965,#39966,#39967,#39968,
#39969,#39970,#39971,#39972,#39973,#39974,#39975,#39976,#39977,#39978,#39979,
#39980,#39981,#39982,#39983,#39984,#39985,#39986,#39987,#39988,#39989,#39990,
#39991,#39992,#39993,#39994,#39995,#39996,#39997,#39998,#39999,#40000,#40001,
#40002,#40003,#40004,#40005,#40006,#40007,#40008,#40009,#40010,#40011,#40012,
#40013,#40014,#40015,#40016,#40017,#40018,#40019,#40020,#40021,#40022,#40023,
#40024,#40025,#40026,#40027,#40028,#40029,#40030,#40031,#40032,#40033,#40034,
#40035,#40036,#40037,#40038,#40039,#40040,#40041,#40042,#40043,#40044,#40045,
#40046,#40047,#40048,#40049,#40050,#40051,#40052,#40053,#40054,#40055,#40056,
#40057,#40058,#40059,#40060,#40061,#40062,#40063,#40064,#40065,#40066,#40067,
#40068,#40069,#40070,#40071,#40072,#40073,#40074,#40075,#40076,#40077,#40078,
#40079,#40080,#40081,#40082,#40083,#40084,#40085,#40086,#40087,#40088,#40089,
#40090,#40091,#40092,#40093,#40094,#40095,#40096,#40097,#40098,#40099,#40100,
#40101,#40102,#40103,#40104,#40105,#40106,#40107,#40108,#40109,#40110,#40111,
#40112,#40113,#40114,#40115,#40116,#40117,#40118,#40119,#40120,#40121,#40122,
#40123,#40124,#40125,#40126,#40127,#40128,#40129,#40130,#40131,#40132,#40133,
#40134,#40135,#40136,#40137,#40138,#40139),(#40140,#40141,#40142,#40143,
#40144,#40145,#40146,#40147,#40148,#40149,#40150,#40151,#40152,#40153,#40154,
#40155,#40156,#40157,#40158,#40159,#40160,#40161,#40162,#40163,#40164,#40165,
#40166,#40167,#40168,#40169,#40170,#40171,#40172,#40173,#40174,#40175,#40176,
#40177,#40178,#40179,#40180,#40181,#40182,#40183,#40184,#40185,#40186,#40187,
#40188,#40189,#40190,#40191,#40192,#40193,#40194,#40195,#40196,#40197,#40198,
#40199,#40200,#40201,#40202,#40203,#40204,#40205,#40206,#40207,#40208,#40209,
#40210,#40211,#40212,#40213,#40214,#40215,#40216,#40217,#40218,#40219,#40220,
#40221,#40222,#40223,#40224,#40225,#40226,#40227,#40228,#40229,#40230,#40231,
#40232,#40233,#40234,#40235,#40236,#40237,#40238,#40239,#40240,#40241,#40242,
#40243,#40244,#40245,#40246,#40247,#40248,#40249,#40250,#40251,#40252,#40253,
#40254,#40255,#40256,#40257,#40258,#40259,#40260,#40261,#40262,#40263,#40264,
#40265,#40266,#40267,#40268,#40269,#40270,#40271,#40272,#40273,#40274,#40275,
#40276,#40277,#40278,#40279,#40280,#40281,#40282,#40283,#40284,#40285,#40286,
#40287,#40288,#40289,#40290,#40291,#40292,#40293,#40294,#40295,#40296,#40297,
#40298,#40299,#40300,#40301,#40302,#40303,#40304,#40305,#40306,#40307,#40308,
#40309,#40310,#40311,#40312,#40313,#40314,#40315,#40316,#40317,#40318,#40319,
#40320,#40321,#40322,#40323,#40324,#40325,#40326,#40327,#40328,#40329,#40330,
#40331,#40332,#40333,#40334,#40335,#40336,#40337,#40338,#40339,#40340,#40341,
#40342,#40343,#40344,#40345,#40346,#40347,#40348,#40349,#40350,#40351,#40352,
#40353,#40354,#40355,#40356,#40357,#40358,#40359,#40360,#40361,#40362,#40363,
#40364,#40365,#40366,#40367,#40368,#40369,#40370,#40371,#40372,#40373,#40374,
#40375,#40376,#40377,#40378,#40379,#40380,#40381,#40382,#40383,#40384,#40385,
#40386,#40387,#40388,#40389,#40390,#40391,#40392,#40393,#40394,#40395,#40396,
#40397,#40398,#40399,#40400,#40401,#40402,#40403,#40404,#40405,#40406,#40407,
#40408,#40409,#40410,#40411,#40412,#40413,#40414,#40415,#40416,#40417,#40418,
#40419,#40420,#40421,#40422,#40423,#40424,#40425,#40426,#40427,#40428,#40429,
#40430,#40431,#40432,#40433,#40434,#40435,#40436,#40437,#40438,#40439,#40440,
#40441,#40442,#40443,#40444,#40445,#40446,#40447,#40448,#40449,#40450,#40451,
#40452,#40453,#40454,#40455,#40456,#40457,#40458,#40459,#40460,#40461,#40462,
#40463,#40464,#40465,#40466,#40467,#40468,#40469,#40470,#40471,#40472,#40473,
#40474,#40475,#40476,#40477,#40478,#40479,#40480,#40481,#40482,#40483,#40484,
#40485,#40486,#40487,#40488,#40489,#40490,#40491,#40492,#40493,#40494,#40495,
#40496,#40497,#40498,#40499,#40500,#40501,#40502,#40503,#40504,#40505,#40506,
#40507,#40508,#40509,#40510,#40511,#40512,#40513,#40514,#40515,#40516,#40517,
#40518,#40519,#40520,#40521,#40522,#40523,#40524,#40525,#40526,#40527,#40528,
#40529,#40530,#40531,#40532,#40533,#40534,#40535,#40536,#40537,#40538,#40539,
#40540,#40541,#40542,#40543,#40544,#40545,#40546,#40547,#40548,#40549,#40550,
#40551,#40552,#40553,#40554,#40555,#40556,#40557,#40558,#40559,#40560,#40561,
#40562,#40563,#40564,#40565,#40566,#40567,#40568,#40569,#40570,#40571,#40572,
#40573,#40574,#40575,#40576,#40577,#40578,#40579,#40580,#40581,#40582,#40583,
#40584,#40585,#40586,#40587,#40588,#40589,#40590,#40591,#40592,#40593,#40594,
#40595,#40596,#40597,#40598,#40599,#40600,#40601,#40602,#40603,#40604,#40605,
#40606,#40607,#40608,#40609,#40610,#40611,#40612,#40613,#40614,#40615,#40616,
#40617,#40618,#40619,#40620,#40621,#40622,#40623,#40624,#40625,#40626,#40627,
#40628,#40629,#40630,#40631,#40632,#40633,#40634,#40635,#40636,#40637,#40638,
#40639,#40640,#40641,#40642,#40643,#40644,#40645,#40646,#40647,#40648,#40649,
#40650,#40651,#40652,#40653,#40654,#40655,#40656,#40657,#40658,#40659,#40660,
#40661,#40662,#40663,#40664,#40665,#40666,#40667,#40668,#40669,#40670,#40671,
#40672,#40673,#40674,#40675,#40676,#40677,#40678,#40679,#40680,#40681,#40682,
#40683,#40684,#40685,#40686,#40687,#40688,#40689,#40690,#40691,#40692,#40693,
#40694,#40695,#40696,#40697,#40698,#40699,#40700,#40701,#40702,#40703,#40704,
#40705,#40706,#40707,#40708,#40709,#40710,#40711,#40712,#40713,#40714,#40715,
#40716,#40717,#40718,#40719,#40720,#40721,#40722,#40723,#40724,#40725,#40726,
#40727,#40728,#40729,#40730,#40731,#40732,#40733,#40734,#40735,#40736,#40737,
#40738,#40739,#40740,#40741,#40742,#40743,#40744,#40745,#40746,#40747,#40748,
#40749,#40750,#40751,#40752,#40753,#40754,#40755,#40756,#40757,#40758,#40759,
#40760,#40761,#40762,#40763,#40764,#40765,#40766,#40767,#40768,#40769,#40770,
#40771,#40772,#40773,#40774,#40775,#40776,#40777,#40778,#40779,#40780,#40781,
#40782,#40783,#40784,#40785,#40786,#40787,#40788,#40789,#40790,#40791,#40792,
#40793,#40794,#40795,#40796,#40797,#40798,#40799,#40800,#40801,#40802,#40803,
#40804,#40805,#40806,#40807,#40808,#40809,#40810,#40811,#40812,#40813,#40814,
#40815,#40816,#40817,#40818,#40819,#40820,#40821,#40822,#40823,#40824,#40825,
#40826,#40827,#40828,#40829,#40830,#40831,#40832,#40833,#40834)),
 .UNSPECIFIED.,.F.,.F.,.F.)
B_SPLINE_SURFACE_WITH_KNOTS((2,2),(3,2,2,2,2,2,2,2,2,2,2,2,2,2,2,2,2,2,
2,2,2,2,2,2,2,2,2,2,2,2,2,2,2,2,2,2,2,2,2,2,2,2,2,2,2,2,2,2,2,2,2,2,2,2,
2,2,2,2,2,2,2,2,2,2,2,2,2,2,2,2,2,2,2,2,2,2,2,2,2,2,2,2,2,2,2,2,2,2,2,2,
2,2,2,2,2,2,2,2,2,2,2,2,2,2,2,2,2,2,2,2,2,2,2,2,2,2,2,2,2,2,2,2,2,2,2,2,
2,2,2,2,2,2,2,2,2,2,2,2,2,2,2,2,2,2,2,2,2,2,2,2,2,2,2,2,2,2,2,2,2,2,2,2,
2,2,2,2,2,2,2,2,2,2,2,2,2,2,2,2,2,2,2,2,2,2,2,2,2,2,2,2,2,2,2,2,2,2,2,2,
2,2,2,2,2,2,2,2,2,2,2,2,2,2,2,2,2,2,2,2,2,2,2,2,2,2,2,2,2,2,2,2,2,2,2,2,
2,2,2,2,2,2,2,2,2,2,2,2,2,2,2,2,2,2,2,2,2,2,2,2,2,2,2,2,2,2,2,2,2,2,2,2,
2,2,2,2,2,2,2,2,2,2,2,2,2,2,2,2,2,2,2,2,2,2,2,2,2,2,2,2,2,2,2,2,2,2,2,2,
2,2,2,2,2,2,2,2,2,2,2,2,2,2,2,2,2,2,2,2,2,2,2,2,2,2,2,2,2,2,2,2,2,2,2,2,
2,2,2,2,2,3),(-3.10535428298811E-6,1.00000310535428),(0.,0.00284090909090909,
0.00568181818181818,0.00852272727272727,0.0113636363636364,0.0142045454545455,
0.0170454545454545,0.0198863636363636,0.0227272727272727,0.0255681818181818,
0.0284090909090909,0.03125,0.0340909090909091,0.0369318181818182,0.0397727272727273,
0.0426136363636364,0.0454545454545455,0.0482954545454545,0.0511363636363636,
0.0539772727272727,0.0568181818181818,0.0596590909090909,0.0625,0.0653409090909091,
0.0681818181818182,0.0710227272727273,0.0738636363636364,0.0767045454545455,
0.0795454545454545,0.0823863636363636,0.0852272727272727,0.0880681818181818,
0.0909090909090909,0.09375,0.0965909090909091,0.0994318181818182,0.102272727272727,
0.105113636363636,0.107954545454545,0.110795454545455,0.113636363636364,
0.116477272727273,0.119318181818182,0.122159090909091,0.125,0.127840909090909,
0.130681818181818,0.133522727272727,0.136363636363636,0.139204545454545,
0.142045454545455,0.144886363636364,0.147727272727273,0.150568181818182,
0.153409090909091,0.15625,0.159090909090909,0.161931818181818,0.164772727272727,
0.167613636363636,0.170454545454545,0.173295454545455,0.176136363636364,
0.178977272727273,0.181818181818182,0.184659090909091,0.1875,0.190340909090909,
0.193181818181818,0.196022727272727,0.198863636363636,0.201704545454545,
0.204545454545455,0.207386363636364,0.210227272727273,0.213068181818182,
0.215909090909091,0.21875,0.221590909090909,0.224431818181818,0.227272727272727,
0.230113636363636,0.232954545454545,0.235795454545455,0.238636363636364,
0.241477272727273,0.244318181818182,0.247159090909091,0.25,0.252840909090909,
0.255681818181818,0.258522727272727,0.261363636363636,0.264204545454545,
0.267045454545455,0.269886363636364,0.272727272727273,0.275568181818182,
0.278409090909091,0.28125,0.284090909090909,0.286931818181818,0.289772727272727,
0.292613636363636,0.295454545454545,0.298295454545455,0.301136363636364,
0.303977272727273,0.306818181818182,0.309659090909091,0.3125,0.315340909090909,
0.318181818181818,0.321022727272727,0.323863636363636,0.326704545454545,
0.329545454545455,0.332386363636364,0.335227272727273,0.338068181818182,
0.340909090909091,0.34375,0.346590909090909,0.349431818181818,0.352272727272727,
0.355113636363636,0.357954545454545,0.360795454545455,0.363636363636364,
0.366477272727273,0.369318181818182,0.372159090909091,0.375,0.377840909090909,
0.380681818181818,0.383522727272727,0.386363636363636,0.389204545454545,
0.392045454545455,0.394886363636364,0.397727272727273,0.400568181818182,
0.403409090909091,0.40625,0.409090909090909,0.411931818181818,0.414772727272727,
0.417613636363636,0.420454545454545,0.423295454545455,0.426136363636364,
0.428977272727273,0.431818181818182,0.434659090909091,0.4375,0.440340909090909,
0.443181818181818,0.446022727272727,0.448863636363636,0.451704545454545,
0.454545454545455,0.457386363636364,0.460227272727273,0.463068181818182,
0.465909090909091,0.46875,0.471590909090909,0.474431818181818,0.477272727272727,
0.480113636363636,0.482954545454545,0.485795454545455,0.488636363636364,
0.491477272727273,0.494318181818182,0.497159090909091,0.5,0.502840909090909,
0.505681818181818,0.508522727272727,0.511363636363636,0.514204545454545,
0.517045454545455,0.519886363636364,0.522727272727273,0.525568181818182,
0.528409090909091,0.53125,0.534090909090909,0.536931818181818,0.539772727272727,
0.542613636363636,0.545454545454545,0.548295454545455,0.551136363636364,
0.553977272727273,0.556818181818182,0.559659090909091,0.5625,0.565340909090909,
0.568181818181818,0.571022727272727,0.573863636363636,0.576704545454545,
0.579545454545455,0.582386363636364,0.585227272727273,0.588068181818182,
0.590909090909091,0.59375,0.596590909090909,0.599431818181818,0.602272727272727,
0.605113636363636,0.607954545454545,0.610795454545455,0.613636363636364,
0.616477272727273,0.619318181818182,0.622159090909091,0.625,0.627840909090909,
0.630681818181818,0.633522727272727,0.636363636363636,0.639204545454545,
0.642045454545455,0.644886363636364,0.647727272727273,0.650568181818182,
0.653409090909091,0.65625,0.659090909090909,0.661931818181818,0.664772727272727,
0.667613636363636,0.670454545454545,0.673295454545455,0.676136363636364,
0.678977272727273,0.681818181818182,0.684659090909091,0.6875,0.690340909090909,
0.693181818181818,0.696022727272727,0.698863636363636,0.701704545454545,
0.704545454545455,0.707386363636364,0.710227272727273,0.713068181818182,
0.715909090909091,0.71875,0.721590909090909,0.724431818181818,0.727272727272727,
0.730113636363636,0.732954545454545,0.735795454545455,0.738636363636364,
0.741477272727273,0.744318181818182,0.747159090909091,0.75,0.752840909090909,
0.755681818181818,0.758522727272727,0.761363636363636,0.764204545454545,
0.767045454545455,0.769886363636364,0.772727272727273,0.775568181818182,
0.778409090909091,0.78125,0.784090909090909,0.786931818181818,0.789772727272727,
0.792613636363636,0.795454545454545,0.798295454545455,0.801136363636364,
0.803977272727273,0.806818181818182,0.809659090909091,0.8125,0.815340909090909,
0.818181818181818,0.821022727272727,0.823863636363636,0.826704545454545,
0.829545454545455,0.832386363636364,0.835227272727273,0.838068181818182,
0.840909090909091,0.84375,0.846590909090909,0.849431818181818,0.852272727272727,
0.855113636363636,0.857954545454545,0.860795454545455,0.863636363636364,
0.866477272727273,0.869318181818182,0.872159090909091,0.875,0.877840909090909,
0.880681818181818,0.883522727272727,0.886363636363636,0.889204545454545,
0.892045454545455,0.894886363636364,0.897727272727273,0.900568181818182,
0.903409090909091,0.90625,0.909090909090909,0.911931818181818,0.914772727272727,
0.917613636363636,0.920454545454545,0.923295454545455,0.926136363636364,
0.928977272727273,0.931818181818182,0.934659090909091,0.9375,0.940340909090909,
0.943181818181818,0.946022727272727,0.948863636363636,0.951704545454545,
0.954545454545455,0.957386363636364,0.960227272727273,0.963068181818182,
0.965909090909091,0.96875,0.971590909090909,0.974431818181818,0.977272727272727,
0.980113636363636,0.982954545454545,0.984843013501228),.UNSPECIFIED.)
GEOMETRIC_REPRESENTATION_ITEM()
RATIONAL_B_SPLINE_SURFACE(((1.,0.923879532511287,1.,0.923879532511287,1.,
0.923879532511287,1.,0.923879532511287,1.,0.923879532511287,1.,0.923879532511287,
1.,0.923879532511287,1.,0.923879532511287,1.,0.923879532511287,1.,0.923879532511287,
1.,0.923879532511287,1.,0.923879532511287,1.,0.923879532511287,1.,0.923879532511287,
1.,0.923879532511287,1.,0.923879532511287,1.,0.923879532511287,1.,0.923879532511287,
1.,0.923879532511287,1.,0.923879532511287,1.,0.923879532511287,1.,0.923879532511287,
1.,0.923879532511287,1.,0.923879532511287,1.,0.923879532511287,1.,0.923879532511287,
1.,0.923879532511287,1.,0.923879532511287,1.,0.923879532511287,1.,0.923879532511287,
1.,0.923879532511287,1.,0.923879532511287,1.,0.923879532511287,1.,0.923879532511287,
1.,0.923879532511287,1.,0.923879532511287,1.,0.923879532511287,1.,0.923879532511287,
1.,0.923879532511287,1.,0.923879532511287,1.,0.923879532511287,1.,0.923879532511287,
1.,0.923879532511287,1.,0.923879532511287,1.,0.923879532511287,1.,0.923879532511287,
1.,0.923879532511287,1.,0.923879532511287,1.,0.923879532511287,1.,0.923879532511287,
1.,0.923879532511287,1.,0.923879532511287,1.,0.923879532511287,1.,0.923879532511287,
1.,0.923879532511287,1.,0.923879532511287,1.,0.923879532511287,1.,0.923879532511287,
1.,0.923879532511287,1.,0.923879532511287,1.,0.923879532511287,1.,0.923879532511287,
1.,0.923879532511287,1.,0.923879532511287,1.,0.923879532511287,1.,0.923879532511287,
1.,0.923879532511287,1.,0.923879532511287,1.,0.923879532511287,1.,0.923879532511287,
1.,0.923879532511287,1.,0.923879532511287,1.,0.923879532511287,1.,0.923879532511287,
1.,0.923879532511287,1.,0.923879532511287,1.,0.923879532511287,1.,0.923879532511287,
1.,0.923879532511287,1.,0.923879532511287,1.,0.923879532511287,1.,0.923879532511287,
1.,0.923879532511287,1.,0.923879532511287,1.,0.923879532511287,1.,0.923879532511287,
1.,0.923879532511287,1.,0.923879532511287,1.,0.923879532511287,1.,0.923879532511287,
1.,0.923879532511287,1.,0.923879532511287,1.,0.923879532511287,1.,0.923879532511287,
1.,0.923879532511287,1.,0.923879532511287,1.,0.923879532511287,1.,0.923879532511287,
1.,0.923879532511287,1.,0.923879532511287,1.,0.923879532511287,1.,0.923879532511287,
1.,0.923879532511287,1.,0.923879532511287,1.,0.923879532511287,1.,0.923879532511287,
1.,0.923879532511287,1.,0.923879532511287,1.,0.923879532511287,1.,0.923879532511287,
1.,0.923879532511287,1.,0.923879532511287,1.,0.923879532511287,1.,0.923879532511287,
1.,0.923879532511287,1.,0.923879532511287,1.,0.923879532511287,1.,0.923879532511287,
1.,0.923879532511287,1.,0.923879532511287,1.,0.923879532511287,1.,0.923879532511287,
1.,0.923879532511287,1.,0.923879532511287,1.,0.923879532511287,1.,0.923879532511287,
1.,0.923879532511287,1.,0.923879532511287,1.,0.923879532511287,1.,0.923879532511287,
1.,0.923879532511287,1.,0.923879532511287,1.,0.923879532511287,1.,0.923879532511287,
1.,0.923879532511287,1.,0.923879532511287,1.,0.923879532511287,1.,0.923879532511287,
1.,0.923879532511287,1.,0.923879532511287,1.,0.923879532511287,1.,0.923879532511287,
1.,0.923879532511287,1.,0.923879532511287,1.,0.923879532511287,1.,0.923879532511287,
1.,0.923879532511287,1.,0.923879532511287,1.,0.923879532511287,1.,0.923879532511287,
1.,0.923879532511287,1.,0.923879532511287,1.,0.923879532511287,1.,0.923879532511287,
1.,0.923879532511287,1.,0.923879532511287,1.,0.923879532511287,1.,0.923879532511287,
1.,0.923879532511287,1.,0.923879532511287,1.,0.923879532511287,1.,0.923879532511287,
1.,0.923879532511287,1.,0.923879532511287,1.,0.923879532511287,1.,0.923879532511287,
1.,0.923879532511287,1.,0.923879532511287,1.,0.923879532511287,1.,0.923879532511287,
1.,0.923879532511287,1.,0.923879532511287,1.,0.923879532511287,1.,0.923879532511287,
1.,0.923879532511287,1.,0.923879532511287,1.,0.923879532511287,1.,0.923879532511287,
1.,0.923879532511287,1.,0.923879532511287,1.,0.923879532511287,1.,0.923879532511287,
1.,0.923879532511287,1.,0.923879532511287,1.,0.923879532511287,1.,0.923879532511287,
1.,0.923879532511287,1.,0.923879532511287,1.,0.923879532511287,1.,0.923879532511287,
1.,0.923879532511287,1.,0.923879532511287,1.,0.923879532511287,1.,0.923879532511287,
1.,0.923879532511287,1.,0.923879532511287,1.,0.923879532511287,1.,0.923879532511287,
1.,0.923879532511287,1.,0.923879532511287,1.,0.923879532511287,1.,0.923879532511287,
1.,0.923879532511287,1.,0.923879532511287,1.,0.923879532511287,1.,0.923879532511287,
1.,0.923879532511287,1.,0.923879532511287,1.,0.923879532511287,1.,0.923879532511287,
1.,0.923879532511287,1.,0.923879532511287,1.,0.923879532511287,1.,0.923879532511287,
1.,0.923879532511287,1.,0.923879532511287,1.,0.923879532511287,1.,0.923879532511287,
1.,0.923879532511287,1.,0.923879532511287,1.,0.923879532511287,1.,0.923879532511287,
1.,0.923879532511287,1.,0.923879532511287,1.,0.923879532511287,1.,0.923879532511287,
1.,0.923879532511287,1.,0.923879532511287,1.,0.923879532511287,1.,0.923879532511287,
1.,0.923879532511287,1.,0.923879532511287,1.,0.923879532511287,1.,0.923879532511287,
1.,0.923879532511287,1.,0.923879532511287,1.,0.923879532511287,1.,0.923879532511287,
1.,0.923879532511287,1.,0.923879532511287,1.,0.923879532511287,1.,0.923879532511287,
1.,0.923879532511287,1.,0.923879532511287,1.,0.923879532511287,1.,0.923879532511287,
1.,0.923879532511287,1.,0.923879532511287,1.,0.923879532511287,1.,0.923879532511287,
1.,0.923879532511287,1.,0.923879532511287,1.,0.923879532511287,1.,0.923879532511287,
1.,0.923879532511287,1.,0.923879532511287,1.,0.923879532511287,1.,0.923879532511287,
1.,0.923879532511287,1.,0.923879532511287,1.,0.923879532511287,1.,0.923879532511287,
1.,0.923879532511287,1.,0.923879532511287,1.,0.923879532511287,1.,0.923879532511287,
1.,0.923879532511287,1.,0.923879532511287,1.,0.923879532511287,1.,0.923879532511287,
1.,0.923879532511287,1.,0.923879532511287,1.,0.923879532511287,1.,0.923879532511287,
1.,0.923879532511287,1.,0.923879532511287,1.,0.923879532511287,1.,0.923879532511287,
1.,0.923879532511287,1.,0.923879532511287,1.,0.923879532511287,1.,0.923879532511287,
1.,0.923879532511287,1.,0.923879532511287,1.,0.923879532511287,1.,0.923879532511287,
1.,0.923879532511287,1.,0.923879532511287,1.,0.923879532511287,1.,0.923879532511287,
1.,0.923879532511287,1.,0.923879532511287,1.,0.923879532511287,1.,0.923879532511287,
1.,0.923879532511287,1.,0.923879532511287,1.,0.923879532511287,1.,0.923879532511287,
1.,0.923879532511287,1.,0.923879532511287,1.,0.923879532511287,1.,0.923879532511287,
1.,0.923879532511287,1.,0.923879532511287,1.,0.923879532511287,1.,0.923879532511287,
1.,0.923879532511287,1.,0.923879532511287,1.,0.923879532511287,1.,0.923879532511287,
1.,0.923879532511287,1.,0.923879532511287,1.,0.923879532511287,1.,0.923879532511287,
1.,0.923879532511287,1.,0.923879532511287,1.,0.923879532511287,1.,0.923879532511287,
1.,0.923879532511287,1.,0.923879532511287,1.,0.923879532511287,1.,0.923879532511287,
1.,0.923879532511287,1.,0.923879532511287,1.,0.923879532511287,1.,0.923879532511287,
1.,0.923879532511287,1.,0.923879532511287,1.,0.923879532511287,1.,0.923879532511287,
1.,0.923879532511287,1.,0.923879532511287,1.,0.923879532511287,1.,0.923879532511287,
1.,0.923879532511287,1.,0.923879532511287,1.,0.923879532511287,1.,0.923879532511287,
1.,0.923879532511287,1.,0.923879532511287,1.,0.923879532511287,1.,0.923879532511287,
1.,0.923879532511287,1.,0.923879532511287,1.,0.923879532511287,1.,0.923879532511287,
1.,0.949399623166069,0.966071511472009),(1.,0.923879532511287,1.,0.923879532511287,
1.,0.923879532511287,1.,0.923879532511287,1.,0.923879532511287,1.,0.923879532511287,
1.,0.923879532511287,1.,0.923879532511287,1.,0.923879532511287,1.,0.923879532511287,
1.,0.923879532511287,1.,0.923879532511287,1.,0.923879532511287,1.,0.923879532511287,
1.,0.923879532511287,1.,0.923879532511287,1.,0.923879532511287,1.,0.923879532511287,
1.,0.923879532511287,1.,0.923879532511287,1.,0.923879532511287,1.,0.923879532511287,
1.,0.923879532511287,1.,0.923879532511287,1.,0.923879532511287,1.,0.923879532511287,
1.,0.923879532511287,1.,0.923879532511287,1.,0.923879532511287,1.,0.923879532511287,
1.,0.923879532511287,1.,0.923879532511287,1.,0.923879532511287,1.,0.923879532511287,
1.,0.923879532511287,1.,0.923879532511287,1.,0.923879532511287,1.,0.923879532511287,
1.,0.923879532511287,1.,0.923879532511287,1.,0.923879532511287,1.,0.923879532511287,
1.,0.923879532511287,1.,0.923879532511287,1.,0.923879532511287,1.,0.923879532511287,
1.,0.923879532511287,1.,0.923879532511287,1.,0.923879532511287,1.,0.923879532511287,
1.,0.923879532511287,1.,0.923879532511287,1.,0.923879532511287,1.,0.923879532511287,
1.,0.923879532511287,1.,0.923879532511287,1.,0.923879532511287,1.,0.923879532511287,
1.,0.923879532511287,1.,0.923879532511287,1.,0.923879532511287,1.,0.923879532511287,
1.,0.923879532511287,1.,0.923879532511287,1.,0.923879532511287,1.,0.923879532511287,
1.,0.923879532511287,1.,0.923879532511287,1.,0.923879532511287,1.,0.923879532511287,
1.,0.923879532511287,1.,0.923879532511287,1.,0.923879532511287,1.,0.923879532511287,
1.,0.923879532511287,1.,0.923879532511287,1.,0.923879532511287,1.,0.923879532511287,
1.,0.923879532511287,1.,0.923879532511287,1.,0.923879532511287,1.,0.923879532511287,
1.,0.923879532511287,1.,0.923879532511287,1.,0.923879532511287,1.,0.923879532511287,
1.,0.923879532511287,1.,0.923879532511287,1.,0.923879532511287,1.,0.923879532511287,
1.,0.923879532511287,1.,0.923879532511287,1.,0.923879532511287,1.,0.923879532511287,
1.,0.923879532511287,1.,0.923879532511287,1.,0.923879532511287,1.,0.923879532511287,
1.,0.923879532511287,1.,0.923879532511287,1.,0.923879532511287,1.,0.923879532511287,
1.,0.923879532511287,1.,0.923879532511287,1.,0.923879532511287,1.,0.923879532511287,
1.,0.923879532511287,1.,0.923879532511287,1.,0.923879532511287,1.,0.923879532511287,
1.,0.923879532511287,1.,0.923879532511287,1.,0.923879532511287,1.,0.923879532511287,
1.,0.923879532511287,1.,0.923879532511287,1.,0.923879532511287,1.,0.923879532511287,
1.,0.923879532511287,1.,0.923879532511287,1.,0.923879532511287,1.,0.923879532511287,
1.,0.923879532511287,1.,0.923879532511287,1.,0.923879532511287,1.,0.923879532511287,
1.,0.923879532511287,1.,0.923879532511287,1.,0.923879532511287,1.,0.923879532511287,
1.,0.923879532511287,1.,0.923879532511287,1.,0.923879532511287,1.,0.923879532511287,
1.,0.923879532511287,1.,0.923879532511287,1.,0.923879532511287,1.,0.923879532511287,
1.,0.923879532511287,1.,0.923879532511287,1.,0.923879532511287,1.,0.923879532511287,
1.,0.923879532511287,1.,0.923879532511287,1.,0.923879532511287,1.,0.923879532511287,
1.,0.923879532511287,1.,0.923879532511287,1.,0.923879532511287,1.,0.923879532511287,
1.,0.923879532511287,1.,0.923879532511287,1.,0.923879532511287,1.,0.923879532511287,
1.,0.923879532511287,1.,0.923879532511287,1.,0.923879532511287,1.,0.923879532511287,
1.,0.923879532511287,1.,0.923879532511287,1.,0.923879532511287,1.,0.923879532511287,
1.,0.923879532511287,1.,0.923879532511287,1.,0.923879532511287,1.,0.923879532511287,
1.,0.923879532511287,1.,0.923879532511287,1.,0.923879532511287,1.,0.923879532511287,
1.,0.923879532511287,1.,0.923879532511287,1.,0.923879532511287,1.,0.923879532511287,
1.,0.923879532511287,1.,0.923879532511287,1.,0.923879532511287,1.,0.923879532511287,
1.,0.923879532511287,1.,0.923879532511287,1.,0.923879532511287,1.,0.923879532511287,
1.,0.923879532511287,1.,0.923879532511287,1.,0.923879532511287,1.,0.923879532511287,
1.,0.923879532511287,1.,0.923879532511287,1.,0.923879532511287,1.,0.923879532511287,
1.,0.923879532511287,1.,0.923879532511287,1.,0.923879532511287,1.,0.923879532511287,
1.,0.923879532511287,1.,0.923879532511287,1.,0.923879532511287,1.,0.923879532511287,
1.,0.923879532511287,1.,0.923879532511287,1.,0.923879532511287,1.,0.923879532511287,
1.,0.923879532511287,1.,0.923879532511287,1.,0.923879532511287,1.,0.923879532511287,
1.,0.923879532511287,1.,0.923879532511287,1.,0.923879532511287,1.,0.923879532511287,
1.,0.923879532511287,1.,0.923879532511287,1.,0.923879532511287,1.,0.923879532511287,
1.,0.923879532511287,1.,0.923879532511287,1.,0.923879532511287,1.,0.923879532511287,
1.,0.923879532511287,1.,0.923879532511287,1.,0.923879532511287,1.,0.923879532511287,
1.,0.923879532511287,1.,0.923879532511287,1.,0.923879532511287,1.,0.923879532511287,
1.,0.923879532511287,1.,0.923879532511287,1.,0.923879532511287,1.,0.923879532511287,
1.,0.923879532511287,1.,0.923879532511287,1.,0.923879532511287,1.,0.923879532511287,
1.,0.923879532511287,1.,0.923879532511287,1.,0.923879532511287,1.,0.923879532511287,
1.,0.923879532511287,1.,0.923879532511287,1.,0.923879532511287,1.,0.923879532511287,
1.,0.923879532511287,1.,0.923879532511287,1.,0.923879532511287,1.,0.923879532511287,
1.,0.923879532511287,1.,0.923879532511287,1.,0.923879532511287,1.,0.923879532511287,
1.,0.923879532511287,1.,0.923879532511287,1.,0.923879532511287,1.,0.923879532511287,
1.,0.923879532511287,1.,0.923879532511287,1.,0.923879532511287,1.,0.923879532511287,
1.,0.923879532511287,1.,0.923879532511287,1.,0.923879532511287,1.,0.923879532511287,
1.,0.923879532511287,1.,0.923879532511287,1.,0.923879532511287,1.,0.923879532511287,
1.,0.923879532511287,1.,0.923879532511287,1.,0.923879532511287,1.,0.923879532511287,
1.,0.923879532511287,1.,0.923879532511287,1.,0.923879532511287,1.,0.923879532511287,
1.,0.923879532511287,1.,0.923879532511287,1.,0.923879532511287,1.,0.923879532511287,
1.,0.923879532511287,1.,0.923879532511287,1.,0.923879532511287,1.,0.923879532511287,
1.,0.923879532511287,1.,0.923879532511287,1.,0.923879532511287,1.,0.923879532511287,
1.,0.923879532511287,1.,0.923879532511287,1.,0.923879532511287,1.,0.923879532511287,
1.,0.923879532511287,1.,0.923879532511287,1.,0.923879532511287,1.,0.923879532511287,
1.,0.923879532511287,1.,0.923879532511287,1.,0.923879532511287,1.,0.923879532511287,
1.,0.923879532511287,1.,0.923879532511287,1.,0.923879532511287,1.,0.923879532511287,
1.,0.923879532511287,1.,0.923879532511287,1.,0.923879532511287,1.,0.923879532511287,
1.,0.923879532511287,1.,0.923879532511287,1.,0.923879532511287,1.,0.923879532511287,
1.,0.923879532511287,1.,0.923879532511287,1.,0.923879532511287,1.,0.923879532511287,
1.,0.923879532511287,1.,0.923879532511287,1.,0.923879532511287,1.,0.923879532511287,
1.,0.923879532511287,1.,0.923879532511287,1.,0.923879532511287,1.,0.923879532511287,
1.,0.923879532511287,1.,0.923879532511287,1.,0.923879532511287,1.,0.923879532511287,
1.,0.923879532511287,1.,0.923879532511287,1.,0.923879532511287,1.,0.923879532511287,
1.,0.923879532511287,1.,0.923879532511287,1.,0.923879532511287,1.,0.923879532511287,
1.,0.923879532511287,1.,0.923879532511287,1.,0.923879532511287,1.,0.923879532511287,
1.,0.923879532511287,1.,0.923879532511287,1.,0.923879532511287,1.,0.923879532511287,
1.,0.923879532511287,1.,0.923879532511287,1.,0.923879532511287,1.,0.923879532511287,
1.,0.949399623166069,0.966071511472009)))
REPRESENTATION_ITEM('')
SURFACE()
);
#589=(
BOUNDED_SURFACE()
B_SPLINE_SURFACE(3,2,((#41478,#41479,#41480,#41481,#41482,#41483,#41484,
#41485,#41486,#41487,#41488,#41489,#41490,#41491,#41492,#41493,#41494,#41495,
#41496,#41497,#41498,#41499,#41500,#41501,#41502,#41503,#41504,#41505,#41506,
#41507,#41508,#41509,#41510,#41511,#41512,#41513,#41514,#41515,#41516,#41517,
#41518,#41519,#41520,#41521,#41522,#41523,#41524,#41525,#41526,#41527,#41528,
#41529,#41530,#41531,#41532,#41533,#41534,#41535,#41536,#41537,#41538,#41539,
#41540,#41541,#41542,#41543,#41544,#41545,#41546,#41547,#41548,#41549,#41550,
#41551,#41552,#41553,#41554,#41555,#41556,#41557,#41558,#41559,#41560,#41561,
#41562,#41563,#41564,#41565,#41566,#41567,#41568,#41569,#41570,#41571,#41572,
#41573,#41574,#41575,#41576,#41577,#41578,#41579,#41580,#41581,#41582,#41583,
#41584,#41585,#41586,#41587,#41588,#41589,#41590,#41591,#41592,#41593,#41594,
#41595,#41596,#41597,#41598,#41599,#41600,#41601,#41602,#41603,#41604,#41605,
#41606,#41607,#41608,#41609,#41610,#41611,#41612,#41613,#41614,#41615,#41616,
#41617,#41618,#41619,#41620,#41621,#41622,#41623,#41624,#41625,#41626,#41627,
#41628,#41629,#41630,#41631,#41632,#41633,#41634,#41635,#41636,#41637,#41638,
#41639,#41640,#41641,#41642,#41643,#41644,#41645,#41646,#41647,#41648,#41649,
#41650,#41651,#41652,#41653,#41654,#41655,#41656,#41657,#41658,#41659,#41660,
#41661,#41662,#41663,#41664,#41665,#41666,#41667,#41668,#41669,#41670,#41671,
#41672,#41673,#41674,#41675,#41676,#41677,#41678,#41679,#41680,#41681,#41682,
#41683,#41684,#41685,#41686,#41687,#41688,#41689,#41690,#41691,#41692,#41693,
#41694,#41695,#41696,#41697,#41698,#41699,#41700,#41701,#41702,#41703,#41704,
#41705,#41706,#41707,#41708,#41709,#41710,#41711,#41712,#41713,#41714,#41715,
#41716,#41717,#41718,#41719,#41720,#41721,#41722,#41723,#41724,#41725,#41726,
#41727,#41728,#41729,#41730,#41731,#41732,#41733,#41734,#41735,#41736,#41737,
#41738,#41739,#41740,#41741,#41742,#41743,#41744,#41745,#41746,#41747,#41748,
#41749,#41750,#41751,#41752,#41753,#41754,#41755,#41756,#41757,#41758,#41759,
#41760,#41761,#41762,#41763,#41764,#41765,#41766,#41767,#41768,#41769,#41770,
#41771,#41772,#41773,#41774,#41775,#41776,#41777,#41778,#41779,#41780,#41781,
#41782,#41783,#41784,#41785,#41786,#41787,#41788,#41789,#41790,#41791,#41792,
#41793,#41794,#41795,#41796,#41797,#41798,#41799,#41800,#41801,#41802,#41803,
#41804,#41805,#41806,#41807,#41808,#41809,#41810,#41811,#41812,#41813,#41814,
#41815,#41816,#41817,#41818,#41819,#41820,#41821,#41822,#41823,#41824,#41825,
#41826,#41827,#41828,#41829,#41830,#41831,#41832,#41833,#41834,#41835,#41836,
#41837,#41838,#41839,#41840,#41841,#41842,#41843,#41844,#41845,#41846,#41847,
#41848,#41849,#41850,#41851,#41852,#41853,#41854,#41855,#41856,#41857,#41858,
#41859,#41860,#41861,#41862,#41863,#41864,#41865,#41866,#41867,#41868,#41869,
#41870,#41871,#41872,#41873,#41874,#41875,#41876,#41877,#41878,#41879,#41880,
#41881,#41882,#41883,#41884,#41885,#41886,#41887,#41888,#41889,#41890,#41891,
#41892,#41893,#41894,#41895,#41896,#41897,#41898,#41899,#41900,#41901,#41902,
#41903,#41904,#41905,#41906,#41907,#41908,#41909,#41910,#41911,#41912,#41913,
#41914,#41915,#41916,#41917,#41918,#41919,#41920,#41921,#41922,#41923,#41924,
#41925,#41926,#41927,#41928,#41929,#41930,#41931,#41932,#41933,#41934,#41935,
#41936,#41937,#41938,#41939,#41940,#41941,#41942,#41943,#41944,#41945,#41946,
#41947,#41948,#41949,#41950,#41951,#41952,#41953,#41954,#41955,#41956,#41957,
#41958,#41959,#41960,#41961,#41962,#41963,#41964,#41965,#41966,#41967,#41968,
#41969,#41970,#41971,#41972,#41973,#41974,#41975,#41976,#41977,#41978,#41979,
#41980,#41981,#41982,#41983,#41984,#41985,#41986,#41987,#41988,#41989,#41990,
#41991,#41992,#41993,#41994,#41995,#41996,#41997,#41998,#41999,#42000,#42001,
#42002,#42003,#42004,#42005,#42006,#42007,#42008,#42009,#42010,#42011,#42012,
#42013,#42014,#42015,#42016,#42017,#42018,#42019,#42020,#42021,#42022,#42023,
#42024,#42025,#42026,#42027,#42028,#42029,#42030,#42031,#42032,#42033,#42034,
#42035,#42036,#42037,#42038,#42039,#42040,#42041,#42042,#42043,#42044,#42045,
#42046,#42047,#42048,#42049,#42050,#42051,#42052,#42053,#42054,#42055,#42056,
#42057,#42058,#42059,#42060,#42061,#42062,#42063,#42064,#42065,#42066,#42067,
#42068,#42069,#42070,#42071,#42072,#42073,#42074,#42075,#42076,#42077,#42078,
#42079,#42080,#42081,#42082,#42083,#42084,#42085,#42086,#42087,#42088,#42089,
#42090,#42091,#42092,#42093,#42094,#42095,#42096,#42097,#42098,#42099,#42100,
#42101,#42102,#42103,#42104,#42105,#42106,#42107,#42108,#42109,#42110,#42111,
#42112,#42113,#42114,#42115,#42116,#42117,#42118,#42119,#42120,#42121,#42122,
#42123,#42124,#42125,#42126,#42127,#42128,#42129,#42130,#42131,#42132,#42133,
#42134,#42135,#42136,#42137,#42138,#42139,#42140,#42141,#42142,#42143,#42144,
#42145,#42146,#42147,#42148,#42149,#42150,#42151,#42152,#42153,#42154,#42155,
#42156,#42157,#42158,#42159,#42160,#42161,#42162,#42163,#42164,#42165,#42166,
#42167,#42168,#42169,#42170,#42171,#42172),(#42173,#42174,#42175,#42176,
#42177,#42178,#42179,#42180,#42181,#42182,#42183,#42184,#42185,#42186,#42187,
#42188,#42189,#42190,#42191,#42192,#42193,#42194,#42195,#42196,#42197,#42198,
#42199,#42200,#42201,#42202,#42203,#42204,#42205,#42206,#42207,#42208,#42209,
#42210,#42211,#42212,#42213,#42214,#42215,#42216,#42217,#42218,#42219,#42220,
#42221,#42222,#42223,#42224,#42225,#42226,#42227,#42228,#42229,#42230,#42231,
#42232,#42233,#42234,#42235,#42236,#42237,#42238,#42239,#42240,#42241,#42242,
#42243,#42244,#42245,#42246,#42247,#42248,#42249,#42250,#42251,#42252,#42253,
#42254,#42255,#42256,#42257,#42258,#42259,#42260,#42261,#42262,#42263,#42264,
#42265,#42266,#42267,#42268,#42269,#42270,#42271,#42272,#42273,#42274,#42275,
#42276,#42277,#42278,#42279,#42280,#42281,#42282,#42283,#42284,#42285,#42286,
#42287,#42288,#42289,#42290,#42291,#42292,#42293,#42294,#42295,#42296,#42297,
#42298,#42299,#42300,#42301,#42302,#42303,#42304,#42305,#42306,#42307,#42308,
#42309,#42310,#42311,#42312,#42313,#42314,#42315,#42316,#42317,#42318,#42319,
#42320,#42321,#42322,#42323,#42324,#42325,#42326,#42327,#42328,#42329,#42330,
#42331,#42332,#42333,#42334,#42335,#42336,#42337,#42338,#42339,#42340,#42341,
#42342,#42343,#42344,#42345,#42346,#42347,#42348,#42349,#42350,#42351,#42352,
#42353,#42354,#42355,#42356,#42357,#42358,#42359,#42360,#42361,#42362,#42363,
#42364,#42365,#42366,#42367,#42368,#42369,#42370,#42371,#42372,#42373,#42374,
#42375,#42376,#42377,#42378,#42379,#42380,#42381,#42382,#42383,#42384,#42385,
#42386,#42387,#42388,#42389,#42390,#42391,#42392,#42393,#42394,#42395,#42396,
#42397,#42398,#42399,#42400,#42401,#42402,#42403,#42404,#42405,#42406,#42407,
#42408,#42409,#42410,#42411,#42412,#42413,#42414,#42415,#42416,#42417,#42418,
#42419,#42420,#42421,#42422,#42423,#42424,#42425,#42426,#42427,#42428,#42429,
#42430,#42431,#42432,#42433,#42434,#42435,#42436,#42437,#42438,#42439,#42440,
#42441,#42442,#42443,#42444,#42445,#42446,#42447,#42448,#42449,#42450,#42451,
#42452,#42453,#42454,#42455,#42456,#42457,#42458,#42459,#42460,#42461,#42462,
#42463,#42464,#42465,#42466,#42467,#42468,#42469,#42470,#42471,#42472,#42473,
#42474,#42475,#42476,#42477,#42478,#42479,#42480,#42481,#42482,#42483,#42484,
#42485,#42486,#42487,#42488,#42489,#42490,#42491,#42492,#42493,#42494,#42495,
#42496,#42497,#42498,#42499,#42500,#42501,#42502,#42503,#42504,#42505,#42506,
#42507,#42508,#42509,#42510,#42511,#42512,#42513,#42514,#42515,#42516,#42517,
#42518,#42519,#42520,#42521,#42522,#42523,#42524,#42525,#42526,#42527,#42528,
#42529,#42530,#42531,#42532,#42533,#42534,#42535,#42536,#42537,#42538,#42539,
#42540,#42541,#42542,#42543,#42544,#42545,#42546,#42547,#42548,#42549,#42550,
#42551,#42552,#42553,#42554,#42555,#42556,#42557,#42558,#42559,#42560,#42561,
#42562,#42563,#42564,#42565,#42566,#42567,#42568,#42569,#42570,#42571,#42572,
#42573,#42574,#42575,#42576,#42577,#42578,#42579,#42580,#42581,#42582,#42583,
#42584,#42585,#42586,#42587,#42588,#42589,#42590,#42591,#42592,#42593,#42594,
#42595,#42596,#42597,#42598,#42599,#42600,#42601,#42602,#42603,#42604,#42605,
#42606,#42607,#42608,#42609,#42610,#42611,#42612,#42613,#42614,#42615,#42616,
#42617,#42618,#42619,#42620,#42621,#42622,#42623,#42624,#42625,#42626,#42627,
#42628,#42629,#42630,#42631,#42632,#42633,#42634,#42635,#42636,#42637,#42638,
#42639,#42640,#42641,#42642,#42643,#42644,#42645,#42646,#42647,#42648,#42649,
#42650,#42651,#42652,#42653,#42654,#42655,#42656,#42657,#42658,#42659,#42660,
#42661,#42662,#42663,#42664,#42665,#42666,#42667,#42668,#42669,#42670,#42671,
#42672,#42673,#42674,#42675,#42676,#42677,#42678,#42679,#42680,#42681,#42682,
#42683,#42684,#42685,#42686,#42687,#42688,#42689,#42690,#42691,#42692,#42693,
#42694,#42695,#42696,#42697,#42698,#42699,#42700,#42701,#42702,#42703,#42704,
#42705,#42706,#42707,#42708,#42709,#42710,#42711,#42712,#42713,#42714,#42715,
#42716,#42717,#42718,#42719,#42720,#42721,#42722,#42723,#42724,#42725,#42726,
#42727,#42728,#42729,#42730,#42731,#42732,#42733,#42734,#42735,#42736,#42737,
#42738,#42739,#42740,#42741,#42742,#42743,#42744,#42745,#42746,#42747,#42748,
#42749,#42750,#42751,#42752,#42753,#42754,#42755,#42756,#42757,#42758,#42759,
#42760,#42761,#42762,#42763,#42764,#42765,#42766,#42767,#42768,#42769,#42770,
#42771,#42772,#42773,#42774,#42775,#42776,#42777,#42778,#42779,#42780,#42781,
#42782,#42783,#42784,#42785,#42786,#42787,#42788,#42789,#42790,#42791,#42792,
#42793,#42794,#42795,#42796,#42797,#42798,#42799,#42800,#42801,#42802,#42803,
#42804,#42805,#42806,#42807,#42808,#42809,#42810,#42811,#42812,#42813,#42814,
#42815,#42816,#42817,#42818,#42819,#42820,#42821,#42822,#42823,#42824,#42825,
#42826,#42827,#42828,#42829,#42830,#42831,#42832,#42833,#42834,#42835,#42836,
#42837,#42838,#42839,#42840,#42841,#42842,#42843,#42844,#42845,#42846,#42847,
#42848,#42849,#42850,#42851,#42852,#42853,#42854,#42855,#42856,#42857,#42858,
#42859,#42860,#42861,#42862,#42863,#42864,#42865,#42866,#42867),(#42868,
#42869,#42870,#42871,#42872,#42873,#42874,#42875,#42876,#42877,#42878,#42879,
#42880,#42881,#42882,#42883,#42884,#42885,#42886,#42887,#42888,#42889,#42890,
#42891,#42892,#42893,#42894,#42895,#42896,#42897,#42898,#42899,#42900,#42901,
#42902,#42903,#42904,#42905,#42906,#42907,#42908,#42909,#42910,#42911,#42912,
#42913,#42914,#42915,#42916,#42917,#42918,#42919,#42920,#42921,#42922,#42923,
#42924,#42925,#42926,#42927,#42928,#42929,#42930,#42931,#42932,#42933,#42934,
#42935,#42936,#42937,#42938,#42939,#42940,#42941,#42942,#42943,#42944,#42945,
#42946,#42947,#42948,#42949,#42950,#42951,#42952,#42953,#42954,#42955,#42956,
#42957,#42958,#42959,#42960,#42961,#42962,#42963,#42964,#42965,#42966,#42967,
#42968,#42969,#42970,#42971,#42972,#42973,#42974,#42975,#42976,#42977,#42978,
#42979,#42980,#42981,#42982,#42983,#42984,#42985,#42986,#42987,#42988,#42989,
#42990,#42991,#42992,#42993,#42994,#42995,#42996,#42997,#42998,#42999,#43000,
#43001,#43002,#43003,#43004,#43005,#43006,#43007,#43008,#43009,#43010,#43011,
#43012,#43013,#43014,#43015,#43016,#43017,#43018,#43019,#43020,#43021,#43022,
#43023,#43024,#43025,#43026,#43027,#43028,#43029,#43030,#43031,#43032,#43033,
#43034,#43035,#43036,#43037,#43038,#43039,#43040,#43041,#43042,#43043,#43044,
#43045,#43046,#43047,#43048,#43049,#43050,#43051,#43052,#43053,#43054,#43055,
#43056,#43057,#43058,#43059,#43060,#43061,#43062,#43063,#43064,#43065,#43066,
#43067,#43068,#43069,#43070,#43071,#43072,#43073,#43074,#43075,#43076,#43077,
#43078,#43079,#43080,#43081,#43082,#43083,#43084,#43085,#43086,#43087,#43088,
#43089,#43090,#43091,#43092,#43093,#43094,#43095,#43096,#43097,#43098,#43099,
#43100,#43101,#43102,#43103,#43104,#43105,#43106,#43107,#43108,#43109,#43110,
#43111,#43112,#43113,#43114,#43115,#43116,#43117,#43118,#43119,#43120,#43121,
#43122,#43123,#43124,#43125,#43126,#43127,#43128,#43129,#43130,#43131,#43132,
#43133,#43134,#43135,#43136,#43137,#43138,#43139,#43140,#43141,#43142,#43143,
#43144,#43145,#43146,#43147,#43148,#43149,#43150,#43151,#43152,#43153,#43154,
#43155,#43156,#43157,#43158,#43159,#43160,#43161,#43162,#43163,#43164,#43165,
#43166,#43167,#43168,#43169,#43170,#43171,#43172,#43173,#43174,#43175,#43176,
#43177,#43178,#43179,#43180,#43181,#43182,#43183,#43184,#43185,#43186,#43187,
#43188,#43189,#43190,#43191,#43192,#43193,#43194,#43195,#43196,#43197,#43198,
#43199,#43200,#43201,#43202,#43203,#43204,#43205,#43206,#43207,#43208,#43209,
#43210,#43211,#43212,#43213,#43214,#43215,#43216,#43217,#43218,#43219,#43220,
#43221,#43222,#43223,#43224,#43225,#43226,#43227,#43228,#43229,#43230,#43231,
#43232,#43233,#43234,#43235,#43236,#43237,#43238,#43239,#43240,#43241,#43242,
#43243,#43244,#43245,#43246,#43247,#43248,#43249,#43250,#43251,#43252,#43253,
#43254,#43255,#43256,#43257,#43258,#43259,#43260,#43261,#43262,#43263,#43264,
#43265,#43266,#43267,#43268,#43269,#43270,#43271,#43272,#43273,#43274,#43275,
#43276,#43277,#43278,#43279,#43280,#43281,#43282,#43283,#43284,#43285,#43286,
#43287,#43288,#43289,#43290,#43291,#43292,#43293,#43294,#43295,#43296,#43297,
#43298,#43299,#43300,#43301,#43302,#43303,#43304,#43305,#43306,#43307,#43308,
#43309,#43310,#43311,#43312,#43313,#43314,#43315,#43316,#43317,#43318,#43319,
#43320,#43321,#43322,#43323,#43324,#43325,#43326,#43327,#43328,#43329,#43330,
#43331,#43332,#43333,#43334,#43335,#43336,#43337,#43338,#43339,#43340,#43341,
#43342,#43343,#43344,#43345,#43346,#43347,#43348,#43349,#43350,#43351,#43352,
#43353,#43354,#43355,#43356,#43357,#43358,#43359,#43360,#43361,#43362,#43363,
#43364,#43365,#43366,#43367,#43368,#43369,#43370,#43371,#43372,#43373,#43374,
#43375,#43376,#43377,#43378,#43379,#43380,#43381,#43382,#43383,#43384,#43385,
#43386,#43387,#43388,#43389,#43390,#43391,#43392,#43393,#43394,#43395,#43396,
#43397,#43398,#43399,#43400,#43401,#43402,#43403,#43404,#43405,#43406,#43407,
#43408,#43409,#43410,#43411,#43412,#43413,#43414,#43415,#43416,#43417,#43418,
#43419,#43420,#43421,#43422,#43423,#43424,#43425,#43426,#43427,#43428,#43429,
#43430,#43431,#43432,#43433,#43434,#43435,#43436,#43437,#43438,#43439,#43440,
#43441,#43442,#43443,#43444,#43445,#43446,#43447,#43448,#43449,#43450,#43451,
#43452,#43453,#43454,#43455,#43456,#43457,#43458,#43459,#43460,#43461,#43462,
#43463,#43464,#43465,#43466,#43467,#43468,#43469,#43470,#43471,#43472,#43473,
#43474,#43475,#43476,#43477,#43478,#43479,#43480,#43481,#43482,#43483,#43484,
#43485,#43486,#43487,#43488,#43489,#43490,#43491,#43492,#43493,#43494,#43495,
#43496,#43497,#43498,#43499,#43500,#43501,#43502,#43503,#43504,#43505,#43506,
#43507,#43508,#43509,#43510,#43511,#43512,#43513,#43514,#43515,#43516,#43517,
#43518,#43519,#43520,#43521,#43522,#43523,#43524,#43525,#43526,#43527,#43528,
#43529,#43530,#43531,#43532,#43533,#43534,#43535,#43536,#43537,#43538,#43539,
#43540,#43541,#43542,#43543,#43544,#43545,#43546,#43547,#43548,#43549,#43550,
#43551,#43552,#43553,#43554,#43555,#43556,#43557,#43558,#43559,#43560,#43561,
#43562),(#43563,#43564,#43565,#43566,#43567,#43568,#43569,#43570,#43571,
#43572,#43573,#43574,#43575,#43576,#43577,#43578,#43579,#43580,#43581,#43582,
#43583,#43584,#43585,#43586,#43587,#43588,#43589,#43590,#43591,#43592,#43593,
#43594,#43595,#43596,#43597,#43598,#43599,#43600,#43601,#43602,#43603,#43604,
#43605,#43606,#43607,#43608,#43609,#43610,#43611,#43612,#43613,#43614,#43615,
#43616,#43617,#43618,#43619,#43620,#43621,#43622,#43623,#43624,#43625,#43626,
#43627,#43628,#43629,#43630,#43631,#43632,#43633,#43634,#43635,#43636,#43637,
#43638,#43639,#43640,#43641,#43642,#43643,#43644,#43645,#43646,#43647,#43648,
#43649,#43650,#43651,#43652,#43653,#43654,#43655,#43656,#43657,#43658,#43659,
#43660,#43661,#43662,#43663,#43664,#43665,#43666,#43667,#43668,#43669,#43670,
#43671,#43672,#43673,#43674,#43675,#43676,#43677,#43678,#43679,#43680,#43681,
#43682,#43683,#43684,#43685,#43686,#43687,#43688,#43689,#43690,#43691,#43692,
#43693,#43694,#43695,#43696,#43697,#43698,#43699,#43700,#43701,#43702,#43703,
#43704,#43705,#43706,#43707,#43708,#43709,#43710,#43711,#43712,#43713,#43714,
#43715,#43716,#43717,#43718,#43719,#43720,#43721,#43722,#43723,#43724,#43725,
#43726,#43727,#43728,#43729,#43730,#43731,#43732,#43733,#43734,#43735,#43736,
#43737,#43738,#43739,#43740,#43741,#43742,#43743,#43744,#43745,#43746,#43747,
#43748,#43749,#43750,#43751,#43752,#43753,#43754,#43755,#43756,#43757,#43758,
#43759,#43760,#43761,#43762,#43763,#43764,#43765,#43766,#43767,#43768,#43769,
#43770,#43771,#43772,#43773,#43774,#43775,#43776,#43777,#43778,#43779,#43780,
#43781,#43782,#43783,#43784,#43785,#43786,#43787,#43788,#43789,#43790,#43791,
#43792,#43793,#43794,#43795,#43796,#43797,#43798,#43799,#43800,#43801,#43802,
#43803,#43804,#43805,#43806,#43807,#43808,#43809,#43810,#43811,#43812,#43813,
#43814,#43815,#43816,#43817,#43818,#43819,#43820,#43821,#43822,#43823,#43824,
#43825,#43826,#43827,#43828,#43829,#43830,#43831,#43832,#43833,#43834,#43835,
#43836,#43837,#43838,#43839,#43840,#43841,#43842,#43843,#43844,#43845,#43846,
#43847,#43848,#43849,#43850,#43851,#43852,#43853,#43854,#43855,#43856,#43857,
#43858,#43859,#43860,#43861,#43862,#43863,#43864,#43865,#43866,#43867,#43868,
#43869,#43870,#43871,#43872,#43873,#43874,#43875,#43876,#43877,#43878,#43879,
#43880,#43881,#43882,#43883,#43884,#43885,#43886,#43887,#43888,#43889,#43890,
#43891,#43892,#43893,#43894,#43895,#43896,#43897,#43898,#43899,#43900,#43901,
#43902,#43903,#43904,#43905,#43906,#43907,#43908,#43909,#43910,#43911,#43912,
#43913,#43914,#43915,#43916,#43917,#43918,#43919,#43920,#43921,#43922,#43923,
#43924,#43925,#43926,#43927,#43928,#43929,#43930,#43931,#43932,#43933,#43934,
#43935,#43936,#43937,#43938,#43939,#43940,#43941,#43942,#43943,#43944,#43945,
#43946,#43947,#43948,#43949,#43950,#43951,#43952,#43953,#43954,#43955,#43956,
#43957,#43958,#43959,#43960,#43961,#43962,#43963,#43964,#43965,#43966,#43967,
#43968,#43969,#43970,#43971,#43972,#43973,#43974,#43975,#43976,#43977,#43978,
#43979,#43980,#43981,#43982,#43983,#43984,#43985,#43986,#43987,#43988,#43989,
#43990,#43991,#43992,#43993,#43994,#43995,#43996,#43997,#43998,#43999,#44000,
#44001,#44002,#44003,#44004,#44005,#44006,#44007,#44008,#44009,#44010,#44011,
#44012,#44013,#44014,#44015,#44016,#44017,#44018,#44019,#44020,#44021,#44022,
#44023,#44024,#44025,#44026,#44027,#44028,#44029,#44030,#44031,#44032,#44033,
#44034,#44035,#44036,#44037,#44038,#44039,#44040,#44041,#44042,#44043,#44044,
#44045,#44046,#44047,#44048,#44049,#44050,#44051,#44052,#44053,#44054,#44055,
#44056,#44057,#44058,#44059,#44060,#44061,#44062,#44063,#44064,#44065,#44066,
#44067,#44068,#44069,#44070,#44071,#44072,#44073,#44074,#44075,#44076,#44077,
#44078,#44079,#44080,#44081,#44082,#44083,#44084,#44085,#44086,#44087,#44088,
#44089,#44090,#44091,#44092,#44093,#44094,#44095,#44096,#44097,#44098,#44099,
#44100,#44101,#44102,#44103,#44104,#44105,#44106,#44107,#44108,#44109,#44110,
#44111,#44112,#44113,#44114,#44115,#44116,#44117,#44118,#44119,#44120,#44121,
#44122,#44123,#44124,#44125,#44126,#44127,#44128,#44129,#44130,#44131,#44132,
#44133,#44134,#44135,#44136,#44137,#44138,#44139,#44140,#44141,#44142,#44143,
#44144,#44145,#44146,#44147,#44148,#44149,#44150,#44151,#44152,#44153,#44154,
#44155,#44156,#44157,#44158,#44159,#44160,#44161,#44162,#44163,#44164,#44165,
#44166,#44167,#44168,#44169,#44170,#44171,#44172,#44173,#44174,#44175,#44176,
#44177,#44178,#44179,#44180,#44181,#44182,#44183,#44184,#44185,#44186,#44187,
#44188,#44189,#44190,#44191,#44192,#44193,#44194,#44195,#44196,#44197,#44198,
#44199,#44200,#44201,#44202,#44203,#44204,#44205,#44206,#44207,#44208,#44209,
#44210,#44211,#44212,#44213,#44214,#44215,#44216,#44217,#44218,#44219,#44220,
#44221,#44222,#44223,#44224,#44225,#44226,#44227,#44228,#44229,#44230,#44231,
#44232,#44233,#44234,#44235,#44236,#44237,#44238,#44239,#44240,#44241,#44242,
#44243,#44244,#44245,#44246,#44247,#44248,#44249,#44250,#44251,#44252,#44253,
#44254,#44255,#44256,#44257)),.UNSPECIFIED.,.F.,.F.,.F.)
B_SPLINE_SURFACE_WITH_KNOTS((4,4),(3,2,2,2,2,2,2,2,2,2,2,2,2,2,2,2,2,2,
2,2,2,2,2,2,2,2,2,2,2,2,2,2,2,2,2,2,2,2,2,2,2,2,2,2,2,2,2,2,2,2,2,2,2,2,
2,2,2,2,2,2,2,2,2,2,2,2,2,2,2,2,2,2,2,2,2,2,2,2,2,2,2,2,2,2,2,2,2,2,2,2,
2,2,2,2,2,2,2,2,2,2,2,2,2,2,2,2,2,2,2,2,2,2,2,2,2,2,2,2,2,2,2,2,2,2,2,2,
2,2,2,2,2,2,2,2,2,2,2,2,2,2,2,2,2,2,2,2,2,2,2,2,2,2,2,2,2,2,2,2,2,2,2,2,
2,2,2,2,2,2,2,2,2,2,2,2,2,2,2,2,2,2,2,2,2,2,2,2,2,2,2,2,2,2,2,2,2,2,2,2,
2,2,2,2,2,2,2,2,2,2,2,2,2,2,2,2,2,2,2,2,2,2,2,2,2,2,2,2,2,2,2,2,2,2,2,2,
2,2,2,2,2,2,2,2,2,2,2,2,2,2,2,2,2,2,2,2,2,2,2,2,2,2,2,2,2,2,2,2,2,2,2,2,
2,2,2,2,2,2,2,2,2,2,2,2,2,2,2,2,2,2,2,2,2,2,2,2,2,2,2,2,2,2,2,2,2,2,2,2,
2,2,2,2,2,2,2,2,2,2,2,2,2,2,2,2,2,2,2,2,2,2,2,2,2,2,2,2,2,2,2,2,2,2,2,2,
2,2,2,2,2,3),(0.,1.),(0.,0.00284090909090909,0.00568181818181818,0.00852272727272727,
0.0113636363636364,0.0142045454545455,0.0170454545454545,0.0198863636363636,
0.0227272727272727,0.0255681818181818,0.0284090909090909,0.03125,0.0340909090909091,
0.0369318181818182,0.0397727272727273,0.0426136363636364,0.0454545454545455,
0.0482954545454545,0.0511363636363636,0.0539772727272727,0.0568181818181818,
0.0596590909090909,0.0625,0.0653409090909091,0.0681818181818182,0.0710227272727273,
0.0738636363636364,0.0767045454545455,0.0795454545454545,0.0823863636363636,
0.0852272727272727,0.0880681818181818,0.0909090909090909,0.09375,0.0965909090909091,
0.0994318181818182,0.102272727272727,0.105113636363636,0.107954545454545,
0.110795454545455,0.113636363636364,0.116477272727273,0.119318181818182,
0.122159090909091,0.125,0.127840909090909,0.130681818181818,0.133522727272727,
0.136363636363636,0.139204545454545,0.142045454545455,0.144886363636364,
0.147727272727273,0.150568181818182,0.153409090909091,0.15625,0.159090909090909,
0.161931818181818,0.164772727272727,0.167613636363636,0.170454545454545,
0.173295454545455,0.176136363636364,0.178977272727273,0.181818181818182,
0.184659090909091,0.1875,0.190340909090909,0.193181818181818,0.196022727272727,
0.198863636363636,0.201704545454545,0.204545454545455,0.207386363636364,
0.210227272727273,0.213068181818182,0.215909090909091,0.21875,0.221590909090909,
0.224431818181818,0.227272727272727,0.230113636363636,0.232954545454545,
0.235795454545455,0.238636363636364,0.241477272727273,0.244318181818182,
0.247159090909091,0.25,0.252840909090909,0.255681818181818,0.258522727272727,
0.261363636363636,0.264204545454545,0.267045454545455,0.269886363636364,
0.272727272727273,0.275568181818182,0.278409090909091,0.28125,0.284090909090909,
0.286931818181818,0.289772727272727,0.292613636363636,0.295454545454545,
0.298295454545455,0.301136363636364,0.303977272727273,0.306818181818182,
0.309659090909091,0.3125,0.315340909090909,0.318181818181818,0.321022727272727,
0.323863636363636,0.326704545454545,0.329545454545455,0.332386363636364,
0.335227272727273,0.338068181818182,0.340909090909091,0.34375,0.346590909090909,
0.349431818181818,0.352272727272727,0.355113636363636,0.357954545454545,
0.360795454545455,0.363636363636364,0.366477272727273,0.369318181818182,
0.372159090909091,0.375,0.377840909090909,0.380681818181818,0.383522727272727,
0.386363636363636,0.389204545454545,0.392045454545455,0.394886363636364,
0.397727272727273,0.400568181818182,0.403409090909091,0.40625,0.409090909090909,
0.411931818181818,0.414772727272727,0.417613636363636,0.420454545454545,
0.423295454545455,0.426136363636364,0.428977272727273,0.431818181818182,
0.434659090909091,0.4375,0.440340909090909,0.443181818181818,0.446022727272727,
0.448863636363636,0.451704545454545,0.454545454545455,0.457386363636364,
0.460227272727273,0.463068181818182,0.465909090909091,0.46875,0.471590909090909,
0.474431818181818,0.477272727272727,0.480113636363636,0.482954545454545,
0.485795454545455,0.488636363636364,0.491477272727273,0.494318181818182,
0.497159090909091,0.5,0.502840909090909,0.505681818181818,0.508522727272727,
0.511363636363636,0.514204545454545,0.517045454545455,0.519886363636364,
0.522727272727273,0.525568181818182,0.528409090909091,0.53125,0.534090909090909,
0.536931818181818,0.539772727272727,0.542613636363636,0.545454545454545,
0.548295454545455,0.551136363636364,0.553977272727273,0.556818181818182,
0.559659090909091,0.5625,0.565340909090909,0.568181818181818,0.571022727272727,
0.573863636363636,0.576704545454545,0.579545454545455,0.582386363636364,
0.585227272727273,0.588068181818182,0.590909090909091,0.59375,0.596590909090909,
0.599431818181818,0.602272727272727,0.605113636363636,0.607954545454545,
0.610795454545455,0.613636363636364,0.616477272727273,0.619318181818182,
0.622159090909091,0.625,0.627840909090909,0.630681818181818,0.633522727272727,
0.636363636363636,0.639204545454545,0.642045454545455,0.644886363636364,
0.647727272727273,0.650568181818182,0.653409090909091,0.65625,0.659090909090909,
0.661931818181818,0.664772727272727,0.667613636363636,0.670454545454545,
0.673295454545455,0.676136363636364,0.678977272727273,0.681818181818182,
0.684659090909091,0.6875,0.690340909090909,0.693181818181818,0.696022727272727,
0.698863636363636,0.701704545454545,0.704545454545455,0.707386363636364,
0.710227272727273,0.713068181818182,0.715909090909091,0.71875,0.721590909090909,
0.724431818181818,0.727272727272727,0.730113636363636,0.732954545454545,
0.735795454545455,0.738636363636364,0.741477272727273,0.744318181818182,
0.747159090909091,0.75,0.752840909090909,0.755681818181818,0.758522727272727,
0.761363636363636,0.764204545454545,0.767045454545455,0.769886363636364,
0.772727272727273,0.775568181818182,0.778409090909091,0.78125,0.784090909090909,
0.786931818181818,0.789772727272727,0.792613636363636,0.795454545454545,
0.798295454545455,0.801136363636364,0.803977272727273,0.806818181818182,
0.809659090909091,0.8125,0.815340909090909,0.818181818181818,0.821022727272727,
0.823863636363636,0.826704545454545,0.829545454545455,0.832386363636364,
0.835227272727273,0.838068181818182,0.840909090909091,0.84375,0.846590909090909,
0.849431818181818,0.852272727272727,0.855113636363636,0.857954545454545,
0.860795454545455,0.863636363636364,0.866477272727273,0.869318181818182,
0.872159090909091,0.875,0.877840909090909,0.880681818181818,0.883522727272727,
0.886363636363636,0.889204545454545,0.892045454545455,0.894886363636364,
0.897727272727273,0.900568181818182,0.903409090909091,0.90625,0.909090909090909,
0.911931818181818,0.914772727272727,0.917613636363636,0.920454545454545,
0.923295454545455,0.926136363636364,0.928977272727273,0.931818181818182,
0.934659090909091,0.9375,0.940340909090909,0.943181818181818,0.946022727272727,
0.948863636363636,0.951704545454545,0.954545454545455,0.957386363636364,
0.960227272727273,0.963068181818182,0.965909090909091,0.96875,0.971590909090909,
0.974431818181818,0.977272727272727,0.980113636363636,0.982954545454545,
0.98484301350122),.UNSPECIFIED.)
GEOMETRIC_REPRESENTATION_ITEM()
RATIONAL_B_SPLINE_SURFACE(((1.,0.923879532511287,1.,0.923879532511287,1.,
0.923879532511287,1.,0.923879532511287,1.,0.923879532511287,1.,0.923879532511287,
1.,0.923879532511287,1.,0.923879532511287,1.,0.923879532511287,1.,0.923879532511287,
1.,0.923879532511287,1.,0.923879532511287,1.,0.923879532511287,1.,0.923879532511287,
1.,0.923879532511287,1.,0.923879532511287,1.,0.923879532511287,1.,0.923879532511287,
1.,0.923879532511287,1.,0.923879532511287,1.,0.923879532511287,1.,0.923879532511287,
1.,0.923879532511287,1.,0.923879532511287,1.,0.923879532511287,1.,0.923879532511287,
1.,0.923879532511287,1.,0.923879532511287,1.,0.923879532511287,1.,0.923879532511287,
1.,0.923879532511287,1.,0.923879532511287,1.,0.923879532511287,1.,0.923879532511287,
1.,0.923879532511287,1.,0.923879532511287,1.,0.923879532511287,1.,0.923879532511287,
1.,0.923879532511287,1.,0.923879532511287,1.,0.923879532511287,1.,0.923879532511287,
1.,0.923879532511287,1.,0.923879532511287,1.,0.923879532511287,1.,0.923879532511287,
1.,0.923879532511287,1.,0.923879532511287,1.,0.923879532511287,1.,0.923879532511287,
1.,0.923879532511287,1.,0.923879532511287,1.,0.923879532511287,1.,0.923879532511287,
1.,0.923879532511287,1.,0.923879532511287,1.,0.923879532511287,1.,0.923879532511287,
1.,0.923879532511287,1.,0.923879532511287,1.,0.923879532511287,1.,0.923879532511287,
1.,0.923879532511287,1.,0.923879532511287,1.,0.923879532511287,1.,0.923879532511287,
1.,0.923879532511287,1.,0.923879532511287,1.,0.923879532511287,1.,0.923879532511287,
1.,0.923879532511287,1.,0.923879532511287,1.,0.923879532511287,1.,0.923879532511287,
1.,0.923879532511287,1.,0.923879532511287,1.,0.923879532511287,1.,0.923879532511287,
1.,0.923879532511287,1.,0.923879532511287,1.,0.923879532511287,1.,0.923879532511287,
1.,0.923879532511287,1.,0.923879532511287,1.,0.923879532511287,1.,0.923879532511287,
1.,0.923879532511287,1.,0.923879532511287,1.,0.923879532511287,1.,0.923879532511287,
1.,0.923879532511287,1.,0.923879532511287,1.,0.923879532511287,1.,0.923879532511287,
1.,0.923879532511287,1.,0.923879532511287,1.,0.923879532511287,1.,0.923879532511287,
1.,0.923879532511287,1.,0.923879532511287,1.,0.923879532511287,1.,0.923879532511287,
1.,0.923879532511287,1.,0.923879532511287,1.,0.923879532511287,1.,0.923879532511287,
1.,0.923879532511287,1.,0.923879532511287,1.,0.923879532511287,1.,0.923879532511287,
1.,0.923879532511287,1.,0.923879532511287,1.,0.923879532511287,1.,0.923879532511287,
1.,0.923879532511287,1.,0.923879532511287,1.,0.923879532511287,1.,0.923879532511287,
1.,0.923879532511287,1.,0.923879532511287,1.,0.923879532511287,1.,0.923879532511287,
1.,0.923879532511287,1.,0.923879532511287,1.,0.923879532511287,1.,0.923879532511287,
1.,0.923879532511287,1.,0.923879532511287,1.,0.923879532511287,1.,0.923879532511287,
1.,0.923879532511287,1.,0.923879532511287,1.,0.923879532511287,1.,0.923879532511287,
1.,0.923879532511287,1.,0.923879532511287,1.,0.923879532511287,1.,0.923879532511287,
1.,0.923879532511287,1.,0.923879532511287,1.,0.923879532511287,1.,0.923879532511287,
1.,0.923879532511287,1.,0.923879532511287,1.,0.923879532511287,1.,0.923879532511287,
1.,0.923879532511287,1.,0.923879532511287,1.,0.923879532511287,1.,0.923879532511287,
1.,0.923879532511287,1.,0.923879532511287,1.,0.923879532511287,1.,0.923879532511287,
1.,0.923879532511287,1.,0.923879532511287,1.,0.923879532511287,1.,0.923879532511287,
1.,0.923879532511287,1.,0.923879532511287,1.,0.923879532511287,1.,0.923879532511287,
1.,0.923879532511287,1.,0.923879532511287,1.,0.923879532511287,1.,0.923879532511287,
1.,0.923879532511287,1.,0.923879532511287,1.,0.923879532511287,1.,0.923879532511287,
1.,0.923879532511287,1.,0.923879532511287,1.,0.923879532511287,1.,0.923879532511287,
1.,0.923879532511287,1.,0.923879532511287,1.,0.923879532511287,1.,0.923879532511287,
1.,0.923879532511287,1.,0.923879532511287,1.,0.923879532511287,1.,0.923879532511287,
1.,0.923879532511287,1.,0.923879532511287,1.,0.923879532511287,1.,0.923879532511287,
1.,0.923879532511287,1.,0.923879532511287,1.,0.923879532511287,1.,0.923879532511287,
1.,0.923879532511287,1.,0.923879532511287,1.,0.923879532511287,1.,0.923879532511287,
1.,0.923879532511287,1.,0.923879532511287,1.,0.923879532511287,1.,0.923879532511287,
1.,0.923879532511287,1.,0.923879532511287,1.,0.923879532511287,1.,0.923879532511287,
1.,0.923879532511287,1.,0.923879532511287,1.,0.923879532511287,1.,0.923879532511287,
1.,0.923879532511287,1.,0.923879532511287,1.,0.923879532511287,1.,0.923879532511287,
1.,0.923879532511287,1.,0.923879532511287,1.,0.923879532511287,1.,0.923879532511287,
1.,0.923879532511287,1.,0.923879532511287,1.,0.923879532511287,1.,0.923879532511287,
1.,0.923879532511287,1.,0.923879532511287,1.,0.923879532511287,1.,0.923879532511287,
1.,0.923879532511287,1.,0.923879532511287,1.,0.923879532511287,1.,0.923879532511287,
1.,0.923879532511287,1.,0.923879532511287,1.,0.923879532511287,1.,0.923879532511287,
1.,0.923879532511287,1.,0.923879532511287,1.,0.923879532511287,1.,0.923879532511287,
1.,0.923879532511287,1.,0.923879532511287,1.,0.923879532511287,1.,0.923879532511287,
1.,0.923879532511287,1.,0.923879532511287,1.,0.923879532511287,1.,0.923879532511287,
1.,0.923879532511287,1.,0.923879532511287,1.,0.923879532511287,1.,0.923879532511287,
1.,0.923879532511287,1.,0.923879532511287,1.,0.923879532511287,1.,0.923879532511287,
1.,0.923879532511287,1.,0.923879532511287,1.,0.923879532511287,1.,0.923879532511287,
1.,0.923879532511287,1.,0.923879532511287,1.,0.923879532511287,1.,0.923879532511287,
1.,0.923879532511287,1.,0.923879532511287,1.,0.923879532511287,1.,0.923879532511287,
1.,0.923879532511287,1.,0.923879532511287,1.,0.923879532511287,1.,0.923879532511287,
1.,0.923879532511287,1.,0.923879532511287,1.,0.923879532511287,1.,0.923879532511287,
1.,0.923879532511287,1.,0.923879532511287,1.,0.923879532511287,1.,0.923879532511287,
1.,0.923879532511287,1.,0.923879532511287,1.,0.923879532511287,1.,0.923879532511287,
1.,0.923879532511287,1.,0.923879532511287,1.,0.923879532511287,1.,0.923879532511287,
1.,0.923879532511287,1.,0.923879532511287,1.,0.923879532511287,1.,0.923879532511287,
1.,0.923879532511287,1.,0.923879532511287,1.,0.923879532511287,1.,0.923879532511287,
1.,0.923879532511287,1.,0.923879532511287,1.,0.923879532511287,1.,0.923879532511287,
1.,0.923879532511287,1.,0.923879532511287,1.,0.923879532511287,1.,0.923879532511287,
1.,0.923879532511287,1.,0.923879532511287,1.,0.923879532511287,1.,0.923879532511287,
1.,0.923879532511287,1.,0.923879532511287,1.,0.923879532511287,1.,0.923879532511287,
1.,0.923879532511287,1.,0.923879532511287,1.,0.923879532511287,1.,0.923879532511287,
1.,0.923879532511287,1.,0.923879532511287,1.,0.923879532511287,1.,0.923879532511287,
1.,0.923879532511287,1.,0.923879532511287,1.,0.923879532511287,1.,0.923879532511287,
1.,0.923879532511287,1.,0.923879532511287,1.,0.923879532511287,1.,0.923879532511287,
1.,0.923879532511287,1.,0.923879532511287,1.,0.923879532511287,1.,0.923879532511287,
1.,0.923879532511287,1.,0.923879532511287,1.,0.923879532511287,1.,0.923879532511287,
1.,0.923879532511287,1.,0.923879532511287,1.,0.923879532511287,1.,0.923879532511287,
1.,0.923879532511287,1.,0.923879532511287,1.,0.923879532511287,1.,0.923879532511287,
1.,0.923879532511287,1.,0.923879532511287,1.,0.923879532511287,1.,0.923879532511287,
1.,0.923879532511287,1.,0.923879532511287,1.,0.923879532511287,1.,0.923879532511287,
1.,0.949399623166265,0.96607151147188),(0.994771161099481,0.919048715272298,
0.994771161099481,0.919048715272298,0.994771161099481,0.919048715272298,
0.994771161099481,0.919048715272298,0.994771161099481,0.919048715272298,
0.994771161099481,0.919048715272298,0.994771161099481,0.919048715272298,
0.994771161099481,0.919048715272298,0.994771161099481,0.919048715272298,
0.994771161099481,0.919048715272298,0.994771161099481,0.919048715272298,
0.994771161099481,0.919048715272298,0.994771161099481,0.919048715272298,
0.994771161099481,0.919048715272298,0.994771161099481,0.919048715272298,
0.994771161099481,0.919048715272298,0.994771161099481,0.919048715272298,
0.994771161099481,0.919048715272298,0.994771161099481,0.919048715272298,
0.994771161099481,0.919048715272298,0.994771161099481,0.919048715272298,
0.994771161099481,0.919048715272298,0.994771161099481,0.919048715272298,
0.994771161099481,0.919048715272298,0.994771161099481,0.919048715272298,
0.994771161099481,0.919048715272298,0.994771161099481,0.919048715272298,
0.994771161099481,0.919048715272298,0.994771161099481,0.919048715272298,
0.994771161099481,0.919048715272298,0.994771161099481,0.919048715272298,
0.994771161099481,0.919048715272298,0.994771161099481,0.919048715272298,
0.994771161099481,0.919048715272298,0.994771161099481,0.919048715272298,
0.994771161099481,0.919048715272298,0.994771161099481,0.919048715272298,
0.994771161099481,0.919048715272298,0.994771161099481,0.919048715272298,
0.994771161099481,0.919048715272298,0.994771161099481,0.919048715272298,
0.994771161099481,0.919048715272298,0.994771161099481,0.919048715272298,
0.994771161099481,0.919048715272298,0.994771161099481,0.919048715272298,
0.994771161099481,0.919048715272298,0.994771161099481,0.919048715272298,
0.994771161099481,0.919048715272298,0.994771161099481,0.919048715272298,
0.994771161099481,0.919048715272298,0.994771161099481,0.919048715272298,
0.994771161099481,0.919048715272298,0.994771161099481,0.919048715272298,
0.994771161099481,0.919048715272298,0.994771161099481,0.919048715272298,
0.994771161099481,0.919048715272298,0.994771161099481,0.919048715272298,
0.994771161099481,0.919048715272298,0.994771161099481,0.919048715272298,
0.994771161099481,0.919048715272298,0.994771161099481,0.919048715272298,
0.994771161099481,0.919048715272298,0.994771161099481,0.919048715272298,
0.994771161099481,0.919048715272298,0.994771161099481,0.919048715272298,
0.994771161099481,0.919048715272298,0.994771161099481,0.919048715272298,
0.994771161099481,0.919048715272298,0.994771161099481,0.919048715272298,
0.994771161099481,0.919048715272298,0.994771161099481,0.919048715272298,
0.994771161099481,0.919048715272298,0.994771161099481,0.919048715272298,
0.994771161099481,0.919048715272298,0.994771161099481,0.919048715272298,
0.994771161099481,0.919048715272298,0.994771161099481,0.919048715272298,
0.994771161099481,0.919048715272298,0.994771161099481,0.919048715272298,
0.994771161099481,0.919048715272298,0.994771161099481,0.919048715272298,
0.994771161099481,0.919048715272298,0.994771161099481,0.919048715272298,
0.994771161099481,0.919048715272298,0.994771161099481,0.919048715272298,
0.994771161099481,0.919048715272298,0.994771161099481,0.919048715272298,
0.994771161099481,0.919048715272298,0.994771161099481,0.919048715272298,
0.994771161099481,0.919048715272298,0.994771161099481,0.919048715272298,
0.994771161099481,0.919048715272298,0.994771161099481,0.919048715272298,
0.994771161099481,0.919048715272298,0.994771161099481,0.919048715272298,
0.994771161099481,0.919048715272298,0.994771161099481,0.919048715272298,
0.994771161099481,0.919048715272298,0.994771161099481,0.919048715272298,
0.994771161099481,0.919048715272298,0.994771161099481,0.919048715272298,
0.994771161099481,0.919048715272298,0.994771161099481,0.919048715272298,
0.994771161099481,0.919048715272298,0.994771161099481,0.919048715272298,
0.994771161099481,0.919048715272298,0.994771161099481,0.919048715272298,
0.994771161099481,0.919048715272298,0.994771161099481,0.919048715272298,
0.994771161099481,0.919048715272298,0.994771161099481,0.919048715272298,
0.994771161099481,0.919048715272298,0.994771161099481,0.919048715272298,
0.994771161099481,0.919048715272298,0.994771161099481,0.919048715272298,
0.994771161099481,0.919048715272298,0.994771161099481,0.919048715272298,
0.994771161099481,0.919048715272298,0.994771161099481,0.919048715272298,
0.994771161099481,0.919048715272298,0.994771161099481,0.919048715272298,
0.994771161099481,0.919048715272298,0.994771161099481,0.919048715272298,
0.994771161099481,0.919048715272298,0.994771161099481,0.919048715272298,
0.994771161099481,0.919048715272298,0.994771161099481,0.919048715272298,
0.994771161099481,0.919048715272298,0.994771161099481,0.919048715272298,
0.994771161099481,0.919048715272298,0.994771161099481,0.919048715272298,
0.994771161099481,0.919048715272298,0.994771161099481,0.919048715272298,
0.994771161099481,0.919048715272298,0.994771161099481,0.919048715272298,
0.994771161099481,0.919048715272298,0.994771161099481,0.919048715272298,
0.994771161099481,0.919048715272298,0.994771161099481,0.919048715272298,
0.994771161099481,0.919048715272298,0.994771161099481,0.919048715272298,
0.994771161099481,0.919048715272298,0.994771161099481,0.919048715272298,
0.994771161099481,0.919048715272298,0.994771161099481,0.919048715272298,
0.994771161099481,0.919048715272298,0.994771161099481,0.919048715272298,
0.994771161099481,0.919048715272298,0.994771161099481,0.919048715272298,
0.994771161099481,0.919048715272298,0.994771161099481,0.919048715272298,
0.994771161099481,0.919048715272298,0.994771161099481,0.919048715272298,
0.994771161099481,0.919048715272298,0.994771161099481,0.919048715272298,
0.994771161099481,0.919048715272298,0.994771161099481,0.919048715272298,
0.994771161099481,0.919048715272298,0.994771161099481,0.919048715272298,
0.994771161099481,0.919048715272298,0.994771161099481,0.919048715272298,
0.994771161099481,0.919048715272298,0.994771161099481,0.919048715272298,
0.994771161099481,0.919048715272298,0.994771161099481,0.919048715272298,
0.994771161099481,0.919048715272298,0.994771161099481,0.919048715272298,
0.994771161099481,0.919048715272298,0.994771161099481,0.919048715272298,
0.994771161099481,0.919048715272298,0.994771161099481,0.919048715272298,
0.994771161099481,0.919048715272298,0.994771161099481,0.919048715272298,
0.994771161099481,0.919048715272298,0.994771161099481,0.919048715272298,
0.994771161099481,0.919048715272298,0.994771161099481,0.919048715272298,
0.994771161099481,0.919048715272298,0.994771161099481,0.919048715272298,
0.994771161099481,0.919048715272298,0.994771161099481,0.919048715272298,
0.994771161099481,0.919048715272298,0.994771161099481,0.919048715272298,
0.994771161099481,0.919048715272298,0.994771161099481,0.919048715272298,
0.994771161099481,0.919048715272298,0.994771161099481,0.919048715272298,
0.994771161099481,0.919048715272298,0.994771161099481,0.919048715272298,
0.994771161099481,0.919048715272298,0.994771161099481,0.919048715272298,
0.994771161099481,0.919048715272298,0.994771161099481,0.919048715272298,
0.994771161099481,0.919048715272298,0.994771161099481,0.919048715272298,
0.994771161099481,0.919048715272298,0.994771161099481,0.919048715272298,
0.994771161099481,0.919048715272298,0.994771161099481,0.919048715272298,
0.994771161099481,0.919048715272298,0.994771161099481,0.919048715272298,
0.994771161099481,0.919048715272298,0.994771161099481,0.919048715272298,
0.994771161099481,0.919048715272298,0.994771161099481,0.919048715272298,
0.994771161099481,0.919048715272298,0.994771161099481,0.919048715272298,
0.994771161099481,0.919048715272298,0.994771161099481,0.919048715272298,
0.994771161099481,0.919048715272298,0.994771161099481,0.919048715272298,
0.994771161099481,0.919048715272298,0.994771161099481,0.919048715272298,
0.994771161099481,0.919048715272298,0.994771161099481,0.919048715272298,
0.994771161099481,0.919048715272298,0.994771161099481,0.919048715272298,
0.994771161099481,0.919048715272298,0.994771161099481,0.919048715272298,
0.994771161099481,0.919048715272298,0.994771161099481,0.919048715272298,
0.994771161099481,0.919048715272298,0.994771161099481,0.919048715272298,
0.994771161099481,0.919048715272298,0.994771161099481,0.919048715272298,
0.994771161099481,0.919048715272298,0.994771161099481,0.919048715272298,
0.994771161099481,0.919048715272298,0.994771161099481,0.919048715272298,
0.994771161099481,0.919048715272298,0.994771161099481,0.919048715272298,
0.994771161099481,0.919048715272298,0.994771161099481,0.919048715272298,
0.994771161099481,0.919048715272298,0.994771161099481,0.919048715272298,
0.994771161099481,0.919048715272298,0.994771161099481,0.919048715272298,
0.994771161099481,0.919048715272298,0.994771161099481,0.919048715272298,
0.994771161099481,0.919048715272298,0.994771161099481,0.919048715272298,
0.994771161099481,0.919048715272298,0.994771161099481,0.919048715272298,
0.994771161099481,0.919048715272298,0.994771161099481,0.919048715272298,
0.994771161099481,0.919048715272298,0.994771161099481,0.919048715272298,
0.994771161099481,0.919048715272298,0.994771161099481,0.919048715272298,
0.994771161099481,0.919048715272298,0.994771161099481,0.919048715272298,
0.994771161099481,0.919048715272298,0.994771161099481,0.919048715272298,
0.994771161099481,0.919048715272298,0.994771161099481,0.919048715272298,
0.994771161099481,0.919048715272298,0.994771161099481,0.919048715272298,
0.994771161099481,0.919048715272298,0.994771161099481,0.919048715272298,
0.994771161099481,0.919048715272298,0.994771161099481,0.919048715272298,
0.994771161099481,0.919048715272298,0.994771161099481,0.919048715272298,
0.994771161099481,0.919048715272298,0.994771161099481,0.919048715272298,
0.994771161099481,0.919048715272298,0.994771161099481,0.919048715272298,
0.994771161099481,0.919048715272298,0.994771161099481,0.919048715272298,
0.994771161099481,0.919048715272298,0.994771161099481,0.919048715272298,
0.994771161099481,0.919048715272298,0.994771161099481,0.919048715272298,
0.994771161099481,0.919048715272298,0.994771161099481,0.919048715272298,
0.994771161099481,0.919048715272298,0.994771161099481,0.919048715272298,
0.994771161099481,0.919048715272298,0.994771161099481,0.919048715272298,
0.994771161099481,0.919048715272298,0.994771161099481,0.919048715272298,
0.994771161099481,0.919048715272298,0.994771161099481,0.919048715272298,
0.994771161099481,0.919048715272298,0.994771161099481,0.919048715272298,
0.994771161099481,0.919048715272298,0.994771161099481,0.919048715272298,
0.994771161099481,0.919048715272298,0.994771161099481,0.919048715272298,
0.994771161099481,0.919048715272298,0.994771161099481,0.919048715272298,
0.994771161099481,0.919048715272298,0.994771161099481,0.919048715272298,
0.994771161099481,0.919048715272298,0.994771161099481,0.919048715272298,
0.994771161099481,0.919048715272298,0.994771161099481,0.919048715272298,
0.994771161099481,0.919048715272298,0.994771161099481,0.919048715272298,
0.994771161099481,0.919048715272298,0.994771161099481,0.919048715272298,
0.994771161099481,0.919048715272298,0.994771161099481,0.919048715272298,
0.994771161099481,0.919048715272298,0.994771161099481,0.919048715272298,
0.994771161099481,0.919048715272298,0.994771161099481,0.919048715272298,
0.994771161099481,0.919048715272298,0.994771161099481,0.919048715272298,
0.994771161099481,0.919048715272298,0.994771161099481,0.919048715272298,
0.994771161099481,0.919048715272298,0.994771161099481,0.919048715272298,
0.994771161099481,0.919048715272298,0.994771161099481,0.919048715272298,
0.994771161099481,0.919048715272298,0.994771161099481,0.919048715272298,
0.994771161099481,0.919048715272298,0.994771161099481,0.919048715272298,
0.994771161099481,0.919048715272298,0.994771161099481,0.919048715272298,
0.994771161099481,0.919048715272298,0.994771161099481,0.919048715272298,
0.994771161099481,0.919048715272298,0.994771161099481,0.919048715272298,
0.994771161099481,0.919048715272298,0.994771161099481,0.919048715272298,
0.994771161099481,0.919048715272298,0.994771161099481,0.919048715272298,
0.994771161099481,0.919048715272298,0.994771161099481,0.919048715272298,
0.994771161099481,0.919048715272298,0.994771161099481,0.919048715272298,
0.994771161099481,0.919048715272298,0.994771161099481,0.919048715272298,
0.994771161099481,0.919048715272298,0.994771161099481,0.919048715272298,
0.994771161099481,0.919048715272298,0.994771161099481,0.919048715272298,
0.994771161099481,0.919048715272298,0.994771161099481,0.919048715272298,
0.994771161099481,0.919048715272298,0.994771161099481,0.919048715272298,
0.994771161099481,0.919048715272298,0.994771161099481,0.919048715272298,
0.994771161099481,0.919048715272298,0.994771161099481,0.944435365484515,
0.961020079172012),(0.994771161099481,0.919048715272298,0.994771161099481,
0.919048715272298,0.994771161099481,0.919048715272298,0.994771161099481,
0.919048715272298,0.994771161099481,0.919048715272298,0.994771161099481,
0.919048715272298,0.994771161099481,0.919048715272298,0.994771161099481,
0.919048715272298,0.994771161099481,0.919048715272298,0.994771161099481,
0.919048715272298,0.994771161099481,0.919048715272298,0.994771161099481,
0.919048715272298,0.994771161099481,0.919048715272298,0.994771161099481,
0.919048715272298,0.994771161099481,0.919048715272298,0.994771161099481,
0.919048715272298,0.994771161099481,0.919048715272298,0.994771161099481,
0.919048715272298,0.994771161099481,0.919048715272298,0.994771161099481,
0.919048715272298,0.994771161099481,0.919048715272298,0.994771161099481,
0.919048715272298,0.994771161099481,0.919048715272298,0.994771161099481,
0.919048715272298,0.994771161099481,0.919048715272298,0.994771161099481,
0.919048715272298,0.994771161099481,0.919048715272298,0.994771161099481,
0.919048715272298,0.994771161099481,0.919048715272298,0.994771161099481,
0.919048715272298,0.994771161099481,0.919048715272298,0.994771161099481,
0.919048715272298,0.994771161099481,0.919048715272298,0.994771161099481,
0.919048715272298,0.994771161099481,0.919048715272298,0.994771161099481,
0.919048715272298,0.994771161099481,0.919048715272298,0.994771161099481,
0.919048715272298,0.994771161099481,0.919048715272298,0.994771161099481,
0.919048715272298,0.994771161099481,0.919048715272298,0.994771161099481,
0.919048715272298,0.994771161099481,0.919048715272298,0.994771161099481,
0.919048715272298,0.994771161099481,0.919048715272298,0.994771161099481,
0.919048715272298,0.994771161099481,0.919048715272298,0.994771161099481,
0.919048715272298,0.994771161099481,0.919048715272298,0.994771161099481,
0.919048715272298,0.994771161099481,0.919048715272298,0.994771161099481,
0.919048715272298,0.994771161099481,0.919048715272298,0.994771161099481,
0.919048715272298,0.994771161099481,0.919048715272298,0.994771161099481,
0.919048715272298,0.994771161099481,0.919048715272298,0.994771161099481,
0.919048715272298,0.994771161099481,0.919048715272298,0.994771161099481,
0.919048715272298,0.994771161099481,0.919048715272298,0.994771161099481,
0.919048715272298,0.994771161099481,0.919048715272298,0.994771161099481,
0.919048715272298,0.994771161099481,0.919048715272298,0.994771161099481,
0.919048715272298,0.994771161099481,0.919048715272298,0.994771161099481,
0.919048715272298,0.994771161099481,0.919048715272298,0.994771161099481,
0.919048715272298,0.994771161099481,0.919048715272298,0.994771161099481,
0.919048715272298,0.994771161099481,0.919048715272298,0.994771161099481,
0.919048715272298,0.994771161099481,0.919048715272298,0.994771161099481,
0.919048715272298,0.994771161099481,0.919048715272298,0.994771161099481,
0.919048715272298,0.994771161099481,0.919048715272298,0.994771161099481,
0.919048715272298,0.994771161099481,0.919048715272298,0.994771161099481,
0.919048715272298,0.994771161099481,0.919048715272298,0.994771161099481,
0.919048715272298,0.994771161099481,0.919048715272298,0.994771161099481,
0.919048715272298,0.994771161099481,0.919048715272298,0.994771161099481,
0.919048715272298,0.994771161099481,0.919048715272298,0.994771161099481,
0.919048715272298,0.994771161099481,0.919048715272298,0.994771161099481,
0.919048715272298,0.994771161099481,0.919048715272298,0.994771161099481,
0.919048715272298,0.994771161099481,0.919048715272298,0.994771161099481,
0.919048715272298,0.994771161099481,0.919048715272298,0.994771161099481,
0.919048715272298,0.994771161099481,0.919048715272298,0.994771161099481,
0.919048715272298,0.994771161099481,0.919048715272298,0.994771161099481,
0.919048715272298,0.994771161099481,0.919048715272298,0.994771161099481,
0.919048715272298,0.994771161099481,0.919048715272298,0.994771161099481,
0.919048715272298,0.994771161099481,0.919048715272298,0.994771161099481,
0.919048715272298,0.994771161099481,0.919048715272298,0.994771161099481,
0.919048715272298,0.994771161099481,0.919048715272298,0.994771161099481,
0.919048715272298,0.994771161099481,0.919048715272298,0.994771161099481,
0.919048715272298,0.994771161099481,0.919048715272298,0.994771161099481,
0.919048715272298,0.994771161099481,0.919048715272298,0.994771161099481,
0.919048715272298,0.994771161099481,0.919048715272298,0.994771161099481,
0.919048715272298,0.994771161099481,0.919048715272298,0.994771161099481,
0.919048715272298,0.994771161099481,0.919048715272298,0.994771161099481,
0.919048715272298,0.994771161099481,0.919048715272298,0.994771161099481,
0.919048715272298,0.994771161099481,0.919048715272298,0.994771161099481,
0.919048715272298,0.994771161099481,0.919048715272298,0.994771161099481,
0.919048715272298,0.994771161099481,0.919048715272298,0.994771161099481,
0.919048715272298,0.994771161099481,0.919048715272298,0.994771161099481,
0.919048715272298,0.994771161099481,0.919048715272298,0.994771161099481,
0.919048715272298,0.994771161099481,0.919048715272298,0.994771161099481,
0.919048715272298,0.994771161099481,0.919048715272298,0.994771161099481,
0.919048715272298,0.994771161099481,0.919048715272298,0.994771161099481,
0.919048715272298,0.994771161099481,0.919048715272298,0.994771161099481,
0.919048715272298,0.994771161099481,0.919048715272298,0.994771161099481,
0.919048715272298,0.994771161099481,0.919048715272298,0.994771161099481,
0.919048715272298,0.994771161099481,0.919048715272298,0.994771161099481,
0.919048715272298,0.994771161099481,0.919048715272298,0.994771161099481,
0.919048715272298,0.994771161099481,0.919048715272298,0.994771161099481,
0.919048715272298,0.994771161099481,0.919048715272298,0.994771161099481,
0.919048715272298,0.994771161099481,0.919048715272298,0.994771161099481,
0.919048715272298,0.994771161099481,0.919048715272298,0.994771161099481,
0.919048715272298,0.994771161099481,0.919048715272298,0.994771161099481,
0.919048715272298,0.994771161099481,0.919048715272298,0.994771161099481,
0.919048715272298,0.994771161099481,0.919048715272298,0.994771161099481,
0.919048715272298,0.994771161099481,0.919048715272298,0.994771161099481,
0.919048715272298,0.994771161099481,0.919048715272298,0.994771161099481,
0.919048715272298,0.994771161099481,0.919048715272298,0.994771161099481,
0.919048715272298,0.994771161099481,0.919048715272298,0.994771161099481,
0.919048715272298,0.994771161099481,0.919048715272298,0.994771161099481,
0.919048715272298,0.994771161099481,0.919048715272298,0.994771161099481,
0.919048715272298,0.994771161099481,0.919048715272298,0.994771161099481,
0.919048715272298,0.994771161099481,0.919048715272298,0.994771161099481,
0.919048715272298,0.994771161099481,0.919048715272298,0.994771161099481,
0.919048715272298,0.994771161099481,0.919048715272298,0.994771161099481,
0.919048715272298,0.994771161099481,0.919048715272298,0.994771161099481,
0.919048715272298,0.994771161099481,0.919048715272298,0.994771161099481,
0.919048715272298,0.994771161099481,0.919048715272298,0.994771161099481,
0.919048715272298,0.994771161099481,0.919048715272298,0.994771161099481,
0.919048715272298,0.994771161099481,0.919048715272298,0.994771161099481,
0.919048715272298,0.994771161099481,0.919048715272298,0.994771161099481,
0.919048715272298,0.994771161099481,0.919048715272298,0.994771161099481,
0.919048715272298,0.994771161099481,0.919048715272298,0.994771161099481,
0.919048715272298,0.994771161099481,0.919048715272298,0.994771161099481,
0.919048715272298,0.994771161099481,0.919048715272298,0.994771161099481,
0.919048715272298,0.994771161099481,0.919048715272298,0.994771161099481,
0.919048715272298,0.994771161099481,0.919048715272298,0.994771161099481,
0.919048715272298,0.994771161099481,0.919048715272298,0.994771161099481,
0.919048715272298,0.994771161099481,0.919048715272298,0.994771161099481,
0.919048715272298,0.994771161099481,0.919048715272298,0.994771161099481,
0.919048715272298,0.994771161099481,0.919048715272298,0.994771161099481,
0.919048715272298,0.994771161099481,0.919048715272298,0.994771161099481,
0.919048715272298,0.994771161099481,0.919048715272298,0.994771161099481,
0.919048715272298,0.994771161099481,0.919048715272298,0.994771161099481,
0.919048715272298,0.994771161099481,0.919048715272298,0.994771161099481,
0.919048715272298,0.994771161099481,0.919048715272298,0.994771161099481,
0.919048715272298,0.994771161099481,0.919048715272298,0.994771161099481,
0.919048715272298,0.994771161099481,0.919048715272298,0.994771161099481,
0.919048715272298,0.994771161099481,0.919048715272298,0.994771161099481,
0.919048715272298,0.994771161099481,0.919048715272298,0.994771161099481,
0.919048715272298,0.994771161099481,0.919048715272298,0.994771161099481,
0.919048715272298,0.994771161099481,0.919048715272298,0.994771161099481,
0.919048715272298,0.994771161099481,0.919048715272298,0.994771161099481,
0.919048715272298,0.994771161099481,0.919048715272298,0.994771161099481,
0.919048715272298,0.994771161099481,0.919048715272298,0.994771161099481,
0.919048715272298,0.994771161099481,0.919048715272298,0.994771161099481,
0.919048715272298,0.994771161099481,0.919048715272298,0.994771161099481,
0.919048715272298,0.994771161099481,0.919048715272298,0.994771161099481,
0.919048715272298,0.994771161099481,0.919048715272298,0.994771161099481,
0.919048715272298,0.994771161099481,0.919048715272298,0.994771161099481,
0.919048715272298,0.994771161099481,0.919048715272298,0.994771161099481,
0.919048715272298,0.994771161099481,0.919048715272298,0.994771161099481,
0.919048715272298,0.994771161099481,0.919048715272298,0.994771161099481,
0.919048715272298,0.994771161099481,0.919048715272298,0.994771161099481,
0.919048715272298,0.994771161099481,0.919048715272298,0.994771161099481,
0.919048715272298,0.994771161099481,0.919048715272298,0.994771161099481,
0.919048715272298,0.994771161099481,0.919048715272298,0.994771161099481,
0.919048715272298,0.994771161099481,0.919048715272298,0.994771161099481,
0.919048715272298,0.994771161099481,0.919048715272298,0.994771161099481,
0.919048715272298,0.994771161099481,0.919048715272298,0.994771161099481,
0.919048715272298,0.994771161099481,0.919048715272298,0.994771161099481,
0.919048715272298,0.994771161099481,0.919048715272298,0.994771161099481,
0.919048715272298,0.994771161099481,0.919048715272298,0.994771161099481,
0.919048715272298,0.994771161099481,0.919048715272298,0.994771161099481,
0.919048715272298,0.994771161099481,0.919048715272298,0.994771161099481,
0.919048715272298,0.994771161099481,0.919048715272298,0.994771161099481,
0.919048715272298,0.994771161099481,0.919048715272298,0.994771161099481,
0.919048715272298,0.994771161099481,0.919048715272298,0.994771161099481,
0.919048715272298,0.994771161099481,0.919048715272298,0.994771161099481,
0.919048715272298,0.994771161099481,0.919048715272298,0.994771161099481,
0.919048715272298,0.994771161099481,0.919048715272298,0.994771161099481,
0.919048715272298,0.994771161099481,0.919048715272298,0.994771161099481,
0.919048715272298,0.994771161099481,0.919048715272298,0.994771161099481,
0.919048715272298,0.994771161099481,0.919048715272298,0.994771161099481,
0.919048715272298,0.994771161099481,0.919048715272298,0.994771161099481,
0.919048715272298,0.994771161099481,0.919048715272298,0.994771161099481,
0.919048715272298,0.994771161099481,0.919048715272298,0.994771161099481,
0.919048715272298,0.994771161099481,0.919048715272298,0.994771161099481,
0.919048715272298,0.994771161099481,0.919048715272298,0.994771161099481,
0.919048715272298,0.994771161099481,0.919048715272298,0.994771161099481,
0.919048715272298,0.994771161099481,0.919048715272298,0.994771161099481,
0.919048715272298,0.994771161099481,0.919048715272298,0.994771161099481,
0.919048715272298,0.994771161099481,0.919048715272298,0.994771161099481,
0.919048715272298,0.994771161099481,0.919048715272298,0.994771161099481,
0.919048715272298,0.994771161099481,0.919048715272298,0.994771161099481,
0.919048715272298,0.994771161099481,0.919048715272298,0.994771161099481,
0.919048715272298,0.994771161099481,0.919048715272298,0.994771161099481,
0.919048715272298,0.994771161099481,0.919048715272298,0.994771161099481,
0.919048715272298,0.994771161099481,0.919048715272298,0.994771161099481,
0.919048715272298,0.994771161099481,0.919048715272298,0.994771161099481,
0.919048715272298,0.994771161099481,0.919048715272298,0.994771161099481,
0.919048715272298,0.994771161099481,0.919048715272298,0.994771161099481,
0.919048715272298,0.994771161099481,0.919048715272298,0.994771161099481,
0.919048715272298,0.994771161099481,0.919048715272298,0.994771161099481,
0.919048715272298,0.994771161099481,0.919048715272298,0.994771161099481,
0.919048715272298,0.994771161099481,0.944435365484515,0.961020079172012),
(1.,0.923879532511287,1.,0.923879532511287,1.,0.923879532511287,1.,0.923879532511287,
1.,0.923879532511287,1.,0.923879532511287,1.,0.923879532511287,1.,0.923879532511287,
1.,0.923879532511287,1.,0.923879532511287,1.,0.923879532511287,1.,0.923879532511287,
1.,0.923879532511287,1.,0.923879532511287,1.,0.923879532511287,1.,0.923879532511287,
1.,0.923879532511287,1.,0.923879532511287,1.,0.923879532511287,1.,0.923879532511287,
1.,0.923879532511287,1.,0.923879532511287,1.,0.923879532511287,1.,0.923879532511287,
1.,0.923879532511287,1.,0.923879532511287,1.,0.923879532511287,1.,0.923879532511287,
1.,0.923879532511287,1.,0.923879532511287,1.,0.923879532511287,1.,0.923879532511287,
1.,0.923879532511287,1.,0.923879532511287,1.,0.923879532511287,1.,0.923879532511287,
1.,0.923879532511287,1.,0.923879532511287,1.,0.923879532511287,1.,0.923879532511287,
1.,0.923879532511287,1.,0.923879532511287,1.,0.923879532511287,1.,0.923879532511287,
1.,0.923879532511287,1.,0.923879532511287,1.,0.923879532511287,1.,0.923879532511287,
1.,0.923879532511287,1.,0.923879532511287,1.,0.923879532511287,1.,0.923879532511287,
1.,0.923879532511287,1.,0.923879532511287,1.,0.923879532511287,1.,0.923879532511287,
1.,0.923879532511287,1.,0.923879532511287,1.,0.923879532511287,1.,0.923879532511287,
1.,0.923879532511287,1.,0.923879532511287,1.,0.923879532511287,1.,0.923879532511287,
1.,0.923879532511287,1.,0.923879532511287,1.,0.923879532511287,1.,0.923879532511287,
1.,0.923879532511287,1.,0.923879532511287,1.,0.923879532511287,1.,0.923879532511287,
1.,0.923879532511287,1.,0.923879532511287,1.,0.923879532511287,1.,0.923879532511287,
1.,0.923879532511287,1.,0.923879532511287,1.,0.923879532511287,1.,0.923879532511287,
1.,0.923879532511287,1.,0.923879532511287,1.,0.923879532511287,1.,0.923879532511287,
1.,0.923879532511287,1.,0.923879532511287,1.,0.923879532511287,1.,0.923879532511287,
1.,0.923879532511287,1.,0.923879532511287,1.,0.923879532511287,1.,0.923879532511287,
1.,0.923879532511287,1.,0.923879532511287,1.,0.923879532511287,1.,0.923879532511287,
1.,0.923879532511287,1.,0.923879532511287,1.,0.923879532511287,1.,0.923879532511287,
1.,0.923879532511287,1.,0.923879532511287,1.,0.923879532511287,1.,0.923879532511287,
1.,0.923879532511287,1.,0.923879532511287,1.,0.923879532511287,1.,0.923879532511287,
1.,0.923879532511287,1.,0.923879532511287,1.,0.923879532511287,1.,0.923879532511287,
1.,0.923879532511287,1.,0.923879532511287,1.,0.923879532511287,1.,0.923879532511287,
1.,0.923879532511287,1.,0.923879532511287,1.,0.923879532511287,1.,0.923879532511287,
1.,0.923879532511287,1.,0.923879532511287,1.,0.923879532511287,1.,0.923879532511287,
1.,0.923879532511287,1.,0.923879532511287,1.,0.923879532511287,1.,0.923879532511287,
1.,0.923879532511287,1.,0.923879532511287,1.,0.923879532511287,1.,0.923879532511287,
1.,0.923879532511287,1.,0.923879532511287,1.,0.923879532511287,1.,0.923879532511287,
1.,0.923879532511287,1.,0.923879532511287,1.,0.923879532511287,1.,0.923879532511287,
1.,0.923879532511287,1.,0.923879532511287,1.,0.923879532511287,1.,0.923879532511287,
1.,0.923879532511287,1.,0.923879532511287,1.,0.923879532511287,1.,0.923879532511287,
1.,0.923879532511287,1.,0.923879532511287,1.,0.923879532511287,1.,0.923879532511287,
1.,0.923879532511287,1.,0.923879532511287,1.,0.923879532511287,1.,0.923879532511287,
1.,0.923879532511287,1.,0.923879532511287,1.,0.923879532511287,1.,0.923879532511287,
1.,0.923879532511287,1.,0.923879532511287,1.,0.923879532511287,1.,0.923879532511287,
1.,0.923879532511287,1.,0.923879532511287,1.,0.923879532511287,1.,0.923879532511287,
1.,0.923879532511287,1.,0.923879532511287,1.,0.923879532511287,1.,0.923879532511287,
1.,0.923879532511287,1.,0.923879532511287,1.,0.923879532511287,1.,0.923879532511287,
1.,0.923879532511287,1.,0.923879532511287,1.,0.923879532511287,1.,0.923879532511287,
1.,0.923879532511287,1.,0.923879532511287,1.,0.923879532511287,1.,0.923879532511287,
1.,0.923879532511287,1.,0.923879532511287,1.,0.923879532511287,1.,0.923879532511287,
1.,0.923879532511287,1.,0.923879532511287,1.,0.923879532511287,1.,0.923879532511287,
1.,0.923879532511287,1.,0.923879532511287,1.,0.923879532511287,1.,0.923879532511287,
1.,0.923879532511287,1.,0.923879532511287,1.,0.923879532511287,1.,0.923879532511287,
1.,0.923879532511287,1.,0.923879532511287,1.,0.923879532511287,1.,0.923879532511287,
1.,0.923879532511287,1.,0.923879532511287,1.,0.923879532511287,1.,0.923879532511287,
1.,0.923879532511287,1.,0.923879532511287,1.,0.923879532511287,1.,0.923879532511287,
1.,0.923879532511287,1.,0.923879532511287,1.,0.923879532511287,1.,0.923879532511287,
1.,0.923879532511287,1.,0.923879532511287,1.,0.923879532511287,1.,0.923879532511287,
1.,0.923879532511287,1.,0.923879532511287,1.,0.923879532511287,1.,0.923879532511287,
1.,0.923879532511287,1.,0.923879532511287,1.,0.923879532511287,1.,0.923879532511287,
1.,0.923879532511287,1.,0.923879532511287,1.,0.923879532511287,1.,0.923879532511287,
1.,0.923879532511287,1.,0.923879532511287,1.,0.923879532511287,1.,0.923879532511287,
1.,0.923879532511287,1.,0.923879532511287,1.,0.923879532511287,1.,0.923879532511287,
1.,0.923879532511287,1.,0.923879532511287,1.,0.923879532511287,1.,0.923879532511287,
1.,0.923879532511287,1.,0.923879532511287,1.,0.923879532511287,1.,0.923879532511287,
1.,0.923879532511287,1.,0.923879532511287,1.,0.923879532511287,1.,0.923879532511287,
1.,0.923879532511287,1.,0.923879532511287,1.,0.923879532511287,1.,0.923879532511287,
1.,0.923879532511287,1.,0.923879532511287,1.,0.923879532511287,1.,0.923879532511287,
1.,0.923879532511287,1.,0.923879532511287,1.,0.923879532511287,1.,0.923879532511287,
1.,0.923879532511287,1.,0.923879532511287,1.,0.923879532511287,1.,0.923879532511287,
1.,0.923879532511287,1.,0.923879532511287,1.,0.923879532511287,1.,0.923879532511287,
1.,0.923879532511287,1.,0.923879532511287,1.,0.923879532511287,1.,0.923879532511287,
1.,0.923879532511287,1.,0.923879532511287,1.,0.923879532511287,1.,0.923879532511287,
1.,0.923879532511287,1.,0.923879532511287,1.,0.923879532511287,1.,0.923879532511287,
1.,0.923879532511287,1.,0.923879532511287,1.,0.923879532511287,1.,0.923879532511287,
1.,0.923879532511287,1.,0.923879532511287,1.,0.923879532511287,1.,0.923879532511287,
1.,0.923879532511287,1.,0.923879532511287,1.,0.923879532511287,1.,0.923879532511287,
1.,0.923879532511287,1.,0.923879532511287,1.,0.923879532511287,1.,0.923879532511287,
1.,0.923879532511287,1.,0.923879532511287,1.,0.923879532511287,1.,0.923879532511287,
1.,0.923879532511287,1.,0.923879532511287,1.,0.923879532511287,1.,0.923879532511287,
1.,0.923879532511287,1.,0.923879532511287,1.,0.923879532511287,1.,0.923879532511287,
1.,0.923879532511287,1.,0.923879532511287,1.,0.923879532511287,1.,0.923879532511287,
1.,0.923879532511287,1.,0.923879532511287,1.,0.923879532511287,1.,0.923879532511287,
1.,0.923879532511287,1.,0.923879532511287,1.,0.923879532511287,1.,0.923879532511287,
1.,0.923879532511287,1.,0.923879532511287,1.,0.923879532511287,1.,0.923879532511287,
1.,0.923879532511287,1.,0.923879532511287,1.,0.923879532511287,1.,0.923879532511287,
1.,0.923879532511287,1.,0.923879532511287,1.,0.923879532511287,1.,0.923879532511287,
1.,0.923879532511287,1.,0.923879532511287,1.,0.923879532511287,1.,0.923879532511287,
1.,0.923879532511287,1.,0.923879532511287,1.,0.923879532511287,1.,0.923879532511287,
1.,0.923879532511287,1.,0.923879532511287,1.,0.949399623166265,0.96607151147188)))
REPRESENTATION_ITEM('')
SURFACE()
);
#628=TOROIDAL_SURFACE('',#9404,6.,1.);
#629=TOROIDAL_SURFACE('',#9434,6.,1.);
#678=SHAPE_REPRESENTATION_RELATIONSHIP('SRR','None',#47765,#690);
#690=ADVANCED_BREP_SHAPE_REPRESENTATION('',(#714),#47709);
#702=STYLED_ITEM('',(#47830),#714);
#714=MANIFOLD_SOLID_BREP('Body1',#8929);
#730=FACE_BOUND('',#2857,.T.);
#808=PLANE('',#9490);
#809=PLANE('',#9491);
#810=PLANE('',#9493);
#811=PLANE('',#9510);
#1051=LINE('',#32346,#1538);
#1052=LINE('',#32362,#1539);
#1053=LINE('',#32436,#1540);
#1054=LINE('',#32512,#1541);
#1055=LINE('',#32588,#1542);
#1056=LINE('',#32664,#1543);
#1057=LINE('',#32740,#1544);
#1058=LINE('',#32816,#1545);
#1059=LINE('',#32892,#1546);
#1060=LINE('',#32968,#1547);
#1061=LINE('',#33044,#1548);
#1062=LINE('',#33120,#1549);
#1063=LINE('',#33196,#1550);
#1064=LINE('',#33272,#1551);
#1065=LINE('',#33348,#1552);
#1066=LINE('',#33424,#1553);
#1067=LINE('',#33500,#1554);
#1068=LINE('',#33576,#1555);
#1069=LINE('',#33652,#1556);
#1070=LINE('',#33728,#1557);
#1071=LINE('',#33804,#1558);
#1072=LINE('',#33880,#1559);
#1073=LINE('',#33956,#1560);
#1074=LINE('',#34032,#1561);
#1075=LINE('',#34108,#1562);
#1076=LINE('',#34184,#1563);
#1077=LINE('',#34260,#1564);
#1078=LINE('',#34336,#1565);
#1079=LINE('',#34412,#1566);
#1080=LINE('',#34488,#1567);
#1081=LINE('',#34564,#1568);
#1082=LINE('',#34640,#1569);
#1083=LINE('',#34716,#1570);
#1084=LINE('',#34792,#1571);
#1085=LINE('',#34868,#1572);
#1086=LINE('',#34944,#1573);
#1087=LINE('',#35020,#1574);
#1088=LINE('',#35096,#1575);
#1089=LINE('',#35172,#1576);
#1090=LINE('',#35248,#1577);
#1091=LINE('',#35324,#1578);
#1092=LINE('',#35399,#1579);
#1093=LINE('',#35438,#1580);
#1094=LINE('',#35472,#1581);
#1095=LINE('',#35509,#1582);
#1096=LINE('',#35543,#1583);
#1097=LINE('',#35580,#1584);
#1098=LINE('',#35614,#1585);
#1099=LINE('',#35651,#1586);
#1100=LINE('',#35685,#1587);
#1101=LINE('',#35722,#1588);
#1102=LINE('',#35756,#1589);
#1103=LINE('',#35793,#1590);
#1104=LINE('',#35827,#1591);
#1105=LINE('',#35864,#1592);
#1106=LINE('',#35898,#1593);
#1107=LINE('',#35935,#1594);
#1108=LINE('',#35969,#1595);
#1109=LINE('',#36006,#1596);
#1110=LINE('',#36040,#1597);
#1111=LINE('',#36077,#1598);
#1112=LINE('',#36111,#1599);
#1113=LINE('',#37277,#1600);
#1114=LINE('',#37287,#1601);
#1115=LINE('',#37289,#1602);
#1116=LINE('',#37290,#1603);
#1117=LINE('',#37292,#1604);
#1118=LINE('',#37293,#1605);
#1119=LINE('',#37295,#1606);
#1120=LINE('',#37296,#1607);
#1121=LINE('',#37298,#1608);
#1122=LINE('',#37299,#1609);
#1123=LINE('',#37301,#1610);
#1124=LINE('',#37302,#1611);
#1125=LINE('',#37304,#1612);
#1126=LINE('',#37305,#1613);
#1127=LINE('',#37307,#1614);
#1128=LINE('',#37308,#1615);
#1129=LINE('',#37310,#1616);
#1130=LINE('',#37311,#1617);
#1131=LINE('',#37313,#1618);
#1132=LINE('',#37314,#1619);
#1133=LINE('',#37316,#1620);
#1134=LINE('',#37317,#1621);
#1135=LINE('',#37319,#1622);
#1136=LINE('',#37320,#1623);
#1137=LINE('',#37322,#1624);
#1138=LINE('',#37323,#1625);
#1139=LINE('',#37325,#1626);
#1140=LINE('',#37326,#1627);
#1141=LINE('',#37328,#1628);
#1142=LINE('',#37329,#1629);
#1143=LINE('',#37369,#1630);
#1144=LINE('',#37370,#1631);
#1538=VECTOR('',#10678,2.99999999999999);
#1539=VECTOR('',#10683,2.99999999999999);
#1540=VECTOR('',#10688,2.99999999999999);
#1541=VECTOR('',#10691,2.99999999999999);
#1542=VECTOR('',#10694,2.99999999999999);
#1543=VECTOR('',#10697,2.99999999999999);
#1544=VECTOR('',#10700,2.99999999999999);
#1545=VECTOR('',#10703,2.99999999999999);
#1546=VECTOR('',#10706,2.99999999999999);
#1547=VECTOR('',#10709,2.99999999999999);
#1548=VECTOR('',#10712,2.99999999999999);
#1549=VECTOR('',#10715,2.99999999999999);
#1550=VECTOR('',#10718,2.99999999999999);
#1551=VECTOR('',#10721,2.99999999999999);
#1552=VECTOR('',#10724,2.99999999999999);
#1553=VECTOR('',#10727,2.99999999999999);
#1554=VECTOR('',#10730,2.99999999999999);
#1555=VECTOR('',#10733,2.99999999999999);
#1556=VECTOR('',#10736,2.99999999999999);
#1557=VECTOR('',#10739,2.99999999999999);
#1558=VECTOR('',#10742,2.99999999999999);
#1559=VECTOR('',#10745,2.99999999999999);
#1560=VECTOR('',#10748,2.99999999999999);
#1561=VECTOR('',#10751,2.99999999999999);
#1562=VECTOR('',#10754,2.99999999999999);
#1563=VECTOR('',#10757,2.99999999999999);
#1564=VECTOR('',#10760,2.99999999999999);
#1565=VECTOR('',#10763,2.99999999999999);
#1566=VECTOR('',#10766,2.99999999999999);
#1567=VECTOR('',#10769,2.99999999999999);
#1568=VECTOR('',#10772,2.99999999999999);
#1569=VECTOR('',#10775,2.99999999999999);
#1570=VECTOR('',#10778,2.99999999999999);
#1571=VECTOR('',#10781,2.99999999999999);
#1572=VECTOR('',#10784,2.99999999999999);
#1573=VECTOR('',#10787,2.99999999999999);
#1574=VECTOR('',#10790,2.99999999999999);
#1575=VECTOR('',#10793,2.99999999999999);
#1576=VECTOR('',#10796,2.99999999999999);
#1577=VECTOR('',#10799,2.99999999999999);
#1578=VECTOR('',#10802,2.99999999999999);
#1579=VECTOR('',#10809,2.99999999999999);
#1580=VECTOR('',#10816,1000.);
#1581=VECTOR('',#10817,1000.);
#1582=VECTOR('',#10820,1000.);
#1583=VECTOR('',#10821,1000.);
#1584=VECTOR('',#10824,1000.);
#1585=VECTOR('',#10825,1000.);
#1586=VECTOR('',#10828,1000.);
#1587=VECTOR('',#10829,1000.);
#1588=VECTOR('',#10832,1000.);
#1589=VECTOR('',#10833,1000.);
#1590=VECTOR('',#10836,1000.);
#1591=VECTOR('',#10837,1000.);
#1592=VECTOR('',#10840,1000.);
#1593=VECTOR('',#10841,1000.);
#1594=VECTOR('',#10844,1000.);
#1595=VECTOR('',#10845,1000.);
#1596=VECTOR('',#10848,1000.);
#1597=VECTOR('',#10849,1000.);
#1598=VECTOR('',#10852,1000.);
#1599=VECTOR('',#10853,1000.);
#1600=VECTOR('',#10980,1000.);
#1601=VECTOR('',#10999,1000.);
#1602=VECTOR('',#11002,1000.);
#1603=VECTOR('',#11003,1000.);
#1604=VECTOR('',#11006,1000.);
#1605=VECTOR('',#11007,1000.);
#1606=VECTOR('',#11010,1000.);
#1607=VECTOR('',#11011,1000.);
#1608=VECTOR('',#11014,1000.);
#1609=VECTOR('',#11015,1000.);
#1610=VECTOR('',#11018,1000.);
#1611=VECTOR('',#11019,1000.);
#1612=VECTOR('',#11022,1000.);
#1613=VECTOR('',#11023,1000.);
#1614=VECTOR('',#11026,1000.);
#1615=VECTOR('',#11027,1000.);
#1616=VECTOR('',#11030,1000.);
#1617=VECTOR('',#11031,1000.);
#1618=VECTOR('',#11034,1000.);
#1619=VECTOR('',#11035,1000.);
#1620=VECTOR('',#11038,1000.);
#1621=VECTOR('',#11039,1000.);
#1622=VECTOR('',#11042,1000.);
#1623=VECTOR('',#11043,1000.);
#1624=VECTOR('',#11046,1000.);
#1625=VECTOR('',#11047,1000.);
#1626=VECTOR('',#11050,1000.);
#1627=VECTOR('',#11051,1000.);
#1628=VECTOR('',#11054,1000.);
#1629=VECTOR('',#11055,1000.);
#1630=VECTOR('',#11062,1000.);
#1631=VECTOR('',#11063,1000.);
#1901=CYLINDRICAL_SURFACE('',#9346,2.99999999999999);
#1902=CYLINDRICAL_SURFACE('',#9348,2.99999999999999);
#1903=CYLINDRICAL_SURFACE('',#9350,2.99999999999999);
#1904=CYLINDRICAL_SURFACE('',#9351,2.99999999999999);
#1905=CYLINDRICAL_SURFACE('',#9352,2.99999999999999);
#1906=CYLINDRICAL_SURFACE('',#9353,2.99999999999999);
#1907=CYLINDRICAL_SURFACE('',#9354,2.99999999999999);
#1908=CYLINDRICAL_SURFACE('',#9355,2.99999999999999);
#1909=CYLINDRICAL_SURFACE('',#9356,2.99999999999999);
#1910=CYLINDRICAL_SURFACE('',#9357,2.99999999999999);
#1911=CYLINDRICAL_SURFACE('',#9358,2.99999999999999);
#1912=CYLINDRICAL_SURFACE('',#9359,2.99999999999999);
#1913=CYLINDRICAL_SURFACE('',#9360,2.99999999999999);
#1914=CYLINDRICAL_SURFACE('',#9361,2.99999999999999);
#1915=CYLINDRICAL_SURFACE('',#9362,2.99999999999999);
#1916=CYLINDRICAL_SURFACE('',#9363,2.99999999999999);
#1917=CYLINDRICAL_SURFACE('',#9364,2.99999999999999);
#1918=CYLINDRICAL_SURFACE('',#9365,2.99999999999999);
#1919=CYLINDRICAL_SURFACE('',#9366,2.99999999999999);
#1920=CYLINDRICAL_SURFACE('',#9367,2.99999999999999);
#1921=CYLINDRICAL_SURFACE('',#9368,2.99999999999999);
#1922=CYLINDRICAL_SURFACE('',#9369,2.99999999999999);
#1923=CYLINDRICAL_SURFACE('',#9370,2.99999999999999);
#1924=CYLINDRICAL_SURFACE('',#9371,2.99999999999999);
#1925=CYLINDRICAL_SURFACE('',#9372,2.99999999999999);
#1926=CYLINDRICAL_SURFACE('',#9373,2.99999999999999);
#1927=CYLINDRICAL_SURFACE('',#9374,2.99999999999999);
#1928=CYLINDRICAL_SURFACE('',#9375,2.99999999999999);
#1929=CYLINDRICAL_SURFACE('',#9376,2.99999999999999);
#1930=CYLINDRICAL_SURFACE('',#9377,2.99999999999999);
#1931=CYLINDRICAL_SURFACE('',#9378,2.99999999999999);
#1932=CYLINDRICAL_SURFACE('',#9379,2.99999999999999);
#1933=CYLINDRICAL_SURFACE('',#9380,2.99999999999999);
#1934=CYLINDRICAL_SURFACE('',#9381,2.99999999999999);
#1935=CYLINDRICAL_SURFACE('',#9382,2.99999999999999);
#1936=CYLINDRICAL_SURFACE('',#9383,2.99999999999999);
#1937=CYLINDRICAL_SURFACE('',#9384,2.99999999999999);
#1938=CYLINDRICAL_SURFACE('',#9385,2.99999999999999);
#1939=CYLINDRICAL_SURFACE('',#9386,2.99999999999999);
#1940=CYLINDRICAL_SURFACE('',#9387,2.99999999999999);
#1941=CYLINDRICAL_SURFACE('',#9388,2.99999999999999);
#1942=CYLINDRICAL_SURFACE('',#9394,0.500000000000008);
#1943=CYLINDRICAL_SURFACE('',#9395,0.500000000000008);
#1944=CYLINDRICAL_SURFACE('',#9396,0.500000000000008);
#1945=CYLINDRICAL_SURFACE('',#9397,0.500000000000008);
#1946=CYLINDRICAL_SURFACE('',#9398,0.500000000000008);
#1947=CYLINDRICAL_SURFACE('',#9399,0.500000000000008);
#1948=CYLINDRICAL_SURFACE('',#9400,0.500000000000008);
#1949=CYLINDRICAL_SURFACE('',#9401,0.500000000000008);
#1950=CYLINDRICAL_SURFACE('',#9402,0.500000000000008);
#1951=CYLINDRICAL_SURFACE('',#9403,0.500000000000008);
#1952=CYLINDRICAL_SURFACE('',#9464,2.99999999999999);
#1953=CYLINDRICAL_SURFACE('',#9465,6.99999999999999);
#1954=CYLINDRICAL_SURFACE('',#9466,6.99999999999999);
#1955=CYLINDRICAL_SURFACE('',#9467,6.99999999999999);
#1956=CYLINDRICAL_SURFACE('',#9468,6.99999999999999);
#1957=CYLINDRICAL_SURFACE('',#9469,6.99999999999999);
#1958=CYLINDRICAL_SURFACE('',#9470,6.99999999999999);
#1959=CYLINDRICAL_SURFACE('',#9471,6.99999999999999);
#1960=CYLINDRICAL_SURFACE('',#9472,6.99999999999999);
#1961=CYLINDRICAL_SURFACE('',#9473,6.99999999999999);
#1962=CYLINDRICAL_SURFACE('',#9474,6.99999999999999);
#1963=CYLINDRICAL_SURFACE('',#9475,6.99999999999999);
#1964=CYLINDRICAL_SURFACE('',#9476,6.99999999999999);
#1965=CYLINDRICAL_SURFACE('',#9477,6.99999999999999);
#1966=CYLINDRICAL_SURFACE('',#9478,6.99999999999999);
#1967=CYLINDRICAL_SURFACE('',#9479,6.99999999999999);
#1968=CYLINDRICAL_SURFACE('',#9480,6.99999999999999);
#1969=CYLINDRICAL_SURFACE('',#9481,6.99999999999999);
#1970=CYLINDRICAL_SURFACE('',#9482,6.99999999999999);
#1971=CYLINDRICAL_SURFACE('',#9483,6.99999999999999);
#1972=CYLINDRICAL_SURFACE('',#9484,6.99999999999999);
#1973=CYLINDRICAL_SURFACE('',#9485,6.99999999999999);
#1974=CYLINDRICAL_SURFACE('',#9486,6.99999999999999);
#1975=CYLINDRICAL_SURFACE('',#9487,6.99999999999999);
#1976=CYLINDRICAL_SURFACE('',#9488,6.99999999999999);
#1977=CYLINDRICAL_SURFACE('',#9489,6.99999999999999);
#1978=CYLINDRICAL_SURFACE('',#9492,6.99999999999999);
#1979=CYLINDRICAL_SURFACE('',#9494,0.500000000000008);
#1980=CYLINDRICAL_SURFACE('',#9495,0.500000000000008);
#1981=CYLINDRICAL_SURFACE('',#9496,0.500000000000008);
#1982=CYLINDRICAL_SURFACE('',#9497,0.500000000000008);
#1983=CYLINDRICAL_SURFACE('',#9498,0.500000000000008);
#1984=CYLINDRICAL_SURFACE('',#9499,0.500000000000009);
#1985=CYLINDRICAL_SURFACE('',#9500,0.500000000000008);
#1986=CYLINDRICAL_SURFACE('',#9501,0.500000000000008);
#1987=CYLINDRICAL_SURFACE('',#9502,0.500000000000008);
#1988=CYLINDRICAL_SURFACE('',#9503,0.500000000000009);
#1989=CYLINDRICAL_SURFACE('',#9504,0.500000000000007);
#1990=CYLINDRICAL_SURFACE('',#9505,0.500000000000007);
#1991=CYLINDRICAL_SURFACE('',#9506,0.500000000000008);
#1992=CYLINDRICAL_SURFACE('',#9507,0.500000000000008);
#1993=CYLINDRICAL_SURFACE('',#9508,0.500000000000008);
#1994=CYLINDRICAL_SURFACE('',#9509,0.500000000000008);
#2256=FACE_OUTER_BOUND('',#2776,.T.);
#2257=FACE_OUTER_BOUND('',#2777,.T.);
#2258=FACE_OUTER_BOUND('',#2778,.T.);
#2259=FACE_OUTER_BOUND('',#2779,.T.);
#2260=FACE_OUTER_BOUND('',#2780,.T.);
#2261=FACE_OUTER_BOUND('',#2781,.T.);
#2262=FACE_OUTER_BOUND('',#2782,.T.);
#2263=FACE_OUTER_BOUND('',#2783,.T.);
#2264=FACE_OUTER_BOUND('',#2784,.T.);
#2265=FACE_OUTER_BOUND('',#2785,.T.);
#2266=FACE_OUTER_BOUND('',#2786,.T.);
#2267=FACE_OUTER_BOUND('',#2787,.T.);
#2268=FACE_OUTER_BOUND('',#2788,.T.);
#2269=FACE_OUTER_BOUND('',#2789,.T.);
#2270=FACE_OUTER_BOUND('',#2790,.T.);
#2271=FACE_OUTER_BOUND('',#2791,.T.);
#2272=FACE_OUTER_BOUND('',#2792,.T.);
#2273=FACE_OUTER_BOUND('',#2793,.T.);
#2274=FACE_OUTER_BOUND('',#2794,.T.);
#2275=FACE_OUTER_BOUND('',#2795,.T.);
#2276=FACE_OUTER_BOUND('',#2796,.T.);
#2277=FACE_OUTER_BOUND('',#2797,.T.);
#2278=FACE_OUTER_BOUND('',#2798,.T.);
#2279=FACE_OUTER_BOUND('',#2799,.T.);
#2280=FACE_OUTER_BOUND('',#2800,.T.);
#2281=FACE_OUTER_BOUND('',#2801,.T.);
#2282=FACE_OUTER_BOUND('',#2802,.T.);
#2283=FACE_OUTER_BOUND('',#2803,.T.);
#2284=FACE_OUTER_BOUND('',#2804,.T.);
#2285=FACE_OUTER_BOUND('',#2805,.T.);
#2286=FACE_OUTER_BOUND('',#2806,.T.);
#2287=FACE_OUTER_BOUND('',#2807,.T.);
#2288=FACE_OUTER_BOUND('',#2808,.T.);
#2289=FACE_OUTER_BOUND('',#2809,.T.);
#2290=FACE_OUTER_BOUND('',#2810,.T.);
#2291=FACE_OUTER_BOUND('',#2811,.T.);
#2292=FACE_OUTER_BOUND('',#2812,.T.);
#2293=FACE_OUTER_BOUND('',#2813,.T.);
#2294=FACE_OUTER_BOUND('',#2814,.T.);
#2295=FACE_OUTER_BOUND('',#2815,.T.);
#2296=FACE_OUTER_BOUND('',#2816,.T.);
#2297=FACE_OUTER_BOUND('',#2817,.T.);
#2298=FACE_OUTER_BOUND('',#2818,.T.);
#2299=FACE_OUTER_BOUND('',#2819,.T.);
#2300=FACE_OUTER_BOUND('',#2820,.T.);
#2301=FACE_OUTER_BOUND('',#2821,.T.);
#2302=FACE_OUTER_BOUND('',#2822,.T.);
#2303=FACE_OUTER_BOUND('',#2823,.T.);
#2304=FACE_OUTER_BOUND('',#2824,.T.);
#2305=FACE_OUTER_BOUND('',#2825,.T.);
#2306=FACE_OUTER_BOUND('',#2826,.T.);
#2307=FACE_OUTER_BOUND('',#2827,.T.);
#2308=FACE_OUTER_BOUND('',#2828,.T.);
#2309=FACE_OUTER_BOUND('',#2829,.T.);
#2310=FACE_OUTER_BOUND('',#2830,.T.);
#2311=FACE_OUTER_BOUND('',#2831,.T.);
#2312=FACE_OUTER_BOUND('',#2832,.T.);
#2313=FACE_OUTER_BOUND('',#2833,.T.);
#2314=FACE_OUTER_BOUND('',#2834,.T.);
#2315=FACE_OUTER_BOUND('',#2835,.T.);
#2316=FACE_OUTER_BOUND('',#2836,.T.);
#2317=FACE_OUTER_BOUND('',#2837,.T.);
#2318=FACE_OUTER_BOUND('',#2838,.T.);
#2319=FACE_OUTER_BOUND('',#2839,.T.);
#2320=FACE_OUTER_BOUND('',#2840,.T.);
#2321=FACE_OUTER_BOUND('',#2841,.T.);
#2322=FACE_OUTER_BOUND('',#2842,.T.);
#2323=FACE_OUTER_BOUND('',#2843,.T.);
#2324=FACE_OUTER_BOUND('',#2844,.T.);
#2325=FACE_OUTER_BOUND('',#2845,.T.);
#2326=FACE_OUTER_BOUND('',#2846,.T.);
#2327=FACE_OUTER_BOUND('',#2847,.T.);
#2328=FACE_OUTER_BOUND('',#2848,.T.);
#2329=FACE_OUTER_BOUND('',#2849,.T.);
#2330=FACE_OUTER_BOUND('',#2850,.T.);
#2331=FACE_OUTER_BOUND('',#2851,.T.);
#2332=FACE_OUTER_BOUND('',#2852,.T.);
#2333=FACE_OUTER_BOUND('',#2853,.T.);
#2334=FACE_OUTER_BOUND('',#2854,.T.);
#2335=FACE_OUTER_BOUND('',#2855,.T.);
#2336=FACE_OUTER_BOUND('',#2856,.T.);
#2337=FACE_OUTER_BOUND('',#2858,.T.);
#2338=FACE_OUTER_BOUND('',#2859,.T.);
#2339=FACE_OUTER_BOUND('',#2860,.T.);
#2340=FACE_OUTER_BOUND('',#2861,.T.);
#2341=FACE_OUTER_BOUND('',#2862,.T.);
#2342=FACE_OUTER_BOUND('',#2863,.T.);
#2343=FACE_OUTER_BOUND('',#2864,.T.);
#2344=FACE_OUTER_BOUND('',#2865,.T.);
#2345=FACE_OUTER_BOUND('',#2866,.T.);
#2346=FACE_OUTER_BOUND('',#2867,.T.);
#2347=FACE_OUTER_BOUND('',#2868,.T.);
#2348=FACE_OUTER_BOUND('',#2869,.T.);
#2349=FACE_OUTER_BOUND('',#2870,.T.);
#2350=FACE_OUTER_BOUND('',#2871,.T.);
#2351=FACE_OUTER_BOUND('',#2872,.T.);
#2352=FACE_OUTER_BOUND('',#2873,.T.);
#2353=FACE_OUTER_BOUND('',#2874,.T.);
#2354=FACE_OUTER_BOUND('',#2875,.T.);
#2355=FACE_OUTER_BOUND('',#2876,.T.);
#2356=FACE_OUTER_BOUND('',#2877,.T.);
#2357=FACE_OUTER_BOUND('',#2878,.T.);
#2358=FACE_OUTER_BOUND('',#2879,.T.);
#2359=FACE_OUTER_BOUND('',#2880,.T.);
#2776=EDGE_LOOP('',(#6739,#6740,#6741));
#2777=EDGE_LOOP('',(#6742,#6743,#6744,#6745,#6746));
#2778=EDGE_LOOP('',(#6747,#6748,#6749,#6750));
#2779=EDGE_LOOP('',(#6751,#6752,#6753,#6754));
#2780=EDGE_LOOP('',(#6755,#6756,#6757,#6758));
#2781=EDGE_LOOP('',(#6759,#6760,#6761,#6762));
#2782=EDGE_LOOP('',(#6763,#6764,#6765,#6766));
#2783=EDGE_LOOP('',(#6767,#6768,#6769,#6770));
#2784=EDGE_LOOP('',(#6771,#6772,#6773,#6774));
#2785=EDGE_LOOP('',(#6775,#6776,#6777,#6778));
#2786=EDGE_LOOP('',(#6779,#6780,#6781,#6782));
#2787=EDGE_LOOP('',(#6783,#6784,#6785,#6786));
#2788=EDGE_LOOP('',(#6787,#6788,#6789,#6790));
#2789=EDGE_LOOP('',(#6791,#6792,#6793,#6794));
#2790=EDGE_LOOP('',(#6795,#6796,#6797,#6798));
#2791=EDGE_LOOP('',(#6799,#6800,#6801,#6802));
#2792=EDGE_LOOP('',(#6803,#6804,#6805,#6806));
#2793=EDGE_LOOP('',(#6807,#6808,#6809,#6810));
#2794=EDGE_LOOP('',(#6811,#6812,#6813,#6814));
#2795=EDGE_LOOP('',(#6815,#6816,#6817,#6818));
#2796=EDGE_LOOP('',(#6819,#6820,#6821,#6822));
#2797=EDGE_LOOP('',(#6823,#6824,#6825,#6826));
#2798=EDGE_LOOP('',(#6827,#6828,#6829,#6830));
#2799=EDGE_LOOP('',(#6831,#6832,#6833,#6834));
#2800=EDGE_LOOP('',(#6835,#6836,#6837,#6838));
#2801=EDGE_LOOP('',(#6839,#6840,#6841,#6842));
#2802=EDGE_LOOP('',(#6843,#6844,#6845,#6846));
#2803=EDGE_LOOP('',(#6847,#6848,#6849,#6850));
#2804=EDGE_LOOP('',(#6851,#6852,#6853,#6854));
#2805=EDGE_LOOP('',(#6855,#6856,#6857,#6858));
#2806=EDGE_LOOP('',(#6859,#6860,#6861,#6862));
#2807=EDGE_LOOP('',(#6863,#6864,#6865,#6866));
#2808=EDGE_LOOP('',(#6867,#6868,#6869,#6870));
#2809=EDGE_LOOP('',(#6871,#6872,#6873,#6874));
#2810=EDGE_LOOP('',(#6875,#6876,#6877,#6878));
#2811=EDGE_LOOP('',(#6879,#6880,#6881,#6882));
#2812=EDGE_LOOP('',(#6883,#6884,#6885,#6886));
#2813=EDGE_LOOP('',(#6887,#6888,#6889,#6890));
#2814=EDGE_LOOP('',(#6891,#6892,#6893,#6894));
#2815=EDGE_LOOP('',(#6895,#6896,#6897,#6898));
#2816=EDGE_LOOP('',(#6899,#6900,#6901,#6902,#6903));
#2817=EDGE_LOOP('',(#6904,#6905,#6906,#6907,#6908,#6909));
#2818=EDGE_LOOP('',(#6910,#6911,#6912,#6913));
#2819=EDGE_LOOP('',(#6914,#6915,#6916,#6917));
#2820=EDGE_LOOP('',(#6918,#6919,#6920,#6921));
#2821=EDGE_LOOP('',(#6922,#6923,#6924,#6925));
#2822=EDGE_LOOP('',(#6926,#6927,#6928,#6929));
#2823=EDGE_LOOP('',(#6930,#6931,#6932,#6933));
#2824=EDGE_LOOP('',(#6934,#6935,#6936,#6937));
#2825=EDGE_LOOP('',(#6938,#6939,#6940,#6941));
#2826=EDGE_LOOP('',(#6942,#6943,#6944,#6945));
#2827=EDGE_LOOP('',(#6946,#6947,#6948,#6949));
#2828=EDGE_LOOP('',(#6950,#6951,#6952,#6953,#6954,#6955,#6956,#6957,#6958,
#6959,#6960,#6961,#6962,#6963,#6964,#6965,#6966,#6967,#6968,#6969,#6970,
#6971,#6972,#6973,#6974,#6975,#6976,#6977,#6978,#6979,#6980,#6981,#6982,
#6983,#6984,#6985,#6986,#6987,#6988,#6989,#6990,#6991,#6992,#6993,#6994,
#6995,#6996,#6997,#6998,#6999,#7000,#7001,#7002,#7003,#7004,#7005));
#2829=EDGE_LOOP('',(#7006,#7007,#7008,#7009,#7010,#7011,#7012,#7013,#7014,
#7015,#7016,#7017,#7018,#7019,#7020,#7021,#7022,#7023,#7024,#7025,#7026,
#7027,#7028,#7029,#7030,#7031,#7032,#7033,#7034,#7035,#7036,#7037,#7038,
#7039,#7040,#7041,#7042,#7043,#7044,#7045,#7046,#7047,#7048,#7049,#7050,
#7051,#7052,#7053,#7054,#7055,#7056,#7057,#7058,#7059,#7060,#7061));
#2830=EDGE_LOOP('',(#7062,#7063,#7064));
#2831=EDGE_LOOP('',(#7065,#7066,#7067,#7068,#7069));
#2832=EDGE_LOOP('',(#7070,#7071,#7072,#7073));
#2833=EDGE_LOOP('',(#7074,#7075,#7076,#7077));
#2834=EDGE_LOOP('',(#7078,#7079,#7080,#7081));
#2835=EDGE_LOOP('',(#7082,#7083,#7084,#7085));
#2836=EDGE_LOOP('',(#7086,#7087,#7088,#7089));
#2837=EDGE_LOOP('',(#7090,#7091,#7092,#7093));
#2838=EDGE_LOOP('',(#7094,#7095,#7096,#7097));
#2839=EDGE_LOOP('',(#7098,#7099,#7100,#7101));
#2840=EDGE_LOOP('',(#7102,#7103,#7104,#7105));
#2841=EDGE_LOOP('',(#7106,#7107,#7108,#7109));
#2842=EDGE_LOOP('',(#7110,#7111,#7112,#7113));
#2843=EDGE_LOOP('',(#7114,#7115,#7116,#7117));
#2844=EDGE_LOOP('',(#7118,#7119,#7120,#7121));
#2845=EDGE_LOOP('',(#7122,#7123,#7124,#7125));
#2846=EDGE_LOOP('',(#7126,#7127,#7128,#7129));
#2847=EDGE_LOOP('',(#7130,#7131,#7132,#7133));
#2848=EDGE_LOOP('',(#7134,#7135,#7136,#7137));
#2849=EDGE_LOOP('',(#7138,#7139,#7140,#7141,#7142));
#2850=EDGE_LOOP('',(#7143,#7144,#7145,#7146));
#2851=EDGE_LOOP('',(#7147,#7148,#7149,#7150));
#2852=EDGE_LOOP('',(#7151,#7152,#7153,#7154));
#2853=EDGE_LOOP('',(#7155,#7156,#7157,#7158));
#2854=EDGE_LOOP('',(#7159,#7160,#7161,#7162));
#2855=EDGE_LOOP('',(#7163,#7164,#7165,#7166));
#2856=EDGE_LOOP('',(#7167));
#2857=EDGE_LOOP('',(#7168,#7169,#7170,#7171,#7172));
#2858=EDGE_LOOP('',(#7173));
#2859=EDGE_LOOP('',(#7174,#7175,#7176,#7177));
#2860=EDGE_LOOP('',(#7178,#7179,#7180,#7181));
#2861=EDGE_LOOP('',(#7182,#7183,#7184,#7185,#7186,#7187,#7188,#7189,#7190,
#7191,#7192,#7193,#7194,#7195,#7196,#7197,#7198,#7199,#7200,#7201,#7202,
#7203,#7204,#7205,#7206,#7207,#7208,#7209,#7210,#7211,#7212,#7213,#7214,
#7215,#7216,#7217,#7218,#7219,#7220,#7221,#7222,#7223,#7224,#7225));
#2862=EDGE_LOOP('',(#7226,#7227,#7228,#7229,#7230,#7231,#7232,#7233,#7234,
#7235,#7236,#7237,#7238,#7239,#7240,#7241,#7242,#7243,#7244,#7245,#7246,
#7247,#7248,#7249,#7250,#7251,#7252,#7253,#7254,#7255,#7256,#7257,#7258,
#7259,#7260,#7261,#7262,#7263,#7264,#7265,#7266,#7267,#7268,#7269));
#2863=EDGE_LOOP('',(#7270,#7271,#7272,#7273));
#2864=EDGE_LOOP('',(#7274,#7275,#7276,#7277));
#2865=EDGE_LOOP('',(#7278,#7279,#7280,#7281));
#2866=EDGE_LOOP('',(#7282,#7283,#7284,#7285));
#2867=EDGE_LOOP('',(#7286,#7287,#7288,#7289));
#2868=EDGE_LOOP('',(#7290,#7291,#7292,#7293));
#2869=EDGE_LOOP('',(#7294,#7295,#7296,#7297));
#2870=EDGE_LOOP('',(#7298,#7299,#7300,#7301));
#2871=EDGE_LOOP('',(#7302,#7303,#7304,#7305));
#2872=EDGE_LOOP('',(#7306,#7307,#7308,#7309));
#2873=EDGE_LOOP('',(#7310,#7311,#7312,#7313));
#2874=EDGE_LOOP('',(#7314,#7315,#7316,#7317));
#2875=EDGE_LOOP('',(#7318,#7319,#7320,#7321));
#2876=EDGE_LOOP('',(#7322,#7323,#7324,#7325));
#2877=EDGE_LOOP('',(#7326,#7327,#7328,#7329));
#2878=EDGE_LOOP('',(#7330,#7331,#7332,#7333));
#2879=EDGE_LOOP('',(#7334,#7335,#7336,#7337));
#2880=EDGE_LOOP('',(#7338));
#3250=CIRCLE('',#9347,2.99999999999999);
#3251=CIRCLE('',#9349,2.99999999999999);
#3252=CIRCLE('',#9389,2.99999999999998);
#3253=CIRCLE('',#9391,2.99999999999999);
#3254=CIRCLE('',#9392,2.24999999999998);
#3255=CIRCLE('',#9393,2.99999999999998);
#3256=CIRCLE('',#9405,6.);
#3257=CIRCLE('',#9406,1.);
#3258=CIRCLE('',#9407,6.99999999999999);
#3259=CIRCLE('',#9408,6.99999999999999);
#3260=CIRCLE('',#9409,7.);
#3261=CIRCLE('',#9410,6.99999999999999);
#3262=CIRCLE('',#9411,7.00000000000001);
#3263=CIRCLE('',#9412,6.99999999999999);
#3264=CIRCLE('',#9413,6.99999999999999);
#3265=CIRCLE('',#9414,6.99999999999999);
#3266=CIRCLE('',#9415,7.);
#3267=CIRCLE('',#9416,7.);
#3268=CIRCLE('',#9417,6.99999999999999);
#3269=CIRCLE('',#9418,6.99999999999999);
#3270=CIRCLE('',#9419,7.00000000000002);
#3271=CIRCLE('',#9420,7.);
#3272=CIRCLE('',#9421,7.00000000000001);
#3273=CIRCLE('',#9422,7.);
#3274=CIRCLE('',#9423,6.99999999999999);
#3275=CIRCLE('',#9424,7.00000000000001);
#3276=CIRCLE('',#9425,7.00000000000001);
#3277=CIRCLE('',#9426,6.99999999999999);
#3278=CIRCLE('',#9427,7.00000000000001);
#3279=CIRCLE('',#9428,7.00000000000001);
#3280=CIRCLE('',#9429,7.00000000000001);
#3281=CIRCLE('',#9430,6.99999999999999);
#3282=CIRCLE('',#9431,7.00000000000001);
#3283=CIRCLE('',#9432,6.99999999999999);
#3284=CIRCLE('',#9433,6.99999999999999);
#3285=CIRCLE('',#9435,6.);
#3286=CIRCLE('',#9436,1.);
#3287=CIRCLE('',#9437,7.);
#3288=CIRCLE('',#9438,7.);
#3289=CIRCLE('',#9439,7.);
#3290=CIRCLE('',#9440,7.);
#3291=CIRCLE('',#9441,7.);
#3292=CIRCLE('',#9442,7.);
#3293=CIRCLE('',#9443,7.);
#3294=CIRCLE('',#9444,7.);
#3295=CIRCLE('',#9445,7.00000000000001);
#3296=CIRCLE('',#9446,7.00000000000001);
#3297=CIRCLE('',#9447,7.00000000000001);
#3298=CIRCLE('',#9448,7.);
#3299=CIRCLE('',#9449,6.99999999999999);
#3300=CIRCLE('',#9450,7.);
#3301=CIRCLE('',#9451,7.);
#3302=CIRCLE('',#9452,7.00000000000001);
#3303=CIRCLE('',#9453,7.);
#3304=CIRCLE('',#9454,7.00000000000001);
#3305=CIRCLE('',#9455,7.);
#3306=CIRCLE('',#9456,6.99999999999999);
#3307=CIRCLE('',#9457,6.99999999999999);
#3308=CIRCLE('',#9458,6.99999999999999);
#3309=CIRCLE('',#9459,7.00000000000001);
#3310=CIRCLE('',#9460,7.);
#3311=CIRCLE('',#9461,6.99999999999999);
#3312=CIRCLE('',#9462,7.);
#3313=CIRCLE('',#9463,7.);
#3857=VERTEX_POINT('',#32344);
#3858=VERTEX_POINT('',#32345);
#3859=VERTEX_POINT('',#32347);
#3860=VERTEX_POINT('',#32360);
#3861=VERTEX_POINT('',#32361);
#3862=VERTEX_POINT('',#32399);
#3863=VERTEX_POINT('',#32434);
#3864=VERTEX_POINT('',#32435);
#3865=VERTEX_POINT('',#32510);
#3866=VERTEX_POINT('',#32511);
#3867=VERTEX_POINT('',#32586);
#3868=VERTEX_POINT('',#32587);
#3869=VERTEX_POINT('',#32662);
#3870=VERTEX_POINT('',#32663);
#3871=VERTEX_POINT('',#32738);
#3872=VERTEX_POINT('',#32739);
#3873=VERTEX_POINT('',#32814);
#3874=VERTEX_POINT('',#32815);
#3875=VERTEX_POINT('',#32890);
#3876=VERTEX_POINT('',#32891);
#3877=VERTEX_POINT('',#32966);
#3878=VERTEX_POINT('',#32967);
#3879=VERTEX_POINT('',#33042);
#3880=VERTEX_POINT('',#33043);
#3881=VERTEX_POINT('',#33118);
#3882=VERTEX_POINT('',#33119);
#3883=VERTEX_POINT('',#33194);
#3884=VERTEX_POINT('',#33195);
#3885=VERTEX_POINT('',#33270);
#3886=VERTEX_POINT('',#33271);
#3887=VERTEX_POINT('',#33346);
#3888=VERTEX_POINT('',#33347);
#3889=VERTEX_POINT('',#33422);
#3890=VERTEX_POINT('',#33423);
#3891=VERTEX_POINT('',#33498);
#3892=VERTEX_POINT('',#33499);
#3893=VERTEX_POINT('',#33574);
#3894=VERTEX_POINT('',#33575);
#3895=VERTEX_POINT('',#33650);
#3896=VERTEX_POINT('',#33651);
#3897=VERTEX_POINT('',#33726);
#3898=VERTEX_POINT('',#33727);
#3899=VERTEX_POINT('',#33802);
#3900=VERTEX_POINT('',#33803);
#3901=VERTEX_POINT('',#33878);
#3902=VERTEX_POINT('',#33879);
#3903=VERTEX_POINT('',#33954);
#3904=VERTEX_POINT('',#33955);
#3905=VERTEX_POINT('',#34030);
#3906=VERTEX_POINT('',#34031);
#3907=VERTEX_POINT('',#34106);
#3908=VERTEX_POINT('',#34107);
#3909=VERTEX_POINT('',#34182);
#3910=VERTEX_POINT('',#34183);
#3911=VERTEX_POINT('',#34258);
#3912=VERTEX_POINT('',#34259);
#3913=VERTEX_POINT('',#34334);
#3914=VERTEX_POINT('',#34335);
#3915=VERTEX_POINT('',#34410);
#3916=VERTEX_POINT('',#34411);
#3917=VERTEX_POINT('',#34486);
#3918=VERTEX_POINT('',#34487);
#3919=VERTEX_POINT('',#34562);
#3920=VERTEX_POINT('',#34563);
#3921=VERTEX_POINT('',#34638);
#3922=VERTEX_POINT('',#34639);
#3923=VERTEX_POINT('',#34714);
#3924=VERTEX_POINT('',#34715);
#3925=VERTEX_POINT('',#34790);
#3926=VERTEX_POINT('',#34791);
#3927=VERTEX_POINT('',#34866);
#3928=VERTEX_POINT('',#34867);
#3929=VERTEX_POINT('',#34942);
#3930=VERTEX_POINT('',#34943);
#3931=VERTEX_POINT('',#35018);
#3932=VERTEX_POINT('',#35019);
#3933=VERTEX_POINT('',#35094);
#3934=VERTEX_POINT('',#35095);
#3935=VERTEX_POINT('',#35170);
#3936=VERTEX_POINT('',#35171);
#3937=VERTEX_POINT('',#35246);
#3938=VERTEX_POINT('',#35247);
#3939=VERTEX_POINT('',#35322);
#3940=VERTEX_POINT('',#35323);
#3941=VERTEX_POINT('',#35325);
#3942=VERTEX_POINT('',#35396);
#3943=VERTEX_POINT('',#35398);
#3944=VERTEX_POINT('',#35403);
#3945=VERTEX_POINT('',#35404);
#3946=VERTEX_POINT('',#35437);
#3947=VERTEX_POINT('',#35439);
#3948=VERTEX_POINT('',#35474);
#3949=VERTEX_POINT('',#35475);
#3950=VERTEX_POINT('',#35508);
#3951=VERTEX_POINT('',#35510);
#3952=VERTEX_POINT('',#35545);
#3953=VERTEX_POINT('',#35546);
#3954=VERTEX_POINT('',#35579);
#3955=VERTEX_POINT('',#35581);
#3956=VERTEX_POINT('',#35616);
#3957=VERTEX_POINT('',#35617);
#3958=VERTEX_POINT('',#35650);
#3959=VERTEX_POINT('',#35652);
#3960=VERTEX_POINT('',#35687);
#3961=VERTEX_POINT('',#35688);
#3962=VERTEX_POINT('',#35721);
#3963=VERTEX_POINT('',#35723);
#3964=VERTEX_POINT('',#35758);
#3965=VERTEX_POINT('',#35759);
#3966=VERTEX_POINT('',#35792);
#3967=VERTEX_POINT('',#35794);
#3968=VERTEX_POINT('',#35829);
#3969=VERTEX_POINT('',#35830);
#3970=VERTEX_POINT('',#35863);
#3971=VERTEX_POINT('',#35865);
#3972=VERTEX_POINT('',#35900);
#3973=VERTEX_POINT('',#35901);
#3974=VERTEX_POINT('',#35934);
#3975=VERTEX_POINT('',#35936);
#3976=VERTEX_POINT('',#35971);
#3977=VERTEX_POINT('',#35972);
#3978=VERTEX_POINT('',#36005);
#3979=VERTEX_POINT('',#36007);
#3980=VERTEX_POINT('',#36042);
#3981=VERTEX_POINT('',#36043);
#3982=VERTEX_POINT('',#36076);
#3983=VERTEX_POINT('',#36078);
#3984=VERTEX_POINT('',#36113);
#3985=VERTEX_POINT('',#36115);
#3986=VERTEX_POINT('',#36117);
#3987=VERTEX_POINT('',#36119);
#3988=VERTEX_POINT('',#36152);
#3989=VERTEX_POINT('',#36154);
#3990=VERTEX_POINT('',#36187);
#3991=VERTEX_POINT('',#36189);
#3992=VERTEX_POINT('',#36222);
#3993=VERTEX_POINT('',#36224);
#3994=VERTEX_POINT('',#36257);
#3995=VERTEX_POINT('',#36259);
#3996=VERTEX_POINT('',#36292);
#3997=VERTEX_POINT('',#36294);
#3998=VERTEX_POINT('',#36327);
#3999=VERTEX_POINT('',#36329);
#4000=VERTEX_POINT('',#36362);
#4001=VERTEX_POINT('',#36364);
#4002=VERTEX_POINT('',#36407);
#4003=VERTEX_POINT('',#36409);
#4004=VERTEX_POINT('',#36442);
#4005=VERTEX_POINT('',#36444);
#4006=VERTEX_POINT('',#36477);
#4007=VERTEX_POINT('',#36479);
#4008=VERTEX_POINT('',#36512);
#4009=VERTEX_POINT('',#36514);
#4010=VERTEX_POINT('',#36547);
#4011=VERTEX_POINT('',#36549);
#4012=VERTEX_POINT('',#36582);
#4013=VERTEX_POINT('',#36584);
#4014=VERTEX_POINT('',#36617);
#4015=VERTEX_POINT('',#36619);
#4016=VERTEX_POINT('',#36652);
#4017=VERTEX_POINT('',#36654);
#4018=VERTEX_POINT('',#36689);
#4019=VERTEX_POINT('',#36691);
#4020=VERTEX_POINT('',#36698);
#4021=VERTEX_POINT('',#36700);
#4022=VERTEX_POINT('',#36733);
#4023=VERTEX_POINT('',#36735);
#4024=VERTEX_POINT('',#36768);
#4025=VERTEX_POINT('',#36770);
#4026=VERTEX_POINT('',#36803);
#4027=VERTEX_POINT('',#36805);
#4028=VERTEX_POINT('',#36838);
#4029=VERTEX_POINT('',#36840);
#4030=VERTEX_POINT('',#36873);
#4031=VERTEX_POINT('',#36875);
#4032=VERTEX_POINT('',#36908);
#4033=VERTEX_POINT('',#36910);
#4034=VERTEX_POINT('',#36943);
#4035=VERTEX_POINT('',#36945);
#4036=VERTEX_POINT('',#36978);
#4037=VERTEX_POINT('',#36980);
#4038=VERTEX_POINT('',#37013);
#4039=VERTEX_POINT('',#37015);
#4040=VERTEX_POINT('',#37048);
#4041=VERTEX_POINT('',#37050);
#4042=VERTEX_POINT('',#37083);
#4043=VERTEX_POINT('',#37085);
#4044=VERTEX_POINT('',#37118);
#4045=VERTEX_POINT('',#37120);
#4046=VERTEX_POINT('',#37153);
#4047=VERTEX_POINT('',#37155);
#4048=VERTEX_POINT('',#37188);
#4049=VERTEX_POINT('',#37190);
#4050=VERTEX_POINT('',#37223);
#4051=VERTEX_POINT('',#37225);
#4052=VERTEX_POINT('',#37331);
#4053=VERTEX_POINT('',#37332);
#4054=VERTEX_POINT('',#37372);
#4055=VERTEX_POINT('',#37383);
#4895=EDGE_CURVE('',#3857,#3858,#1051,.T.);
#4896=EDGE_CURVE('',#3857,#3859,#310,.T.);
#4897=EDGE_CURVE('',#3859,#3858,#3250,.T.);
#4898=EDGE_CURVE('',#3860,#3861,#1052,.T.);
#4899=EDGE_CURVE('',#3860,#3857,#311,.T.);
#4900=EDGE_CURVE('',#3858,#3862,#3251,.T.);
#4901=EDGE_CURVE('',#3861,#3862,#312,.F.);
#4902=EDGE_CURVE('',#3863,#3864,#1053,.T.);
#4903=EDGE_CURVE('',#3863,#3860,#313,.T.);
#4904=EDGE_CURVE('',#3864,#3861,#314,.F.);
#4905=EDGE_CURVE('',#3865,#3866,#1054,.T.);
#4906=EDGE_CURVE('',#3865,#3863,#315,.T.);
#4907=EDGE_CURVE('',#3866,#3864,#316,.F.);
#4908=EDGE_CURVE('',#3867,#3868,#1055,.T.);
#4909=EDGE_CURVE('',#3867,#3865,#317,.T.);
#4910=EDGE_CURVE('',#3868,#3866,#318,.F.);
#4911=EDGE_CURVE('',#3869,#3870,#1056,.T.);
#4912=EDGE_CURVE('',#3869,#3867,#319,.T.);
#4913=EDGE_CURVE('',#3870,#3868,#320,.F.);
#4914=EDGE_CURVE('',#3871,#3872,#1057,.T.);
#4915=EDGE_CURVE('',#3871,#3869,#321,.T.);
#4916=EDGE_CURVE('',#3872,#3870,#322,.F.);
#4917=EDGE_CURVE('',#3873,#3874,#1058,.T.);
#4918=EDGE_CURVE('',#3873,#3871,#323,.T.);
#4919=EDGE_CURVE('',#3874,#3872,#324,.F.);
#4920=EDGE_CURVE('',#3875,#3876,#1059,.T.);
#4921=EDGE_CURVE('',#3875,#3873,#325,.T.);
#4922=EDGE_CURVE('',#3876,#3874,#326,.F.);
#4923=EDGE_CURVE('',#3877,#3878,#1060,.T.);
#4924=EDGE_CURVE('',#3877,#3875,#327,.T.);
#4925=EDGE_CURVE('',#3878,#3876,#328,.F.);
#4926=EDGE_CURVE('',#3879,#3880,#1061,.T.);
#4927=EDGE_CURVE('',#3879,#3877,#329,.T.);
#4928=EDGE_CURVE('',#3880,#3878,#330,.F.);
#4929=EDGE_CURVE('',#3881,#3882,#1062,.T.);
#4930=EDGE_CURVE('',#3881,#3879,#331,.T.);
#4931=EDGE_CURVE('',#3882,#3880,#332,.F.);
#4932=EDGE_CURVE('',#3883,#3884,#1063,.T.);
#4933=EDGE_CURVE('',#3883,#3881,#333,.T.);
#4934=EDGE_CURVE('',#3884,#3882,#334,.F.);
#4935=EDGE_CURVE('',#3885,#3886,#1064,.T.);
#4936=EDGE_CURVE('',#3885,#3883,#335,.T.);
#4937=EDGE_CURVE('',#3886,#3884,#336,.F.);
#4938=EDGE_CURVE('',#3887,#3888,#1065,.T.);
#4939=EDGE_CURVE('',#3887,#3885,#337,.T.);
#4940=EDGE_CURVE('',#3888,#3886,#338,.F.);
#4941=EDGE_CURVE('',#3889,#3890,#1066,.T.);
#4942=EDGE_CURVE('',#3889,#3887,#339,.T.);
#4943=EDGE_CURVE('',#3890,#3888,#340,.F.);
#4944=EDGE_CURVE('',#3891,#3892,#1067,.T.);
#4945=EDGE_CURVE('',#3891,#3889,#341,.T.);
#4946=EDGE_CURVE('',#3892,#3890,#342,.F.);
#4947=EDGE_CURVE('',#3893,#3894,#1068,.T.);
#4948=EDGE_CURVE('',#3893,#3891,#343,.T.);
#4949=EDGE_CURVE('',#3894,#3892,#344,.F.);
#4950=EDGE_CURVE('',#3895,#3896,#1069,.T.);
#4951=EDGE_CURVE('',#3895,#3893,#345,.T.);
#4952=EDGE_CURVE('',#3896,#3894,#346,.F.);
#4953=EDGE_CURVE('',#3897,#3898,#1070,.T.);
#4954=EDGE_CURVE('',#3897,#3895,#347,.T.);
#4955=EDGE_CURVE('',#3898,#3896,#348,.F.);
#4956=EDGE_CURVE('',#3899,#3900,#1071,.T.);
#4957=EDGE_CURVE('',#3899,#3897,#349,.T.);
#4958=EDGE_CURVE('',#3900,#3898,#350,.F.);
#4959=EDGE_CURVE('',#3901,#3902,#1072,.T.);
#4960=EDGE_CURVE('',#3901,#3899,#351,.T.);
#4961=EDGE_CURVE('',#3902,#3900,#352,.F.);
#4962=EDGE_CURVE('',#3903,#3904,#1073,.T.);
#4963=EDGE_CURVE('',#3903,#3901,#353,.T.);
#4964=EDGE_CURVE('',#3904,#3902,#354,.F.);
#4965=EDGE_CURVE('',#3905,#3906,#1074,.T.);
#4966=EDGE_CURVE('',#3905,#3903,#355,.T.);
#4967=EDGE_CURVE('',#3906,#3904,#356,.F.);
#4968=EDGE_CURVE('',#3907,#3908,#1075,.T.);
#4969=EDGE_CURVE('',#3907,#3905,#357,.T.);
#4970=EDGE_CURVE('',#3908,#3906,#358,.F.);
#4971=EDGE_CURVE('',#3909,#3910,#1076,.T.);
#4972=EDGE_CURVE('',#3909,#3907,#359,.T.);
#4973=EDGE_CURVE('',#3910,#3908,#360,.F.);
#4974=EDGE_CURVE('',#3911,#3912,#1077,.T.);
#4975=EDGE_CURVE('',#3911,#3909,#361,.T.);
#4976=EDGE_CURVE('',#3912,#3910,#362,.F.);
#4977=EDGE_CURVE('',#3913,#3914,#1078,.T.);
#4978=EDGE_CURVE('',#3913,#3911,#363,.T.);
#4979=EDGE_CURVE('',#3914,#3912,#364,.F.);
#4980=EDGE_CURVE('',#3915,#3916,#1079,.T.);
#4981=EDGE_CURVE('',#3915,#3913,#365,.T.);
#4982=EDGE_CURVE('',#3916,#3914,#366,.F.);
#4983=EDGE_CURVE('',#3917,#3918,#1080,.T.);
#4984=EDGE_CURVE('',#3917,#3915,#367,.T.);
#4985=EDGE_CURVE('',#3918,#3916,#368,.F.);
#4986=EDGE_CURVE('',#3919,#3920,#1081,.T.);
#4987=EDGE_CURVE('',#3919,#3917,#369,.T.);
#4988=EDGE_CURVE('',#3920,#3918,#370,.F.);
#4989=EDGE_CURVE('',#3921,#3922,#1082,.T.);
#4990=EDGE_CURVE('',#3921,#3919,#371,.T.);
#4991=EDGE_CURVE('',#3922,#3920,#372,.F.);
#4992=EDGE_CURVE('',#3923,#3924,#1083,.T.);
#4993=EDGE_CURVE('',#3923,#3921,#373,.T.);
#4994=EDGE_CURVE('',#3924,#3922,#374,.F.);
#4995=EDGE_CURVE('',#3925,#3926,#1084,.T.);
#4996=EDGE_CURVE('',#3925,#3923,#375,.T.);
#4997=EDGE_CURVE('',#3926,#3924,#376,.F.);
#4998=EDGE_CURVE('',#3927,#3928,#1085,.T.);
#4999=EDGE_CURVE('',#3927,#3925,#377,.T.);
#5000=EDGE_CURVE('',#3928,#3926,#378,.F.);
#5001=EDGE_CURVE('',#3929,#3930,#1086,.T.);
#5002=EDGE_CURVE('',#3929,#3927,#379,.T.);
#5003=EDGE_CURVE('',#3930,#3928,#380,.F.);
#5004=EDGE_CURVE('',#3931,#3932,#1087,.T.);
#5005=EDGE_CURVE('',#3931,#3929,#381,.T.);
#5006=EDGE_CURVE('',#3932,#3930,#382,.F.);
#5007=EDGE_CURVE('',#3933,#3934,#1088,.T.);
#5008=EDGE_CURVE('',#3933,#3931,#383,.T.);
#5009=EDGE_CURVE('',#3934,#3932,#384,.F.);
#5010=EDGE_CURVE('',#3935,#3936,#1089,.T.);
#5011=EDGE_CURVE('',#3935,#3933,#385,.T.);
#5012=EDGE_CURVE('',#3936,#3934,#386,.F.);
#5013=EDGE_CURVE('',#3937,#3938,#1090,.T.);
#5014=EDGE_CURVE('',#3937,#3935,#387,.T.);
#5015=EDGE_CURVE('',#3938,#3936,#388,.F.);
#5016=EDGE_CURVE('',#3939,#3940,#1091,.T.);
#5017=EDGE_CURVE('',#3941,#3939,#3252,.T.);
#5018=EDGE_CURVE('',#3941,#3937,#389,.T.);
#5019=EDGE_CURVE('',#3940,#3938,#390,.F.);
#5020=EDGE_CURVE('',#3942,#3941,#3253,.T.);
#5021=EDGE_CURVE('',#3939,#3943,#1092,.T.);
#5022=EDGE_CURVE('',#3943,#3943,#3254,.T.);
#5023=EDGE_CURVE('',#3939,#3942,#3255,.T.);
#5024=EDGE_CURVE('',#3944,#3945,#391,.T.);
#5025=EDGE_CURVE('',#3945,#3946,#1093,.T.);
#5026=EDGE_CURVE('',#3946,#3947,#392,.T.);
#5027=EDGE_CURVE('',#3947,#3944,#1094,.T.);
#5028=EDGE_CURVE('',#3948,#3949,#393,.T.);
#5029=EDGE_CURVE('',#3949,#3950,#1095,.T.);
#5030=EDGE_CURVE('',#3950,#3951,#394,.T.);
#5031=EDGE_CURVE('',#3951,#3948,#1096,.T.);
#5032=EDGE_CURVE('',#3952,#3953,#395,.T.);
#5033=EDGE_CURVE('',#3953,#3954,#1097,.T.);
#5034=EDGE_CURVE('',#3954,#3955,#396,.T.);
#5035=EDGE_CURVE('',#3955,#3952,#1098,.T.);
#5036=EDGE_CURVE('',#3956,#3957,#397,.T.);
#5037=EDGE_CURVE('',#3957,#3958,#1099,.T.);
#5038=EDGE_CURVE('',#3958,#3959,#398,.T.);
#5039=EDGE_CURVE('',#3959,#3956,#1100,.T.);
#5040=EDGE_CURVE('',#3960,#3961,#399,.T.);
#5041=EDGE_CURVE('',#3961,#3962,#1101,.T.);
#5042=EDGE_CURVE('',#3962,#3963,#400,.T.);
#5043=EDGE_CURVE('',#3963,#3960,#1102,.T.);
#5044=EDGE_CURVE('',#3964,#3965,#401,.T.);
#5045=EDGE_CURVE('',#3965,#3966,#1103,.T.);
#5046=EDGE_CURVE('',#3966,#3967,#402,.T.);
#5047=EDGE_CURVE('',#3967,#3964,#1104,.T.);
#5048=EDGE_CURVE('',#3968,#3969,#403,.T.);
#5049=EDGE_CURVE('',#3969,#3970,#1105,.T.);
#5050=EDGE_CURVE('',#3970,#3971,#404,.T.);
#5051=EDGE_CURVE('',#3971,#3968,#1106,.T.);
#5052=EDGE_CURVE('',#3972,#3973,#405,.T.);
#5053=EDGE_CURVE('',#3973,#3974,#1107,.T.);
#5054=EDGE_CURVE('',#3974,#3975,#406,.T.);
#5055=EDGE_CURVE('',#3975,#3972,#1108,.T.);
#5056=EDGE_CURVE('',#3976,#3977,#407,.T.);
#5057=EDGE_CURVE('',#3977,#3978,#1109,.T.);
#5058=EDGE_CURVE('',#3978,#3979,#408,.T.);
#5059=EDGE_CURVE('',#3979,#3976,#1110,.T.);
#5060=EDGE_CURVE('',#3980,#3981,#409,.T.);
#5061=EDGE_CURVE('',#3981,#3982,#1111,.T.);
#5062=EDGE_CURVE('',#3982,#3983,#410,.T.);
#5063=EDGE_CURVE('',#3983,#3980,#1112,.T.);
#5064=EDGE_CURVE('',#3984,#3984,#3256,.T.);
#5065=EDGE_CURVE('',#3984,#3985,#3257,.T.);
#5066=EDGE_CURVE('',#3986,#3985,#3258,.T.);
#5067=EDGE_CURVE('',#3987,#3986,#411,.T.);
#5068=EDGE_CURVE('',#3988,#3987,#3259,.T.);
#5069=EDGE_CURVE('',#3989,#3988,#412,.T.);
#5070=EDGE_CURVE('',#3990,#3989,#3260,.T.);
#5071=EDGE_CURVE('',#3991,#3990,#413,.T.);
#5072=EDGE_CURVE('',#3992,#3991,#3261,.T.);
#5073=EDGE_CURVE('',#3993,#3992,#414,.T.);
#5074=EDGE_CURVE('',#3994,#3993,#3262,.T.);
#5075=EDGE_CURVE('',#3995,#3994,#415,.T.);
#5076=EDGE_CURVE('',#3996,#3995,#3263,.T.);
#5077=EDGE_CURVE('',#3997,#3996,#416,.T.);
#5078=EDGE_CURVE('',#3998,#3997,#3264,.T.);
#5079=EDGE_CURVE('',#3999,#3998,#417,.T.);
#5080=EDGE_CURVE('',#4000,#3999,#3265,.T.);
#5081=EDGE_CURVE('',#4001,#4000,#418,.T.);
#5082=EDGE_CURVE('',#3945,#4001,#3266,.T.);
#5083=EDGE_CURVE('',#3949,#3944,#3267,.T.);
#5084=EDGE_CURVE('',#3953,#3948,#3268,.T.);
#5085=EDGE_CURVE('',#3957,#3952,#3269,.T.);
#5086=EDGE_CURVE('',#3961,#3956,#3270,.T.);
#5087=EDGE_CURVE('',#3965,#3960,#3271,.T.);
#5088=EDGE_CURVE('',#3969,#3964,#3272,.T.);
#5089=EDGE_CURVE('',#3973,#3968,#3273,.T.);
#5090=EDGE_CURVE('',#3977,#3972,#3274,.T.);
#5091=EDGE_CURVE('',#3981,#3976,#3275,.T.);
#5092=EDGE_CURVE('',#4002,#3980,#3276,.T.);
#5093=EDGE_CURVE('',#4003,#4002,#419,.T.);
#5094=EDGE_CURVE('',#4004,#4003,#3277,.T.);
#5095=EDGE_CURVE('',#4005,#4004,#420,.T.);
#5096=EDGE_CURVE('',#4006,#4005,#3278,.T.);
#5097=EDGE_CURVE('',#4007,#4006,#421,.T.);
#5098=EDGE_CURVE('',#4008,#4007,#3279,.T.);
#5099=EDGE_CURVE('',#4009,#4008,#422,.T.);
#5100=EDGE_CURVE('',#4010,#4009,#3280,.T.);
#5101=EDGE_CURVE('',#4011,#4010,#423,.T.);
#5102=EDGE_CURVE('',#4012,#4011,#3281,.T.);
#5103=EDGE_CURVE('',#4013,#4012,#424,.T.);
#5104=EDGE_CURVE('',#4014,#4013,#3282,.T.);
#5105=EDGE_CURVE('',#4015,#4014,#425,.T.);
#5106=EDGE_CURVE('',#4016,#4015,#3283,.T.);
#5107=EDGE_CURVE('',#4017,#4016,#426,.T.);
#5108=EDGE_CURVE('',#3985,#4017,#3284,.T.);
#5109=EDGE_CURVE('',#4018,#4018,#3285,.T.);
#5110=EDGE_CURVE('',#4018,#4019,#3286,.T.);
#5111=EDGE_CURVE('',#3963,#4019,#3287,.T.);
#5112=EDGE_CURVE('',#3959,#3962,#3288,.T.);
#5113=EDGE_CURVE('',#3955,#3958,#3289,.T.);
#5114=EDGE_CURVE('',#3951,#3954,#3290,.T.);
#5115=EDGE_CURVE('',#3947,#3950,#3291,.T.);
#5116=EDGE_CURVE('',#4020,#3946,#3292,.T.);
#5117=EDGE_CURVE('',#4021,#4020,#427,.T.);
#5118=EDGE_CURVE('',#4022,#4021,#3293,.T.);
#5119=EDGE_CURVE('',#4023,#4022,#428,.T.);
#5120=EDGE_CURVE('',#4024,#4023,#3294,.T.);
#5121=EDGE_CURVE('',#4025,#4024,#429,.T.);
#5122=EDGE_CURVE('',#4026,#4025,#3295,.T.);
#5123=EDGE_CURVE('',#4027,#4026,#430,.T.);
#5124=EDGE_CURVE('',#4028,#4027,#3296,.T.);
#5125=EDGE_CURVE('',#4029,#4028,#431,.T.);
#5126=EDGE_CURVE('',#4030,#4029,#3297,.T.);
#5127=EDGE_CURVE('',#4031,#4030,#432,.T.);
#5128=EDGE_CURVE('',#4032,#4031,#3298,.T.);
#5129=EDGE_CURVE('',#4033,#4032,#433,.T.);
#5130=EDGE_CURVE('',#4034,#4033,#3299,.T.);
#5131=EDGE_CURVE('',#4035,#4034,#434,.T.);
#5132=EDGE_CURVE('',#4036,#4035,#3300,.T.);
#5133=EDGE_CURVE('',#4037,#4036,#435,.T.);
#5134=EDGE_CURVE('',#4038,#4037,#3301,.T.);
#5135=EDGE_CURVE('',#4039,#4038,#436,.T.);
#5136=EDGE_CURVE('',#4040,#4039,#3302,.T.);
#5137=EDGE_CURVE('',#4041,#4040,#437,.T.);
#5138=EDGE_CURVE('',#4042,#4041,#3303,.T.);
#5139=EDGE_CURVE('',#4043,#4042,#438,.T.);
#5140=EDGE_CURVE('',#4044,#4043,#3304,.T.);
#5141=EDGE_CURVE('',#4045,#4044,#439,.T.);
#5142=EDGE_CURVE('',#4046,#4045,#3305,.T.);
#5143=EDGE_CURVE('',#4047,#4046,#440,.T.);
#5144=EDGE_CURVE('',#4048,#4047,#3306,.T.);
#5145=EDGE_CURVE('',#4049,#4048,#441,.T.);
#5146=EDGE_CURVE('',#4050,#4049,#3307,.T.);
#5147=EDGE_CURVE('',#4051,#4050,#442,.T.);
#5148=EDGE_CURVE('',#3983,#4051,#3308,.T.);
#5149=EDGE_CURVE('',#3979,#3982,#3309,.T.);
#5150=EDGE_CURVE('',#3975,#3978,#3310,.T.);
#5151=EDGE_CURVE('',#3971,#3974,#3311,.T.);
#5152=EDGE_CURVE('',#3967,#3970,#3312,.T.);
#5153=EDGE_CURVE('',#4019,#3966,#3313,.T.);
#5154=EDGE_CURVE('',#3942,#3940,#443,.F.);
#5155=EDGE_CURVE('',#4020,#4001,#1113,.T.);
#5156=EDGE_CURVE('',#4002,#4051,#1114,.T.);
#5157=EDGE_CURVE('',#4050,#4003,#1115,.T.);
#5158=EDGE_CURVE('',#4004,#4049,#1116,.T.);
#5159=EDGE_CURVE('',#4048,#4005,#1117,.T.);
#5160=EDGE_CURVE('',#4006,#4047,#1118,.T.);
#5161=EDGE_CURVE('',#4046,#4007,#1119,.T.);
#5162=EDGE_CURVE('',#4008,#4045,#1120,.T.);
#5163=EDGE_CURVE('',#4044,#4009,#1121,.T.);
#5164=EDGE_CURVE('',#4010,#4043,#1122,.T.);
#5165=EDGE_CURVE('',#4042,#4011,#1123,.T.);
#5166=EDGE_CURVE('',#4012,#4041,#1124,.T.);
#5167=EDGE_CURVE('',#4040,#4013,#1125,.T.);
#5168=EDGE_CURVE('',#4014,#4039,#1126,.T.);
#5169=EDGE_CURVE('',#4038,#4015,#1127,.T.);
#5170=EDGE_CURVE('',#4016,#4037,#1128,.T.);
#5171=EDGE_CURVE('',#4036,#4017,#1129,.T.);
#5172=EDGE_CURVE('',#3986,#4035,#1130,.T.);
#5173=EDGE_CURVE('',#4034,#3987,#1131,.T.);
#5174=EDGE_CURVE('',#3988,#4033,#1132,.T.);
#5175=EDGE_CURVE('',#4032,#3989,#1133,.T.);
#5176=EDGE_CURVE('',#3990,#4031,#1134,.T.);
#5177=EDGE_CURVE('',#4030,#3991,#1135,.T.);
#5178=EDGE_CURVE('',#3992,#4029,#1136,.T.);
#5179=EDGE_CURVE('',#4028,#3993,#1137,.T.);
#5180=EDGE_CURVE('',#3994,#4027,#1138,.T.);
#5181=EDGE_CURVE('',#4026,#3995,#1139,.T.);
#5182=EDGE_CURVE('',#3996,#4025,#1140,.T.);
#5183=EDGE_CURVE('',#4024,#3997,#1141,.T.);
#5184=EDGE_CURVE('',#3998,#4023,#1142,.T.);
#5185=EDGE_CURVE('',#4052,#4053,#444,.T.);
#5186=EDGE_CURVE('',#4053,#3862,#445,.T.);
#5187=EDGE_CURVE('',#3859,#4052,#446,.T.);
#5188=EDGE_CURVE('',#4000,#4021,#1143,.T.);
#5189=EDGE_CURVE('',#4022,#3999,#1144,.T.);
#5190=EDGE_CURVE('',#3941,#4054,#447,.T.);
#5191=EDGE_CURVE('',#4055,#3942,#448,.T.);
#5192=EDGE_CURVE('',#4054,#4055,#449,.T.);
#5193=EDGE_CURVE('',#4055,#4053,#88,.T.);
#5194=EDGE_CURVE('',#4054,#4052,#89,.T.);
#6739=ORIENTED_EDGE('',*,*,#4895,.F.);
#6740=ORIENTED_EDGE('',*,*,#4896,.T.);
#6741=ORIENTED_EDGE('',*,*,#4897,.T.);
#6742=ORIENTED_EDGE('',*,*,#4898,.F.);
#6743=ORIENTED_EDGE('',*,*,#4899,.T.);
#6744=ORIENTED_EDGE('',*,*,#4895,.T.);
#6745=ORIENTED_EDGE('',*,*,#4900,.T.);
#6746=ORIENTED_EDGE('',*,*,#4901,.F.);
#6747=ORIENTED_EDGE('',*,*,#4902,.F.);
#6748=ORIENTED_EDGE('',*,*,#4903,.T.);
#6749=ORIENTED_EDGE('',*,*,#4898,.T.);
#6750=ORIENTED_EDGE('',*,*,#4904,.F.);
#6751=ORIENTED_EDGE('',*,*,#4905,.F.);
#6752=ORIENTED_EDGE('',*,*,#4906,.T.);
#6753=ORIENTED_EDGE('',*,*,#4902,.T.);
#6754=ORIENTED_EDGE('',*,*,#4907,.F.);
#6755=ORIENTED_EDGE('',*,*,#4908,.F.);
#6756=ORIENTED_EDGE('',*,*,#4909,.T.);
#6757=ORIENTED_EDGE('',*,*,#4905,.T.);
#6758=ORIENTED_EDGE('',*,*,#4910,.F.);
#6759=ORIENTED_EDGE('',*,*,#4911,.F.);
#6760=ORIENTED_EDGE('',*,*,#4912,.T.);
#6761=ORIENTED_EDGE('',*,*,#4908,.T.);
#6762=ORIENTED_EDGE('',*,*,#4913,.F.);
#6763=ORIENTED_EDGE('',*,*,#4914,.F.);
#6764=ORIENTED_EDGE('',*,*,#4915,.T.);
#6765=ORIENTED_EDGE('',*,*,#4911,.T.);
#6766=ORIENTED_EDGE('',*,*,#4916,.F.);
#6767=ORIENTED_EDGE('',*,*,#4917,.F.);
#6768=ORIENTED_EDGE('',*,*,#4918,.T.);
#6769=ORIENTED_EDGE('',*,*,#4914,.T.);
#6770=ORIENTED_EDGE('',*,*,#4919,.F.);
#6771=ORIENTED_EDGE('',*,*,#4920,.F.);
#6772=ORIENTED_EDGE('',*,*,#4921,.T.);
#6773=ORIENTED_EDGE('',*,*,#4917,.T.);
#6774=ORIENTED_EDGE('',*,*,#4922,.F.);
#6775=ORIENTED_EDGE('',*,*,#4923,.F.);
#6776=ORIENTED_EDGE('',*,*,#4924,.T.);
#6777=ORIENTED_EDGE('',*,*,#4920,.T.);
#6778=ORIENTED_EDGE('',*,*,#4925,.F.);
#6779=ORIENTED_EDGE('',*,*,#4926,.F.);
#6780=ORIENTED_EDGE('',*,*,#4927,.T.);
#6781=ORIENTED_EDGE('',*,*,#4923,.T.);
#6782=ORIENTED_EDGE('',*,*,#4928,.F.);
#6783=ORIENTED_EDGE('',*,*,#4929,.F.);
#6784=ORIENTED_EDGE('',*,*,#4930,.T.);
#6785=ORIENTED_EDGE('',*,*,#4926,.T.);
#6786=ORIENTED_EDGE('',*,*,#4931,.F.);
#6787=ORIENTED_EDGE('',*,*,#4932,.F.);
#6788=ORIENTED_EDGE('',*,*,#4933,.T.);
#6789=ORIENTED_EDGE('',*,*,#4929,.T.);
#6790=ORIENTED_EDGE('',*,*,#4934,.F.);
#6791=ORIENTED_EDGE('',*,*,#4935,.F.);
#6792=ORIENTED_EDGE('',*,*,#4936,.T.);
#6793=ORIENTED_EDGE('',*,*,#4932,.T.);
#6794=ORIENTED_EDGE('',*,*,#4937,.F.);
#6795=ORIENTED_EDGE('',*,*,#4938,.F.);
#6796=ORIENTED_EDGE('',*,*,#4939,.T.);
#6797=ORIENTED_EDGE('',*,*,#4935,.T.);
#6798=ORIENTED_EDGE('',*,*,#4940,.F.);
#6799=ORIENTED_EDGE('',*,*,#4941,.F.);
#6800=ORIENTED_EDGE('',*,*,#4942,.T.);
#6801=ORIENTED_EDGE('',*,*,#4938,.T.);
#6802=ORIENTED_EDGE('',*,*,#4943,.F.);
#6803=ORIENTED_EDGE('',*,*,#4944,.F.);
#6804=ORIENTED_EDGE('',*,*,#4945,.T.);
#6805=ORIENTED_EDGE('',*,*,#4941,.T.);
#6806=ORIENTED_EDGE('',*,*,#4946,.F.);
#6807=ORIENTED_EDGE('',*,*,#4947,.F.);
#6808=ORIENTED_EDGE('',*,*,#4948,.T.);
#6809=ORIENTED_EDGE('',*,*,#4944,.T.);
#6810=ORIENTED_EDGE('',*,*,#4949,.F.);
#6811=ORIENTED_EDGE('',*,*,#4950,.F.);
#6812=ORIENTED_EDGE('',*,*,#4951,.T.);
#6813=ORIENTED_EDGE('',*,*,#4947,.T.);
#6814=ORIENTED_EDGE('',*,*,#4952,.F.);
#6815=ORIENTED_EDGE('',*,*,#4953,.F.);
#6816=ORIENTED_EDGE('',*,*,#4954,.T.);
#6817=ORIENTED_EDGE('',*,*,#4950,.T.);
#6818=ORIENTED_EDGE('',*,*,#4955,.F.);
#6819=ORIENTED_EDGE('',*,*,#4956,.F.);
#6820=ORIENTED_EDGE('',*,*,#4957,.T.);
#6821=ORIENTED_EDGE('',*,*,#4953,.T.);
#6822=ORIENTED_EDGE('',*,*,#4958,.F.);
#6823=ORIENTED_EDGE('',*,*,#4959,.F.);
#6824=ORIENTED_EDGE('',*,*,#4960,.T.);
#6825=ORIENTED_EDGE('',*,*,#4956,.T.);
#6826=ORIENTED_EDGE('',*,*,#4961,.F.);
#6827=ORIENTED_EDGE('',*,*,#4962,.F.);
#6828=ORIENTED_EDGE('',*,*,#4963,.T.);
#6829=ORIENTED_EDGE('',*,*,#4959,.T.);
#6830=ORIENTED_EDGE('',*,*,#4964,.F.);
#6831=ORIENTED_EDGE('',*,*,#4965,.F.);
#6832=ORIENTED_EDGE('',*,*,#4966,.T.);
#6833=ORIENTED_EDGE('',*,*,#4962,.T.);
#6834=ORIENTED_EDGE('',*,*,#4967,.F.);
#6835=ORIENTED_EDGE('',*,*,#4968,.F.);
#6836=ORIENTED_EDGE('',*,*,#4969,.T.);
#6837=ORIENTED_EDGE('',*,*,#4965,.T.);
#6838=ORIENTED_EDGE('',*,*,#4970,.F.);
#6839=ORIENTED_EDGE('',*,*,#4971,.F.);
#6840=ORIENTED_EDGE('',*,*,#4972,.T.);
#6841=ORIENTED_EDGE('',*,*,#4968,.T.);
#6842=ORIENTED_EDGE('',*,*,#4973,.F.);
#6843=ORIENTED_EDGE('',*,*,#4974,.F.);
#6844=ORIENTED_EDGE('',*,*,#4975,.T.);
#6845=ORIENTED_EDGE('',*,*,#4971,.T.);
#6846=ORIENTED_EDGE('',*,*,#4976,.F.);
#6847=ORIENTED_EDGE('',*,*,#4977,.F.);
#6848=ORIENTED_EDGE('',*,*,#4978,.T.);
#6849=ORIENTED_EDGE('',*,*,#4974,.T.);
#6850=ORIENTED_EDGE('',*,*,#4979,.F.);
#6851=ORIENTED_EDGE('',*,*,#4980,.F.);
#6852=ORIENTED_EDGE('',*,*,#4981,.T.);
#6853=ORIENTED_EDGE('',*,*,#4977,.T.);
#6854=ORIENTED_EDGE('',*,*,#4982,.F.);
#6855=ORIENTED_EDGE('',*,*,#4983,.F.);
#6856=ORIENTED_EDGE('',*,*,#4984,.T.);
#6857=ORIENTED_EDGE('',*,*,#4980,.T.);
#6858=ORIENTED_EDGE('',*,*,#4985,.F.);
#6859=ORIENTED_EDGE('',*,*,#4986,.F.);
#6860=ORIENTED_EDGE('',*,*,#4987,.T.);
#6861=ORIENTED_EDGE('',*,*,#4983,.T.);
#6862=ORIENTED_EDGE('',*,*,#4988,.F.);
#6863=ORIENTED_EDGE('',*,*,#4989,.F.);
#6864=ORIENTED_EDGE('',*,*,#4990,.T.);
#6865=ORIENTED_EDGE('',*,*,#4986,.T.);
#6866=ORIENTED_EDGE('',*,*,#4991,.F.);
#6867=ORIENTED_EDGE('',*,*,#4992,.F.);
#6868=ORIENTED_EDGE('',*,*,#4993,.T.);
#6869=ORIENTED_EDGE('',*,*,#4989,.T.);
#6870=ORIENTED_EDGE('',*,*,#4994,.F.);
#6871=ORIENTED_EDGE('',*,*,#4995,.F.);
#6872=ORIENTED_EDGE('',*,*,#4996,.T.);
#6873=ORIENTED_EDGE('',*,*,#4992,.T.);
#6874=ORIENTED_EDGE('',*,*,#4997,.F.);
#6875=ORIENTED_EDGE('',*,*,#4998,.F.);
#6876=ORIENTED_EDGE('',*,*,#4999,.T.);
#6877=ORIENTED_EDGE('',*,*,#4995,.T.);
#6878=ORIENTED_EDGE('',*,*,#5000,.F.);
#6879=ORIENTED_EDGE('',*,*,#5001,.F.);
#6880=ORIENTED_EDGE('',*,*,#5002,.T.);
#6881=ORIENTED_EDGE('',*,*,#4998,.T.);
#6882=ORIENTED_EDGE('',*,*,#5003,.F.);
#6883=ORIENTED_EDGE('',*,*,#5004,.F.);
#6884=ORIENTED_EDGE('',*,*,#5005,.T.);
#6885=ORIENTED_EDGE('',*,*,#5001,.T.);
#6886=ORIENTED_EDGE('',*,*,#5006,.F.);
#6887=ORIENTED_EDGE('',*,*,#5007,.F.);
#6888=ORIENTED_EDGE('',*,*,#5008,.T.);
#6889=ORIENTED_EDGE('',*,*,#5004,.T.);
#6890=ORIENTED_EDGE('',*,*,#5009,.F.);
#6891=ORIENTED_EDGE('',*,*,#5010,.F.);
#6892=ORIENTED_EDGE('',*,*,#5011,.T.);
#6893=ORIENTED_EDGE('',*,*,#5007,.T.);
#6894=ORIENTED_EDGE('',*,*,#5012,.F.);
#6895=ORIENTED_EDGE('',*,*,#5013,.F.);
#6896=ORIENTED_EDGE('',*,*,#5014,.T.);
#6897=ORIENTED_EDGE('',*,*,#5010,.T.);
#6898=ORIENTED_EDGE('',*,*,#5015,.F.);
#6899=ORIENTED_EDGE('',*,*,#5016,.F.);
#6900=ORIENTED_EDGE('',*,*,#5017,.F.);
#6901=ORIENTED_EDGE('',*,*,#5018,.T.);
#6902=ORIENTED_EDGE('',*,*,#5013,.T.);
#6903=ORIENTED_EDGE('',*,*,#5019,.F.);
#6904=ORIENTED_EDGE('',*,*,#5020,.T.);
#6905=ORIENTED_EDGE('',*,*,#5017,.T.);
#6906=ORIENTED_EDGE('',*,*,#5021,.T.);
#6907=ORIENTED_EDGE('',*,*,#5022,.F.);
#6908=ORIENTED_EDGE('',*,*,#5021,.F.);
#6909=ORIENTED_EDGE('',*,*,#5023,.T.);
#6910=ORIENTED_EDGE('',*,*,#5024,.T.);
#6911=ORIENTED_EDGE('',*,*,#5025,.T.);
#6912=ORIENTED_EDGE('',*,*,#5026,.T.);
#6913=ORIENTED_EDGE('',*,*,#5027,.T.);
#6914=ORIENTED_EDGE('',*,*,#5028,.T.);
#6915=ORIENTED_EDGE('',*,*,#5029,.T.);
#6916=ORIENTED_EDGE('',*,*,#5030,.T.);
#6917=ORIENTED_EDGE('',*,*,#5031,.T.);
#6918=ORIENTED_EDGE('',*,*,#5032,.T.);
#6919=ORIENTED_EDGE('',*,*,#5033,.T.);
#6920=ORIENTED_EDGE('',*,*,#5034,.T.);
#6921=ORIENTED_EDGE('',*,*,#5035,.T.);
#6922=ORIENTED_EDGE('',*,*,#5036,.T.);
#6923=ORIENTED_EDGE('',*,*,#5037,.T.);
#6924=ORIENTED_EDGE('',*,*,#5038,.T.);
#6925=ORIENTED_EDGE('',*,*,#5039,.T.);
#6926=ORIENTED_EDGE('',*,*,#5040,.T.);
#6927=ORIENTED_EDGE('',*,*,#5041,.T.);
#6928=ORIENTED_EDGE('',*,*,#5042,.T.);
#6929=ORIENTED_EDGE('',*,*,#5043,.T.);
#6930=ORIENTED_EDGE('',*,*,#5044,.T.);
#6931=ORIENTED_EDGE('',*,*,#5045,.T.);
#6932=ORIENTED_EDGE('',*,*,#5046,.T.);
#6933=ORIENTED_EDGE('',*,*,#5047,.T.);
#6934=ORIENTED_EDGE('',*,*,#5048,.T.);
#6935=ORIENTED_EDGE('',*,*,#5049,.T.);
#6936=ORIENTED_EDGE('',*,*,#5050,.T.);
#6937=ORIENTED_EDGE('',*,*,#5051,.T.);
#6938=ORIENTED_EDGE('',*,*,#5052,.T.);
#6939=ORIENTED_EDGE('',*,*,#5053,.T.);
#6940=ORIENTED_EDGE('',*,*,#5054,.T.);
#6941=ORIENTED_EDGE('',*,*,#5055,.T.);
#6942=ORIENTED_EDGE('',*,*,#5056,.T.);
#6943=ORIENTED_EDGE('',*,*,#5057,.T.);
#6944=ORIENTED_EDGE('',*,*,#5058,.T.);
#6945=ORIENTED_EDGE('',*,*,#5059,.T.);
#6946=ORIENTED_EDGE('',*,*,#5060,.T.);
#6947=ORIENTED_EDGE('',*,*,#5061,.T.);
#6948=ORIENTED_EDGE('',*,*,#5062,.T.);
#6949=ORIENTED_EDGE('',*,*,#5063,.T.);
#6950=ORIENTED_EDGE('',*,*,#5064,.F.);
#6951=ORIENTED_EDGE('',*,*,#5065,.T.);
#6952=ORIENTED_EDGE('',*,*,#5066,.F.);
#6953=ORIENTED_EDGE('',*,*,#5067,.F.);
#6954=ORIENTED_EDGE('',*,*,#5068,.F.);
#6955=ORIENTED_EDGE('',*,*,#5069,.F.);
#6956=ORIENTED_EDGE('',*,*,#5070,.F.);
#6957=ORIENTED_EDGE('',*,*,#5071,.F.);
#6958=ORIENTED_EDGE('',*,*,#5072,.F.);
#6959=ORIENTED_EDGE('',*,*,#5073,.F.);
#6960=ORIENTED_EDGE('',*,*,#5074,.F.);
#6961=ORIENTED_EDGE('',*,*,#5075,.F.);
#6962=ORIENTED_EDGE('',*,*,#5076,.F.);
#6963=ORIENTED_EDGE('',*,*,#5077,.F.);
#6964=ORIENTED_EDGE('',*,*,#5078,.F.);
#6965=ORIENTED_EDGE('',*,*,#5079,.F.);
#6966=ORIENTED_EDGE('',*,*,#5080,.F.);
#6967=ORIENTED_EDGE('',*,*,#5081,.F.);
#6968=ORIENTED_EDGE('',*,*,#5082,.F.);
#6969=ORIENTED_EDGE('',*,*,#5024,.F.);
#6970=ORIENTED_EDGE('',*,*,#5083,.F.);
#6971=ORIENTED_EDGE('',*,*,#5028,.F.);
#6972=ORIENTED_EDGE('',*,*,#5084,.F.);
#6973=ORIENTED_EDGE('',*,*,#5032,.F.);
#6974=ORIENTED_EDGE('',*,*,#5085,.F.);
#6975=ORIENTED_EDGE('',*,*,#5036,.F.);
#6976=ORIENTED_EDGE('',*,*,#5086,.F.);
#6977=ORIENTED_EDGE('',*,*,#5040,.F.);
#6978=ORIENTED_EDGE('',*,*,#5087,.F.);
#6979=ORIENTED_EDGE('',*,*,#5044,.F.);
#6980=ORIENTED_EDGE('',*,*,#5088,.F.);
#6981=ORIENTED_EDGE('',*,*,#5048,.F.);
#6982=ORIENTED_EDGE('',*,*,#5089,.F.);
#6983=ORIENTED_EDGE('',*,*,#5052,.F.);
#6984=ORIENTED_EDGE('',*,*,#5090,.F.);
#6985=ORIENTED_EDGE('',*,*,#5056,.F.);
#6986=ORIENTED_EDGE('',*,*,#5091,.F.);
#6987=ORIENTED_EDGE('',*,*,#5060,.F.);
#6988=ORIENTED_EDGE('',*,*,#5092,.F.);
#6989=ORIENTED_EDGE('',*,*,#5093,.F.);
#6990=ORIENTED_EDGE('',*,*,#5094,.F.);
#6991=ORIENTED_EDGE('',*,*,#5095,.F.);
#6992=ORIENTED_EDGE('',*,*,#5096,.F.);
#6993=ORIENTED_EDGE('',*,*,#5097,.F.);
#6994=ORIENTED_EDGE('',*,*,#5098,.F.);
#6995=ORIENTED_EDGE('',*,*,#5099,.F.);
#6996=ORIENTED_EDGE('',*,*,#5100,.F.);
#6997=ORIENTED_EDGE('',*,*,#5101,.F.);
#6998=ORIENTED_EDGE('',*,*,#5102,.F.);
#6999=ORIENTED_EDGE('',*,*,#5103,.F.);
#7000=ORIENTED_EDGE('',*,*,#5104,.F.);
#7001=ORIENTED_EDGE('',*,*,#5105,.F.);
#7002=ORIENTED_EDGE('',*,*,#5106,.F.);
#7003=ORIENTED_EDGE('',*,*,#5107,.F.);
#7004=ORIENTED_EDGE('',*,*,#5108,.F.);
#7005=ORIENTED_EDGE('',*,*,#5065,.F.);
#7006=ORIENTED_EDGE('',*,*,#5109,.F.);
#7007=ORIENTED_EDGE('',*,*,#5110,.T.);
#7008=ORIENTED_EDGE('',*,*,#5111,.F.);
#7009=ORIENTED_EDGE('',*,*,#5042,.F.);
#7010=ORIENTED_EDGE('',*,*,#5112,.F.);
#7011=ORIENTED_EDGE('',*,*,#5038,.F.);
#7012=ORIENTED_EDGE('',*,*,#5113,.F.);
#7013=ORIENTED_EDGE('',*,*,#5034,.F.);
#7014=ORIENTED_EDGE('',*,*,#5114,.F.);
#7015=ORIENTED_EDGE('',*,*,#5030,.F.);
#7016=ORIENTED_EDGE('',*,*,#5115,.F.);
#7017=ORIENTED_EDGE('',*,*,#5026,.F.);
#7018=ORIENTED_EDGE('',*,*,#5116,.F.);
#7019=ORIENTED_EDGE('',*,*,#5117,.F.);
#7020=ORIENTED_EDGE('',*,*,#5118,.F.);
#7021=ORIENTED_EDGE('',*,*,#5119,.F.);
#7022=ORIENTED_EDGE('',*,*,#5120,.F.);
#7023=ORIENTED_EDGE('',*,*,#5121,.F.);
#7024=ORIENTED_EDGE('',*,*,#5122,.F.);
#7025=ORIENTED_EDGE('',*,*,#5123,.F.);
#7026=ORIENTED_EDGE('',*,*,#5124,.F.);
#7027=ORIENTED_EDGE('',*,*,#5125,.F.);
#7028=ORIENTED_EDGE('',*,*,#5126,.F.);
#7029=ORIENTED_EDGE('',*,*,#5127,.F.);
#7030=ORIENTED_EDGE('',*,*,#5128,.F.);
#7031=ORIENTED_EDGE('',*,*,#5129,.F.);
#7032=ORIENTED_EDGE('',*,*,#5130,.F.);
#7033=ORIENTED_EDGE('',*,*,#5131,.F.);
#7034=ORIENTED_EDGE('',*,*,#5132,.F.);
#7035=ORIENTED_EDGE('',*,*,#5133,.F.);
#7036=ORIENTED_EDGE('',*,*,#5134,.F.);
#7037=ORIENTED_EDGE('',*,*,#5135,.F.);
#7038=ORIENTED_EDGE('',*,*,#5136,.F.);
#7039=ORIENTED_EDGE('',*,*,#5137,.F.);
#7040=ORIENTED_EDGE('',*,*,#5138,.F.);
#7041=ORIENTED_EDGE('',*,*,#5139,.F.);
#7042=ORIENTED_EDGE('',*,*,#5140,.F.);
#7043=ORIENTED_EDGE('',*,*,#5141,.F.);
#7044=ORIENTED_EDGE('',*,*,#5142,.F.);
#7045=ORIENTED_EDGE('',*,*,#5143,.F.);
#7046=ORIENTED_EDGE('',*,*,#5144,.F.);
#7047=ORIENTED_EDGE('',*,*,#5145,.F.);
#7048=ORIENTED_EDGE('',*,*,#5146,.F.);
#7049=ORIENTED_EDGE('',*,*,#5147,.F.);
#7050=ORIENTED_EDGE('',*,*,#5148,.F.);
#7051=ORIENTED_EDGE('',*,*,#5062,.F.);
#7052=ORIENTED_EDGE('',*,*,#5149,.F.);
#7053=ORIENTED_EDGE('',*,*,#5058,.F.);
#7054=ORIENTED_EDGE('',*,*,#5150,.F.);
#7055=ORIENTED_EDGE('',*,*,#5054,.F.);
#7056=ORIENTED_EDGE('',*,*,#5151,.F.);
#7057=ORIENTED_EDGE('',*,*,#5050,.F.);
#7058=ORIENTED_EDGE('',*,*,#5152,.F.);
#7059=ORIENTED_EDGE('',*,*,#5046,.F.);
#7060=ORIENTED_EDGE('',*,*,#5153,.F.);
#7061=ORIENTED_EDGE('',*,*,#5110,.F.);
#7062=ORIENTED_EDGE('',*,*,#5016,.T.);
#7063=ORIENTED_EDGE('',*,*,#5154,.F.);
#7064=ORIENTED_EDGE('',*,*,#5023,.F.);
#7065=ORIENTED_EDGE('',*,*,#5111,.T.);
#7066=ORIENTED_EDGE('',*,*,#5153,.T.);
#7067=ORIENTED_EDGE('',*,*,#5045,.F.);
#7068=ORIENTED_EDGE('',*,*,#5087,.T.);
#7069=ORIENTED_EDGE('',*,*,#5043,.F.);
#7070=ORIENTED_EDGE('',*,*,#5155,.F.);
#7071=ORIENTED_EDGE('',*,*,#5116,.T.);
#7072=ORIENTED_EDGE('',*,*,#5025,.F.);
#7073=ORIENTED_EDGE('',*,*,#5082,.T.);
#7074=ORIENTED_EDGE('',*,*,#5027,.F.);
#7075=ORIENTED_EDGE('',*,*,#5115,.T.);
#7076=ORIENTED_EDGE('',*,*,#5029,.F.);
#7077=ORIENTED_EDGE('',*,*,#5083,.T.);
#7078=ORIENTED_EDGE('',*,*,#5031,.F.);
#7079=ORIENTED_EDGE('',*,*,#5114,.T.);
#7080=ORIENTED_EDGE('',*,*,#5033,.F.);
#7081=ORIENTED_EDGE('',*,*,#5084,.T.);
#7082=ORIENTED_EDGE('',*,*,#5035,.F.);
#7083=ORIENTED_EDGE('',*,*,#5113,.T.);
#7084=ORIENTED_EDGE('',*,*,#5037,.F.);
#7085=ORIENTED_EDGE('',*,*,#5085,.T.);
#7086=ORIENTED_EDGE('',*,*,#5039,.F.);
#7087=ORIENTED_EDGE('',*,*,#5112,.T.);
#7088=ORIENTED_EDGE('',*,*,#5041,.F.);
#7089=ORIENTED_EDGE('',*,*,#5086,.T.);
#7090=ORIENTED_EDGE('',*,*,#5047,.F.);
#7091=ORIENTED_EDGE('',*,*,#5152,.T.);
#7092=ORIENTED_EDGE('',*,*,#5049,.F.);
#7093=ORIENTED_EDGE('',*,*,#5088,.T.);
#7094=ORIENTED_EDGE('',*,*,#5051,.F.);
#7095=ORIENTED_EDGE('',*,*,#5151,.T.);
#7096=ORIENTED_EDGE('',*,*,#5053,.F.);
#7097=ORIENTED_EDGE('',*,*,#5089,.T.);
#7098=ORIENTED_EDGE('',*,*,#5055,.F.);
#7099=ORIENTED_EDGE('',*,*,#5150,.T.);
#7100=ORIENTED_EDGE('',*,*,#5057,.F.);
#7101=ORIENTED_EDGE('',*,*,#5090,.T.);
#7102=ORIENTED_EDGE('',*,*,#5059,.F.);
#7103=ORIENTED_EDGE('',*,*,#5149,.T.);
#7104=ORIENTED_EDGE('',*,*,#5061,.F.);
#7105=ORIENTED_EDGE('',*,*,#5091,.T.);
#7106=ORIENTED_EDGE('',*,*,#5063,.F.);
#7107=ORIENTED_EDGE('',*,*,#5148,.T.);
#7108=ORIENTED_EDGE('',*,*,#5156,.F.);
#7109=ORIENTED_EDGE('',*,*,#5092,.T.);
#7110=ORIENTED_EDGE('',*,*,#5157,.F.);
#7111=ORIENTED_EDGE('',*,*,#5146,.T.);
#7112=ORIENTED_EDGE('',*,*,#5158,.F.);
#7113=ORIENTED_EDGE('',*,*,#5094,.T.);
#7114=ORIENTED_EDGE('',*,*,#5159,.F.);
#7115=ORIENTED_EDGE('',*,*,#5144,.T.);
#7116=ORIENTED_EDGE('',*,*,#5160,.F.);
#7117=ORIENTED_EDGE('',*,*,#5096,.T.);
#7118=ORIENTED_EDGE('',*,*,#5161,.F.);
#7119=ORIENTED_EDGE('',*,*,#5142,.T.);
#7120=ORIENTED_EDGE('',*,*,#5162,.F.);
#7121=ORIENTED_EDGE('',*,*,#5098,.T.);
#7122=ORIENTED_EDGE('',*,*,#5163,.F.);
#7123=ORIENTED_EDGE('',*,*,#5140,.T.);
#7124=ORIENTED_EDGE('',*,*,#5164,.F.);
#7125=ORIENTED_EDGE('',*,*,#5100,.T.);
#7126=ORIENTED_EDGE('',*,*,#5165,.F.);
#7127=ORIENTED_EDGE('',*,*,#5138,.T.);
#7128=ORIENTED_EDGE('',*,*,#5166,.F.);
#7129=ORIENTED_EDGE('',*,*,#5102,.T.);
#7130=ORIENTED_EDGE('',*,*,#5167,.F.);
#7131=ORIENTED_EDGE('',*,*,#5136,.T.);
#7132=ORIENTED_EDGE('',*,*,#5168,.F.);
#7133=ORIENTED_EDGE('',*,*,#5104,.T.);
#7134=ORIENTED_EDGE('',*,*,#5169,.F.);
#7135=ORIENTED_EDGE('',*,*,#5134,.T.);
#7136=ORIENTED_EDGE('',*,*,#5170,.F.);
#7137=ORIENTED_EDGE('',*,*,#5106,.T.);
#7138=ORIENTED_EDGE('',*,*,#5171,.F.);
#7139=ORIENTED_EDGE('',*,*,#5132,.T.);
#7140=ORIENTED_EDGE('',*,*,#5172,.F.);
#7141=ORIENTED_EDGE('',*,*,#5066,.T.);
#7142=ORIENTED_EDGE('',*,*,#5108,.T.);
#7143=ORIENTED_EDGE('',*,*,#5173,.F.);
#7144=ORIENTED_EDGE('',*,*,#5130,.T.);
#7145=ORIENTED_EDGE('',*,*,#5174,.F.);
#7146=ORIENTED_EDGE('',*,*,#5068,.T.);
#7147=ORIENTED_EDGE('',*,*,#5175,.F.);
#7148=ORIENTED_EDGE('',*,*,#5128,.T.);
#7149=ORIENTED_EDGE('',*,*,#5176,.F.);
#7150=ORIENTED_EDGE('',*,*,#5070,.T.);
#7151=ORIENTED_EDGE('',*,*,#5177,.F.);
#7152=ORIENTED_EDGE('',*,*,#5126,.T.);
#7153=ORIENTED_EDGE('',*,*,#5178,.F.);
#7154=ORIENTED_EDGE('',*,*,#5072,.T.);
#7155=ORIENTED_EDGE('',*,*,#5179,.F.);
#7156=ORIENTED_EDGE('',*,*,#5124,.T.);
#7157=ORIENTED_EDGE('',*,*,#5180,.F.);
#7158=ORIENTED_EDGE('',*,*,#5074,.T.);
#7159=ORIENTED_EDGE('',*,*,#5181,.F.);
#7160=ORIENTED_EDGE('',*,*,#5122,.T.);
#7161=ORIENTED_EDGE('',*,*,#5182,.F.);
#7162=ORIENTED_EDGE('',*,*,#5076,.T.);
#7163=ORIENTED_EDGE('',*,*,#5183,.F.);
#7164=ORIENTED_EDGE('',*,*,#5120,.T.);
#7165=ORIENTED_EDGE('',*,*,#5184,.F.);
#7166=ORIENTED_EDGE('',*,*,#5078,.T.);
#7167=ORIENTED_EDGE('',*,*,#5064,.T.);
#7168=ORIENTED_EDGE('',*,*,#5185,.T.);
#7169=ORIENTED_EDGE('',*,*,#5186,.T.);
#7170=ORIENTED_EDGE('',*,*,#4900,.F.);
#7171=ORIENTED_EDGE('',*,*,#4897,.F.);
#7172=ORIENTED_EDGE('',*,*,#5187,.T.);
#7173=ORIENTED_EDGE('',*,*,#5109,.T.);
#7174=ORIENTED_EDGE('',*,*,#5188,.F.);
#7175=ORIENTED_EDGE('',*,*,#5080,.T.);
#7176=ORIENTED_EDGE('',*,*,#5189,.F.);
#7177=ORIENTED_EDGE('',*,*,#5118,.T.);
#7178=ORIENTED_EDGE('',*,*,#5190,.F.);
#7179=ORIENTED_EDGE('',*,*,#5020,.F.);
#7180=ORIENTED_EDGE('',*,*,#5191,.F.);
#7181=ORIENTED_EDGE('',*,*,#5192,.F.);
#7182=ORIENTED_EDGE('',*,*,#5193,.F.);
#7183=ORIENTED_EDGE('',*,*,#5191,.T.);
#7184=ORIENTED_EDGE('',*,*,#5154,.T.);
#7185=ORIENTED_EDGE('',*,*,#5019,.T.);
#7186=ORIENTED_EDGE('',*,*,#5015,.T.);
#7187=ORIENTED_EDGE('',*,*,#5012,.T.);
#7188=ORIENTED_EDGE('',*,*,#5009,.T.);
#7189=ORIENTED_EDGE('',*,*,#5006,.T.);
#7190=ORIENTED_EDGE('',*,*,#5003,.T.);
#7191=ORIENTED_EDGE('',*,*,#5000,.T.);
#7192=ORIENTED_EDGE('',*,*,#4997,.T.);
#7193=ORIENTED_EDGE('',*,*,#4994,.T.);
#7194=ORIENTED_EDGE('',*,*,#4991,.T.);
#7195=ORIENTED_EDGE('',*,*,#4988,.T.);
#7196=ORIENTED_EDGE('',*,*,#4985,.T.);
#7197=ORIENTED_EDGE('',*,*,#4982,.T.);
#7198=ORIENTED_EDGE('',*,*,#4979,.T.);
#7199=ORIENTED_EDGE('',*,*,#4976,.T.);
#7200=ORIENTED_EDGE('',*,*,#4973,.T.);
#7201=ORIENTED_EDGE('',*,*,#4970,.T.);
#7202=ORIENTED_EDGE('',*,*,#4967,.T.);
#7203=ORIENTED_EDGE('',*,*,#4964,.T.);
#7204=ORIENTED_EDGE('',*,*,#4961,.T.);
#7205=ORIENTED_EDGE('',*,*,#4958,.T.);
#7206=ORIENTED_EDGE('',*,*,#4955,.T.);
#7207=ORIENTED_EDGE('',*,*,#4952,.T.);
#7208=ORIENTED_EDGE('',*,*,#4949,.T.);
#7209=ORIENTED_EDGE('',*,*,#4946,.T.);
#7210=ORIENTED_EDGE('',*,*,#4943,.T.);
#7211=ORIENTED_EDGE('',*,*,#4940,.T.);
#7212=ORIENTED_EDGE('',*,*,#4937,.T.);
#7213=ORIENTED_EDGE('',*,*,#4934,.T.);
#7214=ORIENTED_EDGE('',*,*,#4931,.T.);
#7215=ORIENTED_EDGE('',*,*,#4928,.T.);
#7216=ORIENTED_EDGE('',*,*,#4925,.T.);
#7217=ORIENTED_EDGE('',*,*,#4922,.T.);
#7218=ORIENTED_EDGE('',*,*,#4919,.T.);
#7219=ORIENTED_EDGE('',*,*,#4916,.T.);
#7220=ORIENTED_EDGE('',*,*,#4913,.T.);
#7221=ORIENTED_EDGE('',*,*,#4910,.T.);
#7222=ORIENTED_EDGE('',*,*,#4907,.T.);
#7223=ORIENTED_EDGE('',*,*,#4904,.T.);
#7224=ORIENTED_EDGE('',*,*,#4901,.T.);
#7225=ORIENTED_EDGE('',*,*,#5186,.F.);
#7226=ORIENTED_EDGE('',*,*,#5018,.F.);
#7227=ORIENTED_EDGE('',*,*,#5190,.T.);
#7228=ORIENTED_EDGE('',*,*,#5194,.T.);
#7229=ORIENTED_EDGE('',*,*,#5187,.F.);
#7230=ORIENTED_EDGE('',*,*,#4896,.F.);
#7231=ORIENTED_EDGE('',*,*,#4899,.F.);
#7232=ORIENTED_EDGE('',*,*,#4903,.F.);
#7233=ORIENTED_EDGE('',*,*,#4906,.F.);
#7234=ORIENTED_EDGE('',*,*,#4909,.F.);
#7235=ORIENTED_EDGE('',*,*,#4912,.F.);
#7236=ORIENTED_EDGE('',*,*,#4915,.F.);
#7237=ORIENTED_EDGE('',*,*,#4918,.F.);
#7238=ORIENTED_EDGE('',*,*,#4921,.F.);
#7239=ORIENTED_EDGE('',*,*,#4924,.F.);
#7240=ORIENTED_EDGE('',*,*,#4927,.F.);
#7241=ORIENTED_EDGE('',*,*,#4930,.F.);
#7242=ORIENTED_EDGE('',*,*,#4933,.F.);
#7243=ORIENTED_EDGE('',*,*,#4936,.F.);
#7244=ORIENTED_EDGE('',*,*,#4939,.F.);
#7245=ORIENTED_EDGE('',*,*,#4942,.F.);
#7246=ORIENTED_EDGE('',*,*,#4945,.F.);
#7247=ORIENTED_EDGE('',*,*,#4948,.F.);
#7248=ORIENTED_EDGE('',*,*,#4951,.F.);
#7249=ORIENTED_EDGE('',*,*,#4954,.F.);
#7250=ORIENTED_EDGE('',*,*,#4957,.F.);
#7251=ORIENTED_EDGE('',*,*,#4960,.F.);
#7252=ORIENTED_EDGE('',*,*,#4963,.F.);
#7253=ORIENTED_EDGE('',*,*,#4966,.F.);
#7254=ORIENTED_EDGE('',*,*,#4969,.F.);
#7255=ORIENTED_EDGE('',*,*,#4972,.F.);
#7256=ORIENTED_EDGE('',*,*,#4975,.F.);
#7257=ORIENTED_EDGE('',*,*,#4978,.F.);
#7258=ORIENTED_EDGE('',*,*,#4981,.F.);
#7259=ORIENTED_EDGE('',*,*,#4984,.F.);
#7260=ORIENTED_EDGE('',*,*,#4987,.F.);
#7261=ORIENTED_EDGE('',*,*,#4990,.F.);
#7262=ORIENTED_EDGE('',*,*,#4993,.F.);
#7263=ORIENTED_EDGE('',*,*,#4996,.F.);
#7264=ORIENTED_EDGE('',*,*,#4999,.F.);
#7265=ORIENTED_EDGE('',*,*,#5002,.F.);
#7266=ORIENTED_EDGE('',*,*,#5005,.F.);
#7267=ORIENTED_EDGE('',*,*,#5008,.F.);
#7268=ORIENTED_EDGE('',*,*,#5011,.F.);
#7269=ORIENTED_EDGE('',*,*,#5014,.F.);
#7270=ORIENTED_EDGE('',*,*,#5194,.F.);
#7271=ORIENTED_EDGE('',*,*,#5192,.T.);
#7272=ORIENTED_EDGE('',*,*,#5193,.T.);
#7273=ORIENTED_EDGE('',*,*,#5185,.F.);
#7274=ORIENTED_EDGE('',*,*,#5119,.T.);
#7275=ORIENTED_EDGE('',*,*,#5189,.T.);
#7276=ORIENTED_EDGE('',*,*,#5079,.T.);
#7277=ORIENTED_EDGE('',*,*,#5184,.T.);
#7278=ORIENTED_EDGE('',*,*,#5121,.T.);
#7279=ORIENTED_EDGE('',*,*,#5183,.T.);
#7280=ORIENTED_EDGE('',*,*,#5077,.T.);
#7281=ORIENTED_EDGE('',*,*,#5182,.T.);
#7282=ORIENTED_EDGE('',*,*,#5123,.T.);
#7283=ORIENTED_EDGE('',*,*,#5181,.T.);
#7284=ORIENTED_EDGE('',*,*,#5075,.T.);
#7285=ORIENTED_EDGE('',*,*,#5180,.T.);
#7286=ORIENTED_EDGE('',*,*,#5125,.T.);
#7287=ORIENTED_EDGE('',*,*,#5179,.T.);
#7288=ORIENTED_EDGE('',*,*,#5073,.T.);
#7289=ORIENTED_EDGE('',*,*,#5178,.T.);
#7290=ORIENTED_EDGE('',*,*,#5127,.T.);
#7291=ORIENTED_EDGE('',*,*,#5177,.T.);
#7292=ORIENTED_EDGE('',*,*,#5071,.T.);
#7293=ORIENTED_EDGE('',*,*,#5176,.T.);
#7294=ORIENTED_EDGE('',*,*,#5129,.T.);
#7295=ORIENTED_EDGE('',*,*,#5175,.T.);
#7296=ORIENTED_EDGE('',*,*,#5069,.T.);
#7297=ORIENTED_EDGE('',*,*,#5174,.T.);
#7298=ORIENTED_EDGE('',*,*,#5131,.T.);
#7299=ORIENTED_EDGE('',*,*,#5173,.T.);
#7300=ORIENTED_EDGE('',*,*,#5067,.T.);
#7301=ORIENTED_EDGE('',*,*,#5172,.T.);
#7302=ORIENTED_EDGE('',*,*,#5133,.T.);
#7303=ORIENTED_EDGE('',*,*,#5171,.T.);
#7304=ORIENTED_EDGE('',*,*,#5107,.T.);
#7305=ORIENTED_EDGE('',*,*,#5170,.T.);
#7306=ORIENTED_EDGE('',*,*,#5135,.T.);
#7307=ORIENTED_EDGE('',*,*,#5169,.T.);
#7308=ORIENTED_EDGE('',*,*,#5105,.T.);
#7309=ORIENTED_EDGE('',*,*,#5168,.T.);
#7310=ORIENTED_EDGE('',*,*,#5137,.T.);
#7311=ORIENTED_EDGE('',*,*,#5167,.T.);
#7312=ORIENTED_EDGE('',*,*,#5103,.T.);
#7313=ORIENTED_EDGE('',*,*,#5166,.T.);
#7314=ORIENTED_EDGE('',*,*,#5139,.T.);
#7315=ORIENTED_EDGE('',*,*,#5165,.T.);
#7316=ORIENTED_EDGE('',*,*,#5101,.T.);
#7317=ORIENTED_EDGE('',*,*,#5164,.T.);
#7318=ORIENTED_EDGE('',*,*,#5141,.T.);
#7319=ORIENTED_EDGE('',*,*,#5163,.T.);
#7320=ORIENTED_EDGE('',*,*,#5099,.T.);
#7321=ORIENTED_EDGE('',*,*,#5162,.T.);
#7322=ORIENTED_EDGE('',*,*,#5143,.T.);
#7323=ORIENTED_EDGE('',*,*,#5161,.T.);
#7324=ORIENTED_EDGE('',*,*,#5097,.T.);
#7325=ORIENTED_EDGE('',*,*,#5160,.T.);
#7326=ORIENTED_EDGE('',*,*,#5145,.T.);
#7327=ORIENTED_EDGE('',*,*,#5159,.T.);
#7328=ORIENTED_EDGE('',*,*,#5095,.T.);
#7329=ORIENTED_EDGE('',*,*,#5158,.T.);
#7330=ORIENTED_EDGE('',*,*,#5147,.T.);
#7331=ORIENTED_EDGE('',*,*,#5157,.T.);
#7332=ORIENTED_EDGE('',*,*,#5093,.T.);
#7333=ORIENTED_EDGE('',*,*,#5156,.T.);
#7334=ORIENTED_EDGE('',*,*,#5117,.T.);
#7335=ORIENTED_EDGE('',*,*,#5155,.T.);
#7336=ORIENTED_EDGE('',*,*,#5081,.T.);
#7337=ORIENTED_EDGE('',*,*,#5188,.T.);
#7338=ORIENTED_EDGE('',*,*,#5022,.T.);
#8606=ADVANCED_FACE('',(#2256),#1901,.T.);
#8607=ADVANCED_FACE('',(#2257),#1902,.T.);
#8608=ADVANCED_FACE('',(#2258),#1903,.T.);
#8609=ADVANCED_FACE('',(#2259),#1904,.T.);
#8610=ADVANCED_FACE('',(#2260),#1905,.T.);
#8611=ADVANCED_FACE('',(#2261),#1906,.T.);
#8612=ADVANCED_FACE('',(#2262),#1907,.T.);
#8613=ADVANCED_FACE('',(#2263),#1908,.T.);
#8614=ADVANCED_FACE('',(#2264),#1909,.T.);
#8615=ADVANCED_FACE('',(#2265),#1910,.T.);
#8616=ADVANCED_FACE('',(#2266),#1911,.T.);
#8617=ADVANCED_FACE('',(#2267),#1912,.T.);
#8618=ADVANCED_FACE('',(#2268),#1913,.T.);
#8619=ADVANCED_FACE('',(#2269),#1914,.T.);
#8620=ADVANCED_FACE('',(#2270),#1915,.T.);
#8621=ADVANCED_FACE('',(#2271),#1916,.T.);
#8622=ADVANCED_FACE('',(#2272),#1917,.T.);
#8623=ADVANCED_FACE('',(#2273),#1918,.T.);
#8624=ADVANCED_FACE('',(#2274),#1919,.T.);
#8625=ADVANCED_FACE('',(#2275),#1920,.T.);
#8626=ADVANCED_FACE('',(#2276),#1921,.T.);
#8627=ADVANCED_FACE('',(#2277),#1922,.T.);
#8628=ADVANCED_FACE('',(#2278),#1923,.T.);
#8629=ADVANCED_FACE('',(#2279),#1924,.T.);
#8630=ADVANCED_FACE('',(#2280),#1925,.T.);
#8631=ADVANCED_FACE('',(#2281),#1926,.T.);
#8632=ADVANCED_FACE('',(#2282),#1927,.T.);
#8633=ADVANCED_FACE('',(#2283),#1928,.T.);
#8634=ADVANCED_FACE('',(#2284),#1929,.T.);
#8635=ADVANCED_FACE('',(#2285),#1930,.T.);
#8636=ADVANCED_FACE('',(#2286),#1931,.T.);
#8637=ADVANCED_FACE('',(#2287),#1932,.T.);
#8638=ADVANCED_FACE('',(#2288),#1933,.T.);
#8639=ADVANCED_FACE('',(#2289),#1934,.T.);
#8640=ADVANCED_FACE('',(#2290),#1935,.T.);
#8641=ADVANCED_FACE('',(#2291),#1936,.T.);
#8642=ADVANCED_FACE('',(#2292),#1937,.T.);
#8643=ADVANCED_FACE('',(#2293),#1938,.T.);
#8644=ADVANCED_FACE('',(#2294),#1939,.T.);
#8645=ADVANCED_FACE('',(#2295),#1940,.T.);
#8646=ADVANCED_FACE('',(#2296),#1941,.T.);
#8647=ADVANCED_FACE('',(#2297),#141,.T.);
#8648=ADVANCED_FACE('',(#2298),#1942,.F.);
#8649=ADVANCED_FACE('',(#2299),#1943,.F.);
#8650=ADVANCED_FACE('',(#2300),#1944,.F.);
#8651=ADVANCED_FACE('',(#2301),#1945,.F.);
#8652=ADVANCED_FACE('',(#2302),#1946,.F.);
#8653=ADVANCED_FACE('',(#2303),#1947,.F.);
#8654=ADVANCED_FACE('',(#2304),#1948,.F.);
#8655=ADVANCED_FACE('',(#2305),#1949,.F.);
#8656=ADVANCED_FACE('',(#2306),#1950,.F.);
#8657=ADVANCED_FACE('',(#2307),#1951,.F.);
#8658=ADVANCED_FACE('',(#2308),#628,.T.);
#8659=ADVANCED_FACE('',(#2309),#629,.T.);
#8660=ADVANCED_FACE('',(#2310),#1952,.T.);
#8661=ADVANCED_FACE('',(#2311),#1953,.T.);
#8662=ADVANCED_FACE('',(#2312),#1954,.T.);
#8663=ADVANCED_FACE('',(#2313),#1955,.T.);
#8664=ADVANCED_FACE('',(#2314),#1956,.T.);
#8665=ADVANCED_FACE('',(#2315),#1957,.T.);
#8666=ADVANCED_FACE('',(#2316),#1958,.T.);
#8667=ADVANCED_FACE('',(#2317),#1959,.T.);
#8668=ADVANCED_FACE('',(#2318),#1960,.T.);
#8669=ADVANCED_FACE('',(#2319),#1961,.T.);
#8670=ADVANCED_FACE('',(#2320),#1962,.T.);
#8671=ADVANCED_FACE('',(#2321),#1963,.T.);
#8672=ADVANCED_FACE('',(#2322),#1964,.T.);
#8673=ADVANCED_FACE('',(#2323),#1965,.T.);
#8674=ADVANCED_FACE('',(#2324),#1966,.T.);
#8675=ADVANCED_FACE('',(#2325),#1967,.T.);
#8676=ADVANCED_FACE('',(#2326),#1968,.T.);
#8677=ADVANCED_FACE('',(#2327),#1969,.T.);
#8678=ADVANCED_FACE('',(#2328),#1970,.T.);
#8679=ADVANCED_FACE('',(#2329),#1971,.T.);
#8680=ADVANCED_FACE('',(#2330),#1972,.T.);
#8681=ADVANCED_FACE('',(#2331),#1973,.T.);
#8682=ADVANCED_FACE('',(#2332),#1974,.T.);
#8683=ADVANCED_FACE('',(#2333),#1975,.T.);
#8684=ADVANCED_FACE('',(#2334),#1976,.T.);
#8685=ADVANCED_FACE('',(#2335),#1977,.T.);
#8686=ADVANCED_FACE('',(#2336,#730),#808,.T.);
#8687=ADVANCED_FACE('',(#2337),#809,.T.);
#8688=ADVANCED_FACE('',(#2338),#1978,.T.);
#8689=ADVANCED_FACE('',(#2339),#810,.T.);
#8690=ADVANCED_FACE('',(#2340),#587,.F.);
#8691=ADVANCED_FACE('',(#2341),#588,.F.);
#8692=ADVANCED_FACE('',(#2342),#589,.F.);
#8693=ADVANCED_FACE('',(#2343),#1979,.F.);
#8694=ADVANCED_FACE('',(#2344),#1980,.F.);
#8695=ADVANCED_FACE('',(#2345),#1981,.F.);
#8696=ADVANCED_FACE('',(#2346),#1982,.F.);
#8697=ADVANCED_FACE('',(#2347),#1983,.F.);
#8698=ADVANCED_FACE('',(#2348),#1984,.F.);
#8699=ADVANCED_FACE('',(#2349),#1985,.F.);
#8700=ADVANCED_FACE('',(#2350),#1986,.F.);
#8701=ADVANCED_FACE('',(#2351),#1987,.F.);
#8702=ADVANCED_FACE('',(#2352),#1988,.F.);
#8703=ADVANCED_FACE('',(#2353),#1989,.F.);
#8704=ADVANCED_FACE('',(#2354),#1990,.F.);
#8705=ADVANCED_FACE('',(#2355),#1991,.F.);
#8706=ADVANCED_FACE('',(#2356),#1992,.F.);
#8707=ADVANCED_FACE('',(#2357),#1993,.F.);
#8708=ADVANCED_FACE('',(#2358),#1994,.F.);
#8709=ADVANCED_FACE('',(#2359),#811,.T.);
#8929=CLOSED_SHELL('',(#8606,#8607,#8608,#8609,#8610,#8611,#8612,#8613,
#8614,#8615,#8616,#8617,#8618,#8619,#8620,#8621,#8622,#8623,#8624,#8625,
#8626,#8627,#8628,#8629,#8630,#8631,#8632,#8633,#8634,#8635,#8636,#8637,
#8638,#8639,#8640,#8641,#8642,#8643,#8644,#8645,#8646,#8647,#8648,#8649,
#8650,#8651,#8652,#8653,#8654,#8655,#8656,#8657,#8658,#8659,#8660,#8661,
#8662,#8663,#8664,#8665,#8666,#8667,#8668,#8669,#8670,#8671,#8672,#8673,
#8674,#8675,#8676,#8677,#8678,#8679,#8680,#8681,#8682,#8683,#8684,#8685,
#8686,#8687,#8688,#8689,#8690,#8691,#8692,#8693,#8694,#8695,#8696,#8697,
#8698,#8699,#8700,#8701,#8702,#8703,#8704,#8705,#8706,#8707,#8708,#8709));
#9345=AXIS2_PLACEMENT_3D('',#32342,#10674,#10675);
#9346=AXIS2_PLACEMENT_3D('',#32343,#10676,#10677);
#9347=AXIS2_PLACEMENT_3D('',#32358,#10679,#10680);
#9348=AXIS2_PLACEMENT_3D('',#32359,#10681,#10682);
#9349=AXIS2_PLACEMENT_3D('',#32400,#10684,#10685);
#9350=AXIS2_PLACEMENT_3D('',#32433,#10686,#10687);
#9351=AXIS2_PLACEMENT_3D('',#32509,#10689,#10690);
#9352=AXIS2_PLACEMENT_3D('',#32585,#10692,#10693);
#9353=AXIS2_PLACEMENT_3D('',#32661,#10695,#10696);
#9354=AXIS2_PLACEMENT_3D('',#32737,#10698,#10699);
#9355=AXIS2_PLACEMENT_3D('',#32813,#10701,#10702);
#9356=AXIS2_PLACEMENT_3D('',#32889,#10704,#10705);
#9357=AXIS2_PLACEMENT_3D('',#32965,#10707,#10708);
#9358=AXIS2_PLACEMENT_3D('',#33041,#10710,#10711);
#9359=AXIS2_PLACEMENT_3D('',#33117,#10713,#10714);
#9360=AXIS2_PLACEMENT_3D('',#33193,#10716,#10717);
#9361=AXIS2_PLACEMENT_3D('',#33269,#10719,#10720);
#9362=AXIS2_PLACEMENT_3D('',#33345,#10722,#10723);
#9363=AXIS2_PLACEMENT_3D('',#33421,#10725,#10726);
#9364=AXIS2_PLACEMENT_3D('',#33497,#10728,#10729);
#9365=AXIS2_PLACEMENT_3D('',#33573,#10731,#10732);
#9366=AXIS2_PLACEMENT_3D('',#33649,#10734,#10735);
#9367=AXIS2_PLACEMENT_3D('',#33725,#10737,#10738);
#9368=AXIS2_PLACEMENT_3D('',#33801,#10740,#10741);
#9369=AXIS2_PLACEMENT_3D('',#33877,#10743,#10744);
#9370=AXIS2_PLACEMENT_3D('',#33953,#10746,#10747);
#9371=AXIS2_PLACEMENT_3D('',#34029,#10749,#10750);
#9372=AXIS2_PLACEMENT_3D('',#34105,#10752,#10753);
#9373=AXIS2_PLACEMENT_3D('',#34181,#10755,#10756);
#9374=AXIS2_PLACEMENT_3D('',#34257,#10758,#10759);
#9375=AXIS2_PLACEMENT_3D('',#34333,#10761,#10762);
#9376=AXIS2_PLACEMENT_3D('',#34409,#10764,#10765);
#9377=AXIS2_PLACEMENT_3D('',#34485,#10767,#10768);
#9378=AXIS2_PLACEMENT_3D('',#34561,#10770,#10771);
#9379=AXIS2_PLACEMENT_3D('',#34637,#10773,#10774);
#9380=AXIS2_PLACEMENT_3D('',#34713,#10776,#10777);
#9381=AXIS2_PLACEMENT_3D('',#34789,#10779,#10780);
#9382=AXIS2_PLACEMENT_3D('',#34865,#10782,#10783);
#9383=AXIS2_PLACEMENT_3D('',#34941,#10785,#10786);
#9384=AXIS2_PLACEMENT_3D('',#35017,#10788,#10789);
#9385=AXIS2_PLACEMENT_3D('',#35093,#10791,#10792);
#9386=AXIS2_PLACEMENT_3D('',#35169,#10794,#10795);
#9387=AXIS2_PLACEMENT_3D('',#35245,#10797,#10798);
#9388=AXIS2_PLACEMENT_3D('',#35321,#10800,#10801);
#9389=AXIS2_PLACEMENT_3D('',#35326,#10803,#10804);
#9390=AXIS2_PLACEMENT_3D('',#35395,#10805,#10806);
#9391=AXIS2_PLACEMENT_3D('',#35397,#10807,#10808);
#9392=AXIS2_PLACEMENT_3D('',#35400,#10810,#10811);
#9393=AXIS2_PLACEMENT_3D('',#35401,#10812,#10813);
#9394=AXIS2_PLACEMENT_3D('',#35402,#10814,#10815);
#9395=AXIS2_PLACEMENT_3D('',#35473,#10818,#10819);
#9396=AXIS2_PLACEMENT_3D('',#35544,#10822,#10823);
#9397=AXIS2_PLACEMENT_3D('',#35615,#10826,#10827);
#9398=AXIS2_PLACEMENT_3D('',#35686,#10830,#10831);
#9399=AXIS2_PLACEMENT_3D('',#35757,#10834,#10835);
#9400=AXIS2_PLACEMENT_3D('',#35828,#10838,#10839);
#9401=AXIS2_PLACEMENT_3D('',#35899,#10842,#10843);
#9402=AXIS2_PLACEMENT_3D('',#35970,#10846,#10847);
#9403=AXIS2_PLACEMENT_3D('',#36041,#10850,#10851);
#9404=AXIS2_PLACEMENT_3D('',#36112,#10854,#10855);
#9405=AXIS2_PLACEMENT_3D('',#36114,#10856,#10857);
#9406=AXIS2_PLACEMENT_3D('',#36116,#10858,#10859);
#9407=AXIS2_PLACEMENT_3D('',#36118,#10860,#10861);
#9408=AXIS2_PLACEMENT_3D('',#36153,#10862,#10863);
#9409=AXIS2_PLACEMENT_3D('',#36188,#10864,#10865);
#9410=AXIS2_PLACEMENT_3D('',#36223,#10866,#10867);
#9411=AXIS2_PLACEMENT_3D('',#36258,#10868,#10869);
#9412=AXIS2_PLACEMENT_3D('',#36293,#10870,#10871);
#9413=AXIS2_PLACEMENT_3D('',#36328,#10872,#10873);
#9414=AXIS2_PLACEMENT_3D('',#36363,#10874,#10875);
#9415=AXIS2_PLACEMENT_3D('',#36397,#10876,#10877);
#9416=AXIS2_PLACEMENT_3D('',#36398,#10878,#10879);
#9417=AXIS2_PLACEMENT_3D('',#36399,#10880,#10881);
#9418=AXIS2_PLACEMENT_3D('',#36400,#10882,#10883);
#9419=AXIS2_PLACEMENT_3D('',#36401,#10884,#10885);
#9420=AXIS2_PLACEMENT_3D('',#36402,#10886,#10887);
#9421=AXIS2_PLACEMENT_3D('',#36403,#10888,#10889);
#9422=AXIS2_PLACEMENT_3D('',#36404,#10890,#10891);
#9423=AXIS2_PLACEMENT_3D('',#36405,#10892,#10893);
#9424=AXIS2_PLACEMENT_3D('',#36406,#10894,#10895);
#9425=AXIS2_PLACEMENT_3D('',#36408,#10896,#10897);
#9426=AXIS2_PLACEMENT_3D('',#36443,#10898,#10899);
#9427=AXIS2_PLACEMENT_3D('',#36478,#10900,#10901);
#9428=AXIS2_PLACEMENT_3D('',#36513,#10902,#10903);
#9429=AXIS2_PLACEMENT_3D('',#36548,#10904,#10905);
#9430=AXIS2_PLACEMENT_3D('',#36583,#10906,#10907);
#9431=AXIS2_PLACEMENT_3D('',#36618,#10908,#10909);
#9432=AXIS2_PLACEMENT_3D('',#36653,#10910,#10911);
#9433=AXIS2_PLACEMENT_3D('',#36687,#10912,#10913);
#9434=AXIS2_PLACEMENT_3D('',#36688,#10914,#10915);
#9435=AXIS2_PLACEMENT_3D('',#36690,#10916,#10917);
#9436=AXIS2_PLACEMENT_3D('',#36692,#10918,#10919);
#9437=AXIS2_PLACEMENT_3D('',#36693,#10920,#10921);
#9438=AXIS2_PLACEMENT_3D('',#36694,#10922,#10923);
#9439=AXIS2_PLACEMENT_3D('',#36695,#10924,#10925);
#9440=AXIS2_PLACEMENT_3D('',#36696,#10926,#10927);
#9441=AXIS2_PLACEMENT_3D('',#36697,#10928,#10929);
#9442=AXIS2_PLACEMENT_3D('',#36699,#10930,#10931);
#9443=AXIS2_PLACEMENT_3D('',#36734,#10932,#10933);
#9444=AXIS2_PLACEMENT_3D('',#36769,#10934,#10935);
#9445=AXIS2_PLACEMENT_3D('',#36804,#10936,#10937);
#9446=AXIS2_PLACEMENT_3D('',#36839,#10938,#10939);
#9447=AXIS2_PLACEMENT_3D('',#36874,#10940,#10941);
#9448=AXIS2_PLACEMENT_3D('',#36909,#10942,#10943);
#9449=AXIS2_PLACEMENT_3D('',#36944,#10944,#10945);
#9450=AXIS2_PLACEMENT_3D('',#36979,#10946,#10947);
#9451=AXIS2_PLACEMENT_3D('',#37014,#10948,#10949);
#9452=AXIS2_PLACEMENT_3D('',#37049,#10950,#10951);
#9453=AXIS2_PLACEMENT_3D('',#37084,#10952,#10953);
#9454=AXIS2_PLACEMENT_3D('',#37119,#10954,#10955);
#9455=AXIS2_PLACEMENT_3D('',#37154,#10956,#10957);
#9456=AXIS2_PLACEMENT_3D('',#37189,#10958,#10959);
#9457=AXIS2_PLACEMENT_3D('',#37224,#10960,#10961);
#9458=AXIS2_PLACEMENT_3D('',#37258,#10962,#10963);
#9459=AXIS2_PLACEMENT_3D('',#37259,#10964,#10965);
#9460=AXIS2_PLACEMENT_3D('',#37260,#10966,#10967);
#9461=AXIS2_PLACEMENT_3D('',#37261,#10968,#10969);
#9462=AXIS2_PLACEMENT_3D('',#37262,#10970,#10971);
#9463=AXIS2_PLACEMENT_3D('',#37263,#10972,#10973);
#9464=AXIS2_PLACEMENT_3D('',#37264,#10974,#10975);
#9465=AXIS2_PLACEMENT_3D('',#37275,#10976,#10977);
#9466=AXIS2_PLACEMENT_3D('',#37276,#10978,#10979);
#9467=AXIS2_PLACEMENT_3D('',#37278,#10981,#10982);
#9468=AXIS2_PLACEMENT_3D('',#37279,#10983,#10984);
#9469=AXIS2_PLACEMENT_3D('',#37280,#10985,#10986);
#9470=AXIS2_PLACEMENT_3D('',#37281,#10987,#10988);
#9471=AXIS2_PLACEMENT_3D('',#37282,#10989,#10990);
#9472=AXIS2_PLACEMENT_3D('',#37283,#10991,#10992);
#9473=AXIS2_PLACEMENT_3D('',#37284,#10993,#10994);
#9474=AXIS2_PLACEMENT_3D('',#37285,#10995,#10996);
#9475=AXIS2_PLACEMENT_3D('',#37286,#10997,#10998);
#9476=AXIS2_PLACEMENT_3D('',#37288,#11000,#11001);
#9477=AXIS2_PLACEMENT_3D('',#37291,#11004,#11005);
#9478=AXIS2_PLACEMENT_3D('',#37294,#11008,#11009);
#9479=AXIS2_PLACEMENT_3D('',#37297,#11012,#11013);
#9480=AXIS2_PLACEMENT_3D('',#37300,#11016,#11017);
#9481=AXIS2_PLACEMENT_3D('',#37303,#11020,#11021);
#9482=AXIS2_PLACEMENT_3D('',#37306,#11024,#11025);
#9483=AXIS2_PLACEMENT_3D('',#37309,#11028,#11029);
#9484=AXIS2_PLACEMENT_3D('',#37312,#11032,#11033);
#9485=AXIS2_PLACEMENT_3D('',#37315,#11036,#11037);
#9486=AXIS2_PLACEMENT_3D('',#37318,#11040,#11041);
#9487=AXIS2_PLACEMENT_3D('',#37321,#11044,#11045);
#9488=AXIS2_PLACEMENT_3D('',#37324,#11048,#11049);
#9489=AXIS2_PLACEMENT_3D('',#37327,#11052,#11053);
#9490=AXIS2_PLACEMENT_3D('',#37330,#11056,#11057);
#9491=AXIS2_PLACEMENT_3D('',#37367,#11058,#11059);
#9492=AXIS2_PLACEMENT_3D('',#37368,#11060,#11061);
#9493=AXIS2_PLACEMENT_3D('',#37371,#11064,#11065);
#9494=AXIS2_PLACEMENT_3D('',#44258,#11066,#11067);
#9495=AXIS2_PLACEMENT_3D('',#44259,#11068,#11069);
#9496=AXIS2_PLACEMENT_3D('',#44260,#11070,#11071);
#9497=AXIS2_PLACEMENT_3D('',#44261,#11072,#11073);
#9498=AXIS2_PLACEMENT_3D('',#44262,#11074,#11075);
#9499=AXIS2_PLACEMENT_3D('',#44263,#11076,#11077);
#9500=AXIS2_PLACEMENT_3D('',#44264,#11078,#11079);
#9501=AXIS2_PLACEMENT_3D('',#44265,#11080,#11081);
#9502=AXIS2_PLACEMENT_3D('',#44266,#11082,#11083);
#9503=AXIS2_PLACEMENT_3D('',#44267,#11084,#11085);
#9504=AXIS2_PLACEMENT_3D('',#44268,#11086,#11087);
#9505=AXIS2_PLACEMENT_3D('',#44269,#11088,#11089);
#9506=AXIS2_PLACEMENT_3D('',#44270,#11090,#11091);
#9507=AXIS2_PLACEMENT_3D('',#44271,#11092,#11093);
#9508=AXIS2_PLACEMENT_3D('',#44272,#11094,#11095);
#9509=AXIS2_PLACEMENT_3D('',#44273,#11096,#11097);
#9510=AXIS2_PLACEMENT_3D('',#44274,#11098,#11099);
#10674=DIRECTION('axis',(0.,0.,1.));
#10675=DIRECTION('refdir',(1.,0.,0.));
#10676=DIRECTION('center_axis',(0.106006004448151,0.994365489657067,9.53019194070163E-17));
#10677=DIRECTION('ref_axis',(-0.61063877343479,0.0650981728612347,0.789229064510541));
#10678=DIRECTION('',(-0.106006004448151,-0.994365489657067,-9.53019194070163E-17));
#10679=DIRECTION('center_axis',(0.106006004448151,0.994365489657067,9.53019194070163E-17));
#10680=DIRECTION('ref_axis',(-0.61063877343479,0.0650981728612347,0.789229064510541));
#10681=DIRECTION('center_axis',(0.106006004448151,0.994365489657067,9.53019194070163E-17));
#10682=DIRECTION('ref_axis',(-0.61063877343479,0.0650981728612347,0.789229064510541));
#10683=DIRECTION('',(-0.106006004448151,-0.994365489657067,-9.53019194070163E-17));
#10684=DIRECTION('center_axis',(0.106006004448151,0.994365489657067,9.53019194070163E-17));
#10685=DIRECTION('ref_axis',(-0.61063877343479,0.0650981728612347,0.789229064510541));
#10686=DIRECTION('center_axis',(0.106006004448151,0.994365489657067,9.53019194070163E-17));
#10687=DIRECTION('ref_axis',(-0.61063877343479,0.0650981728612347,0.789229064510541));
#10688=DIRECTION('',(-0.106006004448151,-0.994365489657067,-9.53019194070163E-17));
#10689=DIRECTION('center_axis',(0.106006004448151,0.994365489657067,9.53019194070163E-17));
#10690=DIRECTION('ref_axis',(-0.61063877343479,0.0650981728612347,0.789229064510541));
#10691=DIRECTION('',(-0.106006004448151,-0.994365489657067,-9.53019194070163E-17));
#10692=DIRECTION('center_axis',(0.106006004448151,0.994365489657067,9.53019194070163E-17));
#10693=DIRECTION('ref_axis',(-0.61063877343479,0.0650981728612347,0.789229064510541));
#10694=DIRECTION('',(-0.106006004448151,-0.994365489657067,-9.53019194070163E-17));
#10695=DIRECTION('center_axis',(0.106006004448151,0.994365489657067,9.53019194070163E-17));
#10696=DIRECTION('ref_axis',(-0.61063877343479,0.0650981728612347,0.789229064510541));
#10697=DIRECTION('',(-0.106006004448151,-0.994365489657067,-9.53019194070163E-17));
#10698=DIRECTION('center_axis',(0.106006004448151,0.994365489657067,9.53019194070163E-17));
#10699=DIRECTION('ref_axis',(-0.61063877343479,0.0650981728612347,0.789229064510541));
#10700=DIRECTION('',(-0.106006004448151,-0.994365489657067,-9.53019194070163E-17));
#10701=DIRECTION('center_axis',(0.106006004448151,0.994365489657067,9.53019194070163E-17));
#10702=DIRECTION('ref_axis',(-0.61063877343479,0.0650981728612347,0.789229064510541));
#10703=DIRECTION('',(-0.106006004448151,-0.994365489657067,-9.53019194070163E-17));
#10704=DIRECTION('center_axis',(0.106006004448151,0.994365489657067,9.53019194070163E-17));
#10705=DIRECTION('ref_axis',(-0.61063877343479,0.0650981728612347,0.789229064510541));
#10706=DIRECTION('',(-0.106006004448151,-0.994365489657067,-9.53019194070163E-17));
#10707=DIRECTION('center_axis',(0.106006004448151,0.994365489657067,9.53019194070163E-17));
#10708=DIRECTION('ref_axis',(-0.61063877343479,0.0650981728612347,0.789229064510541));
#10709=DIRECTION('',(-0.106006004448151,-0.994365489657067,-9.53019194070163E-17));
#10710=DIRECTION('center_axis',(0.106006004448151,0.994365489657067,9.53019194070163E-17));
#10711=DIRECTION('ref_axis',(-0.61063877343479,0.0650981728612347,0.789229064510541));
#10712=DIRECTION('',(-0.106006004448151,-0.994365489657067,-9.53019194070163E-17));
#10713=DIRECTION('center_axis',(0.106006004448151,0.994365489657067,9.53019194070163E-17));
#10714=DIRECTION('ref_axis',(-0.61063877343479,0.0650981728612347,0.789229064510541));
#10715=DIRECTION('',(-0.106006004448151,-0.994365489657067,-9.53019194070163E-17));
#10716=DIRECTION('center_axis',(0.106006004448151,0.994365489657067,9.53019194070163E-17));
#10717=DIRECTION('ref_axis',(-0.61063877343479,0.0650981728612347,0.789229064510541));
#10718=DIRECTION('',(-0.106006004448151,-0.994365489657067,-9.53019194070163E-17));
#10719=DIRECTION('center_axis',(0.106006004448151,0.994365489657067,9.53019194070163E-17));
#10720=DIRECTION('ref_axis',(-0.61063877343479,0.0650981728612347,0.789229064510541));
#10721=DIRECTION('',(-0.106006004448151,-0.994365489657067,-9.53019194070163E-17));
#10722=DIRECTION('center_axis',(0.106006004448151,0.994365489657067,9.53019194070163E-17));
#10723=DIRECTION('ref_axis',(-0.61063877343479,0.0650981728612347,0.789229064510541));
#10724=DIRECTION('',(-0.106006004448151,-0.994365489657067,-9.53019194070163E-17));
#10725=DIRECTION('center_axis',(0.106006004448151,0.994365489657067,9.53019194070163E-17));
#10726=DIRECTION('ref_axis',(-0.61063877343479,0.0650981728612347,0.789229064510541));
#10727=DIRECTION('',(-0.106006004448151,-0.994365489657067,-9.53019194070163E-17));
#10728=DIRECTION('center_axis',(0.106006004448151,0.994365489657067,9.53019194070163E-17));
#10729=DIRECTION('ref_axis',(-0.61063877343479,0.0650981728612347,0.789229064510541));
#10730=DIRECTION('',(-0.106006004448151,-0.994365489657067,-9.53019194070163E-17));
#10731=DIRECTION('center_axis',(0.106006004448151,0.994365489657067,9.53019194070163E-17));
#10732=DIRECTION('ref_axis',(-0.61063877343479,0.0650981728612347,0.789229064510541));
#10733=DIRECTION('',(-0.106006004448151,-0.994365489657067,-9.53019194070163E-17));
#10734=DIRECTION('center_axis',(0.106006004448151,0.994365489657067,9.53019194070163E-17));
#10735=DIRECTION('ref_axis',(-0.61063877343479,0.0650981728612347,0.789229064510541));
#10736=DIRECTION('',(-0.106006004448151,-0.994365489657067,-9.53019194070163E-17));
#10737=DIRECTION('center_axis',(0.106006004448151,0.994365489657067,9.53019194070163E-17));
#10738=DIRECTION('ref_axis',(-0.61063877343479,0.0650981728612347,0.789229064510541));
#10739=DIRECTION('',(-0.106006004448151,-0.994365489657067,-9.53019194070163E-17));
#10740=DIRECTION('center_axis',(0.106006004448151,0.994365489657067,9.53019194070163E-17));
#10741=DIRECTION('ref_axis',(-0.61063877343479,0.0650981728612347,0.789229064510541));
#10742=DIRECTION('',(-0.106006004448151,-0.994365489657067,-9.53019194070163E-17));
#10743=DIRECTION('center_axis',(0.106006004448151,0.994365489657067,9.53019194070163E-17));
#10744=DIRECTION('ref_axis',(-0.61063877343479,0.0650981728612347,0.789229064510541));
#10745=DIRECTION('',(-0.106006004448151,-0.994365489657067,-9.53019194070163E-17));
#10746=DIRECTION('center_axis',(0.106006004448151,0.994365489657067,9.53019194070163E-17));
#10747=DIRECTION('ref_axis',(-0.61063877343479,0.0650981728612347,0.789229064510541));
#10748=DIRECTION('',(-0.106006004448151,-0.994365489657067,-9.53019194070163E-17));
#10749=DIRECTION('center_axis',(0.106006004448151,0.994365489657067,9.53019194070163E-17));
#10750=DIRECTION('ref_axis',(-0.61063877343479,0.0650981728612347,0.789229064510541));
#10751=DIRECTION('',(-0.106006004448151,-0.994365489657067,-9.53019194070163E-17));
#10752=DIRECTION('center_axis',(0.106006004448151,0.994365489657067,9.53019194070163E-17));
#10753=DIRECTION('ref_axis',(-0.61063877343479,0.0650981728612347,0.789229064510541));
#10754=DIRECTION('',(-0.106006004448151,-0.994365489657067,-9.53019194070163E-17));
#10755=DIRECTION('center_axis',(0.106006004448151,0.994365489657067,9.53019194070163E-17));
#10756=DIRECTION('ref_axis',(-0.61063877343479,0.0650981728612347,0.789229064510541));
#10757=DIRECTION('',(-0.106006004448151,-0.994365489657067,-9.53019194070163E-17));
#10758=DIRECTION('center_axis',(0.106006004448151,0.994365489657067,9.53019194070163E-17));
#10759=DIRECTION('ref_axis',(-0.61063877343479,0.0650981728612347,0.789229064510541));
#10760=DIRECTION('',(-0.106006004448151,-0.994365489657067,-9.53019194070163E-17));
#10761=DIRECTION('center_axis',(0.106006004448151,0.994365489657067,9.53019194070163E-17));
#10762=DIRECTION('ref_axis',(-0.61063877343479,0.0650981728612347,0.789229064510541));
#10763=DIRECTION('',(-0.106006004448151,-0.994365489657067,-9.53019194070163E-17));
#10764=DIRECTION('center_axis',(0.106006004448151,0.994365489657067,9.53019194070163E-17));
#10765=DIRECTION('ref_axis',(-0.61063877343479,0.0650981728612347,0.789229064510541));
#10766=DIRECTION('',(-0.106006004448151,-0.994365489657067,-9.53019194070163E-17));
#10767=DIRECTION('center_axis',(0.106006004448151,0.994365489657067,9.53019194070163E-17));
#10768=DIRECTION('ref_axis',(-0.61063877343479,0.0650981728612347,0.789229064510541));
#10769=DIRECTION('',(-0.106006004448151,-0.994365489657067,-9.53019194070163E-17));
#10770=DIRECTION('center_axis',(0.106006004448151,0.994365489657067,9.53019194070163E-17));
#10771=DIRECTION('ref_axis',(-0.61063877343479,0.0650981728612347,0.789229064510541));
#10772=DIRECTION('',(-0.106006004448151,-0.994365489657067,-9.53019194070163E-17));
#10773=DIRECTION('center_axis',(0.106006004448151,0.994365489657067,9.53019194070163E-17));
#10774=DIRECTION('ref_axis',(-0.61063877343479,0.0650981728612347,0.789229064510541));
#10775=DIRECTION('',(-0.106006004448151,-0.994365489657067,-9.53019194070163E-17));
#10776=DIRECTION('center_axis',(0.106006004448151,0.994365489657067,9.53019194070163E-17));
#10777=DIRECTION('ref_axis',(-0.61063877343479,0.0650981728612347,0.789229064510541));
#10778=DIRECTION('',(-0.106006004448151,-0.994365489657067,-9.53019194070163E-17));
#10779=DIRECTION('center_axis',(0.106006004448151,0.994365489657067,9.53019194070163E-17));
#10780=DIRECTION('ref_axis',(-0.61063877343479,0.0650981728612347,0.789229064510541));
#10781=DIRECTION('',(-0.106006004448151,-0.994365489657067,-9.53019194070163E-17));
#10782=DIRECTION('center_axis',(0.106006004448151,0.994365489657067,9.53019194070163E-17));
#10783=DIRECTION('ref_axis',(-0.61063877343479,0.0650981728612347,0.789229064510541));
#10784=DIRECTION('',(-0.106006004448151,-0.994365489657067,-9.53019194070163E-17));
#10785=DIRECTION('center_axis',(0.106006004448151,0.994365489657067,9.53019194070163E-17));
#10786=DIRECTION('ref_axis',(-0.61063877343479,0.0650981728612347,0.789229064510541));
#10787=DIRECTION('',(-0.106006004448151,-0.994365489657067,-9.53019194070163E-17));
#10788=DIRECTION('center_axis',(0.106006004448151,0.994365489657067,9.53019194070163E-17));
#10789=DIRECTION('ref_axis',(-0.61063877343479,0.0650981728612347,0.789229064510541));
#10790=DIRECTION('',(-0.106006004448151,-0.994365489657067,-9.53019194070163E-17));
#10791=DIRECTION('center_axis',(0.106006004448151,0.994365489657067,9.53019194070163E-17));
#10792=DIRECTION('ref_axis',(-0.61063877343479,0.0650981728612347,0.789229064510541));
#10793=DIRECTION('',(-0.106006004448151,-0.994365489657067,-9.53019194070163E-17));
#10794=DIRECTION('center_axis',(0.106006004448151,0.994365489657067,9.53019194070163E-17));
#10795=DIRECTION('ref_axis',(-0.61063877343479,0.0650981728612347,0.789229064510541));
#10796=DIRECTION('',(-0.106006004448151,-0.994365489657067,-9.53019194070163E-17));
#10797=DIRECTION('center_axis',(0.106006004448151,0.994365489657067,9.53019194070163E-17));
#10798=DIRECTION('ref_axis',(-0.61063877343479,0.0650981728612347,0.789229064510541));
#10799=DIRECTION('',(-0.106006004448151,-0.994365489657067,-9.53019194070163E-17));
#10800=DIRECTION('center_axis',(0.106006004448151,0.994365489657067,9.53019194070163E-17));
#10801=DIRECTION('ref_axis',(-0.61063877343479,0.0650981728612347,0.789229064510541));
#10802=DIRECTION('',(-0.106006004448151,-0.994365489657067,-9.53019194070163E-17));
#10803=DIRECTION('center_axis',(0.106006004448151,0.994365489657067,9.53019194070163E-17));
#10804=DIRECTION('ref_axis',(-0.610638773434788,0.0650981728612345,0.789229064510543));
#10805=DIRECTION('center_axis',(-0.106006004448151,-0.994365489657067,-9.53019194070163E-17));
#10806=DIRECTION('ref_axis',(-0.61063877343479,0.0650981728612347,0.789229064510541));
#10807=DIRECTION('center_axis',(0.106006004448151,0.994365489657067,9.53019194070163E-17));
#10808=DIRECTION('ref_axis',(-0.61063877343479,0.0650981728612347,0.789229064510541));
#10809=DIRECTION('',(-0.356829252959397,0.749153940187426,0.55806922342492));
#10810=DIRECTION('center_axis',(0.106006004448151,0.994365489657067,9.53019194070163E-17));
#10811=DIRECTION('ref_axis',(-0.61063877343479,0.0650981728612347,0.789229064510541));
#10812=DIRECTION('center_axis',(0.106006004448151,0.994365489657067,9.53019194070163E-17));
#10813=DIRECTION('ref_axis',(-0.610638773434788,0.0650981728612345,0.789229064510543));
#10814=DIRECTION('center_axis',(-0.106006004448151,-0.994365489657067,-9.53019194070163E-17));
#10815=DIRECTION('ref_axis',(0.610638773434775,-0.0650981728612332,-0.789229064510553));
#10816=DIRECTION('',(-0.106006004448151,-0.994365489657067,-9.53019194070163E-17));
#10817=DIRECTION('',(0.106006004448151,0.994365489657067,9.53019194070163E-17));
#10818=DIRECTION('center_axis',(-0.106006004448151,-0.994365489657067,-9.53019194070163E-17));
#10819=DIRECTION('ref_axis',(0.610638773434775,-0.0650981728612332,-0.789229064510553));
#10820=DIRECTION('',(-0.106006004448151,-0.994365489657067,-9.53019194070163E-17));
#10821=DIRECTION('',(0.106006004448151,0.994365489657067,9.53019194070163E-17));
#10822=DIRECTION('center_axis',(-0.106006004448151,-0.994365489657067,-9.53019194070163E-17));
#10823=DIRECTION('ref_axis',(0.610638773434775,-0.0650981728612332,-0.789229064510553));
#10824=DIRECTION('',(-0.106006004448151,-0.994365489657067,-9.53019194070163E-17));
#10825=DIRECTION('',(0.106006004448151,0.994365489657067,9.53019194070163E-17));
#10826=DIRECTION('center_axis',(-0.106006004448151,-0.994365489657067,-9.53019194070163E-17));
#10827=DIRECTION('ref_axis',(0.610638773434775,-0.0650981728612332,-0.789229064510553));
#10828=DIRECTION('',(-0.106006004448151,-0.994365489657067,-9.53019194070163E-17));
#10829=DIRECTION('',(0.106006004448151,0.994365489657067,9.53019194070163E-17));
#10830=DIRECTION('center_axis',(-0.106006004448151,-0.994365489657067,-9.53019194070163E-17));
#10831=DIRECTION('ref_axis',(0.610638773434775,-0.0650981728612332,-0.789229064510553));
#10832=DIRECTION('',(-0.106006004448151,-0.994365489657067,-9.53019194070163E-17));
#10833=DIRECTION('',(0.106006004448151,0.994365489657067,9.53019194070163E-17));
#10834=DIRECTION('center_axis',(-0.106006004448151,-0.994365489657067,-9.53019194070163E-17));
#10835=DIRECTION('ref_axis',(0.610638773434775,-0.0650981728612332,-0.789229064510553));
#10836=DIRECTION('',(-0.106006004448151,-0.994365489657067,-9.53019194070163E-17));
#10837=DIRECTION('',(0.106006004448151,0.994365489657067,9.53019194070163E-17));
#10838=DIRECTION('center_axis',(-0.106006004448151,-0.994365489657067,-9.53019194070163E-17));
#10839=DIRECTION('ref_axis',(0.610638773434775,-0.0650981728612332,-0.789229064510553));
#10840=DIRECTION('',(-0.106006004448151,-0.994365489657067,-9.53019194070163E-17));
#10841=DIRECTION('',(0.106006004448151,0.994365489657067,9.53019194070163E-17));
#10842=DIRECTION('center_axis',(-0.106006004448151,-0.994365489657067,-9.53019194070163E-17));
#10843=DIRECTION('ref_axis',(0.610638773434775,-0.0650981728612332,-0.789229064510553));
#10844=DIRECTION('',(-0.106006004448151,-0.994365489657067,-9.53019194070163E-17));
#10845=DIRECTION('',(0.106006004448151,0.994365489657067,9.53019194070163E-17));
#10846=DIRECTION('center_axis',(-0.106006004448151,-0.994365489657067,-9.53019194070163E-17));
#10847=DIRECTION('ref_axis',(0.610638773434775,-0.0650981728612332,-0.789229064510553));
#10848=DIRECTION('',(-0.106006004448151,-0.994365489657067,-9.53019194070163E-17));
#10849=DIRECTION('',(0.106006004448151,0.994365489657067,9.53019194070163E-17));
#10850=DIRECTION('center_axis',(-0.106006004448151,-0.994365489657067,-9.53019194070163E-17));
#10851=DIRECTION('ref_axis',(0.610638773434775,-0.0650981728612332,-0.789229064510553));
#10852=DIRECTION('',(-0.106006004448151,-0.994365489657067,-9.53019194070163E-17));
#10853=DIRECTION('',(0.106006004448151,0.994365489657067,9.53019194070163E-17));
#10854=DIRECTION('center_axis',(0.106006004448151,0.994365489657067,9.53019194070163E-17));
#10855=DIRECTION('ref_axis',(-0.610638773434788,0.0650981728612347,0.789229064510543));
#10856=DIRECTION('center_axis',(0.106006004448151,0.994365489657067,9.53019194070163E-17));
#10857=DIRECTION('ref_axis',(-0.610638773434787,0.0650981728612345,0.789229064510543));
#10858=DIRECTION('center_axis',(-0.784782145183616,0.0836630197231152,-0.614098920151967));
#10859=DIRECTION('ref_axis',(0.610638773434786,-0.0650981728612341,-0.789229064510544));
#10860=DIRECTION('center_axis',(-0.106006004448151,-0.994365489657067,-9.53019194070163E-17));
#10861=DIRECTION('ref_axis',(-0.610638773434768,0.0650981728612323,0.789229064510559));
#10862=DIRECTION('center_axis',(-0.106006004448151,-0.994365489657067,-9.53019194070163E-17));
#10863=DIRECTION('ref_axis',(-0.610638773434788,0.0650981728612345,0.789229064510543));
#10864=DIRECTION('center_axis',(-0.106006004448151,-0.994365489657067,-9.53019194070163E-17));
#10865=DIRECTION('ref_axis',(-0.610638773434769,0.0650981728612324,0.789229064510558));
#10866=DIRECTION('center_axis',(-0.106006004448151,-0.994365489657067,-9.53019194070163E-17));
#10867=DIRECTION('ref_axis',(-0.610638773434788,0.0650981728612345,0.789229064510543));
#10868=DIRECTION('center_axis',(-0.106006004448151,-0.994365489657067,-9.53019194070163E-17));
#10869=DIRECTION('ref_axis',(-0.61063877343478,0.0650981728612337,0.789229064510549));
#10870=DIRECTION('center_axis',(-0.106006004448151,-0.994365489657067,-9.53019194070163E-17));
#10871=DIRECTION('ref_axis',(-0.610638773434788,0.0650981728612345,0.789229064510543));
#10872=DIRECTION('center_axis',(-0.106006004448151,-0.994365489657067,-9.53019194070163E-17));
#10873=DIRECTION('ref_axis',(-0.610638773434782,0.0650981728612339,0.789229064510547));
#10874=DIRECTION('center_axis',(-0.106006004448151,-0.994365489657067,-9.53019194070163E-17));
#10875=DIRECTION('ref_axis',(-0.610638773434798,0.0650981728612356,0.789229064510535));
#10876=DIRECTION('center_axis',(-0.106006004448151,-0.994365489657067,-9.53019194070163E-17));
#10877=DIRECTION('ref_axis',(-0.610638773434789,0.0650981728612346,0.789229064510542));
#10878=DIRECTION('center_axis',(-0.106006004448151,-0.994365489657067,-9.53019194070163E-17));
#10879=DIRECTION('ref_axis',(-0.610638773434784,0.065098172861234,0.789229064510546));
#10880=DIRECTION('center_axis',(-0.106006004448151,-0.994365489657067,-9.53019194070163E-17));
#10881=DIRECTION('ref_axis',(-0.610638773434788,0.0650981728612345,0.789229064510543));
#10882=DIRECTION('center_axis',(-0.106006004448151,-0.994365489657067,-9.53019194070163E-17));
#10883=DIRECTION('ref_axis',(-0.610638773434788,0.0650981728612345,0.789229064510543));
#10884=DIRECTION('center_axis',(-0.106006004448151,-0.994365489657067,-9.53019194070163E-17));
#10885=DIRECTION('ref_axis',(-0.610638773434786,0.0650981728612343,0.789229064510544));
#10886=DIRECTION('center_axis',(-0.106006004448151,-0.994365489657067,-9.53019194070163E-17));
#10887=DIRECTION('ref_axis',(-0.610638773434773,0.065098172861233,0.789229064510554));
#10888=DIRECTION('center_axis',(-0.106006004448151,-0.994365489657067,-9.53019194070163E-17));
#10889=DIRECTION('ref_axis',(-0.6106387734348,0.0650981728612358,0.789229064510533));
#10890=DIRECTION('center_axis',(-0.106006004448151,-0.994365489657067,-9.53019194070163E-17));
#10891=DIRECTION('ref_axis',(-0.610638773434733,0.0650981728612287,0.789229064510586));
#10892=DIRECTION('center_axis',(-0.106006004448151,-0.994365489657067,-9.53019194070163E-17));
#10893=DIRECTION('ref_axis',(-0.610638773434788,0.0650981728612345,0.789229064510543));
#10894=DIRECTION('center_axis',(-0.106006004448151,-0.994365489657067,-9.53019194070163E-17));
#10895=DIRECTION('ref_axis',(-0.6106387734348,0.0650981728612358,0.789229064510533));
#10896=DIRECTION('center_axis',(-0.106006004448151,-0.994365489657067,-9.53019194070163E-17));
#10897=DIRECTION('ref_axis',(-0.610638773434739,0.0650981728612293,0.789229064510581));
#10898=DIRECTION('center_axis',(-0.106006004448151,-0.994365489657067,-9.53019194070163E-17));
#10899=DIRECTION('ref_axis',(-0.610638773434803,0.0650981728612361,0.789229064510531));
#10900=DIRECTION('center_axis',(-0.106006004448151,-0.994365489657067,-9.53019194070163E-17));
#10901=DIRECTION('ref_axis',(-0.61063877343481,0.0650981728612369,0.789229064510525));
#10902=DIRECTION('center_axis',(-0.106006004448151,-0.994365489657067,-9.53019194070163E-17));
#10903=DIRECTION('ref_axis',(-0.61063877343478,0.0650981728612337,0.789229064510549));
#10904=DIRECTION('center_axis',(-0.106006004448151,-0.994365489657067,-9.53019194070163E-17));
#10905=DIRECTION('ref_axis',(-0.610638773434775,0.0650981728612331,0.789229064510553));
#10906=DIRECTION('center_axis',(-0.106006004448151,-0.994365489657067,-9.53019194070163E-17));
#10907=DIRECTION('ref_axis',(-0.610638773434788,0.0650981728612345,0.789229064510543));
#10908=DIRECTION('center_axis',(-0.106006004448151,-0.994365489657067,-9.53019194070163E-17));
#10909=DIRECTION('ref_axis',(-0.6106387734348,0.0650981728612358,0.789229064510533));
#10910=DIRECTION('center_axis',(-0.106006004448151,-0.994365489657067,-9.53019194070163E-17));
#10911=DIRECTION('ref_axis',(-0.610638773434788,0.0650981728612345,0.789229064510543));
#10912=DIRECTION('center_axis',(-0.106006004448151,-0.994365489657067,-9.53019194070163E-17));
#10913=DIRECTION('ref_axis',(-0.610638773434768,0.0650981728612323,0.789229064510559));
#10914=DIRECTION('center_axis',(-0.106006004448151,-0.994365489657067,-9.53019194070163E-17));
#10915=DIRECTION('ref_axis',(0.610638773434788,-0.0650981728612367,-0.789229064510542));
#10916=DIRECTION('center_axis',(-0.106006004448151,-0.994365489657067,-9.53019194070163E-17));
#10917=DIRECTION('ref_axis',(0.610638773434787,-0.0650981728612345,-0.789229064510543));
#10918=DIRECTION('center_axis',(-0.784782145183614,0.0836630197231149,-0.61409892015197));
#10919=DIRECTION('ref_axis',(-0.61063877343479,0.0650981728612343,0.789229064510542));
#10920=DIRECTION('center_axis',(0.106006004448151,0.994365489657067,9.53019194070163E-17));
#10921=DIRECTION('ref_axis',(0.610638773434869,-0.0650981728612432,-0.789229064510479));
#10922=DIRECTION('center_axis',(0.106006004448151,0.994365489657067,9.53019194070163E-17));
#10923=DIRECTION('ref_axis',(0.610638773434769,-0.0650981728612324,-0.789229064510558));
#10924=DIRECTION('center_axis',(0.106006004448151,0.994365489657067,9.53019194070163E-17));
#10925=DIRECTION('ref_axis',(0.610638773434814,-0.0650981728612372,-0.789229064510522));
#10926=DIRECTION('center_axis',(0.106006004448151,0.994365489657067,9.53019194070163E-17));
#10927=DIRECTION('ref_axis',(0.610638773434779,-0.0650981728612335,-0.78922906451055));
#10928=DIRECTION('center_axis',(0.106006004448151,0.994365489657067,9.53019194070163E-17));
#10929=DIRECTION('ref_axis',(0.610638773434794,-0.0650981728612351,-0.789229064510538));
#10930=DIRECTION('center_axis',(0.106006004448151,0.994365489657067,9.53019194070163E-17));
#10931=DIRECTION('ref_axis',(0.6106387734348,-0.0650981728612357,-0.789229064510534));
#10932=DIRECTION('center_axis',(0.106006004448151,0.994365489657067,9.53019194070163E-17));
#10933=DIRECTION('ref_axis',(0.610638773434788,-0.0650981728612346,-0.789229064510543));
#10934=DIRECTION('center_axis',(0.106006004448151,0.994365489657067,9.53019194070163E-17));
#10935=DIRECTION('ref_axis',(0.610638773434794,-0.0650981728612351,-0.789229064510538));
#10936=DIRECTION('center_axis',(0.106006004448151,0.994365489657067,9.53019194070163E-17));
#10937=DIRECTION('ref_axis',(0.610638773434789,-0.0650981728612346,-0.789229064510542));
#10938=DIRECTION('center_axis',(0.106006004448151,0.994365489657067,9.53019194070163E-17));
#10939=DIRECTION('ref_axis',(0.610638773434785,-0.0650981728612342,-0.789229064510545));
#10940=DIRECTION('center_axis',(0.106006004448151,0.994365489657067,9.53019194070163E-17));
#10941=DIRECTION('ref_axis',(0.610638773434789,-0.0650981728612346,-0.789229064510542));
#10942=DIRECTION('center_axis',(0.106006004448151,0.994365489657067,9.53019194070163E-17));
#10943=DIRECTION('ref_axis',(0.610638773434789,-0.0650981728612346,-0.789229064510542));
#10944=DIRECTION('center_axis',(0.106006004448151,0.994365489657067,9.53019194070163E-17));
#10945=DIRECTION('ref_axis',(0.610638773434788,-0.0650981728612345,-0.789229064510543));
#10946=DIRECTION('center_axis',(0.106006004448151,0.994365489657067,9.53019194070163E-17));
#10947=DIRECTION('ref_axis',(0.610638773434677,-0.0650981728612226,-0.78922906451063));
#10948=DIRECTION('center_axis',(0.106006004448151,0.994365489657067,9.53019194070163E-17));
#10949=DIRECTION('ref_axis',(0.610638773434818,-0.0650981728612377,-0.789229064510519));
#10950=DIRECTION('center_axis',(0.106006004448151,0.994365489657067,9.53019194070163E-17));
#10951=DIRECTION('ref_axis',(0.610638773434805,-0.0650981728612363,-0.789229064510529));
#10952=DIRECTION('center_axis',(0.106006004448151,0.994365489657067,9.53019194070163E-17));
#10953=DIRECTION('ref_axis',(0.610638773434784,-0.065098172861234,-0.789229064510546));
#10954=DIRECTION('center_axis',(0.106006004448151,0.994365489657067,9.53019194070163E-17));
#10955=DIRECTION('ref_axis',(0.610638773434769,-0.0650981728612325,-0.789229064510557));
#10956=DIRECTION('center_axis',(0.106006004448151,0.994365489657067,9.53019194070163E-17));
#10957=DIRECTION('ref_axis',(0.610638773434788,-0.0650981728612346,-0.789229064510543));
#10958=DIRECTION('center_axis',(0.106006004448151,0.994365489657067,9.53019194070163E-17));
#10959=DIRECTION('ref_axis',(0.610638773434803,-0.0650981728612361,-0.789229064510531));
#10960=DIRECTION('center_axis',(0.106006004448151,0.994365489657067,9.53019194070163E-17));
#10961=DIRECTION('ref_axis',(0.610638773434803,-0.0650981728612361,-0.789229064510531));
#10962=DIRECTION('center_axis',(0.106006004448151,0.994365489657067,9.53019194070163E-17));
#10963=DIRECTION('ref_axis',(0.610638773434838,-0.0650981728612399,-0.789229064510503));
#10964=DIRECTION('center_axis',(0.106006004448151,0.994365489657067,9.53019194070163E-17));
#10965=DIRECTION('ref_axis',(0.610638773434801,-0.0650981728612359,-0.789229064510533));
#10966=DIRECTION('center_axis',(0.106006004448151,0.994365489657067,9.53019194070163E-17));
#10967=DIRECTION('ref_axis',(0.610638773434788,-0.0650981728612346,-0.789229064510543));
#10968=DIRECTION('center_axis',(0.106006004448151,0.994365489657067,9.53019194070163E-17));
#10969=DIRECTION('ref_axis',(0.610638773434777,-0.0650981728612333,-0.789229064510551));
#10970=DIRECTION('center_axis',(0.106006004448151,0.994365489657067,9.53019194070163E-17));
#10971=DIRECTION('ref_axis',(0.610638773434788,-0.0650981728612346,-0.789229064510543));
#10972=DIRECTION('center_axis',(0.106006004448151,0.994365489657067,9.53019194070163E-17));
#10973=DIRECTION('ref_axis',(0.610638773434869,-0.0650981728612432,-0.789229064510479));
#10974=DIRECTION('center_axis',(0.106006004448151,0.994365489657067,9.53019194070163E-17));
#10975=DIRECTION('ref_axis',(-0.61063877343479,0.0650981728612347,0.789229064510541));
#10976=DIRECTION('center_axis',(0.106006004448151,0.994365489657067,9.53019194070163E-17));
#10977=DIRECTION('ref_axis',(-0.610638773434788,0.0650981728612345,0.789229064510543));
#10978=DIRECTION('center_axis',(0.106006004448151,0.994365489657067,9.53019194070163E-17));
#10979=DIRECTION('ref_axis',(-0.610638773434788,0.0650981728612345,0.789229064510543));
#10980=DIRECTION('',(0.106006004448151,0.994365489657067,9.53019194070163E-17));
#10981=DIRECTION('center_axis',(0.106006004448151,0.994365489657067,9.53019194070163E-17));
#10982=DIRECTION('ref_axis',(-0.610638773434788,0.0650981728612345,0.789229064510543));
#10983=DIRECTION('center_axis',(0.106006004448151,0.994365489657067,9.53019194070163E-17));
#10984=DIRECTION('ref_axis',(-0.610638773434788,0.0650981728612345,0.789229064510543));
#10985=DIRECTION('center_axis',(0.106006004448151,0.994365489657067,9.53019194070163E-17));
#10986=DIRECTION('ref_axis',(-0.610638773434788,0.0650981728612345,0.789229064510543));
#10987=DIRECTION('center_axis',(0.106006004448151,0.994365489657067,9.53019194070163E-17));
#10988=DIRECTION('ref_axis',(-0.610638773434788,0.0650981728612345,0.789229064510543));
#10989=DIRECTION('center_axis',(0.106006004448151,0.994365489657067,9.53019194070163E-17));
#10990=DIRECTION('ref_axis',(-0.610638773434788,0.0650981728612345,0.789229064510543));
#10991=DIRECTION('center_axis',(0.106006004448151,0.994365489657067,9.53019194070163E-17));
#10992=DIRECTION('ref_axis',(-0.610638773434788,0.0650981728612345,0.789229064510543));
#10993=DIRECTION('center_axis',(0.106006004448151,0.994365489657067,9.53019194070163E-17));
#10994=DIRECTION('ref_axis',(-0.610638773434788,0.0650981728612345,0.789229064510543));
#10995=DIRECTION('center_axis',(0.106006004448151,0.994365489657067,9.53019194070163E-17));
#10996=DIRECTION('ref_axis',(-0.610638773434788,0.0650981728612345,0.789229064510543));
#10997=DIRECTION('center_axis',(0.106006004448151,0.994365489657067,9.53019194070163E-17));
#10998=DIRECTION('ref_axis',(-0.610638773434788,0.0650981728612345,0.789229064510543));
#10999=DIRECTION('',(-0.106006004448151,-0.994365489657067,-9.53019194070163E-17));
#11000=DIRECTION('center_axis',(0.106006004448151,0.994365489657067,9.53019194070163E-17));
#11001=DIRECTION('ref_axis',(-0.610638773434788,0.0650981728612345,0.789229064510543));
#11002=DIRECTION('',(0.106006004448151,0.994365489657067,9.53019194070163E-17));
#11003=DIRECTION('',(-0.106006004448151,-0.994365489657067,-9.53019194070163E-17));
#11004=DIRECTION('center_axis',(0.106006004448151,0.994365489657067,9.53019194070163E-17));
#11005=DIRECTION('ref_axis',(-0.610638773434788,0.0650981728612345,0.789229064510543));
#11006=DIRECTION('',(0.106006004448151,0.994365489657067,9.53019194070163E-17));
#11007=DIRECTION('',(-0.106006004448151,-0.994365489657067,-9.53019194070163E-17));
#11008=DIRECTION('center_axis',(0.106006004448151,0.994365489657067,9.53019194070163E-17));
#11009=DIRECTION('ref_axis',(-0.610638773434788,0.0650981728612345,0.789229064510543));
#11010=DIRECTION('',(0.106006004448151,0.994365489657067,9.53019194070163E-17));
#11011=DIRECTION('',(-0.106006004448151,-0.994365489657067,-9.53019194070163E-17));
#11012=DIRECTION('center_axis',(0.106006004448151,0.994365489657067,9.53019194070163E-17));
#11013=DIRECTION('ref_axis',(-0.610638773434788,0.0650981728612345,0.789229064510543));
#11014=DIRECTION('',(0.106006004448151,0.994365489657067,9.53019194070163E-17));
#11015=DIRECTION('',(-0.106006004448151,-0.994365489657067,-9.53019194070163E-17));
#11016=DIRECTION('center_axis',(0.106006004448151,0.994365489657067,9.53019194070163E-17));
#11017=DIRECTION('ref_axis',(-0.610638773434788,0.0650981728612345,0.789229064510543));
#11018=DIRECTION('',(0.106006004448151,0.994365489657067,9.53019194070163E-17));
#11019=DIRECTION('',(-0.106006004448151,-0.994365489657067,-9.53019194070163E-17));
#11020=DIRECTION('center_axis',(0.106006004448151,0.994365489657067,9.53019194070163E-17));
#11021=DIRECTION('ref_axis',(-0.610638773434788,0.0650981728612345,0.789229064510543));
#11022=DIRECTION('',(0.106006004448151,0.994365489657067,9.53019194070163E-17));
#11023=DIRECTION('',(-0.106006004448151,-0.994365489657067,-9.53019194070163E-17));
#11024=DIRECTION('center_axis',(0.106006004448151,0.994365489657067,9.53019194070163E-17));
#11025=DIRECTION('ref_axis',(-0.610638773434788,0.0650981728612345,0.789229064510543));
#11026=DIRECTION('',(0.106006004448151,0.994365489657067,9.53019194070163E-17));
#11027=DIRECTION('',(-0.106006004448151,-0.994365489657067,-9.53019194070163E-17));
#11028=DIRECTION('center_axis',(0.106006004448151,0.994365489657067,9.53019194070163E-17));
#11029=DIRECTION('ref_axis',(0.61063877343478,-0.0650981728612336,-0.789229064510549));
#11030=DIRECTION('',(0.106006004448151,0.994365489657067,9.53019194070163E-17));
#11031=DIRECTION('',(-0.106006004448151,-0.994365489657067,-9.53019194070163E-17));
#11032=DIRECTION('center_axis',(0.106006004448151,0.994365489657067,9.53019194070163E-17));
#11033=DIRECTION('ref_axis',(-0.610638773434788,0.0650981728612345,0.789229064510543));
#11034=DIRECTION('',(0.106006004448151,0.994365489657067,9.53019194070163E-17));
#11035=DIRECTION('',(-0.106006004448151,-0.994365489657067,-9.53019194070163E-17));
#11036=DIRECTION('center_axis',(0.106006004448151,0.994365489657067,9.53019194070163E-17));
#11037=DIRECTION('ref_axis',(-0.610638773434788,0.0650981728612345,0.789229064510543));
#11038=DIRECTION('',(0.106006004448151,0.994365489657067,9.53019194070163E-17));
#11039=DIRECTION('',(-0.106006004448151,-0.994365489657067,-9.53019194070163E-17));
#11040=DIRECTION('center_axis',(0.106006004448151,0.994365489657067,9.53019194070163E-17));
#11041=DIRECTION('ref_axis',(-0.610638773434788,0.0650981728612345,0.789229064510543));
#11042=DIRECTION('',(0.106006004448151,0.994365489657067,9.53019194070163E-17));
#11043=DIRECTION('',(-0.106006004448151,-0.994365489657067,-9.53019194070163E-17));
#11044=DIRECTION('center_axis',(0.106006004448151,0.994365489657067,9.53019194070163E-17));
#11045=DIRECTION('ref_axis',(-0.610638773434788,0.0650981728612345,0.789229064510543));
#11046=DIRECTION('',(0.106006004448151,0.994365489657067,9.53019194070163E-17));
#11047=DIRECTION('',(-0.106006004448151,-0.994365489657067,-9.53019194070163E-17));
#11048=DIRECTION('center_axis',(0.106006004448151,0.994365489657067,9.53019194070163E-17));
#11049=DIRECTION('ref_axis',(-0.610638773434788,0.0650981728612345,0.789229064510543));
#11050=DIRECTION('',(0.106006004448151,0.994365489657067,9.53019194070163E-17));
#11051=DIRECTION('',(-0.106006004448151,-0.994365489657067,-9.53019194070163E-17));
#11052=DIRECTION('center_axis',(0.106006004448151,0.994365489657067,9.53019194070163E-17));
#11053=DIRECTION('ref_axis',(-0.610638773434788,0.0650981728612345,0.789229064510543));
#11054=DIRECTION('',(0.106006004448151,0.994365489657067,9.53019194070163E-17));
#11055=DIRECTION('',(-0.106006004448151,-0.994365489657067,-9.53019194070163E-17));
#11056=DIRECTION('center_axis',(0.106006004448151,0.994365489657067,8.32667268468867E-17));
#11057=DIRECTION('ref_axis',(-0.610638773434788,0.0650981728612344,0.789229064510543));
#11058=DIRECTION('center_axis',(-0.106006004448151,-0.994365489657067,-8.32667268468867E-17));
#11059=DIRECTION('ref_axis',(0.610638773434788,-0.0650981728612344,-0.789229064510543));
#11060=DIRECTION('center_axis',(0.106006004448151,0.994365489657067,9.53019194070163E-17));
#11061=DIRECTION('ref_axis',(-0.610638773434788,0.0650981728612345,0.789229064510543));
#11062=DIRECTION('',(-0.106006004448151,-0.994365489657067,-9.53019194070163E-17));
#11063=DIRECTION('',(0.106006004448151,0.994365489657067,9.53019194070163E-17));
#11064=DIRECTION('center_axis',(0.106006004448151,0.994365489657067,8.32667268468867E-17));
#11065=DIRECTION('ref_axis',(-0.610638773434788,0.0650981728612344,0.789229064510543));
#11066=DIRECTION('center_axis',(-0.106006004448151,-0.994365489657067,-9.53019194070163E-17));
#11067=DIRECTION('ref_axis',(0.610638773434775,-0.0650981728612332,-0.789229064510553));
#11068=DIRECTION('center_axis',(-0.106006004448151,-0.994365489657067,-9.53019194070163E-17));
#11069=DIRECTION('ref_axis',(0.610638773434775,-0.0650981728612332,-0.789229064510553));
#11070=DIRECTION('center_axis',(-0.106006004448151,-0.994365489657067,-9.53019194070163E-17));
#11071=DIRECTION('ref_axis',(0.411112091514325,-0.0438272955518462,0.910530623524178));
#11072=DIRECTION('center_axis',(-0.106006004448151,-0.994365489657067,-9.53019194070163E-17));
#11073=DIRECTION('ref_axis',(0.182489463977752,-0.0194545960528438,0.983015317393139));
#11074=DIRECTION('center_axis',(-0.106006004448151,-0.994365489657067,-9.53019194070163E-17));
#11075=DIRECTION('ref_axis',(-0.0567387878830537,0.00604873385417662,0.998370734130525));
#11076=DIRECTION('center_axis',(-0.106006004448151,-0.994365489657067,-9.53019194070163E-17));
#11077=DIRECTION('ref_axis',(-0.292669587629176,0.0312005333358429,0.955704472730209));
#11078=DIRECTION('center_axis',(-0.106006004448151,-0.994365489657067,-9.53019194070163E-17));
#11079=DIRECTION('ref_axis',(-0.511591494752952,0.0545390712293536,0.857496141219236));
#11080=DIRECTION('center_axis',(-0.106006004448151,-0.994365489657067,-9.53019194070163E-17));
#11081=DIRECTION('ref_axis',(-0.700781563761136,0.0747079965444751,0.709453250852237));
#11082=DIRECTION('center_axis',(-0.106006004448151,-0.994365489657067,-9.53019194070163E-17));
#11083=DIRECTION('ref_axis',(-0.849244755520856,0.0905351646529493,0.520179516303349));
#11084=DIRECTION('center_axis',(-0.106006004448151,-0.994365489657067,-9.53019194070163E-17));
#11085=DIRECTION('ref_axis',(-0.948352928968786,0.101100758073727,0.300674839042517));
#11086=DIRECTION('center_axis',(-0.106006004448151,-0.994365489657067,-9.53019194070163E-17));
#11087=DIRECTION('ref_axis',(-0.992346277307685,0.105790742921563,0.0636960330451088));
#11088=DIRECTION('center_axis',(-0.106006004448151,-0.994365489657067,-9.53019194070163E-17));
#11089=DIRECTION('ref_axis',(-0.978668067041421,0.104332554324503,-0.176984554867181));
#11090=DIRECTION('center_axis',(-0.106006004448151,-0.994365489657067,-9.53019194070163E-17));
#11091=DIRECTION('ref_axis',(0.610638773434775,-0.0650981728612332,-0.789229064510553));
#11092=DIRECTION('center_axis',(-0.106006004448151,-0.994365489657067,-9.53019194070163E-17));
#11093=DIRECTION('ref_axis',(0.610638773434775,-0.0650981728612332,-0.789229064510553));
#11094=DIRECTION('center_axis',(-0.106006004448151,-0.994365489657067,-9.53019194070163E-17));
#11095=DIRECTION('ref_axis',(0.610638773434775,-0.0650981728612332,-0.789229064510553));
#11096=DIRECTION('center_axis',(-0.106006004448151,-0.994365489657067,-9.53019194070163E-17));
#11097=DIRECTION('ref_axis',(0.610638773434775,-0.0650981728612332,-0.789229064510553));
#11098=DIRECTION('center_axis',(0.106006004448151,0.994365489657067,8.32667268468867E-17));
#11099=DIRECTION('ref_axis',(-0.610638773434788,0.0650981728612344,0.789229064510543));
#32342=CARTESIAN_POINT('',(0.,0.,0.));
#32343=CARTESIAN_POINT('Origin',(-54.1598171290174,-67.5719248685924,175.985485069079));
#32344=CARTESIAN_POINT('',(-58.6617595746854,-127.180557396019,173.617797875548));
#32345=CARTESIAN_POINT('',(-58.6882610756022,-127.4291487666,173.617797875548));
#32346=CARTESIAN_POINT('',(-52.327900808713,-67.7672193871761,173.617797875548));
#32347=CARTESIAN_POINT('',(-57.5665324870377,-127.548732528291,176.406000729816));
#32348=CARTESIAN_POINT('Ctrl Pts',(-58.6617595746854,-127.180557396019,
173.617797875548));
#32349=CARTESIAN_POINT('Ctrl Pts',(-58.6326690473956,-127.186500029427,
173.640795835577));
#32350=CARTESIAN_POINT('Ctrl Pts',(-58.6039904583882,-127.192422600679,
173.664361934959));
#32351=CARTESIAN_POINT('Ctrl Pts',(-58.2740033449536,-127.261332757946,
173.946159765466));
#32352=CARTESIAN_POINT('Ctrl Pts',(-58.0269221360586,-127.320492066776,
174.262621377601));
#32353=CARTESIAN_POINT('Ctrl Pts',(-57.7119058734233,-127.412252654383,
174.89391038891));
#32354=CARTESIAN_POINT('Ctrl Pts',(-57.6177265345925,-127.447299103863,
175.18881819412));
#32355=CARTESIAN_POINT('Ctrl Pts',(-57.5224623503741,-127.504840915964,
175.795216859615));
#32356=CARTESIAN_POINT('Ctrl Pts',(-57.5212432809128,-127.528630260883,
176.102947888732));
#32357=CARTESIAN_POINT('Ctrl Pts',(-57.5665324870377,-127.548732528291,
176.406000729816));
#32358=CARTESIAN_POINT('Origin',(-60.5201773959065,-127.233854248016,175.985485069079));
#32359=CARTESIAN_POINT('Origin',(-54.1598171290174,-67.5719248685924,175.985485069079));
#32360=CARTESIAN_POINT('',(-58.502750568013,-125.689009161534,173.617797875548));
#32361=CARTESIAN_POINT('',(-58.5557535702374,-126.186191906362,173.617797875548));
#32362=CARTESIAN_POINT('',(-52.327900808713,-67.7672193871761,173.617797875548));
#32363=CARTESIAN_POINT('Ctrl Pts',(-58.5027505680128,-125.689009161534,
173.617797875548));
#32364=CARTESIAN_POINT('Ctrl Pts',(-58.4595554649872,-125.697833087609,
173.651946423045));
#32365=CARTESIAN_POINT('Ctrl Pts',(-58.417273020125,-125.706611876126,173.687344073633));
#32366=CARTESIAN_POINT('Ctrl Pts',(-58.0794854284382,-125.777931854482,
173.986693413553));
#32367=CARTESIAN_POINT('Ctrl Pts',(-57.8384992972673,-125.83646832066,174.307014661379));
#32368=CARTESIAN_POINT('Ctrl Pts',(-57.5019070438409,-125.936707051767,
175.012129922775));
#32369=CARTESIAN_POINT('Ctrl Pts',(-57.4044285699384,-125.97699712051,175.387614488075));
#32370=CARTESIAN_POINT('Ctrl Pts',(-57.3552475654393,-126.043039273718,
176.170863951934));
#32371=CARTESIAN_POINT('Ctrl Pts',(-57.4100194773212,-126.070042537833,
176.571447096641));
#32372=CARTESIAN_POINT('Ctrl Pts',(-57.6678719428223,-126.10693250791,177.315038171398));
#32373=CARTESIAN_POINT('Ctrl Pts',(-57.863027119267,-126.116088231247,177.652655147584));
#32374=CARTESIAN_POINT('Ctrl Pts',(-58.3793944921056,-126.121793925087,
178.247476301394));
#32375=CARTESIAN_POINT('Ctrl Pts',(-58.7002502206311,-126.120427424016,
178.495125960072));
#32376=CARTESIAN_POINT('Ctrl Pts',(-59.4066692402747,-126.109518767417,
178.844220731714));
#32377=CARTESIAN_POINT('Ctrl Pts',(-59.7827741197176,-126.099444134848,
178.947364493277));
#32378=CARTESIAN_POINT('Ctrl Pts',(-60.5679966693245,-126.076445160719,
179.007265954424));
#32379=CARTESIAN_POINT('Ctrl Pts',(-60.970235802468,-126.066399187525,178.957633872364));
#32380=CARTESIAN_POINT('Ctrl Pts',(-61.7179203138936,-126.051111545171,
178.708683533434));
#32381=CARTESIAN_POINT('Ctrl Pts',(-62.0578100965788,-126.044955448698,
178.517184058802));
#32382=CARTESIAN_POINT('Ctrl Pts',(-62.6583156091933,-126.041607882016,
178.007011011933));
#32383=CARTESIAN_POINT('Ctrl Pts',(-62.9096366389285,-126.047647349706,
177.688832858095));
#32384=CARTESIAN_POINT('Ctrl Pts',(-63.2669005850962,-126.074000042545,
176.98660161232));
#32385=CARTESIAN_POINT('Ctrl Pts',(-63.374361600946,-126.09267780599,176.611931574081));
#32386=CARTESIAN_POINT('Ctrl Pts',(-63.4438548314579,-126.145901209017,
175.828715776295));
#32387=CARTESIAN_POINT('Ctrl Pts',(-63.3997074250098,-126.18343619045,175.427281602623));
#32388=CARTESIAN_POINT('Ctrl Pts',(-63.1620897079078,-126.273224914735,
174.680859755401));
#32389=CARTESIAN_POINT('Ctrl Pts',(-62.9762532016153,-126.323223172721,
174.341333810424));
#32390=CARTESIAN_POINT('Ctrl Pts',(-62.4777155464864,-126.436966076225,
173.741502520989));
#32391=CARTESIAN_POINT('Ctrl Pts',(-62.1656928930358,-126.503055012754,
173.490806570389));
#32392=CARTESIAN_POINT('Ctrl Pts',(-61.4754256817193,-126.641115717402,
173.135363563321));
#32393=CARTESIAN_POINT('Ctrl Pts',(-61.106392475604,-126.710694606539,173.02895052633));
#32394=CARTESIAN_POINT('Ctrl Pts',(-60.3339981872262,-126.853598092212,
172.962334470896));
#32395=CARTESIAN_POINT('Ctrl Pts',(-59.9379422145433,-126.928642280698,
173.008654345021));
#32396=CARTESIAN_POINT('Ctrl Pts',(-59.2365162427146,-127.064829731118,
173.240052707569));
#32397=CARTESIAN_POINT('Ctrl Pts',(-58.9317136446724,-127.125410988432,
173.404381568257));
#32398=CARTESIAN_POINT('Ctrl Pts',(-58.6617595746854,-127.180557396019,
173.617797875548));
#32399=CARTESIAN_POINT('',(-61.6514014972539,-127.113258201155,173.209554841928));
#32400=CARTESIAN_POINT('Origin',(-60.5201773959065,-127.233854248016,175.985485069079));
#32401=CARTESIAN_POINT('Ctrl Pts',(-61.6514014972539,-127.113258201155,
173.209554841928));
#32402=CARTESIAN_POINT('Ctrl Pts',(-61.8857214195736,-127.067339449921,
173.307037826472));
#32403=CARTESIAN_POINT('Ctrl Pts',(-62.1065768825577,-127.022596527121,
173.434691800361));
#32404=CARTESIAN_POINT('Ctrl Pts',(-62.5071713663279,-126.938362080585,
173.741517658033));
#32405=CARTESIAN_POINT('Ctrl Pts',(-62.6859638108831,-126.899124933691,
173.918611232754));
#32406=CARTESIAN_POINT('Ctrl Pts',(-63.0767849285755,-126.808742110419,
174.418572728908));
#32407=CARTESIAN_POINT('Ctrl Pts',(-63.2526273897065,-126.758947602762,
174.76445318312));
#32408=CARTESIAN_POINT('Ctrl Pts',(-63.4679041817175,-126.671297722053,
175.52011789156));
#32409=CARTESIAN_POINT('Ctrl Pts',(-63.499642584004,-126.635152404933,175.924144803172));
#32410=CARTESIAN_POINT('Ctrl Pts',(-63.4051176552899,-126.585177337171,
176.706982606558));
#32411=CARTESIAN_POINT('Ctrl Pts',(-63.285302376919,-126.566901940954,177.078928358304));
#32412=CARTESIAN_POINT('Ctrl Pts',(-62.9042041225712,-126.542829629636,
177.771200206437));
#32413=CARTESIAN_POINT('Ctrl Pts',(-62.6415548816703,-126.538068000193,
178.081915888432));
#32414=CARTESIAN_POINT('Ctrl Pts',(-62.0224310979412,-126.54401866178,178.572749615368));
#32415=CARTESIAN_POINT('Ctrl Pts',(-61.6752270239872,-126.549984453082,
178.752880269944));
#32416=CARTESIAN_POINT('Ctrl Pts',(-60.9170006011623,-126.566116529594,
178.976236545733));
#32417=CARTESIAN_POINT('Ctrl Pts',(-60.5117969159758,-126.576552154303,
179.011628322045));
#32418=CARTESIAN_POINT('Ctrl Pts',(-59.7270399804243,-126.600160402056,
178.922934828744));
#32419=CARTESIAN_POINT('Ctrl Pts',(-59.3539170563406,-126.608889340411,
178.805732529249));
#32420=CARTESIAN_POINT('Ctrl Pts',(-58.6587254122993,-126.61830149431,178.42933450653));
#32421=CARTESIAN_POINT('Ctrl Pts',(-58.3463067253257,-126.618845616172,
178.168670455854));
#32422=CARTESIAN_POINT('Ctrl Pts',(-57.8519076813661,-126.611499757347,
177.552405199745));
#32423=CARTESIAN_POINT('Ctrl Pts',(-57.6695186672383,-126.599895212944,
177.206525382876));
#32424=CARTESIAN_POINT('Ctrl Pts',(-57.4405997529608,-126.559599585113,
176.45086158733));
#32425=CARTESIAN_POINT('Ctrl Pts',(-57.4019533413936,-126.53095775106,176.046834917067));
#32426=CARTESIAN_POINT('Ctrl Pts',(-57.4838157207256,-126.462178557917,
175.263997055208));
#32427=CARTESIAN_POINT('Ctrl Pts',(-57.5970842070223,-126.419054977016,
174.892051029029));
#32428=CARTESIAN_POINT('Ctrl Pts',(-57.9645401889828,-126.315181807793,
174.19977815377));
#32429=CARTESIAN_POINT('Ctrl Pts',(-58.220281537424,-126.255156269262,173.889061697831));
#32430=CARTESIAN_POINT('Ctrl Pts',(-58.5381763977807,-126.189788457904,
173.63177570516));
#32431=CARTESIAN_POINT('Ctrl Pts',(-58.5469462268658,-126.187991076671,
173.624760655177));
#32432=CARTESIAN_POINT('Ctrl Pts',(-58.5557535702374,-126.186191906362,
173.617797875548));
#32433=CARTESIAN_POINT('Origin',(-54.1598171290174,-67.5719248685924,175.985485069079));
#32434=CARTESIAN_POINT('',(-58.3437415613406,-124.197460927048,173.617797875548));
#32435=CARTESIAN_POINT('',(-58.3967445635652,-124.694643671877,173.617797875548));
#32436=CARTESIAN_POINT('',(-52.327900808713,-67.7672193871761,173.617797875548));
#32437=CARTESIAN_POINT('Ctrl Pts',(-58.34374156134,-124.197460927048,173.617797875549));
#32438=CARTESIAN_POINT('Ctrl Pts',(-58.278717133321,-124.210744163011,173.669203928853));
#32439=CARTESIAN_POINT('Ctrl Pts',(-58.2157774981849,-124.223921711853,
173.72342734048));
#32440=CARTESIAN_POINT('Ctrl Pts',(-57.86693839971,-124.29887647475,174.05071991815));
#32441=CARTESIAN_POINT('Ctrl Pts',(-57.6354963747508,-124.356416599752,
174.3767912935));
#32442=CARTESIAN_POINT('Ctrl Pts',(-57.3185687959958,-124.454312505303,
175.089710227681));
#32443=CARTESIAN_POINT('Ctrl Pts',(-57.231181633938,-124.492963368992,175.467464387374));
#32444=CARTESIAN_POINT('Ctrl Pts',(-57.2029760494815,-124.557220016337,
176.25061306551));
#32445=CARTESIAN_POINT('Ctrl Pts',(-57.2680216060115,-124.583151041461,
176.648644116405));
#32446=CARTESIAN_POINT('Ctrl Pts',(-57.5443231429321,-124.617842409801,
177.384195000057));
#32447=CARTESIAN_POINT('Ctrl Pts',(-57.7477568818853,-124.625564489675,
177.716476460062));
#32448=CARTESIAN_POINT('Ctrl Pts',(-58.2781818661706,-124.630202209204,
178.297117940058));
#32449=CARTESIAN_POINT('Ctrl Pts',(-58.604261517692,-124.628303276316,178.536132441238));
#32450=CARTESIAN_POINT('Ctrl Pts',(-59.3177217901214,-124.616426130427,
178.867360173637));
#32451=CARTESIAN_POINT('Ctrl Pts',(-59.6958031886026,-124.605603623277,
178.961296587042));
#32452=CARTESIAN_POINT('Ctrl Pts',(-60.4810402787824,-124.583014024349,
179.002234079384));
#32453=CARTESIAN_POINT('Ctrl Pts',(-60.8810526741571,-124.573231018561,
178.943280655469));
#32454=CARTESIAN_POINT('Ctrl Pts',(-61.6215604887575,-124.558503910591,
178.677569971472));
#32455=CARTESIAN_POINT('Ctrl Pts',(-61.9566204442423,-124.552340819203,
178.47852898906));
#32456=CARTESIAN_POINT('Ctrl Pts',(-62.5445331674686,-124.550727218005,
177.955650796022));
#32457=CARTESIAN_POINT('Ctrl Pts',(-62.7881669620093,-124.557612561274,
177.632707660284));
#32458=CARTESIAN_POINT('Ctrl Pts',(-63.1294599313677,-124.585475952162,
176.924046814847));
#32459=CARTESIAN_POINT('Ctrl Pts',(-63.2286500430818,-124.604529935403,
176.547543416596));
#32460=CARTESIAN_POINT('Ctrl Pts',(-63.2812732486243,-124.659924223454,
175.764303698241));
#32461=CARTESIAN_POINT('Ctrl Pts',(-63.2288064432854,-124.698372966086,
175.364833513626));
#32462=CARTESIAN_POINT('Ctrl Pts',(-62.9762088974864,-124.789578710455,
174.624824536462));
#32463=CARTESIAN_POINT('Ctrl Pts',(-62.7836064185933,-124.839809985127,
174.289599988599));
#32464=CARTESIAN_POINT('Ctrl Pts',(-62.2737713821488,-124.955111065801,
173.701104946398));
#32465=CARTESIAN_POINT('Ctrl Pts',(-61.9574763394134,-125.021682562797,
173.457305591578));
#32466=CARTESIAN_POINT('Ctrl Pts',(-61.2614358576456,-125.160190156705,
173.11620009463));
#32467=CARTESIAN_POINT('Ctrl Pts',(-60.8907253797158,-125.229477448949,
173.017172068597));
#32468=CARTESIAN_POINT('Ctrl Pts',(-60.1183056212707,-125.372719312397,
172.965738372967));
#32469=CARTESIAN_POINT('Ctrl Pts',(-59.7239590747349,-125.447608374899,
173.019538943988));
#32470=CARTESIAN_POINT('Ctrl Pts',(-59.0449242978319,-125.579760897032,
173.257771910224));
#32471=CARTESIAN_POINT('Ctrl Pts',(-58.7581639442399,-125.636833137111,
173.41587693548));
#32472=CARTESIAN_POINT('Ctrl Pts',(-58.5027505680127,-125.689009161534,
173.617797875548));
#32473=CARTESIAN_POINT('Ctrl Pts',(-58.5557535702374,-126.186191906362,
173.617797875548));
#32474=CARTESIAN_POINT('Ctrl Pts',(-58.8468157571489,-126.12673351778,173.387694224487));
#32475=CARTESIAN_POINT('Ctrl Pts',(-59.1781285607066,-126.061010728778,
173.21487622303));
#32476=CARTESIAN_POINT('Ctrl Pts',(-59.9119867119162,-125.91900878874,172.994735293252));
#32477=CARTESIAN_POINT('Ctrl Pts',(-60.31028336115,-125.843785900072,172.959342060538));
#32478=CARTESIAN_POINT('Ctrl Pts',(-61.0823803308402,-125.701423051036,
173.048032618572));
#32479=CARTESIAN_POINT('Ctrl Pts',(-61.4489580270192,-125.631295079213,
173.165233479167));
#32480=CARTESIAN_POINT('Ctrl Pts',(-62.1305109850442,-125.493937089217,
173.541628707431));
#32481=CARTESIAN_POINT('Ctrl Pts',(-62.4360238034073,-125.42860557392,173.80229143814));
#32482=CARTESIAN_POINT('Ctrl Pts',(-62.9177650813467,-125.31719656074,174.418554513344));
#32483=CARTESIAN_POINT('Ctrl Pts',(-63.0936098866123,-125.267402024571,
174.764433477334));
#32484=CARTESIAN_POINT('Ctrl Pts',(-63.3088919467895,-125.179751635932,
175.520096051261));
#32485=CARTESIAN_POINT('Ctrl Pts',(-63.3406332741939,-125.143605987515,
175.924122398547));
#32486=CARTESIAN_POINT('Ctrl Pts',(-63.2461142301944,-125.093630152303,
176.706960338648));
#32487=CARTESIAN_POINT('Ctrl Pts',(-63.1263018689129,-125.075354683216,
177.078906732069));
#32488=CARTESIAN_POINT('Ctrl Pts',(-62.7452092371237,-125.051281830243,
177.771180981795));
#32489=CARTESIAN_POINT('Ctrl Pts',(-62.482562646969,-125.046519897283,178.081898473403));
#32490=CARTESIAN_POINT('Ctrl Pts',(-61.8634432306732,-125.052469942589,
178.572736816437));
#32491=CARTESIAN_POINT('Ctrl Pts',(-61.5162408978839,-125.058435804369,
178.752870170917));
#32492=CARTESIAN_POINT('Ctrl Pts',(-60.7580169368939,-125.074567680543,
178.976232568843));
#32493=CARTESIAN_POINT('Ctrl Pts',(-60.352813898473,-125.085003213792,179.011627750477));
#32494=CARTESIAN_POINT('Ctrl Pts',(-59.5680567885864,-125.108611318063,
178.922941120341));
#32495=CARTESIAN_POINT('Ctrl Pts',(-59.1949331554322,-125.117340607453,
178.805742185244));
#32496=CARTESIAN_POINT('Ctrl Pts',(-58.4997387559432,-125.126753121904,
178.429350696446));
#32497=CARTESIAN_POINT('Ctrl Pts',(-58.1873179848685,-125.127297441734,
178.168689732086));
#32498=CARTESIAN_POINT('Ctrl Pts',(-57.6929136127509,-125.119951976616,
177.552429575312));
#32499=CARTESIAN_POINT('Ctrl Pts',(-57.5105215242164,-125.108348056214,
177.206551752621));
#32500=CARTESIAN_POINT('Ctrl Pts',(-57.2815955753712,-125.068053250165,
176.450890813437));
#32501=CARTESIAN_POINT('Ctrl Pts',(-57.2429452440014,-125.03941180795,176.046864898358));
#32502=CARTESIAN_POINT('Ctrl Pts',(-57.3247997090401,-124.970633271046,
175.26402685357));
#32503=CARTESIAN_POINT('Ctrl Pts',(-57.4380643589416,-124.927510417756,
174.892079968718));
#32504=CARTESIAN_POINT('Ctrl Pts',(-57.8055128332414,-124.823638126178,
174.199803879735));
#32505=CARTESIAN_POINT('Ctrl Pts',(-58.0612506286147,-124.763612938422,
173.88908500224));
#32506=CARTESIAN_POINT('Ctrl Pts',(-58.3791506952548,-124.698243645248,
173.63178906037));
#32507=CARTESIAN_POINT('Ctrl Pts',(-58.3879288364918,-124.696444554813,
173.624767283041));
#32508=CARTESIAN_POINT('Ctrl Pts',(-58.3967445635651,-124.694643671877,
173.617797875548));
#32509=CARTESIAN_POINT('Origin',(-54.1598171290174,-67.5719248685924,175.985485069079));
#32510=CARTESIAN_POINT('',(-58.1847325546685,-122.705912692563,173.617797875548));
#32511=CARTESIAN_POINT('',(-58.2377355568929,-123.203095437391,173.617797875548));
#32512=CARTESIAN_POINT('',(-52.327900808713,-67.7672193871761,173.617797875548));
#32513=CARTESIAN_POINT('Ctrl Pts',(-58.1847325546681,-122.705912692563,
173.617797875548));
#32514=CARTESIAN_POINT('Ctrl Pts',(-58.0888037581628,-122.72550909469,173.693635848704));
#32515=CARTESIAN_POINT('Ctrl Pts',(-57.9974675052454,-122.744864161319,
173.775561284347));
#32516=CARTESIAN_POINT('Ctrl Pts',(-57.635193264641,-122.824746707671,174.143923073571));
#32517=CARTESIAN_POINT('Ctrl Pts',(-57.4174742924988,-122.880811110816,
174.477660857283));
#32518=CARTESIAN_POINT('Ctrl Pts',(-57.1284820778,-122.975343264355,175.201169564384));
#32519=CARTESIAN_POINT('Ctrl Pts',(-57.0554958265115,-123.011890461818,
175.58217845336));
#32520=CARTESIAN_POINT('Ctrl Pts',(-57.0572909473777,-123.073553655012,
176.364680651823));
#32521=CARTESIAN_POINT('Ctrl Pts',(-57.1369028743213,-123.097925409945,
176.75859945057));
#32522=CARTESIAN_POINT('Ctrl Pts',(-57.4394283465603,-123.129454707669,
177.482254367609));
#32523=CARTESIAN_POINT('Ctrl Pts',(-57.6548410632274,-123.135320137726,
177.806852553459));
#32524=CARTESIAN_POINT('Ctrl Pts',(-58.2053009099689,-123.138409294449,
178.366627513958));
#32525=CARTESIAN_POINT('Ctrl Pts',(-58.5385649216933,-123.135743765666,
178.592913316506));
#32526=CARTESIAN_POINT('Ctrl Pts',(-59.2618597324605,-123.122470579587,
178.898109819127));
#32527=CARTESIAN_POINT('Ctrl Pts',(-59.6428651617749,-123.110749483957,
178.978602970774));
#32528=CARTESIAN_POINT('Ctrl Pts',(-60.4276995799954,-123.088771782396,
178.991737724848));
#32529=CARTESIAN_POINT('Ctrl Pts',(-60.8240557545849,-123.079382925796,
178.91922063596));
#32530=CARTESIAN_POINT('Ctrl Pts',(-61.5537076523256,-123.065483845327,
178.62907684617));
#32531=CARTESIAN_POINT('Ctrl Pts',(-61.8816641007378,-123.059487581138,
178.41888613984));
#32532=CARTESIAN_POINT('Ctrl Pts',(-62.4506266599793,-123.06044421288,177.877438877806));
#32533=CARTESIAN_POINT('Ctrl Pts',(-62.6826700572172,-123.068573995083,
177.547746392789));
#32534=CARTESIAN_POINT('Ctrl Pts',(-63.0001500560096,-123.098664511368,
176.829855484596));
#32535=CARTESIAN_POINT('Ctrl Pts',(-63.0870062275806,-123.118442728469,
176.450600259355));
#32536=CARTESIAN_POINT('Ctrl Pts',(-63.1143318720006,-123.177064485505,
175.667676176508));
#32537=CARTESIAN_POINT('Ctrl Pts',(-63.0494694161852,-123.216847380813,
175.271476563352));
#32538=CARTESIAN_POINT('Ctrl Pts',(-62.7745240797572,-123.310141261318,
174.541360502104));
#32539=CARTESIAN_POINT('Ctrl Pts',(-62.5717178576519,-123.360872587181,
174.212618504973));
#32540=CARTESIAN_POINT('Ctrl Pts',(-62.0449874310108,-123.4784856219,173.641525042349));
#32541=CARTESIAN_POINT('Ctrl Pts',(-61.7224759660809,-123.545735839993,
173.408333024239));
#32542=CARTESIAN_POINT('Ctrl Pts',(-61.0179373514153,-123.684871698295,
173.089054639054));
#32543=CARTESIAN_POINT('Ctrl Pts',(-60.644673418105,-123.753849182772,173.001283842222));
#32544=CARTESIAN_POINT('Ctrl Pts',(-59.8724994791847,-123.897555628781,
172.973083438963));
#32545=CARTESIAN_POINT('Ctrl Pts',(-59.4810335737413,-123.972156402458,
173.038266935018));
#32546=CARTESIAN_POINT('Ctrl Pts',(-58.8363428602948,-124.098087770071,
173.28551300444));
#32547=CARTESIAN_POINT('Ctrl Pts',(-58.5768781736677,-124.149835615648,
173.43348817094));
#32548=CARTESIAN_POINT('Ctrl Pts',(-58.34374156134,-124.197460927048,173.617797875549));
#32549=CARTESIAN_POINT('Ctrl Pts',(-58.3967445635652,-124.694643671877,
173.617797875548));
#32550=CARTESIAN_POINT('Ctrl Pts',(-58.6877979782988,-124.635187075281,
173.387701159466));
#32551=CARTESIAN_POINT('Ctrl Pts',(-59.0190996859056,-124.569466434783,
173.214886551717));
#32552=CARTESIAN_POINT('Ctrl Pts',(-59.7529443816364,-124.427466899675,
172.994740615175));
#32553=CARTESIAN_POINT('Ctrl Pts',(-60.1512401590161,-124.35224407383,172.959342825569));
#32554=CARTESIAN_POINT('Ctrl Pts',(-60.9233373162518,-124.20988098793,173.048024199532));
#32555=CARTESIAN_POINT('Ctrl Pts',(-61.2899160389894,-124.139753275246,
173.165220558003));
#32556=CARTESIAN_POINT('Ctrl Pts',(-61.9714727030833,-124.002394979554,
173.541607042789));
#32557=CARTESIAN_POINT('Ctrl Pts',(-62.2769883034669,-123.937063135279,
173.802265643482));
#32558=CARTESIAN_POINT('Ctrl Pts',(-62.75873666217,-123.82565313399,174.418521894913));
#32559=CARTESIAN_POINT('Ctrl Pts',(-62.9345856650678,-123.775858546739,
174.764398190367));
#32560=CARTESIAN_POINT('Ctrl Pts',(-63.1498771588972,-123.688207248561,
175.520056941991));
#32561=CARTESIAN_POINT('Ctrl Pts',(-63.1816237242831,-123.652061006897,
175.924082278689));
#32562=CARTESIAN_POINT('Ctrl Pts',(-63.0871152180042,-123.602083797421,
176.706920463546));
#32563=CARTESIAN_POINT('Ctrl Pts',(-62.9673080803201,-123.58380819782,177.078868006009));
#32564=CARTESIAN_POINT('Ctrl Pts',(-62.5862255167875,-123.559734374918,
177.77114655618));
#32565=CARTESIAN_POINT('Ctrl Pts',(-62.3235836733225,-123.554971898455,
178.081867288186));
#32566=CARTESIAN_POINT('Ctrl Pts',(-61.7044720777724,-123.560920840194,
178.572713897156));
#32567=CARTESIAN_POINT('Ctrl Pts',(-61.357272862849,-123.566886828148,178.7528520863));
#32568=CARTESIAN_POINT('Ctrl Pts',(-60.5990533102727,-123.583018345583,
178.976225446972));
#32569=CARTESIAN_POINT('Ctrl Pts',(-60.1938514300712,-123.593453715054,
179.011626726427));
#32570=CARTESIAN_POINT('Ctrl Pts',(-59.4090940080818,-123.617061562393,
178.922952386006));
#32571=CARTESIAN_POINT('Ctrl Pts',(-59.0359691052097,-123.625791480335,
178.805759475439));
#32572=CARTESIAN_POINT('Ctrl Pts',(-58.3407697716994,-123.635204640415,
178.429379686755));
#32573=CARTESIAN_POINT('Ctrl Pts',(-58.0283452687598,-123.63574931474,178.16872424901));
#32574=CARTESIAN_POINT('Ctrl Pts',(-57.5339313557417,-123.628404554622,
177.552473223514));
#32575=CARTESIAN_POINT('Ctrl Pts',(-57.3515337619774,-123.616801751553,
177.20659897172));
#32576=CARTESIAN_POINT('Ctrl Pts',(-57.122595216661,-123.57650841704,176.450943147388));
#32577=CARTESIAN_POINT('Ctrl Pts',(-57.083937866281,-123.547867676478,176.046918584679));
#32578=CARTESIAN_POINT('Ctrl Pts',(-57.1657781595267,-123.479090314682,
175.264080212427));
#32579=CARTESIAN_POINT('Ctrl Pts',(-57.2790359397733,-123.435968764243,
174.89213178999));
#32580=CARTESIAN_POINT('Ctrl Pts',(-57.6464709704613,-123.332098044232,
174.199849946451));
#32581=CARTESIAN_POINT('Ctrl Pts',(-57.9022024034783,-123.272073484604,
173.889126732894));
#32582=CARTESIAN_POINT('Ctrl Pts',(-58.2201117923249,-123.206701538053,
173.631812975112));
#32583=CARTESIAN_POINT('Ctrl Pts',(-58.2289048175451,-123.204899387046,
173.624779151223));
#32584=CARTESIAN_POINT('Ctrl Pts',(-58.237735556893,-123.203095437391,173.617797875548));
#32585=CARTESIAN_POINT('Origin',(-54.1598171290174,-67.5719248685924,175.985485069079));
#32586=CARTESIAN_POINT('',(-58.0257235479966,-121.214364458077,173.617797875548));
#32587=CARTESIAN_POINT('',(-58.0787265502207,-121.711547202905,173.617797875548));
#32588=CARTESIAN_POINT('',(-52.327900808713,-67.7672193871761,173.617797875548));
#32589=CARTESIAN_POINT('Ctrl Pts',(-58.0257235479965,-121.214364458077,
173.617797875548));
#32590=CARTESIAN_POINT('Ctrl Pts',(-57.8910902662336,-121.241867439718,
173.724234269834));
#32591=CARTESIAN_POINT('Ctrl Pts',(-57.7656471951412,-121.268865446389,
173.842545061126));
#32592=CARTESIAN_POINT('Ctrl Pts',(-57.3903884722706,-121.354511789475,
174.264562857379));
#32593=CARTESIAN_POINT('Ctrl Pts',(-57.1901588288744,-121.408625641651,
174.607097380125));
#32594=CARTESIAN_POINT('Ctrl Pts',(-56.9363076872888,-121.498868093884,
175.343114408043));
#32595=CARTESIAN_POINT('Ctrl Pts',(-56.8815900839742,-121.533146279122,
175.728280734596));
#32596=CARTESIAN_POINT('Ctrl Pts',(-56.9214577980342,-121.591449874668,
176.509097195586));
#32597=CARTESIAN_POINT('Ctrl Pts',(-57.0192951420369,-121.613803657037,
176.89702240998));
#32598=CARTESIAN_POINT('Ctrl Pts',(-57.3548253195761,-121.641290023581,
177.604904883751));
#32599=CARTESIAN_POINT('Ctrl Pts',(-57.5857160543015,-121.645137650408,
177.919643118704));
#32600=CARTESIAN_POINT('Ctrl Pts',(-58.1614516226242,-121.646225356556,
178.451906240832));
#32601=CARTESIAN_POINT('Ctrl Pts',(-58.503295822017,-121.642580716861,178.661411828903));
#32602=CARTESIAN_POINT('Ctrl Pts',(-59.2386444508246,-121.627517586945,
178.932744590103));
#32603=CARTESIAN_POINT('Ctrl Pts',(-59.6235445743797,-121.614971454751,
178.995662154724));
#32604=CARTESIAN_POINT('Ctrl Pts',(-60.4070754139044,-121.593817885247,
178.972324662672));
#32605=CARTESIAN_POINT('Ctrl Pts',(-60.7979355978628,-121.584960646956,
178.882235457376));
#32606=CARTESIAN_POINT('Ctrl Pts',(-61.5127413959487,-121.57215913929,178.560288614066));
#32607=CARTESIAN_POINT('Ctrl Pts',(-61.8313235414465,-121.566714699417,
178.335269783198));
#32608=CARTESIAN_POINT('Ctrl Pts',(-62.3745155498307,-121.57109409288,177.769590456732));
#32609=CARTESIAN_POINT('Ctrl Pts',(-62.5907877898474,-121.580860453187,
177.431512229467));
#32610=CARTESIAN_POINT('Ctrl Pts',(-62.8762946514684,-121.613894393029,
176.701887873391));
#32611=CARTESIAN_POINT('Ctrl Pts',(-62.9465577724403,-121.634960807152,
176.318893024691));
#32612=CARTESIAN_POINT('Ctrl Pts',(-62.9396479590941,-121.697896378297,
175.537075933605));
#32613=CARTESIAN_POINT('Ctrl Pts',(-62.8581926713311,-121.73941240673,175.145919171686));
#32614=CARTESIAN_POINT('Ctrl Pts',(-62.553222792541,-121.835462033537,174.429720497847));
#32615=CARTESIAN_POINT('Ctrl Pts',(-62.3364713059894,-121.887170647192,
174.109825587998));
#32616=CARTESIAN_POINT('Ctrl Pts',(-61.7869816303679,-122.007861169625,
173.563074998768));
#32617=CARTESIAN_POINT('Ctrl Pts',(-61.4564544944988,-122.075938466264,
173.344736476158));
#32618=CARTESIAN_POINT('Ctrl Pts',(-60.7407356703104,-122.215841139421,
173.055634861287));
#32619=CARTESIAN_POINT('Ctrl Pts',(-60.3639329205162,-122.284662414731,
172.983479930204));
#32620=CARTESIAN_POINT('Ctrl Pts',(-59.592681777914,-122.428907413695,172.987637390073));
#32621=CARTESIAN_POINT('Ctrl Pts',(-59.2057579301147,-122.50300420502,173.068519815426));
#32622=CARTESIAN_POINT('Ctrl Pts',(-58.6089227159464,-122.620202316533,
173.325384475355));
#32623=CARTESIAN_POINT('Ctrl Pts',(-58.3868146007374,-122.664631229834,
173.458038831931));
#32624=CARTESIAN_POINT('Ctrl Pts',(-58.1847325546681,-122.705912692563,
173.617797875548));
#32625=CARTESIAN_POINT('Ctrl Pts',(-58.237735556893,-123.203095437391,173.617797875548));
#32626=CARTESIAN_POINT('Ctrl Pts',(-58.5287732638245,-123.143642049596,
173.387713577509));
#32627=CARTESIAN_POINT('Ctrl Pts',(-58.8600551027551,-123.077925256269,
173.214905046944));
#32628=CARTESIAN_POINT('Ctrl Pts',(-59.5938757045305,-122.935930027545,
172.994750145778));
#32629=CARTESIAN_POINT('Ctrl Pts',(-59.9921699206112,-122.86070731422,172.959344196458));
#32630=CARTESIAN_POINT('Ctrl Pts',(-60.7642674135403,-122.718343804205,
173.04800912509));
#32631=CARTESIAN_POINT('Ctrl Pts',(-61.1308479744597,-122.64821655548,173.165197421926));
#32632=CARTESIAN_POINT('Ctrl Pts',(-61.8124112746046,-122.510857712428,
173.541568250379));
#32633=CARTESIAN_POINT('Ctrl Pts',(-62.1179318564219,-122.445525279102,
173.802219455678));
#32634=CARTESIAN_POINT('Ctrl Pts',(-62.5996928940023,-122.334113508502,
174.418463488186));
#32635=CARTESIAN_POINT('Ctrl Pts',(-62.7755494132449,-122.284318829716,
174.764335005319));
#32636=CARTESIAN_POINT('Ctrl Pts',(-62.9908577990156,-122.196665902924,
175.519986912537));
#32637=CARTESIAN_POINT('Ctrl Pts',(-63.0226137435619,-122.160518599003,
175.924010439495));
#32638=CARTESIAN_POINT('Ctrl Pts',(-62.9281241062413,-122.110538928769,
176.706849062437));
#32639=CARTESIAN_POINT('Ctrl Pts',(-62.8083263219376,-122.092263095387,
177.078798662381));
#32640=CARTESIAN_POINT('Ctrl Pts',(-62.4272617866629,-122.06818753574,177.771084912746));
#32641=CARTESIAN_POINT('Ctrl Pts',(-62.164628442723,-122.063424086087,178.081811446834));
#32642=CARTESIAN_POINT('Ctrl Pts',(-61.5455308511229,-122.069371051784,
178.572672856614));
#32643=CARTESIAN_POINT('Ctrl Pts',(-61.1983372190016,-122.075337265567,
178.752819702656));
#32644=CARTESIAN_POINT('Ctrl Pts',(-60.440125560244,-122.091468140645,178.976212692936));
#32645=CARTESIAN_POINT('Ctrl Pts',(-60.0349257541581,-122.101903216854,
179.011624891001));
#32646=CARTESIAN_POINT('Ctrl Pts',(-59.2501677735642,-122.12551060413,178.922972556315));
#32647=CARTESIAN_POINT('Ctrl Pts',(-58.8770405971546,-122.134241647429,
178.805790433108));
#32648=CARTESIAN_POINT('Ctrl Pts',(-58.1818324291849,-122.143655963546,
178.429431594332));
#32649=CARTESIAN_POINT('Ctrl Pts',(-57.8694012443158,-122.144201272616,
178.168786052508));
#32650=CARTESIAN_POINT('Ctrl Pts',(-57.3749702478911,-122.136857774846,
177.552551377356));
#32651=CARTESIAN_POINT('Ctrl Pts',(-57.1925627966907,-122.125256972299,
177.206683519448));
#32652=CARTESIAN_POINT('Ctrl Pts',(-56.9636016969033,-122.084966272651,
176.451036853763));
#32653=CARTESIAN_POINT('Ctrl Pts',(-56.9249317787034,-122.056326788452,
176.047014712842));
#32654=CARTESIAN_POINT('Ctrl Pts',(-57.0067466966813,-121.987551530768,
175.264175754574));
#32655=CARTESIAN_POINT('Ctrl Pts',(-57.1199921765401,-121.944432312985,
174.892224579027));
#32656=CARTESIAN_POINT('Ctrl Pts',(-57.4874031359341,-121.840564406947,
174.199932432095));
#32657=CARTESIAN_POINT('Ctrl Pts',(-57.7431231767648,-121.780540972055,
173.889201454985));
#32658=CARTESIAN_POINT('Ctrl Pts',(-58.061049255969,-121.715164274657,173.631855795998));
#32659=CARTESIAN_POINT('Ctrl Pts',(-58.0698689309023,-121.71335664362,173.624800401594));
#32660=CARTESIAN_POINT('Ctrl Pts',(-58.0787265502207,-121.711547202905,
173.617797875548));
#32661=CARTESIAN_POINT('Origin',(-54.1598171290174,-67.5719248685924,175.985485069079));
#32662=CARTESIAN_POINT('',(-57.8667145413245,-119.722816223591,173.617797875548));
#32663=CARTESIAN_POINT('',(-57.9197175435485,-120.21999896842,173.617797875548));
#32664=CARTESIAN_POINT('',(-52.327900808713,-67.7672193871761,173.617797875548));
#32665=CARTESIAN_POINT('Ctrl Pts',(-57.8667145413246,-119.722816223591,
173.617797875548));
#32666=CARTESIAN_POINT('Ctrl Pts',(-57.6914471639414,-119.758619966911,
173.756358173866));
#32667=CARTESIAN_POINT('Ctrl Pts',(-57.532019262434,-119.793513567425,173.914828966194));
#32668=CARTESIAN_POINT('Ctrl Pts',(-57.1465332178751,-119.884996020418,
174.397186504441));
#32669=CARTESIAN_POINT('Ctrl Pts',(-56.9642747443631,-119.937213881699,
174.750270474763));
#32670=CARTESIAN_POINT('Ctrl Pts',(-56.7491012600445,-120.022682791733,
175.499327684857));
#32671=CARTESIAN_POINT('Ctrl Pts',(-56.7145927550832,-120.054810410505,
175.886962757056));
#32672=CARTESIAN_POINT('Ctrl Pts',(-56.7952337262314,-120.10941431512,176.664685479809));
#32673=CARTESIAN_POINT('Ctrl Pts',(-56.9130994766506,-120.129621476025,
177.046922740441));
#32674=CARTESIAN_POINT('Ctrl Pts',(-57.2850225644234,-120.152590512418,
177.736662194168));
#32675=CARTESIAN_POINT('Ctrl Pts',(-57.5322239088185,-120.154674458871,
178.039183324876));
#32676=CARTESIAN_POINT('Ctrl Pts',(-58.1347931906971,-120.153559985664,
178.540318042894));
#32677=CARTESIAN_POINT('Ctrl Pts',(-58.4864450863061,-120.148827001235,
178.731408524917));
#32678=CARTESIAN_POINT('Ctrl Pts',(-59.2347724041748,-120.13175680159,178.964298242534));
#32679=CARTESIAN_POINT('Ctrl Pts',(-59.623093824967,-120.11879287224,179.007120014528));
#32680=CARTESIAN_POINT('Ctrl Pts',(-60.403856401275,-120.098602649356,178.942741236308));
#32681=CARTESIAN_POINT('Ctrl Pts',(-60.7883583544615,-120.09034912906,178.832846215453));
#32682=CARTESIAN_POINT('Ctrl Pts',(-61.4855725740688,-120.078815064133,
178.474746987524));
#32683=CARTESIAN_POINT('Ctrl Pts',(-61.7929159484235,-120.074488583628,
178.232888600283));
#32684=CARTESIAN_POINT('Ctrl Pts',(-62.3054851758825,-120.082808761327,
177.640193174294));
#32685=CARTESIAN_POINT('Ctrl Pts',(-62.5032680503643,-120.094440744594,
177.293029773678));
#32686=CARTESIAN_POINT('Ctrl Pts',(-62.7514324671375,-120.130869850592,
176.550300113879));
#32687=CARTESIAN_POINT('Ctrl Pts',(-62.8021576249081,-120.153918370995,
176.162849262917));
#32688=CARTESIAN_POINT('Ctrl Pts',(-62.7547694302776,-120.221872828282,
175.383368750423));
#32689=CARTESIAN_POINT('Ctrl Pts',(-62.6540228035417,-120.265324439071,
174.999075580255));
#32690=CARTESIAN_POINT('Ctrl Pts',(-62.3138754992907,-120.364527975419,
174.300125140517));
#32691=CARTESIAN_POINT('Ctrl Pts',(-62.0803823928511,-120.417860930305,
173.990833581451));
#32692=CARTESIAN_POINT('Ctrl Pts',(-61.5041786598013,-120.542104915372,
173.474093635012));
#32693=CARTESIAN_POINT('Ctrl Pts',(-61.1648286858917,-120.611013630438,
173.274035009477));
#32694=CARTESIAN_POINT('Ctrl Pts',(-60.4364022663505,-120.751691527133,
173.021589071245));
#32695=CARTESIAN_POINT('Ctrl Pts',(-60.0552761315911,-120.820756285235,
172.968535643119));
#32696=CARTESIAN_POINT('Ctrl Pts',(-59.2860945509954,-120.965486127467,
173.012361011038));
#32697=CARTESIAN_POINT('Ctrl Pts',(-58.9055699766426,-121.0388032346,173.112192942474));
#32698=CARTESIAN_POINT('Ctrl Pts',(-58.3671317600356,-121.145242801056,
173.376173693532));
#32699=CARTESIAN_POINT('Ctrl Pts',(-58.1897246329056,-121.18086220092,173.488144316575));
#32700=CARTESIAN_POINT('Ctrl Pts',(-58.0257235479965,-121.214364458077,
173.617797875548));
#32701=CARTESIAN_POINT('Ctrl Pts',(-58.0787265502207,-121.711547202905,
173.617797875548));
#32702=CARTESIAN_POINT('Ctrl Pts',(-58.3697361321289,-121.65209956051,173.387735812175));
#32703=CARTESIAN_POINT('Ctrl Pts',(-58.7009823964628,-121.586389655514,
173.214938163782));
#32704=CARTESIAN_POINT('Ctrl Pts',(-59.4347598575272,-121.444402137507,
172.994767213526));
#32705=CARTESIAN_POINT('Ctrl Pts',(-59.833051277686,-121.369179625724,172.959346654237));
#32706=CARTESIAN_POINT('Ctrl Pts',(-60.6051493712523,-121.22681535641,173.047982137366));
#32707=CARTESIAN_POINT('Ctrl Pts',(-60.9717332234154,-121.156688938203,
173.165155999873));
#32708=CARTESIAN_POINT('Ctrl Pts',(-61.6533084049214,-121.019329115187,
173.541498795707));
#32709=CARTESIAN_POINT('Ctrl Pts',(-61.9588379055462,-120.953995627252,
173.802136759374));
#32710=CARTESIAN_POINT('Ctrl Pts',(-62.4406216441401,-120.842580688804,
174.418358913714));
#32711=CARTESIAN_POINT('Ctrl Pts',(-62.6164916211797,-120.792785845895,
174.764221875393));
#32712=CARTESIAN_POINT('Ctrl Pts',(-62.831830251157,-120.705130003192,175.519861527492));
#32713=CARTESIAN_POINT('Ctrl Pts',(-62.8636029886591,-120.668980797393,
175.923881813629));
#32714=CARTESIAN_POINT('Ctrl Pts',(-62.7691471355156,-120.618996721308,
176.706721220368));
#32715=CARTESIAN_POINT('Ctrl Pts',(-62.6493660979336,-120.60072046909,177.078674504138));
#32716=CARTESIAN_POINT('Ctrl Pts',(-62.2683338413584,-120.576641799933,
177.770974540679));
#32717=CARTESIAN_POINT('Ctrl Pts',(-62.0057157156663,-120.571876607854,
178.081711462514));
#32718=CARTESIAN_POINT('Ctrl Pts',(-61.386643197741,-120.577820035574,178.572599371752));
#32719=CARTESIAN_POINT('Ctrl Pts',(-61.0394595611544,-120.583786653381,
178.752761717307));
#32720=CARTESIAN_POINT('Ctrl Pts',(-60.2812620362002,-120.599916378367,
178.976189852383));
#32721=CARTESIAN_POINT('Ctrl Pts',(-59.8760659443662,-120.610350929496,
179.011621599123));
#32722=CARTESIAN_POINT('Ctrl Pts',(-59.0913069644141,-120.633957493048,
178.923008663735));
#32723=CARTESIAN_POINT('Ctrl Pts',(-58.7181757174253,-120.642690550831,
178.805845854155));
#32724=CARTESIAN_POINT('Ctrl Pts',(-58.0229517331321,-120.65210693668,178.429524524002));
#32725=CARTESIAN_POINT('Ctrl Pts',(-57.710508585761,-120.65265338218,178.168896700149));
#32726=CARTESIAN_POINT('Ctrl Pts',(-57.2160470041594,-120.645312144498,
177.552691298977));
#32727=CARTESIAN_POINT('Ctrl Pts',(-57.0336219045084,-120.633714923204,
177.206834888442));
#32728=CARTESIAN_POINT('Ctrl Pts',(-56.8046204246826,-120.593428940922,
176.451204620774));
#32729=CARTESIAN_POINT('Ctrl Pts',(-56.7659280058564,-120.564791706116,
176.047186816681));
#32730=CARTESIAN_POINT('Ctrl Pts',(-56.8476974932369,-120.496020215608,
175.26434681027));
#32731=CARTESIAN_POINT('Ctrl Pts',(-56.9609209512799,-120.452905173578,
174.892390705729));
#32732=CARTESIAN_POINT('Ctrl Pts',(-57.3282888150645,-120.34904230557,174.200080113435));
#32733=CARTESIAN_POINT('Ctrl Pts',(-57.5839884596258,-120.289020884472,
173.889335238043));
#32734=CARTESIAN_POINT('Ctrl Pts',(-57.9019444156091,-120.223635681883,
173.631932461655));
#32735=CARTESIAN_POINT('Ctrl Pts',(-57.9108118003911,-120.221818239906,
173.624838446629));
#32736=CARTESIAN_POINT('Ctrl Pts',(-57.9197175435485,-120.21999896842,173.617797875548));
#32737=CARTESIAN_POINT('Origin',(-54.1598171290174,-67.5719248685924,175.985485069079));
#32738=CARTESIAN_POINT('',(-57.7077055346527,-118.231267989106,173.617797875547));
#32739=CARTESIAN_POINT('',(-57.7607085368763,-118.728450733934,173.617797875548));
#32740=CARTESIAN_POINT('',(-52.327900808713,-67.7672193871761,173.617797875548));
#32741=CARTESIAN_POINT('Ctrl Pts',(-57.7077055346532,-118.231267989105,
173.617797875547));
#32742=CARTESIAN_POINT('Ctrl Pts',(-57.4959621896365,-118.274523068789,
173.785194806399));
#32743=CARTESIAN_POINT('Ctrl Pts',(-57.3076732924635,-118.316380953857,
173.981384137499));
#32744=CARTESIAN_POINT('Ctrl Pts',(-56.9166317085334,-118.412777038229,
174.520832622239));
#32745=CARTESIAN_POINT('Ctrl Pts',(-56.750514647398,-118.463346246606,174.884149145073));
#32746=CARTESIAN_POINT('Ctrl Pts',(-56.5714891759017,-118.544263785547,
175.644138037827));
#32747=CARTESIAN_POINT('Ctrl Pts',(-56.5556667163322,-118.574733608663,
176.032265300035));
#32748=CARTESIAN_POINT('Ctrl Pts',(-56.6733470037069,-118.625927257235,
176.806552565876));
#32749=CARTESIAN_POINT('Ctrl Pts',(-56.810230408708,-118.644190079599,177.184578227962));
#32750=CARTESIAN_POINT('Ctrl Pts',(-57.2161301513622,-118.662834557244,
177.856022857159));
#32751=CARTESIAN_POINT('Ctrl Pts',(-57.4771708165094,-118.663728203223,
178.145359811132));
#32752=CARTESIAN_POINT('Ctrl Pts',(-58.1040538177718,-118.660578695295,
178.617304601394));
#32753=CARTESIAN_POINT('Ctrl Pts',(-58.4664849731559,-118.65479096,178.791666699017));
#32754=CARTESIAN_POINT('Ctrl Pts',(-59.2262807590043,-118.635793046171,
178.98675832149));
#32755=CARTESIAN_POINT('Ctrl Pts',(-59.6151252160864,-118.623005534561,
179.010088454037));
#32756=CARTESIAN_POINT('Ctrl Pts',(-60.3926306750729,-118.603737382819,
178.907203912237));
#32757=CARTESIAN_POINT('Ctrl Pts',(-60.7730525089593,-118.596024833953,
178.777492732011));
#32758=CARTESIAN_POINT('Ctrl Pts',(-61.4515994433801,-118.585775083933,
178.383836348125));
#32759=CARTESIAN_POINT('Ctrl Pts',(-61.7453936668036,-118.583069027208,
178.127620143533));
#32760=CARTESIAN_POINT('Ctrl Pts',(-62.2282783918895,-118.595145616927,
177.509631408275));
#32761=CARTESIAN_POINT('Ctrl Pts',(-62.4090968626334,-118.608703934463,
177.151113681912));
#32762=CARTESIAN_POINT('Ctrl Pts',(-62.6185406180347,-118.648551184006,
176.39623447214));
#32763=CARTESIAN_POINT('Ctrl Pts',(-62.6493280119049,-118.673837331507,
176.008347577506));
#32764=CARTESIAN_POINT('Ctrl Pts',(-62.5628115219606,-118.746549626409,
175.232305764503));
#32765=CARTESIAN_POINT('Ctrl Pts',(-62.4419634897019,-118.792258059477,
174.8521407814));
#32766=CARTESIAN_POINT('Ctrl Pts',(-62.0654492724426,-118.894660541694,
174.171798112607));
#32767=CARTESIAN_POINT('Ctrl Pts',(-61.8170828921811,-118.949666263393,
173.876129109712));
#32768=CARTESIAN_POINT('Ctrl Pts',(-61.2152216894388,-119.077249068476,
173.390024925554));
#32769=CARTESIAN_POINT('Ctrl Pts',(-60.8648129210778,-119.147419241121,
173.207514866718));
#32770=CARTESIAN_POINT('Ctrl Pts',(-60.1235724595637,-119.288792655129,
172.994139736444));
#32771=CARTESIAN_POINT('Ctrl Pts',(-59.7409990374732,-119.358072166465,
172.9613972216));
#32772=CARTESIAN_POINT('Ctrl Pts',(-58.975156012803,-119.503065519046,173.045611951922));
#32773=CARTESIAN_POINT('Ctrl Pts',(-58.5995443177483,-119.575910058344,
173.165726609417));
#32774=CARTESIAN_POINT('Ctrl Pts',(-58.1205711238936,-119.671308320629,
173.433040081355));
#32775=CARTESIAN_POINT('Ctrl Pts',(-57.9898008994096,-119.697672055653,
173.520490077886));
#32776=CARTESIAN_POINT('Ctrl Pts',(-57.8667145413246,-119.722816223591,
173.617797875548));
#32777=CARTESIAN_POINT('Ctrl Pts',(-57.9197175435485,-120.21999896842,173.617797875548));
#32778=CARTESIAN_POINT('Ctrl Pts',(-58.2106767735707,-120.160561611943,
173.387775618626));
#32779=CARTESIAN_POINT('Ctrl Pts',(-58.5418593508223,-120.09486403879,173.214997455317));
#32780=CARTESIAN_POINT('Ctrl Pts',(-59.2755595770514,-119.952890325441,
172.99479777958));
#32781=CARTESIAN_POINT('Ctrl Pts',(-59.6738459904375,-119.877668174723,
172.959351064575));
#32782=CARTESIAN_POINT('Ctrl Pts',(-60.4459451579516,-119.735302546304,
173.047933832021));
#32783=CARTESIAN_POINT('Ctrl Pts',(-60.8125349022444,-119.665177614304,
173.165081853359));
#32784=CARTESIAN_POINT('Ctrl Pts',(-61.494131352967,-119.527816037166,173.54137446353));
#32785=CARTESIAN_POINT('Ctrl Pts',(-61.7996768191756,-119.462480661484,
173.801988720596));
#32786=CARTESIAN_POINT('Ctrl Pts',(-62.2815011969325,-119.35106005207,174.418171706624));
#32787=CARTESIAN_POINT('Ctrl Pts',(-62.4573952662902,-119.30126491461,174.764019352204));
#32788=CARTESIAN_POINT('Ctrl Pts',(-62.6727880387899,-119.213603852045,
175.519637063711));
#32789=CARTESIAN_POINT('Ctrl Pts',(-62.7045908387443,-119.177451241683,
175.923651546385));
#32790=CARTESIAN_POINT('Ctrl Pts',(-62.6101954659949,-119.127459278395,
176.706492354431));
#32791=CARTESIAN_POINT('Ctrl Pts',(-62.490444407855,-119.109182275538,177.078452232915));
#32792=CARTESIAN_POINT('Ctrl Pts',(-62.1094699358185,-119.085098039957,
177.770776947088));
#32793=CARTESIAN_POINT('Ctrl Pts',(-61.8468790543294,-119.08032972871,178.081532462913));
#32794=CARTESIAN_POINT('Ctrl Pts',(-61.2278514236408,-119.086266822916,
178.572467808727));
#32795=CARTESIAN_POINT('Ctrl Pts',(-60.8806856801912,-119.092234162999,
178.752657900388));
#32796=CARTESIAN_POINT('Ctrl Pts',(-60.1225134582295,-119.108361829161,
178.976148947484));
#32797=CARTESIAN_POINT('Ctrl Pts',(-59.717324017646,-119.118795440289,179.011615688008));
#32798=CARTESIAN_POINT('Ctrl Pts',(-58.9325632512169,-119.14240052922,178.92307328148));
#32799=CARTESIAN_POINT('Ctrl Pts',(-58.5594247174237,-119.151137191948,
178.805945044747));
#32800=CARTESIAN_POINT('Ctrl Pts',(-57.8641724234153,-119.160557282684,
178.429690857934));
#32801=CARTESIAN_POINT('Ctrl Pts',(-57.5517078647856,-119.161105762437,
178.169094751776));
#32802=CARTESIAN_POINT('Ctrl Pts',(-57.0571915361592,-119.15376857044,177.552941754575));
#32803=CARTESIAN_POINT('Ctrl Pts',(-56.8747348452426,-119.142177758356,
177.20710583504));
#32804=CARTESIAN_POINT('Ctrl Pts',(-56.6456610864564,-119.101900220253,
176.451504922429));
#32805=CARTESIAN_POINT('Ctrl Pts',(-56.6069283921423,-119.073267012053,
176.047494884375));
#32806=CARTESIAN_POINT('Ctrl Pts',(-56.6886165589738,-119.004502265035,
175.264653005099));
#32807=CARTESIAN_POINT('Ctrl Pts',(-56.8018005986401,-118.961394695927,
174.892688077791));
#32808=CARTESIAN_POINT('Ctrl Pts',(-57.1690913228373,-118.857540846071,
174.200344472601));
#32809=CARTESIAN_POINT('Ctrl Pts',(-57.4247544572965,-118.797523030058,
173.88957472317));
#32810=CARTESIAN_POINT('Ctrl Pts',(-57.7427638772072,-118.732122604775,
173.632069696993));
#32811=CARTESIAN_POINT('Ctrl Pts',(-57.7517166545312,-118.730287601994,
173.624906545277));
#32812=CARTESIAN_POINT('Ctrl Pts',(-57.7607085368763,-118.728450733934,
173.617797875548));
#32813=CARTESIAN_POINT('Origin',(-54.1598171290174,-67.5719248685924,175.985485069079));
#32814=CARTESIAN_POINT('',(-57.5486965279805,-116.73971975462,173.617797875547));
#32815=CARTESIAN_POINT('',(-57.601699530204,-117.236902499449,173.617797875548));
#32816=CARTESIAN_POINT('',(-52.327900808713,-67.7672193871761,173.617797875548));
#32817=CARTESIAN_POINT('Ctrl Pts',(-57.548696527981,-116.73971975462,173.617797875547));
#32818=CARTESIAN_POINT('Ctrl Pts',(-57.3083599148635,-116.788815887254,
173.807799650592));
#32819=CARTESIAN_POINT('Ctrl Pts',(-57.0985524074229,-116.836048388882,
174.034651071404));
#32820=CARTESIAN_POINT('Ctrl Pts',(-56.7063045242392,-116.935899466992,
174.619800438034));
#32821=CARTESIAN_POINT('Ctrl Pts',(-56.5531790359681,-116.985088492272,
174.990610114756));
#32822=CARTESIAN_POINT('Ctrl Pts',(-56.4026615921244,-117.062366679206,
175.758523970475));
#32823=CARTESIAN_POINT('Ctrl Pts',(-56.4015627571165,-117.091838693313,
176.147067054867));
#32824=CARTESIAN_POINT('Ctrl Pts',(-56.5486985717973,-117.140272647945,
176.91801861918));
#32825=CARTESIAN_POINT('Ctrl Pts',(-56.7006082724247,-117.156944551056,
177.292024778325));
#32826=CARTESIAN_POINT('Ctrl Pts',(-57.133243173484,-117.172121812282,177.948259104063));
#32827=CARTESIAN_POINT('Ctrl Pts',(-57.4054042916933,-117.172387581818,
178.227077251624));
#32828=CARTESIAN_POINT('Ctrl Pts',(-58.0515087032864,-117.167588897825,
178.674943552142));
#32829=CARTESIAN_POINT('Ctrl Pts',(-58.4220892300848,-117.160950207667,
178.835329306316));
#32830=CARTESIAN_POINT('Ctrl Pts',(-59.1904533167627,-117.140405969468,
178.99954710651));
#32831=CARTESIAN_POINT('Ctrl Pts',(-59.5797920359974,-117.128104936031,
179.007024670633));
#32832=CARTESIAN_POINT('Ctrl Pts',(-60.3539318250452,-117.109615318493,
178.872415935096));
#32833=CARTESIAN_POINT('Ctrl Pts',(-60.7302326391108,-117.102367420638,
178.726472928545));
#32834=CARTESIAN_POINT('Ctrl Pts',(-61.3926513698913,-117.093189541362,
178.303843026263));
#32835=CARTESIAN_POINT('Ctrl Pts',(-61.6752938263682,-117.092188612567,
178.035719473275));
#32836=CARTESIAN_POINT('Ctrl Pts',(-62.1327621306332,-117.107414460568,
177.397017325779));
#32837=CARTESIAN_POINT('Ctrl Pts',(-62.2988430834852,-117.122577373761,
177.029604538182));
#32838=CARTESIAN_POINT('Ctrl Pts',(-62.4754944817019,-117.165259733133,
176.265275719895));
#32839=CARTESIAN_POINT('Ctrl Pts',(-62.4895199837143,-117.192821668892,
175.876927760014));
#32840=CARTESIAN_POINT('Ctrl Pts',(-62.3694967178749,-117.269565760154,
175.10436597572));
#32841=CARTESIAN_POINT('Ctrl Pts',(-62.2314564271143,-117.317149273094,
174.728426354695));
#32842=CARTESIAN_POINT('Ctrl Pts',(-61.8241467766779,-117.422162195221,
174.065080856857));
#32843=CARTESIAN_POINT('Ctrl Pts',(-61.5632570996869,-117.478959868437,
173.781389383671));
#32844=CARTESIAN_POINT('Ctrl Pts',(-60.9395057722688,-117.609356080022,
173.322282674548));
#32845=CARTESIAN_POINT('Ctrl Pts',(-60.5795755617375,-117.680592973706,
173.155355436889));
#32846=CARTESIAN_POINT('Ctrl Pts',(-59.8281154054219,-117.822373149151,
172.97675877957));
#32847=CARTESIAN_POINT('Ctrl Pts',(-59.4451103376711,-117.892119058604,
172.961902562141));
#32848=CARTESIAN_POINT('Ctrl Pts',(-58.6827834569909,-118.037237208823,
173.081704619415));
#32849=CARTESIAN_POINT('Ctrl Pts',(-58.3114025141392,-118.109692363721,
173.220085431791));
#32850=CARTESIAN_POINT('Ctrl Pts',(-57.8840410361413,-118.195417984603,
173.486217673092));
#32851=CARTESIAN_POINT('Ctrl Pts',(-57.7939584776156,-118.213648177156,
173.549609295983));
#32852=CARTESIAN_POINT('Ctrl Pts',(-57.7077055346532,-118.231267989105,
173.617797875547));
#32853=CARTESIAN_POINT('Ctrl Pts',(-57.7607085368762,-118.728450733934,
173.617797875548));
#32854=CARTESIAN_POINT('Ctrl Pts',(-58.0515776428276,-118.669031788066,
173.387846867585));
#32855=CARTESIAN_POINT('Ctrl Pts',(-58.3826462329409,-118.603356286683,
173.215103589513));
#32856=CARTESIAN_POINT('Ctrl Pts',(-59.1162082159644,-118.461407282903,
172.994852520928));
#32857=CARTESIAN_POINT('Ctrl Pts',(-59.5144856637423,-118.38618577923,172.959358991275));
#32858=CARTESIAN_POINT('Ctrl Pts',(-60.2865867491216,-118.243817719005,
173.047847404498));
#32859=CARTESIAN_POINT('Ctrl Pts',(-60.653187039188,-118.173695445026,173.164949174507));
#32860=CARTESIAN_POINT('Ctrl Pts',(-61.3348215534645,-118.036330729164,
173.541151960673));
#32861=CARTESIAN_POINT('Ctrl Pts',(-61.640395590947,-117.970991975614,173.801723784791));
#32862=CARTESIAN_POINT('Ctrl Pts',(-62.1222927011249,-117.859561217089,
174.417836663756));
#32863=CARTESIAN_POINT('Ctrl Pts',(-62.2982298897146,-117.809765550101,
174.763656897282));
#32864=CARTESIAN_POINT('Ctrl Pts',(-62.5137195604792,-117.72209514605,175.519235336379));
#32865=CARTESIAN_POINT('Ctrl Pts',(-62.5455761630827,-117.685936443013,
175.923239426838));
#32866=CARTESIAN_POINT('Ctrl Pts',(-62.4512890336388,-117.635930364266,
176.706082736919));
#32867=CARTESIAN_POINT('Ctrl Pts',(-62.3315916288074,-117.617652015292,
177.078054417928));
#32868=CARTESIAN_POINT('Ctrl Pts',(-61.9507205728282,-117.593557818036,
177.770423290715));
#32869=CARTESIAN_POINT('Ctrl Pts',(-61.6881784526301,-117.588783924713,
178.081212077816));
#32870=CARTESIAN_POINT('Ctrl Pts',(-61.0692311589717,-117.594709684208,
178.572232313359));
#32871=CARTESIAN_POINT('Ctrl Pts',(-60.7220974365814,-117.600678313742,
178.752472059403));
#32872=CARTESIAN_POINT('Ctrl Pts',(-59.9639705021903,-117.616802295402,
178.976075688442));
#32873=CARTESIAN_POINT('Ctrl Pts',(-59.5587929719279,-117.627234224161,
179.011605051095));
#32874=CARTESIAN_POINT('Ctrl Pts',(-58.7740290164334,-117.650836673956,
178.923188859954));
#32875=CARTESIAN_POINT('Ctrl Pts',(-58.4008774423528,-117.659579784133,
178.806122491485));
#32876=CARTESIAN_POINT('Ctrl Pts',(-57.7055744966176,-117.669006504483,
178.429988458243));
#32877=CARTESIAN_POINT('Ctrl Pts',(-57.3930716305156,-117.669558624411,
178.16944911486));
#32878=CARTESIAN_POINT('Ctrl Pts',(-56.8984573406303,-117.662228672049,
177.553389899095));
#32879=CARTESIAN_POINT('Ctrl Pts',(-56.7159441195295,-117.650649324458,
177.207590646192));
#32880=CARTESIAN_POINT('Ctrl Pts',(-56.486741031144,-117.610386896422,176.452042268985));
#32881=CARTESIAN_POINT('Ctrl Pts',(-56.4479362711177,-117.581760893924,
176.048046137231));
#32882=CARTESIAN_POINT('Ctrl Pts',(-56.5294789261214,-117.513008214282,
175.265200917308));
#32883=CARTESIAN_POINT('Ctrl Pts',(-56.6425924338899,-117.469914011628,
174.893220203229));
#32884=CARTESIAN_POINT('Ctrl Pts',(-57.0097451318139,-117.366076298834,
174.200817539525));
#32885=CARTESIAN_POINT('Ctrl Pts',(-57.2653429337035,-117.306064934913,
173.890003293683));
#32886=CARTESIAN_POINT('Ctrl Pts',(-57.58344797069,-117.240637275718,173.63231527396));
#32887=CARTESIAN_POINT('Ctrl Pts',(-57.5925535209534,-117.238770852661,
173.625028392653));
#32888=CARTESIAN_POINT('Ctrl Pts',(-57.601699530204,-117.236902499449,173.617797875548));
#32889=CARTESIAN_POINT('Origin',(-54.1598171290174,-67.5719248685924,175.985485069079));
#32890=CARTESIAN_POINT('',(-57.389687521308,-115.248171520134,173.617797875548));
#32891=CARTESIAN_POINT('',(-57.4426905235318,-115.745354264963,173.617797875548));
#32892=CARTESIAN_POINT('',(-52.327900808713,-67.7672193871761,173.617797875548));
#32893=CARTESIAN_POINT('Ctrl Pts',(-57.3896875213082,-115.248171520134,
173.617797875547));
#32894=CARTESIAN_POINT('Ctrl Pts',(-57.1294513039164,-115.301332757948,
173.823531586255));
#32895=CARTESIAN_POINT('Ctrl Pts',(-56.9052436706449,-115.352261519648,
174.072290913891));
#32896=CARTESIAN_POINT('Ctrl Pts',(-56.5138092385919,-115.454302586941,
174.689656594133));
#32897=CARTESIAN_POINT('Ctrl Pts',(-56.3698913538831,-115.502486587136,
175.065402645794));
#32898=CARTESIAN_POINT('Ctrl Pts',(-56.2393156442174,-115.577193603871,
175.838505933654));
#32899=CARTESIAN_POINT('Ctrl Pts',(-56.2485300800921,-115.606126432242,
176.227354066961));
#32900=CARTESIAN_POINT('Ctrl Pts',(-56.4164065131603,-115.652591749473,
176.99563475266));
#32901=CARTESIAN_POINT('Ctrl Pts',(-56.5788247100044,-115.668121707705,
177.366458368768));
#32902=CARTESIAN_POINT('Ctrl Pts',(-57.0301337226059,-115.680842882183,
178.011634487482));
#32903=CARTESIAN_POINT('Ctrl Pts',(-57.31020217626,-115.680836901443,178.283012481517));
#32904=CARTESIAN_POINT('Ctrl Pts',(-57.9697747695641,-115.674859991022,
178.713444416283));
#32905=CARTESIAN_POINT('Ctrl Pts',(-58.3458441823813,-115.667616675278,
178.863635062624));
#32906=CARTESIAN_POINT('Ctrl Pts',(-59.1199365044752,-115.645976364494,
179.00566581141));
#32907=CARTESIAN_POINT('Ctrl Pts',(-59.5096679381343,-115.634213519229,
179.001762009582));
#32908=CARTESIAN_POINT('Ctrl Pts',(-60.2809866109783,-115.616298003549,
178.844193354825));
#32909=CARTESIAN_POINT('Ctrl Pts',(-60.653881599363,-115.609396381106,178.686581914147));
#32910=CARTESIAN_POINT('Ctrl Pts',(-61.3042109045463,-115.601001870185,
178.243163587925));
#32911=CARTESIAN_POINT('Ctrl Pts',(-61.5787705876214,-115.601449085696,
177.9663575889));
#32912=CARTESIAN_POINT('Ctrl Pts',(-62.0172788459717,-115.618985978262,
177.312741458275));
#32913=CARTESIAN_POINT('Ctrl Pts',(-62.1722693180302,-115.635317575529,
176.93918102279));
#32914=CARTESIAN_POINT('Ctrl Pts',(-62.3246579353953,-115.680061206192,
176.168372574323));
#32915=CARTESIAN_POINT('Ctrl Pts',(-62.3263274665632,-115.709530529282,
175.779662774806));
#32916=CARTESIAN_POINT('Ctrl Pts',(-62.1813255083139,-115.789244339945,
175.010147786758));
#32917=CARTESIAN_POINT('Ctrl Pts',(-62.0305522343798,-115.838175355501,
174.637857013707));
#32918=CARTESIAN_POINT('Ctrl Pts',(-61.6004962439435,-115.945068340475,
173.987671895184));
#32919=CARTESIAN_POINT('Ctrl Pts',(-61.3302278998166,-116.003456669163,
173.71294337057));
#32920=CARTESIAN_POINT('Ctrl Pts',(-60.6902452992533,-116.135907704359,
173.27462006307));
#32921=CARTESIAN_POINT('Ctrl Pts',(-60.3235454023058,-116.207860667075,
173.119808132163));
#32922=CARTESIAN_POINT('Ctrl Pts',(-59.5648797333026,-116.349845053487,
172.967752007192));
#32923=CARTESIAN_POINT('Ctrl Pts',(-59.1815493155087,-116.420213825367,
172.966512880429));
#32924=CARTESIAN_POINT('Ctrl Pts',(-58.4224463099306,-116.565330938028,
173.113689703508));
#32925=CARTESIAN_POINT('Ctrl Pts',(-58.0548941280946,-116.637377196498,
173.26602941121));
#32926=CARTESIAN_POINT('Ctrl Pts',(-57.6663208572241,-116.715768960606,
173.528339014525));
#32927=CARTESIAN_POINT('Ctrl Pts',(-57.6066355545438,-116.727883929458,
173.571993294428));
#32928=CARTESIAN_POINT('Ctrl Pts',(-57.548696527981,-116.73971975462,173.617797875547));
#32929=CARTESIAN_POINT('Ctrl Pts',(-57.601699530204,-117.236902499449,173.617797875548));
#32930=CARTESIAN_POINT('Ctrl Pts',(-57.8924073894534,-117.177516493171,
173.387974343625));
#32931=CARTESIAN_POINT('Ctrl Pts',(-58.2232720552108,-117.111880479211,
173.215293510345));
#32932=CARTESIAN_POINT('Ctrl Pts',(-58.9565866929256,-116.969975687516,
172.994950563429));
#32933=CARTESIAN_POINT('Ctrl Pts',(-59.3548480867578,-116.894755344021,
172.959373278143));
#32934=CARTESIAN_POINT('Ctrl Pts',(-60.1269525894985,-116.752382935572,
173.047692878696));
#32935=CARTESIAN_POINT('Ctrl Pts',(-60.4935717462103,-116.682265410449,
173.164711901945));
#32936=CARTESIAN_POINT('Ctrl Pts',(-61.1752743435507,-116.544895081938,
173.540753986414));
#32937=CARTESIAN_POINT('Ctrl Pts',(-61.4808994828104,-116.479550287966,
173.801249888292));
#32938=CARTESIAN_POINT('Ctrl Pts',(-61.9629267007928,-116.368101375068,
174.41723733329));
#32939=CARTESIAN_POINT('Ctrl Pts',(-62.1389410263743,-116.318304753252,
174.763008528566));
#32940=CARTESIAN_POINT('Ctrl Pts',(-62.3546040300313,-116.230617640446,
175.518516698796));
#32941=CARTESIAN_POINT('Ctrl Pts',(-62.3865568762075,-116.194448040141,
175.922502180891));
#32942=CARTESIAN_POINT('Ctrl Pts',(-62.292463380927,-116.144416712053,176.705349947868));
#32943=CARTESIAN_POINT('Ctrl Pts',(-62.1728619500436,-116.126135946456,
177.077342741514));
#32944=CARTESIAN_POINT('Ctrl Pts',(-61.7921758851629,-116.102023931203,
177.769790584473));
#32945=CARTESIAN_POINT('Ctrl Pts',(-61.5297209982687,-116.097240053436,
178.080638867891));
#32946=CARTESIAN_POINT('Ctrl Pts',(-60.9109174216561,-116.103145538237,
178.571810932972));
#32947=CARTESIAN_POINT('Ctrl Pts',(-60.5638409722789,-116.10911646412,178.752139493388));
#32948=CARTESIAN_POINT('Ctrl Pts',(-59.8057950587711,-116.125233855381,
178.97594447532));
#32949=CARTESIAN_POINT('Ctrl Pts',(-59.4006388551323,-116.135662774514,
179.011585838522));
#32950=CARTESIAN_POINT('Ctrl Pts',(-58.6158692211454,-116.159260503308,
178.923395393299));
#32951=CARTESIAN_POINT('Ctrl Pts',(-58.242694323062,-116.168015133066,178.806439675221));
#32952=CARTESIAN_POINT('Ctrl Pts',(-57.5473008151624,-116.177453709431,
178.430520535517));
#32953=CARTESIAN_POINT('Ctrl Pts',(-57.2347294625985,-116.178012339331,
178.170082723635));
#32954=CARTESIAN_POINT('Ctrl Pts',(-56.7399399987164,-116.170695334496,
177.554191248178));
#32955=CARTESIAN_POINT('Ctrl Pts',(-56.5573256823801,-116.159136475564,
177.208457566208));
#32956=CARTESIAN_POINT('Ctrl Pts',(-56.3278913346571,-116.118901068969,
176.453003161774));
#32957=CARTESIAN_POINT('Ctrl Pts',(-56.2889577101339,-116.090287953991,
176.049031929797));
#32958=CARTESIAN_POINT('Ctrl Pts',(-56.3702401569045,-116.021556856233,
175.266180769898));
#32959=CARTESIAN_POINT('Ctrl Pts',(-56.483227543392,-115.978486538889,174.894171826583));
#32960=CARTESIAN_POINT('Ctrl Pts',(-56.8501334327227,-115.874677683887,
174.20166359593));
#32961=CARTESIAN_POINT('Ctrl Pts',(-57.1056143961393,-115.814677861905,
173.890769819493));
#32962=CARTESIAN_POINT('Ctrl Pts',(-57.423890260819,-115.749201518234,173.632754464228));
#32963=CARTESIAN_POINT('Ctrl Pts',(-57.4332689233803,-115.747278916079,
173.625246265243));
#32964=CARTESIAN_POINT('Ctrl Pts',(-57.4426905235318,-115.745354264963,
173.617797875548));
#32965=CARTESIAN_POINT('Origin',(-54.1598171290174,-67.5719248685924,175.985485069079));
#32966=CARTESIAN_POINT('',(-57.2306785146355,-113.756623285649,173.617797875548));
#32967=CARTESIAN_POINT('',(-57.2836815168596,-114.253806030477,173.617797875548));
#32968=CARTESIAN_POINT('',(-52.327900808713,-67.7672193871761,173.617797875548));
#32969=CARTESIAN_POINT('Ctrl Pts',(-57.230686260479,-113.756621703323,173.617791751974));
#32970=CARTESIAN_POINT('Ctrl Pts',(-56.9391520032908,-113.816176526754,
173.848268605392));
#32971=CARTESIAN_POINT('Ctrl Pts',(-56.6932758300137,-113.872841127714,
174.132419081623));
#32972=CARTESIAN_POINT('Ctrl Pts',(-56.3182567509192,-113.974598128388,
174.779611919365));
#32973=CARTESIAN_POINT('Ctrl Pts',(-56.1928240859027,-114.018738792552,
175.137018307616));
#32974=CARTESIAN_POINT('Ctrl Pts',(-56.0786149232731,-114.089571808378,
175.889782503794));
#32975=CARTESIAN_POINT('Ctrl Pts',(-56.0944605876305,-114.118226185,176.278831751245));
#32976=CARTESIAN_POINT('Ctrl Pts',(-56.2757092205817,-114.163411034205,
177.045248412219));
#32977=CARTESIAN_POINT('Ctrl Pts',(-56.4448647956619,-114.178195885927,
177.413867474309));
#32978=CARTESIAN_POINT('Ctrl Pts',(-56.9081477547668,-114.189327126592,
178.051762152112));
#32979=CARTESIAN_POINT('Ctrl Pts',(-57.1933528069892,-114.189220667881,
178.318322809599));
#32980=CARTESIAN_POINT('Ctrl Pts',(-57.8615774554013,-114.182476464193,
178.737296757641));
#32981=CARTESIAN_POINT('Ctrl Pts',(-58.24106860038,-114.17484128849,178.880760888487));
#32982=CARTESIAN_POINT('Ctrl Pts',(-59.0187163975137,-114.152491052106,
179.00828533427));
#32983=CARTESIAN_POINT('Ctrl Pts',(-59.4087205826764,-114.141164658589,
178.996936233929));
#32984=CARTESIAN_POINT('Ctrl Pts',(-60.1780082358599,-114.123631305916,
178.824279651137));
#32985=CARTESIAN_POINT('Ctrl Pts',(-60.5484738132297,-114.116961555137,
178.659045201321));
#32986=CARTESIAN_POINT('Ctrl Pts',(-61.1906692006231,-114.10908528641,178.202048242943));
#32987=CARTESIAN_POINT('Ctrl Pts',(-61.4599045154499,-114.110583658141,
177.919500596901));
#32988=CARTESIAN_POINT('Ctrl Pts',(-61.8856854300552,-114.129654195603,
177.256122027241));
#32989=CARTESIAN_POINT('Ctrl Pts',(-62.0331959862368,-114.146756256848,
176.878665009532));
#32990=CARTESIAN_POINT('Ctrl Pts',(-62.1693912717361,-114.192858816441,
176.10376818939));
#32991=CARTESIAN_POINT('Ctrl Pts',(-62.162823924056,-114.223707214386,175.714807996739));
#32992=CARTESIAN_POINT('Ctrl Pts',(-62.0010577572282,-114.305396839896,
174.947555617494));
#32993=CARTESIAN_POINT('Ctrl Pts',(-61.8417904801587,-114.355206848899,
174.577949784827));
#32994=CARTESIAN_POINT('Ctrl Pts',(-61.3965692401005,-114.46333021106,173.936829693498));
#32995=CARTESIAN_POINT('Ctrl Pts',(-61.1199773222918,-114.522910269248,
173.668142587039));
#32996=CARTESIAN_POINT('Ctrl Pts',(-60.4691467286856,-114.656718870453,
173.244094882701));
#32997=CARTESIAN_POINT('Ctrl Pts',(-60.0980748242194,-114.729112095771,
173.097649947013));
#32998=CARTESIAN_POINT('Ctrl Pts',(-59.3347779164793,-114.871184521411,
172.963709202852));
#32999=CARTESIAN_POINT('Ctrl Pts',(-58.9512280542984,-114.94210987731,172.971764400139));
#33000=CARTESIAN_POINT('Ctrl Pts',(-58.1946015258564,-115.087177195723,
173.137739855785));
#33001=CARTESIAN_POINT('Ctrl Pts',(-57.8299643801731,-115.15888788711,173.29960349534));
#33002=CARTESIAN_POINT('Ctrl Pts',(-57.4674731119605,-115.232315692349,
173.557862745655));
#33003=CARTESIAN_POINT('Ctrl Pts',(-57.4281921345336,-115.24030577062,173.587357466301));
#33004=CARTESIAN_POINT('Ctrl Pts',(-57.3896875213082,-115.248171520134,
173.617797875547));
#33005=CARTESIAN_POINT('Ctrl Pts',(-57.4426905235318,-115.745354264963,
173.617797875548));
#33006=CARTESIAN_POINT('Ctrl Pts',(-57.7331100939653,-115.686027150527,
173.388202254745));
#33007=CARTESIAN_POINT('Ctrl Pts',(-58.0636102238676,-115.620461726853,
173.215633158892));
#33008=CARTESIAN_POINT('Ctrl Pts',(-58.7964826214188,-115.478635989196,
172.995126174909));
#33009=CARTESIAN_POINT('Ctrl Pts',(-59.1947152712333,-115.403417727966,
172.959399156046));
#33010=CARTESIAN_POINT('Ctrl Pts',(-59.966825838982,-115.261037553985,173.04741694866));
#33011=CARTESIAN_POINT('Ctrl Pts',(-60.3334787221989,-115.19092849755,173.164288045249));
#33012=CARTESIAN_POINT('Ctrl Pts',(-61.0153029832218,-115.053548144051,
173.540042841311));
#33013=CARTESIAN_POINT('Ctrl Pts',(-61.3210194319925,-114.988192560594,
173.800402994964));
#33014=CARTESIAN_POINT('Ctrl Pts',(-61.8032791948,-114.876711202894,174.416166176717));
#33015=CARTESIAN_POINT('Ctrl Pts',(-61.9794313985134,-114.826912850261,
174.761849718203));
#33016=CARTESIAN_POINT('Ctrl Pts',(-62.1954041910925,-114.73919587929,175.51723224345));
#33017=CARTESIAN_POINT('Ctrl Pts',(-62.2275290505995,-114.703006807309,
175.921184408229));
#33018=CARTESIAN_POINT('Ctrl Pts',(-62.1337816503851,-114.652930354216,
176.70404008077));
#33019=CARTESIAN_POINT('Ctrl Pts',(-62.0143517430599,-114.634645241808,
177.076070608353));
#33020=CARTESIAN_POINT('Ctrl Pts',(-61.6339963003143,-114.610501386406,
177.768659522463));
#33021=CARTESIAN_POINT('Ctrl Pts',(-61.3716973480183,-114.605699666669,
178.07961407736));
#33022=CARTESIAN_POINT('Ctrl Pts',(-60.7531506585592,-114.611568918709,
178.571057428201));
#33023=CARTESIAN_POINT('Ctrl Pts',(-60.4061765489483,-114.617543916026,
178.751544696308));
#33024=CARTESIAN_POINT('Ctrl Pts',(-59.6482754714225,-114.633649530162,
178.97570943353));
#33025=CARTESIAN_POINT('Ctrl Pts',(-59.243157451725,-114.644073069761,179.011550909639));
#33026=CARTESIAN_POINT('Ctrl Pts',(-58.458377752376,-114.667662360705,178.92376383316));
#33027=CARTESIAN_POINT('Ctrl Pts',(-58.0851611769012,-114.676437535059,
178.807005809767));
#33028=CARTESIAN_POINT('Ctrl Pts',(-57.389605953392,-114.685897291084,178.431470614418));
#33029=CARTESIAN_POINT('Ctrl Pts',(-57.0769123212988,-114.686467550742,
178.171214243736));
#33030=CARTESIAN_POINT('Ctrl Pts',(-56.5818099708201,-114.679173677331,
177.555622507053));
#33031=CARTESIAN_POINT('Ctrl Pts',(-56.3990150574061,-114.667651375495,
177.210005956547));
#33032=CARTESIAN_POINT('Ctrl Pts',(-56.1691676700437,-114.627464238523,
176.454719494352));
#33033=CARTESIAN_POINT('Ctrl Pts',(-56.130003884674,-114.598874149911,176.050792841041));
#33034=CARTESIAN_POINT('Ctrl Pts',(-56.2108215468567,-114.530181610307,
175.267931179225));
#33035=CARTESIAN_POINT('Ctrl Pts',(-56.3235836736219,-114.487153902853,
174.895871816253));
#33036=CARTESIAN_POINT('Ctrl Pts',(-56.6900487567697,-114.38339659709,174.203175159166));
#33037=CARTESIAN_POINT('Ctrl Pts',(-56.9453209944096,-114.323417404517,
173.892139449795));
#33038=CARTESIAN_POINT('Ctrl Pts',(-57.2639014894801,-114.257854151479,
173.633539083492));
#33039=CARTESIAN_POINT('Ctrl Pts',(-57.2737677291267,-114.255831226019,
173.625635371642));
#33040=CARTESIAN_POINT('Ctrl Pts',(-57.2836815168596,-114.253806030477,
173.617797875548));
#33041=CARTESIAN_POINT('Origin',(-54.1598171290174,-67.5719248685924,175.985485069079));
#33042=CARTESIAN_POINT('',(-57.0716695079633,-112.265075051163,173.617797875548));
#33043=CARTESIAN_POINT('',(-57.1246725101874,-112.762257795992,173.617797875548));
#33044=CARTESIAN_POINT('',(-52.327900808713,-67.7672193871761,173.617797875548));
#33045=CARTESIAN_POINT('Ctrl Pts',(-57.0716695079633,-112.265075051163,
173.617797875548));
#33046=CARTESIAN_POINT('Ctrl Pts',(-57.0627343906797,-112.266900323216,
173.624861668792));
#33047=CARTESIAN_POINT('Ctrl Pts',(-57.0538378855726,-112.268723753602,
173.631979258842));
#33048=CARTESIAN_POINT('Ctrl Pts',(-56.7358636959649,-112.334114147414,
173.88941690138));
#33049=CARTESIAN_POINT('Ctrl Pts',(-56.4801765013653,-112.394134339222,
174.200170259468));
#33050=CARTESIAN_POINT('Ctrl Pts',(-56.112834942677,-112.497994132019,174.892492109895));
#33051=CARTESIAN_POINT('Ctrl Pts',(-55.9996249265372,-112.541106625516,
175.26445122305));
#33052=CARTESIAN_POINT('Ctrl Pts',(-55.9178831697836,-112.609875816504,
176.047291868592));
#33053=CARTESIAN_POINT('Ctrl Pts',(-55.956589322785,-112.638511678251,176.451307024888));
#33054=CARTESIAN_POINT('Ctrl Pts',(-56.1856154501808,-112.678794781052,
177.206927282754));
#33055=CARTESIAN_POINT('Ctrl Pts',(-56.3680513224875,-112.690389816605,
177.552776705815));
#33056=CARTESIAN_POINT('Ctrl Pts',(-56.8625315730818,-112.697729674712,
178.168964237558));
#33057=CARTESIAN_POINT('Ctrl Pts',(-57.1749820220013,-112.697182535531,
178.429581245929));
#33058=CARTESIAN_POINT('Ctrl Pts',(-57.8702156602254,-112.687764886311,
178.805879680385));
#33059=CARTESIAN_POINT('Ctrl Pts',(-58.2433493919726,-112.679030599089,
178.923030700711));
#33060=CARTESIAN_POINT('Ctrl Pts',(-59.0281089814614,-112.655424538366,
179.011619586101));
#33061=CARTESIAN_POINT('Ctrl Pts',(-59.4333028055902,-112.644990307764,
178.976175906596));
#33062=CARTESIAN_POINT('Ctrl Pts',(-60.1914917026374,-112.628861284821,
178.752726318707));
#33063=CARTESIAN_POINT('Ctrl Pts',(-60.5386692377639,-112.622894420582,
178.572554511917));
#33064=CARTESIAN_POINT('Ctrl Pts',(-61.1577264497552,-112.616953152536,
178.081650427006));
#33065=CARTESIAN_POINT('Ctrl Pts',(-61.420335285588,-112.621719408229,177.770907164543));
#33066=CARTESIAN_POINT('Ctrl Pts',(-61.801347838248,-112.645799975499,177.078598712896));
#33067=CARTESIAN_POINT('Ctrl Pts',(-61.9211186531393,-112.664076483555,
176.706643180403));
#33068=CARTESIAN_POINT('Ctrl Pts',(-62.0155538832229,-112.714063249099,
175.923803295569));
#33069=CARTESIAN_POINT('Ctrl Pts',(-61.9837708947597,-112.750213615836,
175.519784988088));
#33070=CARTESIAN_POINT('Ctrl Pts',(-61.7684138027681,-112.837871238476,
174.764152817242));
#33071=CARTESIAN_POINT('Ctrl Pts',(-61.5925356105753,-112.887666181717,
174.418295078142));
#33072=CARTESIAN_POINT('Ctrl Pts',(-61.1107380145101,-112.99908305391,173.802086279413));
#33073=CARTESIAN_POINT('Ctrl Pts',(-60.8052030696972,-113.064417185573,
173.541456399193));
#33074=CARTESIAN_POINT('Ctrl Pts',(-60.1236206355408,-113.201777606753,
173.165130715799));
#33075=CARTESIAN_POINT('Ctrl Pts',(-59.7570347742566,-113.271903518097,
173.047965664686));
#33076=CARTESIAN_POINT('Ctrl Pts',(-58.9978043319857,-113.411895558799,
172.960825081789));
#33077=CARTESIAN_POINT('Ctrl Pts',(-58.6125648708664,-113.484596976178,
172.992533613084));
#33078=CARTESIAN_POINT('Ctrl Pts',(-57.876087918505,-113.626875740639,173.20299707846));
#33079=CARTESIAN_POINT('Ctrl Pts',(-57.5318946593438,-113.695090639415,
173.379666858286));
#33080=CARTESIAN_POINT('Ctrl Pts',(-57.2306785146356,-113.756623285649,
173.617797875548));
#33081=CARTESIAN_POINT('Ctrl Pts',(-57.2836815168596,-114.253806030477,
173.617797875548));
#33082=CARTESIAN_POINT('Ctrl Pts',(-57.5735863268685,-114.194584071664,
173.38860920645));
#33083=CARTESIAN_POINT('Ctrl Pts',(-57.9034357279494,-114.129144665683,
173.216239925632));
#33084=CARTESIAN_POINT('Ctrl Pts',(-58.6355184171523,-113.987460111408,
172.995440774764));
#33085=CARTESIAN_POINT('Ctrl Pts',(-59.0336996098216,-113.912245593771,
172.959446430816));
#33086=CARTESIAN_POINT('Ctrl Pts',(-59.805820864167,-113.769851581135,173.046925348647));
#33087=CARTESIAN_POINT('Ctrl Pts',(-60.1725339536146,-113.699757577027,
173.163532356499));
#33088=CARTESIAN_POINT('Ctrl Pts',(-60.8545752618224,-113.562359354176,
173.538774261281));
#33089=CARTESIAN_POINT('Ctrl Pts',(-61.1604545779857,-113.496984537301,
173.798891998665));
#33090=CARTESIAN_POINT('Ctrl Pts',(-61.6431293382452,-113.38544528829,174.414254732326));
#33091=CARTESIAN_POINT('Ctrl Pts',(-61.8195276279145,-113.335643769574,
174.759781826746));
#33092=CARTESIAN_POINT('Ctrl Pts',(-62.0360532252756,-113.247873532447,
175.514939962153));
#33093=CARTESIAN_POINT('Ctrl Pts',(-62.0684850418152,-113.211649728303,
175.918832483867));
#33094=CARTESIAN_POINT('Ctrl Pts',(-61.9753553055497,-113.161492757481,
176.701702072252));
#33095=CARTESIAN_POINT('Ctrl Pts',(-61.8562314564137,-113.143199800051,
177.073799935792));
#33096=CARTESIAN_POINT('Ctrl Pts',(-61.476465985183,-113.118999143335,177.76664036815));
#33097=CARTESIAN_POINT('Ctrl Pts',(-61.214445377309,-113.114165594034,178.077784358413));
#33098=CARTESIAN_POINT('Ctrl Pts',(-60.5963571844697,-113.119970200329,
178.569711579633));
#33099=CARTESIAN_POINT('Ctrl Pts',(-60.2495656278064,-113.125952358746,
178.750481973186));
#33100=CARTESIAN_POINT('Ctrl Pts',(-59.491923104094,-113.142036962072,178.975288320393));
#33101=CARTESIAN_POINT('Ctrl Pts',(-59.0868734382955,-113.152450900272,
179.01148669837));
#33102=CARTESIAN_POINT('Ctrl Pts',(-58.3020760435979,-113.176025133447,
178.924419112465));
#33103=CARTESIAN_POINT('Ctrl Pts',(-57.9287851232326,-113.184836829471,
178.808013659741));
#33104=CARTESIAN_POINT('Ctrl Pts',(-57.2329417753444,-113.194334347895,
178.433163202329));
#33105=CARTESIAN_POINT('Ctrl Pts',(-56.9200303315871,-113.194925343858,
178.173230539031));
#33106=CARTESIAN_POINT('Ctrl Pts',(-56.42437026228,-113.18767271874,177.558173498531));
#33107=CARTESIAN_POINT('Ctrl Pts',(-56.2412533521598,-113.176215456699,
177.212765772886));
#33108=CARTESIAN_POINT('Ctrl Pts',(-56.0106697986407,-113.136114377111,
176.457778962724));
#33109=CARTESIAN_POINT('Ctrl Pts',(-55.9710957851752,-113.107565356253,
176.053932101379));
#33110=CARTESIAN_POINT('Ctrl Pts',(-56.0510849253777,-113.03894157732,175.271052062676));
#33111=CARTESIAN_POINT('Ctrl Pts',(-56.1634455638887,-112.995989653942,
174.898902832797));
#33112=CARTESIAN_POINT('Ctrl Pts',(-56.5291250084888,-112.892324250224,
174.205870724865));
#33113=CARTESIAN_POINT('Ctrl Pts',(-56.7840250823298,-112.832381873329,
173.894582403637));
#33114=CARTESIAN_POINT('Ctrl Pts',(-57.1031470110203,-112.76666385856,173.634938174122));
#33115=CARTESIAN_POINT('Ctrl Pts',(-57.113881585975,-112.764462173592,173.626328805264));
#33116=CARTESIAN_POINT('Ctrl Pts',(-57.1246725101874,-112.762257795992,
173.617797875548));
#33117=CARTESIAN_POINT('Origin',(-54.1598171290174,-67.5719248685924,175.985485069079));
#33118=CARTESIAN_POINT('',(-56.9126605012911,-110.773526816678,173.617797875548));
#33119=CARTESIAN_POINT('',(-56.9656635035151,-111.270709561506,173.617797875548));
#33120=CARTESIAN_POINT('',(-52.327900808713,-67.7672193871761,173.617797875548));
#33121=CARTESIAN_POINT('Ctrl Pts',(-56.912660501291,-110.773526816678,173.617797875548));
#33122=CARTESIAN_POINT('Ctrl Pts',(-56.9036160521539,-110.775374423119,
173.624948102757));
#33123=CARTESIAN_POINT('Ctrl Pts',(-56.8946111672271,-110.77722014228,173.632153450317));
#33124=CARTESIAN_POINT('Ctrl Pts',(-56.5765691295408,-110.842629856544,
173.889720882783));
#33125=CARTESIAN_POINT('Ctrl Pts',(-56.3209282766764,-110.902645472224,
174.200505809701));
#33126=CARTESIAN_POINT('Ctrl Pts',(-55.9536846276516,-111.006493818502,
174.892869559036));
#33127=CARTESIAN_POINT('Ctrl Pts',(-55.8405246435036,-111.049596828151,
175.264839870551));
#33128=CARTESIAN_POINT('Ctrl Pts',(-55.7588861042098,-111.11835745965,176.047682890698));
#33129=CARTESIAN_POINT('Ctrl Pts',(-55.7976433771382,-111.146988210403,
176.451688187388));
#33130=CARTESIAN_POINT('Ctrl Pts',(-56.0267612449455,-111.187260595197,
177.207271183777));
#33131=CARTESIAN_POINT('Ctrl Pts',(-56.2092372154757,-111.198847496697,
177.553094598093));
#33132=CARTESIAN_POINT('Ctrl Pts',(-56.7037869544156,-111.206182219643,
178.169215612368));
#33133=CARTESIAN_POINT('Ctrl Pts',(-57.0162645787218,-111.205632498413,
178.429792360503));
#33134=CARTESIAN_POINT('Ctrl Pts',(-57.7115341484149,-111.196210146648,
178.806005569765));
#33135=CARTESIAN_POINT('Ctrl Pts',(-58.0846771294381,-111.187471284538,
178.923112706732));
#33136=CARTESIAN_POINT('Ctrl Pts',(-58.8694389846079,-111.163867095625,
179.011612068858));
#33137=CARTESIAN_POINT('Ctrl Pts',(-59.2746243643901,-111.153434058225,
178.976123971552));
#33138=CARTESIAN_POINT('Ctrl Pts',(-60.03278114244,-111.137307648605,178.752594529208));
#33139=CARTESIAN_POINT('Ctrl Pts',(-60.3799359654912,-111.131339868321,
178.572387503619));
#33140=CARTESIAN_POINT('Ctrl Pts',(-60.9989361993644,-111.12540663962,178.081423206973));
#33141=CARTESIAN_POINT('Ctrl Pts',(-61.2615104522396,-111.130176854553,
177.770656343799));
#33142=CARTESIAN_POINT('Ctrl Pts',(-61.642449656401,-111.154264487422,177.078316569314));
#33143=CARTESIAN_POINT('Ctrl Pts',(-61.7621824171466,-111.172541948953,
176.706352665837));
#33144=CARTESIAN_POINT('Ctrl Pts',(-61.8565408761524,-111.222538726042,
175.92351100368));
#33145=CARTESIAN_POINT('Ctrl Pts',(-61.8247197279864,-111.258693414243,
175.519500064209));
#33146=CARTESIAN_POINT('Ctrl Pts',(-61.6092939104062,-111.346357662586,
174.763895744913));
#33147=CARTESIAN_POINT('Ctrl Pts',(-61.4333851363702,-111.396152980288,
174.418057447483));
#33148=CARTESIAN_POINT('Ctrl Pts',(-60.9515359549162,-111.507577050861,
173.80189836882));
#33149=CARTESIAN_POINT('Ctrl Pts',(-60.6459807447754,-111.57291357858,173.541298581809));
#33150=CARTESIAN_POINT('Ctrl Pts',(-59.964371313043,-111.7102762262,173.165036603142));
#33151=CARTESIAN_POINT('Ctrl Pts',(-59.59777797244,-111.780400251476,173.0479043543));
#33152=CARTESIAN_POINT('Ctrl Pts',(-58.8256781502785,-111.922766709292,
172.959353762966));
#33153=CARTESIAN_POINT('Ctrl Pts',(-58.4273947936942,-111.997988639473,
172.994816442521));
#33154=CARTESIAN_POINT('Ctrl Pts',(-57.6937417099188,-112.13995392666,173.215033647115));
#33155=CARTESIAN_POINT('Ctrl Pts',(-57.3625980045214,-112.20564397294,173.387799915435));
#33156=CARTESIAN_POINT('Ctrl Pts',(-57.0716695079633,-112.265075051163,
173.617797875548));
#33157=CARTESIAN_POINT('Ctrl Pts',(-57.1246725101874,-112.762257795992,
173.617797875548));
#33158=CARTESIAN_POINT('Ctrl Pts',(-57.413660289602,-112.703223168834,173.389334178972));
#33159=CARTESIAN_POINT('Ctrl Pts',(-57.742350995899,-112.638008176024,173.217321815072));
#33160=CARTESIAN_POINT('Ctrl Pts',(-58.4730266643655,-112.496575220331,
172.996004506073));
#33161=CARTESIAN_POINT('Ctrl Pts',(-58.8711157663971,-112.421367452974,
172.959534041656));
#33162=CARTESIAN_POINT('Ctrl Pts',(-59.6432556046902,-112.278948873754,
173.046053048715));
#33163=CARTESIAN_POINT('Ctrl Pts',(-60.0100759029152,-112.208881465366,
173.162189732229));
#33164=CARTESIAN_POINT('Ctrl Pts',(-60.6925032651767,-112.071451507064,
173.536518198727));
#33165=CARTESIAN_POINT('Ctrl Pts',(-60.9986721778529,-112.006042527929,
173.796203989923));
#33166=CARTESIAN_POINT('Ctrl Pts',(-61.4820855205812,-111.894400277994,
174.410853305157));
#33167=CARTESIAN_POINT('Ctrl Pts',(-61.6589218717488,-111.844592879084,
174.756101899925));
#33168=CARTESIAN_POINT('Ctrl Pts',(-61.8764311790495,-111.756727901188,
175.510860159495));
#33169=CARTESIAN_POINT('Ctrl Pts',(-61.9094092428966,-111.720442336648,
175.914645945218));
#33170=CARTESIAN_POINT('Ctrl Pts',(-61.8173788624534,-111.670142104047,
176.697539689913));
#33171=CARTESIAN_POINT('Ctrl Pts',(-61.6987995837909,-111.651834906258,
177.069757381944));
#33172=CARTESIAN_POINT('Ctrl Pts',(-61.3200839310779,-111.627533223033,
177.763044700792));
#33173=CARTESIAN_POINT('Ctrl Pts',(-61.0585589056476,-111.622643060867,
178.074525150415));
#33174=CARTESIAN_POINT('Ctrl Pts',(-60.4412868963765,-111.628332662555,
178.567312693833));
#33175=CARTESIAN_POINT('Ctrl Pts',(-60.0948199758521,-111.634327233912,
178.748586648949));
#33176=CARTESIAN_POINT('Ctrl Pts',(-59.3376378629081,-111.650374464427,
178.974533602147));
#33177=CARTESIAN_POINT('Ctrl Pts',(-58.932710516522,-111.660771311206,179.011366477713));
#33178=CARTESIAN_POINT('Ctrl Pts',(-58.147882474537,-111.684318746739,178.92557825714));
#33179=CARTESIAN_POINT('Ctrl Pts',(-57.7744593417187,-111.693194992019,
178.809799546446));
#33180=CARTESIAN_POINT('Ctrl Pts',(-57.0781047024549,-111.702759607706,
178.436166325688));
#33181=CARTESIAN_POINT('Ctrl Pts',(-56.7648069018154,-111.703387451443,
178.176809484026));
#33182=CARTESIAN_POINT('Ctrl Pts',(-56.26815631875,-111.696208136346,177.562703376644));
#33183=CARTESIAN_POINT('Ctrl Pts',(-56.0844672742459,-111.684865996432,
177.217666648423));
#33184=CARTESIAN_POINT('Ctrl Pts',(-55.8525765184924,-111.644917809419,
176.463212957767));
#33185=CARTESIAN_POINT('Ctrl Pts',(-55.8122740399269,-111.616441799022,
176.059508852572));
#33186=CARTESIAN_POINT('Ctrl Pts',(-55.8907915716628,-111.547940237584,
175.276597259374));
#33187=CARTESIAN_POINT('Ctrl Pts',(-56.0024392749427,-111.505122377378,
174.904288442366));
#33188=CARTESIAN_POINT('Ctrl Pts',(-56.3667237210741,-111.401620242415,
174.210661889557));
#33189=CARTESIAN_POINT('Ctrl Pts',(-56.620962479084,-111.341743388782,173.898926136395));
#33190=CARTESIAN_POINT('Ctrl Pts',(-56.9410410403329,-111.275751002892,
173.63742458343));
#33191=CARTESIAN_POINT('Ctrl Pts',(-56.9533153611321,-111.273232048731,
173.627559887839));
#33192=CARTESIAN_POINT('Ctrl Pts',(-56.9656635035151,-111.270709561506,
173.617797875548));
#33193=CARTESIAN_POINT('Origin',(-54.1598171290174,-67.5719248685924,175.985485069079));
#33194=CARTESIAN_POINT('',(-56.7536514946188,-109.281978582192,173.617797875548));
#33195=CARTESIAN_POINT('',(-56.8066544968429,-109.779161327021,173.617797875548));
#33196=CARTESIAN_POINT('',(-52.327900808713,-67.7672193871761,173.617797875548));
#33197=CARTESIAN_POINT('Ctrl Pts',(-56.7536514946188,-109.281978582192,
173.617797875548));
#33198=CARTESIAN_POINT('Ctrl Pts',(-56.7444114652081,-109.283866141909,
173.625102721725));
#33199=CARTESIAN_POINT('Ctrl Pts',(-56.7352127320762,-109.285751731342,
173.632465095959));
#33200=CARTESIAN_POINT('Ctrl Pts',(-56.4170493951529,-109.351196001371,
173.890264770392));
#33201=CARTESIAN_POINT('Ctrl Pts',(-56.1614914509907,-109.411203428396,
174.201106153446));
#33202=CARTESIAN_POINT('Ctrl Pts',(-55.7944229529086,-109.515031296611,
174.893544837145));
#33203=CARTESIAN_POINT('Ctrl Pts',(-55.6813524717919,-109.558117348435,
175.265535181684));
#33204=CARTESIAN_POINT('Ctrl Pts',(-55.5998985858842,-109.626862665881,
176.048382432889));
#33205=CARTESIAN_POINT('Ctrl Pts',(-55.6387473083432,-109.655484272148,
176.452370074809));
#33206=CARTESIAN_POINT('Ctrl Pts',(-55.868029291656,-109.695737482092,177.207886397512));
#33207=CARTESIAN_POINT('Ctrl Pts',(-56.0505770001051,-109.707309838255,
177.553663281513));
#33208=CARTESIAN_POINT('Ctrl Pts',(-56.5452510503984,-109.714635373818,
178.169665278726));
#33209=CARTESIAN_POINT('Ctrl Pts',(-56.8577772827169,-109.714081033111,
178.430169988861));
#33210=CARTESIAN_POINT('Ctrl Pts',(-57.5531111255177,-109.704650268233,
178.806230716513));
#33211=CARTESIAN_POINT('Ctrl Pts',(-57.9262706557755,-109.695903226762,
178.923259339289));
#33212=CARTESIAN_POINT('Ctrl Pts',(-58.7110365519678,-109.672302387285,
179.011598524387));
#33213=CARTESIAN_POINT('Ctrl Pts',(-59.1162068108045,-109.661871485081,
178.976030955739));
#33214=CARTESIAN_POINT('Ctrl Pts',(-59.874306110465,-109.645749751471,178.752358640327));
#33215=CARTESIAN_POINT('Ctrl Pts',(-60.2214202961156,-109.639780337178,
178.572088598617));
#33216=CARTESIAN_POINT('Ctrl Pts',(-60.8403185693232,-109.633861493506,
178.081016570927));
#33217=CARTESIAN_POINT('Ctrl Pts',(-61.1028309355344,-109.638638792637,
177.77020748683));
#33218=CARTESIAN_POINT('Ctrl Pts',(-61.4836388910742,-109.662739067824,
177.077811674308));
#33219=CARTESIAN_POINT('Ctrl Pts',(-61.6033035590136,-109.681018239856,
176.705832791815));
#33220=CARTESIAN_POINT('Ctrl Pts',(-61.6975246410322,-109.731032931215,
175.922987958783));
#33221=CARTESIAN_POINT('Ctrl Pts',(-61.6656352099253,-109.767195351502,
175.518990212935));
#33222=CARTESIAN_POINT('Ctrl Pts',(-61.4500864154564,-109.854871455099,
174.763435739915));
#33223=CARTESIAN_POINT('Ctrl Pts',(-61.2741229161873,-109.904667446682,
174.417632232832));
#33224=CARTESIAN_POINT('Ctrl Pts',(-60.792181426792,-110.016104397719,173.801562135608));
#33225=CARTESIAN_POINT('Ctrl Pts',(-60.486589957542,-110.081445211935,173.54101620596));
#33226=CARTESIAN_POINT('Ctrl Pts',(-59.8049322193929,-110.218811842546,
173.164868231645));
#33227=CARTESIAN_POINT('Ctrl Pts',(-59.4383254942508,-110.288932495851,
173.047794684789));
#33228=CARTESIAN_POINT('Ctrl Pts',(-58.6662232412889,-110.431302039515,
172.959363849016));
#33229=CARTESIAN_POINT('Ctrl Pts',(-58.2679512671702,-110.506523147845,
172.994885945774));
#33230=CARTESIAN_POINT('Ctrl Pts',(-57.5344736456333,-110.648457072547,
173.215168361749));
#33231=CARTESIAN_POINT('Ctrl Pts',(-57.2034746106801,-110.714119105546,
173.387890345956));
#33232=CARTESIAN_POINT('Ctrl Pts',(-56.912660501291,-110.773526816678,173.617797875548));
#33233=CARTESIAN_POINT('Ctrl Pts',(-56.9656635035151,-111.270709561506,
173.617797875548));
#33234=CARTESIAN_POINT('Ctrl Pts',(-57.2530242924217,-111.212007297116,
173.390620421133));
#33235=CARTESIAN_POINT('Ctrl Pts',(-57.5796610124049,-111.147190193251,
173.219244299193));
#33236=CARTESIAN_POINT('Ctrl Pts',(-58.3078397992584,-111.006203887084,
172.997015018109));
#33237=CARTESIAN_POINT('Ctrl Pts',(-58.7057641868601,-110.931008351939,
172.95970017545));
#33238=CARTESIAN_POINT('Ctrl Pts',(-59.4779355658374,-110.78854645965,173.044516359449));
#33239=CARTESIAN_POINT('Ctrl Pts',(-59.8449459276702,-110.7185255451,173.159819039321));
#33240=CARTESIAN_POINT('Ctrl Pts',(-60.5280563098773,-110.581039590946,
173.532527712615));
#33241=CARTESIAN_POINT('Ctrl Pts',(-60.8347373006261,-110.515570320914,
173.791446869636));
#33242=CARTESIAN_POINT('Ctrl Pts',(-61.3194587580523,-110.403745738482,
174.404830339381));
#33243=CARTESIAN_POINT('Ctrl Pts',(-61.4970712714973,-110.353927151605,
174.749585468772));
#33244=CARTESIAN_POINT('Ctrl Pts',(-61.7163224303376,-110.265894560392,
175.503633857603));
#33245=CARTESIAN_POINT('Ctrl Pts',(-61.7502677930237,-110.229499779283,
175.907228754417));
#33246=CARTESIAN_POINT('Ctrl Pts',(-61.6601847599457,-110.178945932191,
176.690163364291));
#33247=CARTESIAN_POINT('Ctrl Pts',(-61.5425695762014,-110.160612637411,
177.062593254234));
#33248=CARTESIAN_POINT('Ctrl Pts',(-61.1657127416764,-110.13613222623,177.756669717359));
#33249=CARTESIAN_POINT('Ctrl Pts',(-60.9050660910469,-110.131141906601,
178.068743926659));
#33250=CARTESIAN_POINT('Ctrl Pts',(-60.2892402183872,-110.136627969695,
178.563052580947));
#33251=CARTESIAN_POINT('Ctrl Pts',(-59.9433474574605,-110.142643484303,
178.745217390532));
#33252=CARTESIAN_POINT('Ctrl Pts',(-59.1869815832755,-110.158624588141,
178.97318046481));
#33253=CARTESIAN_POINT('Ctrl Pts',(-58.782272969959,-110.1689911531,179.011134939961));
#33254=CARTESIAN_POINT('Ctrl Pts',(-57.9973932965281,-110.192491130305,
178.927609078305));
#33255=CARTESIAN_POINT('Ctrl Pts',(-57.6237363130985,-110.20148029302,178.81293809646));
#33256=CARTESIAN_POINT('Ctrl Pts',(-56.9264807797385,-110.211163403075,
178.441456326529));
#33257=CARTESIAN_POINT('Ctrl Pts',(-56.6125027299724,-110.211856329087,
178.183118417219));
#33258=CARTESIAN_POINT('Ctrl Pts',(-56.1141043193472,-110.204806539356,
177.570694390137));
#33259=CARTESIAN_POINT('Ctrl Pts',(-55.9294048654883,-110.19366632275,177.226312697729));
#33260=CARTESIAN_POINT('Ctrl Pts',(-55.6952081929263,-110.153988093797,
176.472802651947));
#33261=CARTESIAN_POINT('Ctrl Pts',(-55.65362061935,-110.125641145017,176.069353712619));
#33262=CARTESIAN_POINT('Ctrl Pts',(-55.7295409368849,-110.057355550999,
175.286389822705));
#33263=CARTESIAN_POINT('Ctrl Pts',(-55.8399309532616,-110.014772600424,
174.913799450684));
#33264=CARTESIAN_POINT('Ctrl Pts',(-56.2017547688197,-109.911558719943,
174.21912806331));
#33265=CARTESIAN_POINT('Ctrl Pts',(-56.4548255081651,-109.851797916736,
173.9066065584));
#33266=CARTESIAN_POINT('Ctrl Pts',(-56.7765766114406,-109.785322912825,
173.641817041259));
#33267=CARTESIAN_POINT('Ctrl Pts',(-56.7915603540426,-109.782244769145,
173.62973078035));
#33268=CARTESIAN_POINT('Ctrl Pts',(-56.8066544968429,-109.779161327021,
173.617797875548));
#33269=CARTESIAN_POINT('Origin',(-54.1598171290174,-67.5719248685924,175.985485069079));
#33270=CARTESIAN_POINT('',(-56.5946424879466,-107.790430347706,173.617797875548));
#33271=CARTESIAN_POINT('',(-56.6476454901706,-108.287613092535,173.617797875548));
#33272=CARTESIAN_POINT('',(-52.327900808713,-67.7672193871761,173.617797875548));
#33273=CARTESIAN_POINT('Ctrl Pts',(-56.5946424879466,-107.790430347706,
173.617797875548));
#33274=CARTESIAN_POINT('Ctrl Pts',(-56.5850528888066,-107.792389317774,
173.625379079406));
#33275=CARTESIAN_POINT('Ctrl Pts',(-56.5755077744589,-107.794346164695,
173.63302224271));
#33276=CARTESIAN_POINT('Ctrl Pts',(-56.2571278640508,-107.859852178723,
173.89123722131));
#33277=CARTESIAN_POINT('Ctrl Pts',(-56.0017181366438,-107.919844961586,
174.20217945882));
#33278=CARTESIAN_POINT('Ctrl Pts',(-55.6349627050625,-108.023636222819,
174.894752021053));
#33279=CARTESIAN_POINT('Ctrl Pts',(-55.5220522045499,-108.066691989198,
175.266778173584));
#33280=CARTESIAN_POINT('Ctrl Pts',(-55.4409283932585,-108.135409927915,
176.049632933467));
#33281=CARTESIAN_POINT('Ctrl Pts',(-55.4799405763947,-108.164015184729,
176.453588965104));
#33282=CARTESIAN_POINT('Ctrl Pts',(-55.7095159037854,-108.20423411699,177.208986061887));
#33283=CARTESIAN_POINT('Ctrl Pts',(-55.8921918566918,-108.215780492895,
177.554679766979));
#33284=CARTESIAN_POINT('Ctrl Pts',(-56.3870881131878,-108.223089603402,
178.170468956079));
#33285=CARTESIAN_POINT('Ctrl Pts',(-56.6997012083162,-108.222527004388,
178.430844852629));
#33286=CARTESIAN_POINT('Ctrl Pts',(-57.3951499180593,-108.213081199548,
178.806632962964));
#33287=CARTESIAN_POINT('Ctrl Pts',(-57.7683390387316,-108.204319553149,
178.92352121324));
#33288=CARTESIAN_POINT('Ctrl Pts',(-58.5531121193096,-108.180724703527,
179.011574005107));
#33289=CARTESIAN_POINT('Ctrl Pts',(-58.9582553034152,-108.170297619943,
178.975864349681));
#33290=CARTESIAN_POINT('Ctrl Pts',(-59.716251799764,-108.154184247559,178.75193659395));
#33291=CARTESIAN_POINT('Ctrl Pts',(-60.0632933251485,-108.148211927685,
178.571553874758));
#33292=CARTESIAN_POINT('Ctrl Pts',(-60.6820092495562,-108.142318806873,
178.080289229826));
#33293=CARTESIAN_POINT('Ctrl Pts',(-60.944410931511,-108.147108773163,177.769404674777));
#33294=CARTESIAN_POINT('Ctrl Pts',(-61.3249841793317,-108.171231653807,
177.076908684947));
#33295=CARTESIAN_POINT('Ctrl Pts',(-61.4445270812119,-108.189513898651,
176.704903015587));
#33296=CARTESIAN_POINT('Ctrl Pts',(-61.5385024833708,-108.239560624799,
175.92205254238));
#33297=CARTESIAN_POINT('Ctrl Pts',(-61.506490942202,-108.275736869974,175.518078420413));
#33298=CARTESIAN_POINT('Ctrl Pts',(-61.2907222307222,-108.363434171794,
174.762613115205));
#33299=CARTESIAN_POINT('Ctrl Pts',(-61.1146608598201,-108.413231380705,
174.416871828143));
#33300=CARTESIAN_POINT('Ctrl Pts',(-60.6325542930779,-108.524691364817,
173.800960895677));
#33301=CARTESIAN_POINT('Ctrl Pts',(-60.3268979935203,-108.590039841336,
173.540511306411));
#33302=CARTESIAN_POINT('Ctrl Pts',(-59.6451538789054,-108.727413591522,
173.16456724127));
#33303=CARTESIAN_POINT('Ctrl Pts',(-59.2785232148838,-108.797528224217,
173.047598688914));
#33304=CARTESIAN_POINT('Ctrl Pts',(-58.5064166364563,-108.939903283303,
172.959382058774));
#33305=CARTESIAN_POINT('Ctrl Pts',(-58.108165043366,-109.015122917537,172.995010430971));
#33306=CARTESIAN_POINT('Ctrl Pts',(-57.3750012843017,-109.15700073919,173.215409376339));
#33307=CARTESIAN_POINT('Ctrl Pts',(-57.0442609969736,-109.22261266833,173.388052101168));
#33308=CARTESIAN_POINT('Ctrl Pts',(-56.7536514946188,-109.281978582192,
173.617797875548));
#33309=CARTESIAN_POINT('Ctrl Pts',(-56.8066544968429,-109.779161327021,
173.617797875548));
#33310=CARTESIAN_POINT('Ctrl Pts',(-57.0911495393457,-109.721044479324,
173.39288598066));
#33311=CARTESIAN_POINT('Ctrl Pts',(-57.4141738946121,-109.656927388934,
173.222639859508));
#33312=CARTESIAN_POINT('Ctrl Pts',(-58.1379530574512,-109.516728615689,
172.998827087965));
#33313=CARTESIAN_POINT('Ctrl Pts',(-58.5355831915522,-109.44155542204,172.96002607628));
#33314=CARTESIAN_POINT('Ctrl Pts',(-59.3078056750551,-109.299018087244,
173.041843688515));
#33315=CARTESIAN_POINT('Ctrl Pts',(-59.6751503694515,-109.229076912984,
173.155678725912));
#33316=CARTESIAN_POINT('Ctrl Pts',(-60.3594578804737,-109.091493285794,
173.525536872694));
#33317=CARTESIAN_POINT('Ctrl Pts',(-60.6670354869716,-109.025918812521,
173.783104843788));
#33318=CARTESIAN_POINT('Ctrl Pts',(-61.1540539887737,-108.913774347019,
174.394258350367));
#33319=CARTESIAN_POINT('Ctrl Pts',(-61.3330304093029,-108.863933709409,
174.73814629728));
#33320=CARTESIAN_POINT('Ctrl Pts',(-61.5553389931981,-108.775607355957,
175.490943063268));
#33321=CARTESIAN_POINT('Ctrl Pts',(-61.5909823940636,-108.739021313527,
175.894197042022));
#33322=CARTESIAN_POINT('Ctrl Pts',(-61.5043197220977,-108.688022485585,
176.677197469897));
#33323=CARTESIAN_POINT('Ctrl Pts',(-61.38839627213,-108.669640650694,177.049999895134));
#33324=CARTESIAN_POINT('Ctrl Pts',(-61.014801889141,-108.644847014232,177.745454875642));
#33325=CARTESIAN_POINT('Ctrl Pts',(-60.755699625328,-108.639681161078,178.0585650829));
#33326=CARTESIAN_POINT('Ctrl Pts',(-60.1424149719043,-108.644810265419,
178.555536733806));
#33327=CARTESIAN_POINT('Ctrl Pts',(-59.7975279520725,-108.650859342097,
178.739262801913));
#33328=CARTESIAN_POINT('Ctrl Pts',(-59.0425978361606,-108.666724527345,
178.970753810606));
#33329=CARTESIAN_POINT('Ctrl Pts',(-58.6382797420984,-108.677037884769,
179.010671108535));
#33330=CARTESIAN_POINT('Ctrl Pts',(-57.8533175485435,-108.700454535644,
178.931107044723));
#33331=CARTESIAN_POINT('Ctrl Pts',(-57.4792508646161,-108.709637658776,
178.818374185432));
#33332=CARTESIAN_POINT('Ctrl Pts',(-56.7804276486958,-108.719527793124,
178.450656786394));
#33333=CARTESIAN_POINT('Ctrl Pts',(-56.4652674748089,-108.720334450473,
178.19410526483));
#33334=CARTESIAN_POINT('Ctrl Pts',(-55.9638197847289,-108.713511139287,
177.584628405587));
#33335=CARTESIAN_POINT('Ctrl Pts',(-55.7773549261986,-108.702719464541,
177.241390696198));
#33336=CARTESIAN_POINT('Ctrl Pts',(-55.5391375163741,-108.663512727931,
176.489535882969));
#33337=CARTESIAN_POINT('Ctrl Pts',(-55.495308995132,-108.635391641772,176.08654209288));
#33338=CARTESIAN_POINT('Ctrl Pts',(-55.5666967264702,-108.567483768668,
175.303497323436));
#33339=CARTESIAN_POINT('Ctrl Pts',(-55.6748935190697,-108.525305592323,
174.930415854593));
#33340=CARTESIAN_POINT('Ctrl Pts',(-56.0324273128658,-108.422595081495,
174.233934107104));
#33341=CARTESIAN_POINT('Ctrl Pts',(-56.283457047243,-108.36303804919,173.920053289181));
#33342=CARTESIAN_POINT('Ctrl Pts',(-56.6080785837145,-108.295725776454,
173.649495489686));
#33343=CARTESIAN_POINT('Ctrl Pts',(-56.6277661435339,-108.29167405947,173.633513796226));
#33344=CARTESIAN_POINT('Ctrl Pts',(-56.6476454901706,-108.287613092535,
173.617797875548));
#33345=CARTESIAN_POINT('Origin',(-54.1598171290174,-67.5719248685924,175.985485069079));
#33346=CARTESIAN_POINT('',(-56.4356334812744,-106.298882113221,173.617797875548));
#33347=CARTESIAN_POINT('',(-56.4886364834984,-106.796064858049,173.617797875548));
#33348=CARTESIAN_POINT('',(-52.327900808713,-67.7672193871761,173.617797875548));
#33349=CARTESIAN_POINT('Ctrl Pts',(-56.4356334812744,-106.298882113221,
173.617797875548));
#33350=CARTESIAN_POINT('Ctrl Pts',(-56.4254200290466,-106.300968524437,
173.625872275979));
#33351=CARTESIAN_POINT('Ctrl Pts',(-56.4152570474672,-106.30305252532,173.634016952005));
#33352=CARTESIAN_POINT('Ctrl Pts',(-56.0964913676981,-106.368668668546,
173.892973755425));
#33353=CARTESIAN_POINT('Ctrl Pts',(-55.8413462486002,-106.428635290865,
174.204095814467));
#33354=CARTESIAN_POINT('Ctrl Pts',(-55.4751495605777,-106.53236120433,174.896907124857));
#33355=CARTESIAN_POINT('Ctrl Pts',(-55.3625245910191,-106.575362999072,
175.268997188014));
#33356=CARTESIAN_POINT('Ctrl Pts',(-55.2819899528662,-106.644032053867,
176.051865176928));
#33357=CARTESIAN_POINT('Ctrl Pts',(-55.3212938805754,-106.672608116728,
176.455764620233));
#33358=CARTESIAN_POINT('Ctrl Pts',(-55.5513927597733,-106.712765858169,
177.210948761198));
#33359=CARTESIAN_POINT('Ctrl Pts',(-55.7342976581586,-106.724265924084,
177.556493980804));
#33360=CARTESIAN_POINT('Ctrl Pts',(-56.229590530456,-106.731545709104,178.171903119991));
#33361=CARTESIAN_POINT('Ctrl Pts',(-56.5423585907699,-106.730968366645,
178.432048950983));
#33362=CARTESIAN_POINT('Ctrl Pts',(-57.2380122593381,-106.721495712049,
178.807350285382));
#33363=CARTESIAN_POINT('Ctrl Pts',(-57.6112542237444,-106.712708047288,
178.923987893515));
#33364=CARTESIAN_POINT('Ctrl Pts',(-58.3960400034764,-106.689123897715,
179.011529255791));
#33365=CARTESIAN_POINT('Ctrl Pts',(-58.80113471485,-106.678703636253,178.975565887805));
#33366=CARTESIAN_POINT('Ctrl Pts',(-59.5589475234609,-106.662605196984,
178.751182020938));
#33367=CARTESIAN_POINT('Ctrl Pts',(-59.9058592904742,-106.656627739491,
178.570598067742));
#33368=CARTESIAN_POINT('Ctrl Pts',(-60.5242494393363,-106.650780562228,
178.078989466319));
#33369=CARTESIAN_POINT('Ctrl Pts',(-60.7864533631301,-106.655593151436,
177.767970199565));
#33370=CARTESIAN_POINT('Ctrl Pts',(-61.1666073584006,-106.679756403993,
177.075295373119));
#33371=CARTESIAN_POINT('Ctrl Pts',(-61.2859327593645,-106.698044182358,
176.703241853839));
#33372=CARTESIAN_POINT('Ctrl Pts',(-61.379469268274,-106.748148129126,175.920381402153));
#33373=CARTESIAN_POINT('Ctrl Pts',(-61.3472395990604,-106.784349062473,
175.516449575185));
#33374=CARTESIAN_POINT('Ctrl Pts',(-61.1310780509395,-106.872084223286,
174.761143641781));
#33375=CARTESIAN_POINT('Ctrl Pts',(-60.9548418280128,-106.921883645804,
174.415513514529));
#33376=CARTESIAN_POINT('Ctrl Pts',(-60.4724403685815,-107.033384771253,
173.79988702853));
#33377=CARTESIAN_POINT('Ctrl Pts',(-60.1666682984753,-107.098746924849,
173.539609622196));
#33378=CARTESIAN_POINT('Ctrl Pts',(-59.4847699184305,-107.236133382704,
173.164029918927));
#33379=CARTESIAN_POINT('Ctrl Pts',(-59.1180964810416,-107.306237290906,
173.04724897829));
#33380=CARTESIAN_POINT('Ctrl Pts',(-58.3459822447139,-107.448622192787,
172.959415139878));
#33381=CARTESIAN_POINT('Ctrl Pts',(-57.9477671412253,-107.523839179786,
172.99523341803));
#33382=CARTESIAN_POINT('Ctrl Pts',(-57.2151643108154,-107.665616726848,
173.215840241925));
#33383=CARTESIAN_POINT('Ctrl Pts',(-56.8848863394666,-107.731139129254,
173.388341172012));
#33384=CARTESIAN_POINT('Ctrl Pts',(-56.5946424879466,-107.790430347706,
173.617797875548));
#33385=CARTESIAN_POINT('Ctrl Pts',(-56.6476454901706,-108.287613092535,
173.617797875548));
#33386=CARTESIAN_POINT('Ctrl Pts',(-56.9271567322471,-108.230514339101,
173.396826000098));
#33387=CARTESIAN_POINT('Ctrl Pts',(-57.2439154945503,-108.16761214956,173.228573427838));
#33388=CARTESIAN_POINT('Ctrl Pts',(-57.9600385015072,-108.028785391668,
173.002076223596));
#33389=CARTESIAN_POINT('Ctrl Pts',(-58.3571443608821,-107.953653470066,
172.96069400138));
#33390=CARTESIAN_POINT('Ctrl Pts',(-59.1294421972055,-107.810987508801,
173.037298982509));
#33391=CARTESIAN_POINT('Ctrl Pts',(-59.4973670458519,-107.741178468716,
173.148585634684));
#33392=CARTESIAN_POINT('Ctrl Pts',(-60.183738614452,-107.603427863765,173.513494069579));
#33393=CARTESIAN_POINT('Ctrl Pts',(-60.4928593242721,-107.537673434034,
173.768709668626));
#33394=CARTESIAN_POINT('Ctrl Pts',(-60.9838513802244,-107.42497650289,174.375984000262));
#33395=CARTESIAN_POINT('Ctrl Pts',(-61.1651902167986,-107.375090420716,
174.718369817544));
#33396=CARTESIAN_POINT('Ctrl Pts',(-61.3927839950836,-107.286257596546,
175.468986101822));
#33397=CARTESIAN_POINT('Ctrl Pts',(-61.4313630690126,-107.249342283814,
175.871633114773));
#33398=CARTESIAN_POINT('Ctrl Pts',(-61.3506197086899,-107.197574793199,
176.654729483581));
#33399=CARTESIAN_POINT('Ctrl Pts',(-61.2376192257481,-107.179100797428,
177.028176172647));
#33400=CARTESIAN_POINT('Ctrl Pts',(-60.8696636141788,-107.15376717538,177.725994234135));
#33401=CARTESIAN_POINT('Ctrl Pts',(-60.6132387257904,-107.148298710394,
178.040876606816));
#33402=CARTESIAN_POINT('Ctrl Pts',(-60.0043555131084,-107.152811678755,
178.542430749144));
#33403=CARTESIAN_POINT('Ctrl Pts',(-59.6612009197382,-107.158909180165,
178.728848560318));
#33404=CARTESIAN_POINT('Ctrl Pts',(-58.9087617030258,-107.174574437879,
178.966405587943));
#33405=CARTESIAN_POINT('Ctrl Pts',(-58.5051382541458,-107.18479566087,179.009698156442));
#33406=CARTESIAN_POINT('Ctrl Pts',(-57.7200575738111,-107.208068199376,
178.936955000543));
#33407=CARTESIAN_POINT('Ctrl Pts',(-57.3452848574596,-107.217573992269,
178.827554031224));
#33408=CARTESIAN_POINT('Ctrl Pts',(-56.6437920571633,-107.227819128835,
178.466308091154));
#33409=CARTESIAN_POINT('Ctrl Pts',(-56.3266238180267,-107.228820871757,
178.212838044334));
#33410=CARTESIAN_POINT('Ctrl Pts',(-55.8199603392634,-107.222386462151,
177.60843981115));
#33411=CARTESIAN_POINT('Ctrl Pts',(-55.6304676592532,-107.212179880791,
177.267162528894));
#33412=CARTESIAN_POINT('Ctrl Pts',(-55.3853790529965,-107.173781187623,
176.518165416363));
#33413=CARTESIAN_POINT('Ctrl Pts',(-55.3377206422314,-107.146048492687,
176.115979638056));
#33414=CARTESIAN_POINT('Ctrl Pts',(-55.401350875959,-107.078789512188,175.332827144021));
#33415=CARTESIAN_POINT('Ctrl Pts',(-55.5057985904533,-107.037288828511,
174.958905787373));
#33416=CARTESIAN_POINT('Ctrl Pts',(-55.856002399949,-106.935440746386,174.259363819959));
#33417=CARTESIAN_POINT('Ctrl Pts',(-56.1035315863118,-106.876236083587,
173.943191795572));
#33418=CARTESIAN_POINT('Ctrl Pts',(-56.4329223458913,-106.807505761024,
173.662674453979));
#33419=CARTESIAN_POINT('Ctrl Pts',(-56.4605880039554,-106.801794621209,
173.639972028838));
#33420=CARTESIAN_POINT('Ctrl Pts',(-56.4886364834982,-106.796064858049,
173.617797875548));
#33421=CARTESIAN_POINT('Origin',(-54.1598171290174,-67.5719248685924,175.985485069079));
#33422=CARTESIAN_POINT('',(-56.2766244746021,-104.807333878735,173.617797875548));
#33423=CARTESIAN_POINT('',(-56.3296274768259,-105.304516623564,173.617797875548));
#33424=CARTESIAN_POINT('',(-52.327900808713,-67.7672193871761,173.617797875548));
#33425=CARTESIAN_POINT('Ctrl Pts',(-56.2766244746021,-104.807333878735,
173.617797875548));
#33426=CARTESIAN_POINT('Ctrl Pts',(-56.2653006888845,-104.809647109659,
173.626750067054));
#33427=CARTESIAN_POINT('Ctrl Pts',(-56.2540389651426,-104.811957373387,
173.635788627629));
#33428=CARTESIAN_POINT('Ctrl Pts',(-55.9345890254792,-104.877769330124,
173.896067820171));
#33429=CARTESIAN_POINT('Ctrl Pts',(-55.6799151601245,-104.93768930917,174.207509397213));
#33430=CARTESIAN_POINT('Ctrl Pts',(-55.3147130356128,-105.041298860261,
174.900745074777));
#33431=CARTESIAN_POINT('Ctrl Pts',(-55.2025963324754,-105.084204839733,
175.272948907266));
#33432=CARTESIAN_POINT('Ctrl Pts',(-55.1231106586534,-105.152786818001,
176.055839897832));
#33433=CARTESIAN_POINT('Ctrl Pts',(-55.1629339199115,-105.181310870104,
176.459638067914));
#33434=CARTESIAN_POINT('Ctrl Pts',(-55.3939647457702,-105.221359647692,
177.214442614334));
#33435=CARTESIAN_POINT('Ctrl Pts',(-55.5772773642361,-105.232777466452,
177.559723426792));
#33436=CARTESIAN_POINT('Ctrl Pts',(-56.0732763221029,-105.240005017301,
178.174455309114));
#33437=CARTESIAN_POINT('Ctrl Pts',(-56.3863200207768,-105.239401417322,
178.434191095882));
#33438=CARTESIAN_POINT('Ctrl Pts',(-57.0823383594249,-105.229880947087,
178.808625258783));
#33439=CARTESIAN_POINT('Ctrl Pts',(-57.4556744888722,-105.22104712134,178.924816364367));
#33440=CARTESIAN_POINT('Ctrl Pts',(-58.2404824815195,-105.197482048637,
179.011446458192));
#33441=CARTESIAN_POINT('Ctrl Pts',(-58.6454904306518,-105.187073952339,
178.9750310886));
#33442=CARTESIAN_POINT('Ctrl Pts',(-59.4029756075432,-105.17100212725,178.749834659797));
#33443=CARTESIAN_POINT('Ctrl Pts',(-59.7496561557124,-105.165015677895,
178.568892085678));
#33444=CARTESIAN_POINT('Ctrl Pts',(-60.3674653767356,-105.159250390754,
178.076670657764));
#33445=CARTESIAN_POINT('Ctrl Pts',(-60.6293166077287,-105.164103297252,
177.765411556099));
#33446=CARTESIAN_POINT('Ctrl Pts',(-61.0087231919709,-105.188338497418,
177.072418255627));
#33447=CARTESIAN_POINT('Ctrl Pts',(-61.1276608703734,-105.206636282563,
176.700279429192));
#33448=CARTESIAN_POINT('Ctrl Pts',(-61.2204148225146,-105.256842230424,
175.917401495486));
#33449=CARTESIAN_POINT('Ctrl Pts',(-61.1877962730522,-105.293087154001,
175.513545374999));
#33450=CARTESIAN_POINT('Ctrl Pts',(-60.9709343922714,-105.380889785063,
174.758523854962));
#33451=CARTESIAN_POINT('Ctrl Pts',(-60.7943863725805,-105.430693278442,
174.413091951295));
#33452=CARTESIAN_POINT('Ctrl Pts',(-60.3114591405253,-105.54226774086,173.797972982327));
#33453=CARTESIAN_POINT('Ctrl Pts',(-60.0054807927948,-105.607654245323,
173.53800282471));
#33454=CARTESIAN_POINT('Ctrl Pts',(-59.3233074853434,-105.745063326069,
173.163073072182));
#33455=CARTESIAN_POINT('Ctrl Pts',(-58.9565577567983,-105.815148211003,
173.046626790759));
#33456=CARTESIAN_POINT('Ctrl Pts',(-58.184430087075,-105.957550630314,172.959475878003));
#33457=CARTESIAN_POINT('Ctrl Pts',(-57.7862803003474,-106.03276285313,172.99563292452));
#33458=CARTESIAN_POINT('Ctrl Pts',(-57.0546783531652,-106.174361450359,
173.21660946132));
#33459=CARTESIAN_POINT('Ctrl Pts',(-56.7252249493366,-106.239724164121,
173.388856923705));
#33460=CARTESIAN_POINT('Ctrl Pts',(-56.4356334812743,-106.298882113221,
173.617797875548));
#33461=CARTESIAN_POINT('Ctrl Pts',(-56.4886364834982,-106.796064858049,
173.617797875548));
#33462=CARTESIAN_POINT('Ctrl Pts',(-56.7596693332081,-106.74069807658,173.403528722494));
#33463=CARTESIAN_POINT('Ctrl Pts',(-57.0658176208757,-106.679855420073,
173.238750333755));
#33464=CARTESIAN_POINT('Ctrl Pts',(-57.768903450155,-106.543369527441,173.007888959857));
#33465=CARTESIAN_POINT('Ctrl Pts',(-58.1650808581089,-106.468314870845,
172.962125616787));
#33466=CARTESIAN_POINT('Ctrl Pts',(-58.9374674226472,-106.325437595314,
173.02986875357));
#33467=CARTESIAN_POINT('Ctrl Pts',(-59.306375777374,-106.255834256616,173.136831075859));
#33468=CARTESIAN_POINT('Ctrl Pts',(-59.9962073277028,-106.117807896946,
173.493340806289));
#33469=CARTESIAN_POINT('Ctrl Pts',(-60.3079061661428,-106.051756025524,
173.74454746787));
#33470=CARTESIAN_POINT('Ctrl Pts',(-60.8055969341733,-105.93813031074,174.345219194373));
#33471=CARTESIAN_POINT('Ctrl Pts',(-60.9909278410113,-105.888146352887,
174.685066619392));
#33472=CARTESIAN_POINT('Ctrl Pts',(-61.2274212948024,-105.798464534594,
175.431962757536));
#33473=CARTESIAN_POINT('Ctrl Pts',(-61.270944175395,-105.760998732939,175.833536994212));
#33474=CARTESIAN_POINT('Ctrl Pts',(-61.2001876164997,-105.707938494202,
176.616743498004));
#33475=CARTESIAN_POINT('Ctrl Pts',(-61.0921055453824,-105.689285486627,
176.991276212819));
#33476=CARTESIAN_POINT('Ctrl Pts',(-60.7336426290013,-105.66304676212,177.693016934879));
#33477=CARTESIAN_POINT('Ctrl Pts',(-60.4817475119257,-105.657071142152,
178.010829710717));
#33478=CARTESIAN_POINT('Ctrl Pts',(-59.8803004238055,-105.660549212733,
178.52004077432));
#33479=CARTESIAN_POINT('Ctrl Pts',(-59.5400458076867,-105.666700898019,
178.710971772271));
#33480=CARTESIAN_POINT('Ctrl Pts',(-58.7918260736236,-105.682030791257,
178.958651454036));
#33481=CARTESIAN_POINT('Ctrl Pts',(-58.3894273848151,-105.692096451067,
179.007576569016));
#33482=CARTESIAN_POINT('Ctrl Pts',(-57.6042154056154,-105.715126122877,
178.946240936123));
#33483=CARTESIAN_POINT('Ctrl Pts',(-57.2282595229731,-105.725139729359,
178.842399324893));
#33484=CARTESIAN_POINT('Ctrl Pts',(-56.522384265223,-105.735974594548,178.491949605217));
#33485=CARTESIAN_POINT('Ctrl Pts',(-56.2019343365732,-105.737300525353,
178.243648763131));
#33486=CARTESIAN_POINT('Ctrl Pts',(-55.6866432506554,-105.731513670933,
177.64775703023));
#33487=CARTESIAN_POINT('Ctrl Pts',(-55.4921181006516,-105.722243834646,
177.309733209288));
#33488=CARTESIAN_POINT('Ctrl Pts',(-55.2356800943781,-105.685186175791,
176.565536774304));
#33489=CARTESIAN_POINT('Ctrl Pts',(-55.1816963441142,-105.658101573039,
176.164769489015));
#33490=CARTESIAN_POINT('Ctrl Pts',(-55.2324810832818,-105.591923835622,
175.381524112892));
#33491=CARTESIAN_POINT('Ctrl Pts',(-55.3307322750497,-105.551502685792,
175.006213016851));
#33492=CARTESIAN_POINT('Ctrl Pts',(-55.668832645442,-105.451085144376,174.301708294574));
#33493=CARTESIAN_POINT('Ctrl Pts',(-55.9105463702708,-105.392473767471,
173.981839983604));
#33494=CARTESIAN_POINT('Ctrl Pts',(-56.2474333770332,-105.321437836364,
173.684598278449));
#33495=CARTESIAN_POINT('Ctrl Pts',(-56.2881090861829,-105.312998029652,
173.650620872498));
#33496=CARTESIAN_POINT('Ctrl Pts',(-56.3296274768257,-105.304516623564,
173.617797875548));
#33497=CARTESIAN_POINT('Origin',(-54.1598171290174,-67.5719248685924,175.985485069079));
#33498=CARTESIAN_POINT('',(-56.1176154679299,-103.31578564425,173.617797875548));
#33499=CARTESIAN_POINT('',(-56.1706184701534,-103.812968389078,173.617797875548));
#33500=CARTESIAN_POINT('',(-52.327900808713,-67.7672193871761,173.617797875548));
#33501=CARTESIAN_POINT('Ctrl Pts',(-56.1176154679299,-103.31578564425,173.617797875548));
#33502=CARTESIAN_POINT('Ctrl Pts',(-56.1043250103344,-103.31850062829,173.628304849502));
#33503=CARTESIAN_POINT('Ctrl Pts',(-56.0911200963041,-103.321211514357,
173.638930756877));
#33504=CARTESIAN_POINT('Ctrl Pts',(-55.7704655142177,-103.387369689626,
173.901558773232));
#33505=CARTESIAN_POINT('Ctrl Pts',(-55.5166273065249,-103.447206792302,
174.213564632224));
#33506=CARTESIAN_POINT('Ctrl Pts',(-55.1531871492074,-103.550610059877,
174.907550219798));
#33507=CARTESIAN_POINT('Ctrl Pts',(-55.0419709606547,-103.593347093109,
175.27995563458));
#33508=CARTESIAN_POINT('Ctrl Pts',(-54.9643443732856,-103.661774607987,
176.062885655826));
#33509=CARTESIAN_POINT('Ctrl Pts',(-55.0050877700344,-103.690206374978,
176.466502692261));
#33510=CARTESIAN_POINT('Ctrl Pts',(-55.2377697079123,-103.730061973367,
177.22063307226));
#33511=CARTESIAN_POINT('Ctrl Pts',(-55.4218052661154,-103.741334665286,
177.565445136868));
#33512=CARTESIAN_POINT('Ctrl Pts',(-55.9190554664435,-103.748469568618,
178.178974772616));
#33513=CARTESIAN_POINT('Ctrl Pts',(-56.2325868532032,-103.747819406367,
178.437982466093));
#33514=CARTESIAN_POINT('Ctrl Pts',(-56.9292507462071,-103.738214153437,
178.810878113076));
#33515=CARTESIAN_POINT('Ctrl Pts',(-57.3027540248708,-103.729299028287,
178.926277061376));
#33516=CARTESIAN_POINT('Ctrl Pts',(-58.0876001328413,-103.705767849205,
179.011289843778));
#33517=CARTESIAN_POINT('Ctrl Pts',(-58.4924528567469,-103.695381373337,
178.97407247311));
#33518=CARTESIAN_POINT('Ctrl Pts',(-59.2493554969251,-103.679356802607,
178.747434357108));
#33519=CARTESIAN_POINT('Ctrl Pts',(-59.5956256336748,-103.673354907713,
178.565855111501));
#33520=CARTESIAN_POINT('Ctrl Pts',(-60.2124023796431,-103.667735045613,
178.072546163384));
#33521=CARTESIAN_POINT('Ctrl Pts',(-60.473626626211,-103.672659530759,177.760862023247));
#33522=CARTESIAN_POINT('Ctrl Pts',(-60.8517054991565,-103.697022462893,
177.067304060869));
#33523=CARTESIAN_POINT('Ctrl Pts',(-60.969954487591,-103.71533847361,176.695013679978));
#33524=CARTESIAN_POINT('Ctrl Pts',(-61.0613178783777,-103.765725594179,
175.912105661457));
#33525=CARTESIAN_POINT('Ctrl Pts',(-61.0280084599689,-103.802048593057,
175.508384995241));
#33526=CARTESIAN_POINT('Ctrl Pts',(-60.8099024547815,-103.889971010162,
174.753869651874));
#33527=CARTESIAN_POINT('Ctrl Pts',(-60.6328002879148,-103.939782129816,
174.408790054078));
#33528=CARTESIAN_POINT('Ctrl Pts',(-60.1489388748962,-104.051486847896,
173.794573999267));
#33529=CARTESIAN_POINT('Ctrl Pts',(-59.8425944395784,-104.116916509466,
173.535150572824));
#33530=CARTESIAN_POINT('Ctrl Pts',(-59.1599330169716,-104.25436567854,173.161376649719));
#33531=CARTESIAN_POINT('Ctrl Pts',(-58.7930476426981,-104.324417073302,
173.045525493603));
#33532=CARTESIAN_POINT('Ctrl Pts',(-58.0208968026134,-104.466850517053,
172.959589366222));
#33533=CARTESIAN_POINT('Ctrl Pts',(-57.6228638881136,-104.542054134394,
172.996348896332));
#33534=CARTESIAN_POINT('Ctrl Pts',(-56.8930427766736,-104.683334248274,
173.217979413356));
#33535=CARTESIAN_POINT('Ctrl Pts',(-56.5650553654821,-104.74841301316,173.389774435697));
#33536=CARTESIAN_POINT('Ctrl Pts',(-56.2766244746021,-104.807333878735,
173.617797875548));
#33537=CARTESIAN_POINT('Ctrl Pts',(-56.3296274768257,-105.304516623564,
173.617797875548));
#33538=CARTESIAN_POINT('Ctrl Pts',(-56.586763420517,-105.251988711846,173.414515133499));
#33539=CARTESIAN_POINT('Ctrl Pts',(-56.8756518272909,-105.194502166347,
173.255656785927));
#33540=CARTESIAN_POINT('Ctrl Pts',(-57.5573407106282,-105.061870497886,
173.018194256532));
#33541=CARTESIAN_POINT('Ctrl Pts',(-57.9518968201824,-104.986961694801,
172.965277848296));
#33542=CARTESIAN_POINT('Ctrl Pts',(-58.7243212130768,-104.843758468797,
173.018509289468));
#33543=CARTESIAN_POINT('Ctrl Pts',(-59.0948334933741,-104.774440321286,
173.118410470703));
#33544=CARTESIAN_POINT('Ctrl Pts',(-59.7901995520874,-104.635984124741,
173.461210596147));
#33545=CARTESIAN_POINT('Ctrl Pts',(-60.10599739235,-104.569468147798,173.70582815698));
#33546=CARTESIAN_POINT('Ctrl Pts',(-60.6145053935603,-104.454349598348,
174.29566698968));
#33547=CARTESIAN_POINT('Ctrl Pts',(-60.8063109448197,-104.404149819734,
174.6313980876));
#33548=CARTESIAN_POINT('Ctrl Pts',(-61.0571505412047,-104.313109652798,
175.37216866749));
#33549=CARTESIAN_POINT('Ctrl Pts',(-61.1086413032927,-104.274767358923,
175.771878782708));
#33550=CARTESIAN_POINT('Ctrl Pts',(-61.0540347236212,-104.219627528265,
176.555125379641));
#33551=CARTESIAN_POINT('Ctrl Pts',(-60.9538742878482,-104.200622191814,
176.931413228329));
#33552=CARTESIAN_POINT('Ctrl Pts',(-60.6107074521862,-104.172935338366,
177.63932970722));
#33553=CARTESIAN_POINT('Ctrl Pts',(-60.3661679600611,-104.166148788114,
177.961723631706));
#33554=CARTESIAN_POINT('Ctrl Pts',(-59.7767728721284,-104.167965410298,
178.483121614131));
#33555=CARTESIAN_POINT('Ctrl Pts',(-59.4411490653884,-104.174132651873,
178.681280605116));
#33556=CARTESIAN_POINT('Ctrl Pts',(-58.6997947488505,-104.188925309346,
178.945040591799));
#33557=CARTESIAN_POINT('Ctrl Pts',(-58.2995114737861,-104.198739234453,
179.002909619764));
#33558=CARTESIAN_POINT('Ctrl Pts',(-57.5142640536464,-104.221376908929,
178.959760465797));
#33559=CARTESIAN_POINT('Ctrl Pts',(-57.13641383133,-104.232117846913,178.864752057889));
#33560=CARTESIAN_POINT('Ctrl Pts',(-56.4321068286097,-104.243744947958,
178.535348806015));
#33561=CARTESIAN_POINT('Ctrl Pts',(-56.1131999486625,-104.245634487,178.302395783125));
#33562=CARTESIAN_POINT('Ctrl Pts',(-55.5795544736227,-104.241255906255,
177.725362130028));
#33563=CARTESIAN_POINT('Ctrl Pts',(-55.3708710635326,-104.233514167147,
177.385921844193));
#33564=CARTESIAN_POINT('Ctrl Pts',(-55.0963565925498,-104.198634152299,
176.64990001692));
#33565=CARTESIAN_POINT('Ctrl Pts',(-55.0320013973361,-104.173357805299,
176.26089693273));
#33566=CARTESIAN_POINT('Ctrl Pts',(-55.0552588305459,-104.109543147896,
175.478035139983));
#33567=CARTESIAN_POINT('Ctrl Pts',(-55.1437153211815,-104.070226160898,
175.09181330523));
#33568=CARTESIAN_POINT('Ctrl Pts',(-55.4618994607109,-103.972199550823,
174.379658006443));
#33569=CARTESIAN_POINT('Ctrl Pts',(-55.6876222709348,-103.915969317528,
174.060082353081));
#33570=CARTESIAN_POINT('Ctrl Pts',(-56.0329504084051,-103.841462858177,
173.731815046431));
#33571=CARTESIAN_POINT('Ctrl Pts',(-56.1005740309949,-103.827277116453,
173.673172575223));
#33572=CARTESIAN_POINT('Ctrl Pts',(-56.1706184701527,-103.812968389078,
173.617797875549));
#33573=CARTESIAN_POINT('Origin',(-54.1598171290174,-67.5719248685924,175.985485069079));
#33574=CARTESIAN_POINT('',(-55.9586064612577,-101.824237409764,173.617797875548));
#33575=CARTESIAN_POINT('',(-56.0116094634814,-102.321420154593,173.617797875548));
#33576=CARTESIAN_POINT('',(-52.327900808713,-67.7672193871761,173.617797875548));
#33577=CARTESIAN_POINT('Ctrl Pts',(-55.9586064612576,-101.824237409764,
173.617797875548));
#33578=CARTESIAN_POINT('Ctrl Pts',(-55.9418620792744,-101.827657963911,
173.631035402105));
#33579=CARTESIAN_POINT('Ctrl Pts',(-55.9252536280251,-101.831071983287,
173.644461594472));
#33580=CARTESIAN_POINT('Ctrl Pts',(-55.602506261032,-101.897836272007,173.911234848305));
#33581=CARTESIAN_POINT('Ctrl Pts',(-55.3501385871355,-101.957527023001,
174.224226559646));
#33582=CARTESIAN_POINT('Ctrl Pts',(-54.9897939381547,-102.060567461356,
174.919523761195));
#33583=CARTESIAN_POINT('Ctrl Pts',(-54.8801600543654,-102.103010161683,
175.29228342645));
#33584=CARTESIAN_POINT('Ctrl Pts',(-54.8058019006491,-102.171165691404,
176.075276683873));
#33585=CARTESIAN_POINT('Ctrl Pts',(-54.8481620778904,-102.199434886067,
176.478570168191));
#33586=CARTESIAN_POINT('Ctrl Pts',(-55.0837450049315,-102.238950667311,
177.231510942236));
#33587=CARTESIAN_POINT('Ctrl Pts',(-55.26905260861,-102.249970204585,177.575498479078));
#33588=CARTESIAN_POINT('Ctrl Pts',(-55.7685021015342,-102.256942000512,
178.186908434787));
#33589=CARTESIAN_POINT('Ctrl Pts',(-56.0828882984817,-102.256209898393,
178.444631835812));
#33590=CARTESIAN_POINT('Ctrl Pts',(-56.7806847889233,-102.246455470237,
178.814817605309));
#33591=CARTESIAN_POINT('Ctrl Pts',(-57.1544827460279,-102.23739901161,178.928821322706));
#33592=CARTESIAN_POINT('Ctrl Pts',(-57.9393919543218,-102.213927680494,
179.010983698272));
#33593=CARTESIAN_POINT('Ctrl Pts',(-58.3439672415085,-102.203579401748,
178.97235351188));
#33594=CARTESIAN_POINT('Ctrl Pts',(-59.0998399032848,-102.1876381752,178.743175887637));
#33595=CARTESIAN_POINT('Ctrl Pts',(-59.4453865710874,-102.181610661658,
178.560473933994));
#33596=CARTESIAN_POINT('Ctrl Pts',(-60.0603391240182,-102.176247373325,
178.065248679065));
#33597=CARTESIAN_POINT('Ctrl Pts',(-60.3204551505627,-102.181298084424,
177.752817376281));
#33598=CARTESIAN_POINT('Ctrl Pts',(-60.6961902382117,-102.205886260206,
177.058265992882));
#33599=CARTESIAN_POINT('Ctrl Pts',(-60.8132236920275,-102.224235850889,
176.685708027717));
#33600=CARTESIAN_POINT('Ctrl Pts',(-60.9021310470988,-102.27494271889,175.90274993751));
#33601=CARTESIAN_POINT('Ctrl Pts',(-60.8676018815838,-102.311403324081,
175.499271413988));
#33602=CARTESIAN_POINT('Ctrl Pts',(-60.6472995091625,-102.399536981531,
174.745652556018));
#33603=CARTESIAN_POINT('Ctrl Pts',(-60.4692182742589,-102.449362802166,
174.40119543767));
#33604=CARTESIAN_POINT('Ctrl Pts',(-59.9837071749626,-102.561297391055,
173.788577520703));
#33605=CARTESIAN_POINT('Ctrl Pts',(-59.6767175857298,-102.626802922418,
173.530122137022));
#33606=CARTESIAN_POINT('Ctrl Pts',(-58.9931953493747,-102.764322547424,
173.158392483586));
#33607=CARTESIAN_POINT('Ctrl Pts',(-58.6260701402944,-102.834315775566,
173.043593874296));
#33608=CARTESIAN_POINT('Ctrl Pts',(-57.8538805758677,-102.976803691064,
172.959807279232));
#33609=CARTESIAN_POINT('Ctrl Pts',(-57.4560566189888,-103.051991670284,
172.997632518835));
#33610=CARTESIAN_POINT('Ctrl Pts',(-56.7293880942506,-103.192707713498,
173.220408735396));
#33611=CARTESIAN_POINT('Ctrl Pts',(-56.4039923758953,-103.257284367751,
173.391398243217));
#33612=CARTESIAN_POINT('Ctrl Pts',(-56.1176154679299,-103.31578564425,173.617797875548));
#33613=CARTESIAN_POINT('Ctrl Pts',(-56.1706184701527,-103.812968389078,
173.617797875549));
#33614=CARTESIAN_POINT('Ctrl Pts',(-56.404804740164,-103.765128652867,173.432658348049));
#33615=CARTESIAN_POINT('Ctrl Pts',(-56.6655756121463,-103.713125305891,
173.28416603257));
#33616=CARTESIAN_POINT('Ctrl Pts',(-57.3044614716826,-103.588350311415,
173.040169017636));
#33617=CARTESIAN_POINT('Ctrl Pts',(-57.6876611425556,-103.515301776179,
172.975313466901));
#33618=CARTESIAN_POINT('Ctrl Pts',(-58.459499061551,-103.371543657016,172.998304157061));
#33619=CARTESIAN_POINT('Ctrl Pts',(-58.8405222939703,-103.301242302207,
173.086729527027));
#33620=CARTESIAN_POINT('Ctrl Pts',(-59.544647309321,-103.162157013392,173.40658130172));
#33621=CARTESIAN_POINT('Ctrl Pts',(-59.8614447323563,-103.096156684249,
173.634213697219));
#33622=CARTESIAN_POINT('Ctrl Pts',(-60.3916584272211,-102.978084198385,
174.201298967928));
#33623=CARTESIAN_POINT('Ctrl Pts',(-60.5994160828054,-102.926356504137,
174.535657821284));
#33624=CARTESIAN_POINT('Ctrl Pts',(-60.8740312425169,-102.833106151377,
175.265760314739));
#33625=CARTESIAN_POINT('Ctrl Pts',(-60.93892768182,-102.793929024314,175.654271971896));
#33626=CARTESIAN_POINT('Ctrl Pts',(-60.9169777722008,-102.734645718886,
176.436822929872));
#33627=CARTESIAN_POINT('Ctrl Pts',(-60.8298978453232,-102.714451234301,
176.82326307178));
#33628=CARTESIAN_POINT('Ctrl Pts',(-60.512540236509,-102.684358018243,177.541078380302));
#33629=CARTESIAN_POINT('Ctrl Pts',(-60.285789784968,-102.676240964764,177.865680022517));
#33630=CARTESIAN_POINT('Ctrl Pts',(-59.7209647535357,-102.674754719218,
178.410737605796));
#33631=CARTESIAN_POINT('Ctrl Pts',(-59.3882039794029,-102.680851603804,
178.625795338374));
#33632=CARTESIAN_POINT('Ctrl Pts',(-58.6588191637221,-102.694734749673,
178.916334908194));
#33633=CARTESIAN_POINT('Ctrl Pts',(-58.2694213622247,-102.703925358076,
178.989125475152));
#33634=CARTESIAN_POINT('Ctrl Pts',(-57.4849943314814,-102.725771328283,
178.981565949238));
#33635=CARTESIAN_POINT('Ctrl Pts',(-57.0975304536677,-102.737798083385,
178.901359005251));
#33636=CARTESIAN_POINT('Ctrl Pts',(-56.373984974966,-102.751112893838,178.596975999604));
#33637=CARTESIAN_POINT('Ctrl Pts',(-56.0450780673281,-102.75382305394,178.37562206328));
#33638=CARTESIAN_POINT('Ctrl Pts',(-55.4909578422365,-102.751036339809,
177.820144068511));
#33639=CARTESIAN_POINT('Ctrl Pts',(-55.2708822806514,-102.745313930212,
177.491617213069));
#33640=CARTESIAN_POINT('Ctrl Pts',(-54.9672570694395,-102.713919309601,
176.768487387816));
#33641=CARTESIAN_POINT('Ctrl Pts',(-54.8871168552745,-102.690077603063,
176.380711597023));
#33642=CARTESIAN_POINT('Ctrl Pts',(-54.8796652807629,-102.628930472901,
175.598674121186));
#33643=CARTESIAN_POINT('Ctrl Pts',(-54.9518913884919,-102.592139071519,
175.211999444296));
#33644=CARTESIAN_POINT('Ctrl Pts',(-55.2394031848712,-102.497784884128,
174.487925439198));
#33645=CARTESIAN_POINT('Ctrl Pts',(-55.4526238491403,-102.442637439968,
174.157716548369));
#33646=CARTESIAN_POINT('Ctrl Pts',(-55.8135995248757,-102.362651165773,
173.785235233275));
#33647=CARTESIAN_POINT('Ctrl Pts',(-55.9100255219117,-102.342171793738,
173.698106609885));
#33648=CARTESIAN_POINT('Ctrl Pts',(-56.0116094634811,-102.321420154593,
173.617797875548));
#33649=CARTESIAN_POINT('Origin',(-54.1598171290174,-67.5719248685924,175.985485069079));
#33650=CARTESIAN_POINT('',(-55.7995974545854,-100.332689175279,173.617797875548));
#33651=CARTESIAN_POINT('',(-55.8526004568095,-100.829871920107,173.617797875548));
#33652=CARTESIAN_POINT('',(-52.327900808713,-67.7672193871761,173.617797875548));
#33653=CARTESIAN_POINT('Ctrl Pts',(-55.7995974545853,-100.332689175279,
173.617797875548));
#33654=CARTESIAN_POINT('Ctrl Pts',(-55.7768768391306,-100.337330558609,
173.635760004624));
#33655=CARTESIAN_POINT('Ctrl Pts',(-55.7544069815204,-100.341959811824,
173.654069124129));
#33656=CARTESIAN_POINT('Ctrl Pts',(-55.4281078338695,-100.409766928785,
173.928074962219));
#33657=CARTESIAN_POINT('Ctrl Pts',(-55.1782933068223,-100.469202046876,
174.242756886089));
#33658=CARTESIAN_POINT('Ctrl Pts',(-54.8233080316795,-100.571613042545,
174.940307330757));
#33659=CARTESIAN_POINT('Ctrl Pts',(-54.7164144709026,-100.613553643858,
175.31368069076));
#33660=CARTESIAN_POINT('Ctrl Pts',(-54.6477220275006,-100.681236411179,
176.096767285812));
#33661=CARTESIAN_POINT('Ctrl Pts',(-54.692882020349,-100.709222813559,176.499484491269));
#33662=CARTESIAN_POINT('Ctrl Pts',(-54.9334882488888,-100.748148956567,
177.250349960554));
#33663=CARTESIAN_POINT('Ctrl Pts',(-55.1210041782264,-100.758735702979,
177.592906895632));
#33664=CARTESIAN_POINT('Ctrl Pts',(-55.624264502085,-100.765424077113,178.200624182367));
#33665=CARTESIAN_POINT('Ctrl Pts',(-55.9401245508787,-100.764549700056,
178.456108510789));
#33666=CARTESIAN_POINT('Ctrl Pts',(-56.639877235172,-100.754536320114,178.821581568571));
#33667=CARTESIAN_POINT('Ctrl Pts',(-57.0141885239434,-100.745239747563,
178.933158919805));
#33668=CARTESIAN_POINT('Ctrl Pts',(-57.7991951657605,-100.721872951851,
179.010358891003));
#33669=CARTESIAN_POINT('Ctrl Pts',(-58.2032756935156,-100.71159145232,178.969271146376));
#33670=CARTESIAN_POINT('Ctrl Pts',(-58.9573451962122,-100.69579551028,178.735676551618));
#33671=CARTESIAN_POINT('Ctrl Pts',(-59.3016318924727,-100.689728304205,
178.551018089997));
#33672=CARTESIAN_POINT('Ctrl Pts',(-59.9133948054434,-100.684812524346,
178.052457832929));
#33673=CARTESIAN_POINT('Ctrl Pts',(-60.1715717458335,-100.690083204903,
177.738731743298));
#33674=CARTESIAN_POINT('Ctrl Pts',(-60.5432149011014,-100.715063895377,
177.042456253659));
#33675=CARTESIAN_POINT('Ctrl Pts',(-60.6581267585883,-100.733476433594,
176.669430948199));
#33676=CARTESIAN_POINT('Ctrl Pts',(-60.7427422172093,-100.784741310593,
175.886394761431));
#33677=CARTESIAN_POINT('Ctrl Pts',(-60.7060830699926,-100.82144148114,175.483348270929));
#33678=CARTESIAN_POINT('Ctrl Pts',(-60.4819457218199,-100.909943273934,
174.731303566548));
#33679=CARTESIAN_POINT('Ctrl Pts',(-60.3021525491174,-100.959798580448,
174.387934937461));
#33680=CARTESIAN_POINT('Ctrl Pts',(-59.8137595275919,-101.072134280656,
173.778120185689));
#33681=CARTESIAN_POINT('Ctrl Pts',(-59.5056469930805,-101.137771296492,
173.521363784633));
#33682=CARTESIAN_POINT('Ctrl Pts',(-58.8206245124076,-101.275412969076,
173.153215134721));
#33683=CARTESIAN_POINT('Ctrl Pts',(-58.453079395942,-101.345307598008,173.040260243925));
#33684=CARTESIAN_POINT('Ctrl Pts',(-57.6808289635357,-101.487889698087,
172.96024209395));
#33685=CARTESIAN_POINT('Ctrl Pts',(-57.2833779854965,-101.563048993529,
172.999934506361));
#33686=CARTESIAN_POINT('Ctrl Pts',(-56.5622407027566,-101.702774554781,
173.224683780349));
#33687=CARTESIAN_POINT('Ctrl Pts',(-56.2413813271945,-101.766471960948,
173.39424589248));
#33688=CARTESIAN_POINT('Ctrl Pts',(-55.9586064612576,-101.824237409764,
173.617797875548));
#33689=CARTESIAN_POINT('Ctrl Pts',(-56.0116094634811,-102.321420154593,
173.617797875548));
#33690=CARTESIAN_POINT('Ctrl Pts',(-56.2117256298421,-102.280540283156,
173.459592988117));
#33691=CARTESIAN_POINT('Ctrl Pts',(-56.4315113442584,-102.236567527639,
173.32794348206));
#33692=CARTESIAN_POINT('Ctrl Pts',(-57.0210459134878,-102.120764142274,
173.072451862829));
#33693=CARTESIAN_POINT('Ctrl Pts',(-57.4027420083367,-102.04762488143,172.990678263125));
#33694=CARTESIAN_POINT('Ctrl Pts',(-58.1734791760833,-101.903350281501,
172.980801890339));
#33695=CARTESIAN_POINT('Ctrl Pts',(-58.555048337918,-101.833753291797,173.051813399071));
#33696=CARTESIAN_POINT('Ctrl Pts',(-59.2716187222599,-101.693785878013,
173.338771470462));
#33697=CARTESIAN_POINT('Ctrl Pts',(-59.59950055985,-101.626352796783,173.552932301273));
#33698=CARTESIAN_POINT('Ctrl Pts',(-60.152626675811,-101.505191935652,174.095270609366));
#33699=CARTESIAN_POINT('Ctrl Pts',(-60.3733722096372,-101.452818719277,
174.417318372121));
#33700=CARTESIAN_POINT('Ctrl Pts',(-60.6807670840991,-101.356539785396,
175.132477821969));
#33701=CARTESIAN_POINT('Ctrl Pts',(-60.7634495819521,-101.31521637537,175.519219398591));
#33702=CARTESIAN_POINT('Ctrl Pts',(-60.7760051648476,-101.251598266524,
176.300490372137));
#33703=CARTESIAN_POINT('Ctrl Pts',(-60.7072285105988,-101.230163282846,
176.687412322417));
#33704=CARTESIAN_POINT('Ctrl Pts',(-60.4244698747711,-101.196868880839,
177.418150190422));
#33705=CARTESIAN_POINT('Ctrl Pts',(-60.2119626544106,-101.186985144412,
177.754385613528));
#33706=CARTESIAN_POINT('Ctrl Pts',(-59.6731240769558,-101.18206326524,178.323655970417));
#33707=CARTESIAN_POINT('Ctrl Pts',(-59.3532738220543,-101.187461424002,
178.552315730304));
#33708=CARTESIAN_POINT('Ctrl Pts',(-58.6397518992478,-101.200161996454,
178.877291385991));
#33709=CARTESIAN_POINT('Ctrl Pts',(-58.2523927315438,-101.208889944517,
178.968885456107));
#33710=CARTESIAN_POINT('Ctrl Pts',(-57.4694270027641,-101.229907422773,
178.997798186083));
#33711=CARTESIAN_POINT('Ctrl Pts',(-57.0815394412167,-101.242619116289,
178.93672303185));
#33712=CARTESIAN_POINT('Ctrl Pts',(-56.3448618659264,-101.257863366675,
178.668720994274));
#33713=CARTESIAN_POINT('Ctrl Pts',(-56.0040013908307,-101.261606484908,
178.462523802351));
#33714=CARTESIAN_POINT('Ctrl Pts',(-55.4248118944299,-101.260813912043,
177.934557342879));
#33715=CARTESIAN_POINT('Ctrl Pts',(-55.1907517584213,-101.257179714369,
177.619451304459));
#33716=CARTESIAN_POINT('Ctrl Pts',(-54.8516849912401,-101.230113400579,
176.913092274527));
#33717=CARTESIAN_POINT('Ctrl Pts',(-54.7520715760218,-101.208111268598,
176.527713217197));
#33718=CARTESIAN_POINT('Ctrl Pts',(-54.7068453558597,-101.150308825965,
175.747492359658));
#33719=CARTESIAN_POINT('Ctrl Pts',(-54.7594532240998,-101.116159496669,
175.36031299947));
#33720=CARTESIAN_POINT('Ctrl Pts',(-55.0094861140096,-101.026370753261,
174.62276410895));
#33721=CARTESIAN_POINT('Ctrl Pts',(-55.2069070993651,-100.972677229107,
174.280310302316));
#33722=CARTESIAN_POINT('Ctrl Pts',(-55.5827888417636,-100.88647057148,173.851760673119));
#33723=CARTESIAN_POINT('Ctrl Pts',(-55.7127247867848,-100.858445820516,
173.72837871983));
#33724=CARTESIAN_POINT('Ctrl Pts',(-55.8526004568095,-100.829871920107,
173.617797875548));
#33725=CARTESIAN_POINT('Origin',(-54.1598171290174,-67.5719248685924,175.985485069079));
#33726=CARTESIAN_POINT('',(-55.6405884479131,-98.8411409407929,173.617797875548));
#33727=CARTESIAN_POINT('',(-55.6935914501374,-99.3383236856214,173.617797875548));
#33728=CARTESIAN_POINT('',(-52.327900808713,-67.7672193871761,173.617797875548));
#33729=CARTESIAN_POINT('Ctrl Pts',(-55.640588447913,-98.8411409407929,173.617797875548));
#33730=CARTESIAN_POINT('Ctrl Pts',(-55.607788426525,-98.8478413522682,173.643728432713));
#33731=CARTESIAN_POINT('Ctrl Pts',(-55.575512754977,-98.8545161247301,173.670380738806));
#33732=CARTESIAN_POINT('Ctrl Pts',(-55.2434249722054,-98.9240644878506,
173.956755143452));
#33733=CARTESIAN_POINT('Ctrl Pts',(-54.9979411072923,-98.983061603104,174.274242696089));
#33734=CARTESIAN_POINT('Ctrl Pts',(-54.6520043673395,-99.0844062653321,
174.975547078861));
#33735=CARTESIAN_POINT('Ctrl Pts',(-54.5497403041806,-99.1255207794924,
175.349957929002));
#33736=CARTESIAN_POINT('Ctrl Pts',(-54.490633611945,-99.1923999624474,176.133155312395));
#33737=CARTESIAN_POINT('Ctrl Pts',(-54.5405219281655,-99.2199051296011,
176.534853017101));
#33738=CARTESIAN_POINT('Ctrl Pts',(-54.7896112751938,-99.2578320053393,
177.282169330645));
#33739=CARTESIAN_POINT('Ctrl Pts',(-54.9808733909374,-99.2677041213008,
177.622301954674));
#33740=CARTESIAN_POINT('Ctrl Pts',(-55.4905764275471,-99.273911004575,178.223718473287));
#33741=CARTESIAN_POINT('Ctrl Pts',(-55.80890658979,-99.2727952582687,178.475377649671));
#33742=CARTESIAN_POINT('Ctrl Pts',(-56.5119481278214,-99.2623427169079,
178.832833145827));
#33743=CARTESIAN_POINT('Ctrl Pts',(-56.8871354514819,-99.2526542811345,
178.940282456497));
#33744=CARTESIAN_POINT('Ctrl Pts',(-57.6722717244173,-99.2294666609831,
179.009024583519));
#33745=CARTESIAN_POINT('Ctrl Pts',(-58.0754745824138,-99.2192997909092,
178.963754653268));
#33746=CARTESIAN_POINT('Ctrl Pts',(-58.8264415096819,-99.2037520153808,
178.722644060913));
#33747=CARTESIAN_POINT('Ctrl Pts',(-59.168579358959,-99.1976316660925,178.534644993543));
#33748=CARTESIAN_POINT('Ctrl Pts',(-59.7748651888666,-99.1934810387267,
178.030404263522));
#33749=CARTESIAN_POINT('Ctrl Pts',(-60.0297087292874,-99.1991272360973,
177.714489261805));
#33750=CARTESIAN_POINT('Ctrl Pts',(-60.3943437977552,-99.2247780241239,
177.01529115874));
#33751=CARTESIAN_POINT('Ctrl Pts',(-60.5056235297006,-99.2433112190769,
176.64146480497));
#33752=CARTESIAN_POINT('Ctrl Pts',(-60.582876625282,-99.2955310960124,175.858322552814));
#33753=CARTESIAN_POINT('Ctrl Pts',(-60.5425684063517,-99.3326395226713,
175.456043508555));
#33754=CARTESIAN_POINT('Ctrl Pts',(-60.3118618363862,-99.4217698445741,
174.706721474383));
#33755=CARTESIAN_POINT('Ctrl Pts',(-60.1291287544452,-99.4716870873749,
174.36522220523));
#33756=CARTESIAN_POINT('Ctrl Pts',(-59.6357948033637,-99.5847090949079,
173.760247118106));
#33757=CARTESIAN_POINT('Ctrl Pts',(-59.3257694087996,-99.6505683657844,
173.506426873974));
#33758=CARTESIAN_POINT('Ctrl Pts',(-58.6381854022676,-99.7884161986188,
173.144446851875));
#33759=CARTESIAN_POINT('Ctrl Pts',(-58.2699175162785,-99.8581508629596,
173.034667925421));
#33760=CARTESIAN_POINT('Ctrl Pts',(-57.4975831329424,-100.000891499135,
172.961150408848));
#33761=CARTESIAN_POINT('Ctrl Pts',(-57.1007954373251,-100.075997516825,
173.004060058922));
#33762=CARTESIAN_POINT('Ctrl Pts',(-56.3892116996093,-100.214009883933,
173.232106306747));
#33763=CARTESIAN_POINT('Ctrl Pts',(-56.0761555924101,-100.276193684061,
173.399160621705));
#33764=CARTESIAN_POINT('Ctrl Pts',(-55.7995974545854,-100.332689175279,
173.617797875548));
#33765=CARTESIAN_POINT('Ctrl Pts',(-55.8526004568095,-100.829871920107,
173.617797875548));
#33766=CARTESIAN_POINT('Ctrl Pts',(-56.0122382705985,-100.797260995049,
173.491593767107));
#33767=CARTESIAN_POINT('Ctrl Pts',(-56.1846045510077,-100.762638723928,
173.382123827381));
#33768=CARTESIAN_POINT('Ctrl Pts',(-56.7157333838001,-100.657561827589,
173.117982968677));
#33769=CARTESIAN_POINT('Ctrl Pts',(-57.094698693149,-100.584490179927,173.016058522839));
#33770=CARTESIAN_POINT('Ctrl Pts',(-57.8632760701796,-100.439761135245,
172.967130150488));
#33771=CARTESIAN_POINT('Ctrl Pts',(-58.2454035950996,-100.370550178192,
173.0178651937));
#33772=CARTESIAN_POINT('Ctrl Pts',(-58.9755114142945,-100.229746977069,
173.266016957432));
#33773=CARTESIAN_POINT('Ctrl Pts',(-59.3156712917826,-100.160789298229,
173.463728513916));
#33774=CARTESIAN_POINT('Ctrl Pts',(-59.8949166349951,-100.036160879726,
173.97655855762));
#33775=CARTESIAN_POINT('Ctrl Pts',(-60.1304479748,-99.9825994660196,174.284510981315));
#33776=CARTESIAN_POINT('Ctrl Pts',(-60.4749888012005,-99.8829850771357,
174.981520655192));
#33777=CARTESIAN_POINT('Ctrl Pts',(-60.5780912424543,-99.8392777678074,
175.365219219352));
#33778=CARTESIAN_POINT('Ctrl Pts',(-60.6301874634811,-99.7707646401272,
176.144112017309));
#33779=CARTESIAN_POINT('Ctrl Pts',(-60.5819096245653,-99.7474725453235,
176.531552855466));
#33780=CARTESIAN_POINT('Ctrl Pts',(-60.3384998584582,-99.7106236091981,
177.275775863669));
#33781=CARTESIAN_POINT('Ctrl Pts',(-60.142764833812,-99.698754297114,177.624377307971));
#33782=CARTESIAN_POINT('Ctrl Pts',(-59.6338082020946,-99.6899722706143,
178.220216958606));
#33783=CARTESIAN_POINT('Ctrl Pts',(-59.3281466891011,-99.6941240637893,
178.463851602083));
#33784=CARTESIAN_POINT('Ctrl Pts',(-58.6331919999401,-99.7054999209037,
178.826382081363));
#33785=CARTESIAN_POINT('Ctrl Pts',(-58.2491406899139,-99.713687805704,178.938738164386));
#33786=CARTESIAN_POINT('Ctrl Pts',(-57.4687325225704,-99.7337650841091,
179.007890508407));
#33787=CARTESIAN_POINT('Ctrl Pts',(-57.0803506489573,-99.7467323005111,
178.967502295266));
#33788=CARTESIAN_POINT('Ctrl Pts',(-56.3305357616791,-99.7640445546346,
178.739317008762));
#33789=CARTESIAN_POINT('Ctrl Pts',(-55.9774945802472,-99.7689094944188,
178.550283591324));
#33790=CARTESIAN_POINT('Ctrl Pts',(-55.3718512221691,-99.7702782468859,
178.052764535689));
#33791=CARTESIAN_POINT('Ctrl Pts',(-55.1229119696622,-99.7683688291766,
177.751904538663));
#33792=CARTESIAN_POINT('Ctrl Pts',(-54.7466827634431,-99.7459428741996,
177.064420399678));
#33793=CARTESIAN_POINT('Ctrl Pts',(-54.6264136550257,-99.7259772250701,
176.682662160461));
#33794=CARTESIAN_POINT('Ctrl Pts',(-54.5411023803683,-99.6717996406146,
175.905326025461));
#33795=CARTESIAN_POINT('Ctrl Pts',(-54.5732422656808,-99.6399064579199,
175.517630649645));
#33796=CARTESIAN_POINT('Ctrl Pts',(-54.7838400046977,-99.5550096737611,
174.767133841076));
#33797=CARTESIAN_POINT('Ctrl Pts',(-54.9640775679547,-99.5029939958601,
174.412709780171));
#33798=CARTESIAN_POINT('Ctrl Pts',(-55.3505156020313,-99.4108574829576,
173.92319016178));
#33799=CARTESIAN_POINT('Ctrl Pts',(-55.5136939909607,-99.3750732653116,
173.760018555645));
#33800=CARTESIAN_POINT('Ctrl Pts',(-55.6935914501376,-99.3383236856213,
173.617797875548));
#33801=CARTESIAN_POINT('Origin',(-54.1598171290174,-67.5719248685924,175.985485069079));
#33802=CARTESIAN_POINT('',(-55.4815794412406,-97.3495927063074,173.617797875548));
#33803=CARTESIAN_POINT('',(-55.5345824434656,-97.8467754511356,173.617797875547));
#33804=CARTESIAN_POINT('',(-52.327900808713,-67.7672193871761,173.617797875548));
#33805=CARTESIAN_POINT('Ctrl Pts',(-55.4815794412403,-97.3495927063074,
173.617797875548));
#33806=CARTESIAN_POINT('Ctrl Pts',(-55.4324890366522,-97.3596209287386,
173.656607043608));
#33807=CARTESIAN_POINT('Ctrl Pts',(-55.3845798951133,-97.3695903433992,
173.697027556825));
#33808=CARTESIAN_POINT('Ctrl Pts',(-55.0436838390214,-97.4419036621428,
174.003831822454));
#33809=CARTESIAN_POINT('Ctrl Pts',(-54.8052622584124,-97.5001748970722,
174.325732895783));
#33810=CARTESIAN_POINT('Ctrl Pts',(-54.4739751665481,-97.5997836371241,
175.032982163991));
#33811=CARTESIAN_POINT('Ctrl Pts',(-54.3792161531924,-97.6396186592439,
175.40907756234));
#33812=CARTESIAN_POINT('Ctrl Pts',(-54.3356822249732,-97.705182341791,176.192328114917));
#33813=CARTESIAN_POINT('Ctrl Pts',(-54.3932265261256,-97.7318984584026,
176.592250427641));
#33814=CARTESIAN_POINT('Ctrl Pts',(-54.6560551944903,-97.7681974970615,
177.33369930248));
#33815=CARTESIAN_POINT('Ctrl Pts',(-54.853432028735,-97.7769564622805,177.669882492492));
#33816=CARTESIAN_POINT('Ctrl Pts',(-55.3735876312399,-97.7823758155381,
178.260918672993));
#33817=CARTESIAN_POINT('Ctrl Pts',(-55.695865173458,-97.7808662960632,178.506265131895));
#33818=CARTESIAN_POINT('Ctrl Pts',(-56.4041928409522,-97.7696975138237,
178.850576320867));
#33819=CARTESIAN_POINT('Ctrl Pts',(-56.7808247104566,-97.7594122769474,
178.951256000448));
#33820=CARTESIAN_POINT('Ctrl Pts',(-57.5660739648741,-97.736522069505,179.006089715428));
#33821=CARTESIAN_POINT('Ctrl Pts',(-57.9677393275844,-97.7265458884034,
178.953961714379));
#33822=CARTESIAN_POINT('Ctrl Pts',(-58.7135241150777,-97.7114077004069,
178.700524956017));
#33823=CARTESIAN_POINT('Ctrl Pts',(-59.0521242732877,-97.7052403557551,
178.507014713227));
#33824=CARTESIAN_POINT('Ctrl Pts',(-59.6492906014397,-97.702354641487,177.993443668406));
#33825=CARTESIAN_POINT('Ctrl Pts',(-59.8985748487986,-97.7086198657127,
177.6739799838));
#33826=CARTESIAN_POINT('Ctrl Pts',(-60.2515922105049,-97.7353755898406,
176.970020213686));
#33827=CARTESIAN_POINT('Ctrl Pts',(-60.3568537551407,-97.7541449326304,
176.594863477064));
#33828=CARTESIAN_POINT('Ctrl Pts',(-60.4218689325865,-97.8079460282848,
175.811623141943));
#33829=CARTESIAN_POINT('Ctrl Pts',(-60.3755094456941,-97.8457253912998,
175.410693317903));
#33830=CARTESIAN_POINT('Ctrl Pts',(-60.1339094023174,-97.9358921711707,
174.665959338533));
#33831=CARTESIAN_POINT('Ctrl Pts',(-59.9462795676491,-97.9859446250264,
174.327573621966));
#33832=CARTESIAN_POINT('Ctrl Pts',(-59.4447409410051,-98.1001023645264,
173.730730865837));
#33833=CARTESIAN_POINT('Ctrl Pts',(-59.1315747563405,-98.1663216537997,
173.481851668649));
#33834=CARTESIAN_POINT('Ctrl Pts',(-58.4397669818307,-98.3045031186173,
173.130197603657));
#33835=CARTESIAN_POINT('Ctrl Pts',(-58.0702903996877,-98.3739982357447,
173.025735741239));
#33836=CARTESIAN_POINT('Ctrl Pts',(-57.2978751733484,-98.5169936655727,
172.96312581397));
#33837=CARTESIAN_POINT('Ctrl Pts',(-56.9022569518373,-98.5919994740118,
173.011422547399));
#33838=CARTESIAN_POINT('Ctrl Pts',(-56.2067337174236,-98.7271248655238,
173.244696526083));
#33839=CARTESIAN_POINT('Ctrl Pts',(-55.9067072812291,-98.7867779980545,
173.407413573101));
#33840=CARTESIAN_POINT('Ctrl Pts',(-55.640588447913,-98.8411409407929,173.617797875548));
#33841=CARTESIAN_POINT('Ctrl Pts',(-55.6935914501376,-99.3383236856214,
173.617797875548));
#33842=CARTESIAN_POINT('Ctrl Pts',(-55.8119561040419,-99.3141440707393,
173.52422289314));
#33843=CARTESIAN_POINT('Ctrl Pts',(-55.9374403171867,-99.2888338257374,
173.439753139739));
#33844=CARTESIAN_POINT('Ctrl Pts',(-56.4097362742124,-99.1946815732135,
173.172347526528));
#33845=CARTESIAN_POINT('Ctrl Pts',(-56.7848532814029,-99.1218779352154,
173.049886449515));
#33846=CARTESIAN_POINT('Ctrl Pts',(-57.550288318462,-98.9768606303945,172.961111387978));
#33847=CARTESIAN_POINT('Ctrl Pts',(-57.9329176837078,-98.9075434504376,
172.991548501756));
#33848=CARTESIAN_POINT('Ctrl Pts',(-58.6755232042986,-98.7661086789391,
173.200450042894));
#33849=CARTESIAN_POINT('Ctrl Pts',(-59.0271977849536,-98.6957931179957,
173.38097589479));
#33850=CARTESIAN_POINT('Ctrl Pts',(-59.6319148992309,-98.5678406174091,
173.863622452769));
#33851=CARTESIAN_POINT('Ctrl Pts',(-59.8819084866275,-98.5126235340329,
174.157734558481));
#33852=CARTESIAN_POINT('Ctrl Pts',(-60.2624486880925,-98.4098755731448,
174.835908151001));
#33853=CARTESIAN_POINT('Ctrl Pts',(-60.38553977356,-98.3639189197615,175.215566976975));
#33854=CARTESIAN_POINT('Ctrl Pts',(-60.4764166993533,-98.2906788232303,
175.991195226444));
#33855=CARTESIAN_POINT('Ctrl Pts',(-60.4478242869101,-98.2651150805417,
176.379140518398));
#33856=CARTESIAN_POINT('Ctrl Pts',(-60.2426635425665,-98.2248942633597,
177.135299993822));
#33857=CARTESIAN_POINT('Ctrl Pts',(-60.0637521456281,-98.211124838614,177.495017551851));
#33858=CARTESIAN_POINT('Ctrl Pts',(-59.5841734003338,-98.1986352035317,
178.115748546278));
#33859=CARTESIAN_POINT('Ctrl Pts',(-59.2918518313182,-98.2011354802375,
178.373532359831));
#33860=CARTESIAN_POINT('Ctrl Pts',(-58.6153963646659,-98.2112443778198,
178.771031797104));
#33861=CARTESIAN_POINT('Ctrl Pts',(-58.2354796130484,-98.2188965152296,
178.902892638674));
#33862=CARTESIAN_POINT('Ctrl Pts',(-57.4583833275023,-98.238062825233,179.009966870332));
#33863=CARTESIAN_POINT('Ctrl Pts',(-57.0694769111357,-98.2508035073108,
178.988739952553));
#33864=CARTESIAN_POINT('Ctrl Pts',(-56.3085049635686,-98.2700077840799,
178.797739873155));
#33865=CARTESIAN_POINT('Ctrl Pts',(-55.9449597657812,-98.2759088831958,
178.625214785807));
#33866=CARTESIAN_POINT('Ctrl Pts',(-55.3154969191486,-98.2792776073073,
178.156448816577));
#33867=CARTESIAN_POINT('Ctrl Pts',(-55.052973867085,-98.278484464857,177.868517942429));
#33868=CARTESIAN_POINT('Ctrl Pts',(-54.6434796448366,-98.2603028194195,
177.199076188219));
#33869=CARTESIAN_POINT('Ctrl Pts',(-54.5045782719281,-98.2422508173813,
176.821554461221));
#33870=CARTESIAN_POINT('Ctrl Pts',(-54.3829538671168,-98.1914242422077,
176.047682812831));
#33871=CARTESIAN_POINT('Ctrl Pts',(-54.396798663844,-98.1611041902518,175.659501141255));
#33872=CARTESIAN_POINT('Ctrl Pts',(-54.5719943824211,-98.080673037502,174.898412435821));
#33873=CARTESIAN_POINT('Ctrl Pts',(-54.7363787847236,-98.0302852478859,
174.53405956253));
#33874=CARTESIAN_POINT('Ctrl Pts',(-55.1277451028881,-97.9334031371019,
173.988501298653));
#33875=CARTESIAN_POINT('Ctrl Pts',(-55.3189885889602,-97.8908171156101,
173.788238885403));
#33876=CARTESIAN_POINT('Ctrl Pts',(-55.5345824434661,-97.8467754511356,
173.617797875547));
#33877=CARTESIAN_POINT('Origin',(-54.1598171290174,-67.5719248685924,175.985485069079));
#33878=CARTESIAN_POINT('',(-55.3225704345682,-95.8580444718219,173.617797875548));
#33879=CARTESIAN_POINT('',(-55.3755734367933,-96.3552272166501,173.617797875547));
#33880=CARTESIAN_POINT('',(-52.327900808713,-67.7672193871761,173.617797875548));
#33881=CARTESIAN_POINT('Ctrl Pts',(-55.3225704345676,-95.8580444718219,
173.617797875549));
#33882=CARTESIAN_POINT('Ctrl Pts',(-55.2488731603477,-95.8730994029159,
173.676060379693));
#33883=CARTESIAN_POINT('Ctrl Pts',(-55.1778627825142,-95.8880167521154,
173.737934784587));
#33884=CARTESIAN_POINT('Ctrl Pts',(-54.8249870529423,-95.9643813640093,
174.076580476363));
#33885=CARTESIAN_POINT('Ctrl Pts',(-54.597372284845,-96.0215149400869,174.404859949676));
#33886=CARTESIAN_POINT('Ctrl Pts',(-54.2882731068297,-96.1184723951104,
175.120804814625));
#33887=CARTESIAN_POINT('Ctrl Pts',(-54.2049127919938,-96.1565070312605,
175.499467074234));
#33888=CARTESIAN_POINT('Ctrl Pts',(-54.1850904046615,-96.2200437067127,
176.282494925006));
#33889=CARTESIAN_POINT('Ctrl Pts',(-54.2542224515368,-96.2455419636194,
176.679431477551));
#33890=CARTESIAN_POINT('Ctrl Pts',(-54.5378711477107,-96.2793518199959,
177.411705233674));
#33891=CARTESIAN_POINT('Ctrl Pts',(-54.7446348646939,-96.2865318732696,
177.741846305529));
#33892=CARTESIAN_POINT('Ctrl Pts',(-55.2806673506312,-96.2907393806808,
178.316727233652));
#33893=CARTESIAN_POINT('Ctrl Pts',(-55.6087897538596,-96.2886267840918,
178.552229429508));
#33894=CARTESIAN_POINT('Ctrl Pts',(-56.3250267020568,-96.2763608196003,
178.876240067672));
#33895=CARTESIAN_POINT('Ctrl Pts',(-56.7039131937275,-96.2652663653476,
178.966453550718));
#33896=CARTESIAN_POINT('Ctrl Pts',(-57.4890895773673,-96.2428445615668,
178.999703351349));
#33897=CARTESIAN_POINT('Ctrl Pts',(-57.8881374663501,-96.2331695364305,
178.936986522126));
#33898=CARTESIAN_POINT('Ctrl Pts',(-58.6256832980654,-96.2186706420911,
178.664503387791));
#33899=CARTESIAN_POINT('Ctrl Pts',(-58.9587820211762,-96.2125323238485,
178.462391207497));
#33900=CARTESIAN_POINT('Ctrl Pts',(-59.5415135492665,-96.2116260635046,
177.934371177825));
#33901=CARTESIAN_POINT('Ctrl Pts',(-59.781980393862,-96.2188550670068,177.609532782097));
#33902=CARTESIAN_POINT('Ctrl Pts',(-60.1167365593899,-96.2473328199456,
176.898295990638));
#33903=CARTESIAN_POINT('Ctrl Pts',(-60.2125417189749,-96.2665659682249,
176.521039619842));
#33904=CARTESIAN_POINT('Ctrl Pts',(-60.25823774542,-96.3228473669527,175.737844252544));
#33905=CARTESIAN_POINT('Ctrl Pts',(-60.2023665625948,-96.3616658116569,
175.33923089605));
#33906=CARTESIAN_POINT('Ctrl Pts',(-59.9436358359537,-96.4534477282677,
174.601897903333));
#33907=CARTESIAN_POINT('Ctrl Pts',(-59.7482466819457,-96.5037977056866,
174.268444396503));
#33908=CARTESIAN_POINT('Ctrl Pts',(-59.2337794277028,-96.6197348806844,
173.684665947776));
#33909=CARTESIAN_POINT('Ctrl Pts',(-58.9157588068247,-96.6864976977044,
173.443739655222));
#33910=CARTESIAN_POINT('Ctrl Pts',(-58.217372008235,-96.8251823854556,173.108571771223));
#33911=CARTESIAN_POINT('Ctrl Pts',(-57.8459670981744,-96.8943692598478,
173.012603888321));
#33912=CARTESIAN_POINT('Ctrl Pts',(-57.0735798911608,-97.0377436029253,
172.967475998217));
#33913=CARTESIAN_POINT('Ctrl Pts',(-56.6799835746226,-97.1125605083365,
173.024374207843));
#33914=CARTESIAN_POINT('Ctrl Pts',(-56.0102631250932,-97.2430296646259,
173.265226820711));
#33915=CARTESIAN_POINT('Ctrl Pts',(-55.7309492235603,-97.2986512715054,
173.420654790818));
#33916=CARTESIAN_POINT('Ctrl Pts',(-55.4815794412403,-97.3495927063074,
173.617797875548));
#33917=CARTESIAN_POINT('Ctrl Pts',(-55.5345824434661,-97.8467754511356,
173.617797875547));
#33918=CARTESIAN_POINT('Ctrl Pts',(-55.6169947154963,-97.8299402141496,
173.552645596965));
#33919=CARTESIAN_POINT('Ctrl Pts',(-55.7029083231513,-97.812546688353,173.491868566507));
#33920=CARTESIAN_POINT('Ctrl Pts',(-56.1249583779839,-97.7278219892561,
173.226108125279));
#33921=CARTESIAN_POINT('Ctrl Pts',(-56.4958492165941,-97.6554167225456,
173.085828859448));
#33922=CARTESIAN_POINT('Ctrl Pts',(-57.2577653903279,-97.5102937615483,
172.962314436423));
#33923=CARTESIAN_POINT('Ctrl Pts',(-57.6408149160444,-97.4404766568418,
172.97531750956));
#33924=CARTESIAN_POINT('Ctrl Pts',(-58.3932849875013,-97.2986633757301,
173.150303933633));
#33925=CARTESIAN_POINT('Ctrl Pts',(-58.7541614205803,-97.2273241008258,
173.315593868565));
#33926=CARTESIAN_POINT('Ctrl Pts',(-59.3801444776652,-97.0966437361646,
173.771882659817));
#33927=CARTESIAN_POINT('Ctrl Pts',(-59.6423184034501,-97.0396408082212,
174.054346491916));
#33928=CARTESIAN_POINT('Ctrl Pts',(-60.0527598071511,-96.9343665917044,
174.715910845847));
#33929=CARTESIAN_POINT('Ctrl Pts',(-60.192552060891,-96.8865955714797,175.091374886531));
#33930=CARTESIAN_POINT('Ctrl Pts',(-60.3160027291459,-96.809442177424,175.8635415251));
#33931=CARTESIAN_POINT('Ctrl Pts',(-60.3036791023499,-96.7816290859376,
176.25193825129));
#33932=CARTESIAN_POINT('Ctrl Pts',(-60.1303662911291,-96.7386612800413,
177.017184179734));
#33933=CARTESIAN_POINT('Ctrl Pts',(-59.9658025339903,-96.7233365783403,
177.385464851777));
#33934=CARTESIAN_POINT('Ctrl Pts',(-59.5109353546182,-96.7077917799697,
178.026239753016));
#33935=CARTESIAN_POINT('Ctrl Pts',(-59.2294130920298,-96.7086026675069,
178.295564051087));
#33936=CARTESIAN_POINT('Ctrl Pts',(-58.5686504671049,-96.7176722648981,
178.721086600531));
#33937=CARTESIAN_POINT('Ctrl Pts',(-58.1928009595376,-96.7248726180441,
178.868652601948));
#33938=CARTESIAN_POINT('Ctrl Pts',(-57.4190331249111,-96.743283136341,179.00644614402));
#33939=CARTESIAN_POINT('Ctrl Pts',(-57.0296416326923,-96.7555187290039,
179.00055145821));
#33940=CARTESIAN_POINT('Ctrl Pts',(-56.2604596669238,-96.7762161512854,
178.839419262271));
#33941=CARTESIAN_POINT('Ctrl Pts',(-55.8890973332672,-96.7829392925134,
178.680444217046));
#33942=CARTESIAN_POINT('Ctrl Pts',(-55.2411027402459,-96.7879021772012,
178.234996012765));
#33943=CARTESIAN_POINT('Ctrl Pts',(-54.9678379975261,-96.7876829656282,
177.957218172685));
#33944=CARTESIAN_POINT('Ctrl Pts',(-54.5325795329967,-96.7728490488621,
177.302515713011));
#33945=CARTESIAN_POINT('Ctrl Pts',(-54.3791937444477,-96.7563360778038,
176.928937952964));
#33946=CARTESIAN_POINT('Ctrl Pts',(-54.2291523730752,-96.7081766400537,
176.158344477697));
#33947=CARTESIAN_POINT('Ctrl Pts',(-54.2288040560873,-96.6787881573269,
175.769759226876));
#33948=CARTESIAN_POINT('Ctrl Pts',(-54.3765212283317,-96.6018697724001,
175.001099244294));
#33949=CARTESIAN_POINT('Ctrl Pts',(-54.5283593919543,-96.5528199541182,
174.629581185717));
#33950=CARTESIAN_POINT('Ctrl Pts',(-54.9205751349598,-96.4526499836936,
174.039918340427));
#33951=CARTESIAN_POINT('Ctrl Pts',(-55.1324371633112,-96.4048952658755,
173.810012964794));
#33952=CARTESIAN_POINT('Ctrl Pts',(-55.3755734367937,-96.35522721665,173.617797875547));
#33953=CARTESIAN_POINT('Origin',(-54.1598171290174,-67.5719248685924,175.985485069079));
#33954=CARTESIAN_POINT('',(-55.1635614278963,-94.3664962373362,173.617797875548));
#33955=CARTESIAN_POINT('',(-55.2165644301208,-94.8636789821645,173.617797875548));
#33956=CARTESIAN_POINT('',(-52.327900808713,-67.7672193871761,173.617797875548));
#33957=CARTESIAN_POINT('Ctrl Pts',(-55.163561427896,-94.3664962373362,173.617797875548));
#33958=CARTESIAN_POINT('Ctrl Pts',(-55.056218364382,-94.3884243539691,173.702659571575));
#33959=CARTESIAN_POINT('Ctrl Pts',(-54.9546523839058,-94.4100448203152,
173.795122112537));
#33960=CARTESIAN_POINT('Ctrl Pts',(-54.588095380377,-94.4916767822101,174.17906603512));
#33961=CARTESIAN_POINT('Ctrl Pts',(-54.375501714509,-94.5471774826487,174.515492085468));
#33962=CARTESIAN_POINT('Ctrl Pts',(-54.0968551211791,-94.6404534404216,
175.242776758176));
#33963=CARTESIAN_POINT('Ctrl Pts',(-54.0292270717692,-94.6762889180113,
175.62500182216));
#33964=CARTESIAN_POINT('Ctrl Pts',(-54.0421926615871,-94.7369743988195,
176.407110581385));
#33965=CARTESIAN_POINT('Ctrl Pts',(-54.1271843755252,-94.7607583875431,
176.799360193194));
#33966=CARTESIAN_POINT('Ctrl Pts',(-54.4394251787236,-94.7911050175151,
177.518466198867));
#33967=CARTESIAN_POINT('Ctrl Pts',(-54.6593448976417,-94.7963387031362,
177.84018550867));
#33968=CARTESIAN_POINT('Ctrl Pts',(-55.2172395846646,-94.798844867514,178.392010226581));
#33969=CARTESIAN_POINT('Ctrl Pts',(-55.5530860010683,-94.7958926645089,
178.613444558317));
#33970=CARTESIAN_POINT('Ctrl Pts',(-56.2799683754373,-94.7820964283054,
178.908802794561));
#33971=CARTESIAN_POINT('Ctrl Pts',(-56.662094212939,-94.7700953287221,178.984201982332));
#33972=CARTESIAN_POINT('Ctrl Pts',(-57.4466423122614,-94.7483537445882,
178.986775780572));
#33973=CARTESIAN_POINT('Ctrl Pts',(-57.8414883194669,-94.739117177713,178.909142731616));
#33974=CARTESIAN_POINT('Ctrl Pts',(-58.5669122135515,-94.7255345791514,
178.609761049303));
#33975=CARTESIAN_POINT('Ctrl Pts',(-58.892161692691,-94.7196585115898,178.395302043432));
#33976=CARTESIAN_POINT('Ctrl Pts',(-59.4537702240862,-94.7216002585186,
177.846821950288));
#33977=CARTESIAN_POINT('Ctrl Pts',(-59.6813123838403,-94.730203656332,177.514644370105));
#33978=CARTESIAN_POINT('Ctrl Pts',(-59.989620948833,-94.7611439463418,176.793310965176));
#33979=CARTESIAN_POINT('Ctrl Pts',(-60.0717228469572,-94.7812542368023,
176.412988750328));
#33980=CARTESIAN_POINT('Ctrl Pts',(-60.0892594696137,-94.841115825725,175.630300886533));
#33981=CARTESIAN_POINT('Ctrl Pts',(-60.0196295797508,-94.8814029590579,
175.235471098125));
#33982=CARTESIAN_POINT('Ctrl Pts',(-59.7360736259875,-94.9754930330783,
174.509272205753));
#33983=CARTESIAN_POINT('Ctrl Pts',(-59.5292974353456,-95.0264678405705,
174.183050393779));
#33984=CARTESIAN_POINT('Ctrl Pts',(-58.9960460002618,-95.1449670913247,
173.618822843707));
#33985=CARTESIAN_POINT('Ctrl Pts',(-58.6711941602365,-95.2124648371533,
173.389819924504));
#33986=CARTESIAN_POINT('Ctrl Pts',(-57.9634202187307,-95.3518299433625,
173.079094406885));
#33987=CARTESIAN_POINT('Ctrl Pts',(-57.5891546966644,-95.4207308213124,
172.99574207915));
#33988=CARTESIAN_POINT('Ctrl Pts',(-56.8171726429903,-95.5646023159323,
172.976684919917));
#33989=CARTESIAN_POINT('Ctrl Pts',(-56.4269278469765,-95.6390727589893,
173.046323931544));
#33990=CARTESIAN_POINT('Ctrl Pts',(-55.7957642864128,-95.7625431312478,
173.296634934914));
#33991=CARTESIAN_POINT('Ctrl Pts',(-55.5469343965475,-95.8122112436145,
173.44042352347));
#33992=CARTESIAN_POINT('Ctrl Pts',(-55.3225704345677,-95.8580444718219,
173.617797875549));
#33993=CARTESIAN_POINT('Ctrl Pts',(-55.3755734367937,-96.35522721665,173.617797875547));
#33994=CARTESIAN_POINT('Ctrl Pts',(-55.4307651910792,-96.3439526062045,
173.574165192428));
#33995=CARTESIAN_POINT('Ctrl Pts',(-55.4875430741737,-96.3324243840167,
173.532482528561));
#33996=CARTESIAN_POINT('Ctrl Pts',(-55.8724009271436,-96.2547381147215,
173.270675811687));
#33997=CARTESIAN_POINT('Ctrl Pts',(-56.2395551487011,-96.182736586261,173.116986678507));
#33998=CARTESIAN_POINT('Ctrl Pts',(-56.9983211435042,-96.0376240798129,
172.967152893997));
#33999=CARTESIAN_POINT('Ctrl Pts',(-57.3816828039697,-95.9671829248927,
172.967075834089));
#34000=CARTESIAN_POINT('Ctrl Pts',(-58.1410184669512,-95.8251835602254,
173.116566059386));
#34001=CARTESIAN_POINT('Ctrl Pts',(-58.5083499151732,-95.753165851405,173.270197441364));
#34002=CARTESIAN_POINT('Ctrl Pts',(-59.1498803587327,-95.6205203225493,
173.70650315128));
#34003=CARTESIAN_POINT('Ctrl Pts',(-59.4210480577474,-95.5619683302694,
173.980372408889));
#34004=CARTESIAN_POINT('Ctrl Pts',(-59.8532696072757,-95.4548985128898,
174.629277399653));
#34005=CARTESIAN_POINT('Ctrl Pts',(-60.0052557757833,-95.4058409991536,
175.001197164812));
#34006=CARTESIAN_POINT('Ctrl Pts',(-60.1526461672196,-95.3258448395883,
175.770400507816));
#34007=CARTESIAN_POINT('Ctrl Pts',(-60.1521527002433,-95.2961838508183,
176.159145644728));
#34008=CARTESIAN_POINT('Ctrl Pts',(-60.0020756560049,-95.25124541977,176.930549171593));
#34009=CARTESIAN_POINT('Ctrl Pts',(-59.8481492936629,-95.2348033599355,
177.304675965347));
#34010=CARTESIAN_POINT('Ctrl Pts',(-59.4114542618371,-95.2170471154485,
177.959694992412));
#34011=CARTESIAN_POINT('Ctrl Pts',(-59.1376578950276,-95.2164539288486,
178.237323092304));
#34012=CARTESIAN_POINT('Ctrl Pts',(-58.4884866437325,-95.2247742367641,
178.682694049653));
#34013=CARTESIAN_POINT('Ctrl Pts',(-58.115931013141,-95.2316427901242,178.841401776965));
#34014=CARTESIAN_POINT('Ctrl Pts',(-57.3448951470266,-95.2495037021288,
179.001135652719));
#34015=CARTESIAN_POINT('Ctrl Pts',(-56.955125254993,-95.2612079064579,179.00610941923));
#34016=CARTESIAN_POINT('Ctrl Pts',(-56.1805126479013,-95.2829505974448,
178.866164044176));
#34017=CARTESIAN_POINT('Ctrl Pts',(-55.803943202269,-95.290250419438,178.716937553678));
#34018=CARTESIAN_POINT('Ctrl Pts',(-55.1431193746723,-95.2963377805561,
178.288149902574));
#34019=CARTESIAN_POINT('Ctrl Pts',(-54.8623109504861,-95.296361893453,178.017466611653));
#34020=CARTESIAN_POINT('Ctrl Pts',(-54.4092692797554,-95.2838700527111,
177.373334850441));
#34021=CARTESIAN_POINT('Ctrl Pts',(-54.2458760236569,-95.2684472974855,
177.002822289733));
#34022=CARTESIAN_POINT('Ctrl Pts',(-54.0760681605979,-95.2221663811948,
176.234803937473));
#34023=CARTESIAN_POINT('Ctrl Pts',(-54.0658951530641,-95.1932770792832,
175.845926949155));
#34024=CARTESIAN_POINT('Ctrl Pts',(-54.1946194628085,-95.1188098143918,
175.072356420616));
#34025=CARTESIAN_POINT('Ctrl Pts',(-54.3376779401713,-95.0707207130394,
174.696164868778));
#34026=CARTESIAN_POINT('Ctrl Pts',(-54.7289680209749,-94.9684859243212,
174.075800391413));
#34027=CARTESIAN_POINT('Ctrl Pts',(-54.9544853247051,-94.9172166864417,
173.82498850949));
#34028=CARTESIAN_POINT('Ctrl Pts',(-55.216564430121,-94.8636789821645,173.617797875547));
#34029=CARTESIAN_POINT('Origin',(-54.1598171290174,-67.5719248685924,175.985485069079));
#34030=CARTESIAN_POINT('',(-55.0045524212243,-92.8749480028505,173.617797875548));
#34031=CARTESIAN_POINT('',(-55.0575554234485,-93.372130747679,173.617797875548));
#34032=CARTESIAN_POINT('',(-52.327900808713,-67.7672193871761,173.617797875548));
#34033=CARTESIAN_POINT('Ctrl Pts',(-55.0045524212243,-92.8749480028505,
173.617797875548));
#34034=CARTESIAN_POINT('Ctrl Pts',(-54.8569032582738,-92.9051098778702,
173.734524173221));
#34035=CARTESIAN_POINT('Ctrl Pts',(-54.7203662707415,-92.9346522820336,
173.865484200462));
#34036=CARTESIAN_POINT('Ctrl Pts',(-54.3417383663621,-93.0221247962368,
174.306035059822));
#34037=CARTESIAN_POINT('Ctrl Pts',(-54.1474550333502,-93.0755584336755,
174.651322880573));
#34038=CARTESIAN_POINT('Ctrl Pts',(-53.9054598013013,-93.1643391309631,
175.391357838398));
#34039=CARTESIAN_POINT('Ctrl Pts',(-53.8569545310989,-93.1979466769663,
175.777944186085));
#34040=CARTESIAN_POINT('Ctrl Pts',(-53.9097491119168,-93.2550918971405,
176.557964426028));
#34041=CARTESIAN_POINT('Ctrl Pts',(-54.0136985785005,-93.2767515783228,
176.94366000401));
#34042=CARTESIAN_POINT('Ctrl Pts',(-54.3603654084999,-93.3028574026009,
177.646013455223));
#34043=CARTESIAN_POINT('Ctrl Pts',(-54.5965912360363,-93.3061079766006,
177.957369754161));
#34044=CARTESIAN_POINT('Ctrl Pts',(-55.1808634586347,-93.3065067763144,
178.480019859168));
#34045=CARTESIAN_POINT('Ctrl Pts',(-55.5254726227184,-93.3025286745695,
178.683672507102));
#34046=CARTESIAN_POINT('Ctrl Pts',(-56.2647985713167,-93.2868531592762,
178.943290967325));
#34047=CARTESIAN_POINT('Ctrl Pts',(-56.651071733831,-93.2741130933769,179.000096571975));
#34048=CARTESIAN_POINT('Ctrl Pts',(-57.4339392821045,-93.2532521783921,
178.964063884305));
#34049=CARTESIAN_POINT('Ctrl Pts',(-57.8227022361252,-93.2445836133361,
178.867925910384));
#34050=CARTESIAN_POINT('Ctrl Pts',(-58.5321780022402,-93.2321672139304,
178.534974955654));
#34051=CARTESIAN_POINT('Ctrl Pts',(-58.8474774466859,-93.2270067601978,
178.304732794236));
#34052=CARTESIAN_POINT('Ctrl Pts',(-59.3814483982118,-93.2325912463974,
177.730658867794));
#34053=CARTESIAN_POINT('Ctrl Pts',(-59.5920834337611,-93.242927406223,177.389796722879));
#34054=CARTESIAN_POINT('Ctrl Pts',(-59.8662607427621,-93.2769916073557,
176.656193721462));
#34055=CARTESIAN_POINT('Ctrl Pts',(-59.9306275100233,-93.2986032359834,
176.271859584237));
#34056=CARTESIAN_POINT('Ctrl Pts',(-59.911513575484,-93.3630613791081,175.490628628338));
#34057=CARTESIAN_POINT('Ctrl Pts',(-59.8242017213171,-93.4051742501552,
175.101439271628));
#34058=CARTESIAN_POINT('Ctrl Pts',(-59.5085893254885,-93.5021867078949,
174.390349822164));
#34059=CARTESIAN_POINT('Ctrl Pts',(-59.2868218922751,-93.554330421169,174.073633436082));
#34060=CARTESIAN_POINT('Ctrl Pts',(-58.7292535184541,-93.6761025352044,
173.535787883294));
#34061=CARTESIAN_POINT('Ctrl Pts',(-58.3959881887055,-93.7444477798263,
173.322880107027));
#34062=CARTESIAN_POINT('Ctrl Pts',(-57.6763776517792,-93.8845996153561,
173.044716985648));
#34063=CARTESIAN_POINT('Ctrl Pts',(-57.2982879865103,-93.9534434547723,
172.978244121145));
#34064=CARTESIAN_POINT('Ctrl Pts',(-56.5275433446037,-94.097852994184,172.994197789256));
#34065=CARTESIAN_POINT('Ctrl Pts',(-56.1424275208482,-94.1717364822287,
173.080752024789));
#34066=CARTESIAN_POINT('Ctrl Pts',(-55.5630058610648,-94.2857381652413,
173.340270659517));
#34067=CARTESIAN_POINT('Ctrl Pts',(-55.3543190155038,-94.3275281429596,
173.466991555285));
#34068=CARTESIAN_POINT('Ctrl Pts',(-55.163561427896,-94.3664962373362,173.617797875548));
#34069=CARTESIAN_POINT('Ctrl Pts',(-55.216564430121,-94.8636789821645,173.617797875547));
#34070=CARTESIAN_POINT('Ctrl Pts',(-55.2532799768635,-94.8561787044115,
173.588771840095));
#34071=CARTESIAN_POINT('Ctrl Pts',(-55.2907018285174,-94.8485652993067,
173.560605332552));
#34072=CARTESIAN_POINT('Ctrl Pts',(-55.6508164104634,-94.775591169922,173.302776237068));
#34073=CARTESIAN_POINT('Ctrl Pts',(-56.0151735547999,-94.7039136072724,
173.140038565322));
#34074=CARTESIAN_POINT('Ctrl Pts',(-56.7715612575832,-94.5588528925702,
172.97233220456));
#34075=CARTESIAN_POINT('Ctrl Pts',(-57.1551311161026,-94.4878711261834,
172.963423206831));
#34076=CARTESIAN_POINT('Ctrl Pts',(-57.918841782984,-94.3457926735877,173.095700543124));
#34077=CARTESIAN_POINT('Ctrl Pts',(-58.2903049931619,-94.2733609867026,
173.241373548713));
#34078=CARTESIAN_POINT('Ctrl Pts',(-58.9421223829594,-94.1394295431226,
173.664106773207));
#34079=CARTESIAN_POINT('Ctrl Pts',(-59.2192919982907,-94.0797358692806,
173.932241960795));
#34080=CARTESIAN_POINT('Ctrl Pts',(-59.6658914264387,-93.9715016179453,
174.572526583826));
#34081=CARTESIAN_POINT('Ctrl Pts',(-59.8259305467065,-93.9216125355567,
174.941878357353));
#34082=CARTESIAN_POINT('Ctrl Pts',(-59.9892246444878,-93.8397435228945,
175.708915779253));
#34083=CARTESIAN_POINT('Ctrl Pts',(-59.9965407460571,-93.8087655348136,
176.097899047269));
#34084=CARTESIAN_POINT('Ctrl Pts',(-59.8618177030415,-93.7625400837011,
176.873158317106));
#34085=CARTESIAN_POINT('Ctrl Pts',(-59.7149900573912,-93.7453683695564,
177.250961385648));
#34086=CARTESIAN_POINT('Ctrl Pts',(-59.2903691729418,-93.7261587425722,
177.915219986264));
#34087=CARTESIAN_POINT('Ctrl Pts',(-59.0216153581125,-93.7245615280262,
178.198287673508));
#34088=CARTESIAN_POINT('Ctrl Pts',(-58.3801618852297,-93.7323908620532,
178.656507648529));
#34089=CARTESIAN_POINT('Ctrl Pts',(-58.0099231073576,-93.7390395105877,
178.822428560122));
#34090=CARTESIAN_POINT('Ctrl Pts',(-57.2408258148254,-93.7565381598963,
178.996447660266));
#34091=CARTESIAN_POINT('Ctrl Pts',(-56.8507964687961,-93.7678219607524,
179.008467958561));
#34092=CARTESIAN_POINT('Ctrl Pts',(-56.0728355882105,-93.7902359073096,
178.882250596652));
#34093=CARTESIAN_POINT('Ctrl Pts',(-55.6930426259906,-93.7979062500858,
178.739394748503));
#34094=CARTESIAN_POINT('Ctrl Pts',(-55.0240443173154,-93.8047194732275,
178.321455511669));
#34095=CARTESIAN_POINT('Ctrl Pts',(-54.7383776431007,-93.8048320736551,
178.055327229978));
#34096=CARTESIAN_POINT('Ctrl Pts',(-54.2740247564696,-93.7938434797566,
177.418090509773));
#34097=CARTESIAN_POINT('Ctrl Pts',(-54.1042673274708,-93.779125687626,177.049674695849));
#34098=CARTESIAN_POINT('Ctrl Pts',(-53.9218210197265,-93.734055954135,176.283430443779));
#34099=CARTESIAN_POINT('Ctrl Pts',(-53.9053820092821,-93.7054239240535,
175.894363042321));
#34100=CARTESIAN_POINT('Ctrl Pts',(-54.0220154697562,-93.6325267082092,
175.117801278641));
#34101=CARTESIAN_POINT('Ctrl Pts',(-54.1594435951317,-93.5850638346546,
174.738753876289));
#34102=CARTESIAN_POINT('Ctrl Pts',(-54.5495048403043,-93.4816043007811,
174.09877951738));
#34103=CARTESIAN_POINT('Ctrl Pts',(-54.7834613811529,-93.4281228717259,
173.834487101089));
#34104=CARTESIAN_POINT('Ctrl Pts',(-55.0575554234485,-93.372130747679,173.617797875548));
#34105=CARTESIAN_POINT('Origin',(-54.1598171290174,-67.5719248685924,175.985485069079));
#34106=CARTESIAN_POINT('',(-54.8455434145523,-91.3833997683648,173.617797875548));
#34107=CARTESIAN_POINT('',(-54.8985464167762,-91.8805825131934,173.617797875548));
#34108=CARTESIAN_POINT('',(-52.327900808713,-67.7672193871761,173.617797875548));
#34109=CARTESIAN_POINT('Ctrl Pts',(-54.8455434145526,-91.3833997683648,
173.617797875547));
#34110=CARTESIAN_POINT('Ctrl Pts',(-54.6565253335548,-91.4220125151056,
173.76722900233));
#34111=CARTESIAN_POINT('Ctrl Pts',(-54.4860219465301,-91.4595477719293,
173.939743355083));
#34112=CARTESIAN_POINT('Ctrl Pts',(-54.1001265638809,-91.5524166507176,
174.440593638359));
#34113=CARTESIAN_POINT('Ctrl Pts',(-53.9249220525858,-91.6036119642123,
174.79393662834));
#34114=CARTESIAN_POINT('Ctrl Pts',(-53.7207399973051,-91.6876830864498,
175.546124447473));
#34115=CARTESIAN_POINT('Ctrl Pts',(-53.6922572054311,-91.7194669392612,
175.937272343594));
#34116=CARTESIAN_POINT('Ctrl Pts',(-53.7865525319358,-91.7728324375254,
176.713966170903));
#34117=CARTESIAN_POINT('Ctrl Pts',(-53.9098262191694,-91.7922372835231,
177.091848532611));
#34118=CARTESIAN_POINT('Ctrl Pts',(-54.292013977408,-91.8138836063467,177.775855580414));
#34119=CARTESIAN_POINT('Ctrl Pts',(-54.5456631560371,-91.8155251406082,
178.076189528251));
#34120=CARTESIAN_POINT('Ctrl Pts',(-55.1571631643673,-91.8136797426504,
178.567013800483));
#34121=CARTESIAN_POINT('Ctrl Pts',(-55.5100946048466,-91.808629984099,178.751362100129));
#34122=CARTESIAN_POINT('Ctrl Pts',(-56.2617722088354,-91.7909724493156,
178.972609206582));
#34123=CARTESIAN_POINT('Ctrl Pts',(-56.6526203471813,-91.7779293408117,
179.009236096806));
#34124=CARTESIAN_POINT('Ctrl Pts',(-57.4325276120376,-91.758054815642,178.93134134647));
#34125=CARTESIAN_POINT('Ctrl Pts',(-57.813712217306,-91.7500205513923,178.815543006379));
#34126=CARTESIAN_POINT('Ctrl Pts',(-58.5050152274851,-91.7388854271101,
178.446542967835));
#34127=CARTESIAN_POINT('Ctrl Pts',(-58.8093801021319,-91.7350109740523,
178.198823734832));
#34128=CARTESIAN_POINT('Ctrl Pts',(-59.3119933624224,-91.7446198199896,
177.597240068657));
#34129=CARTESIAN_POINT('Ctrl Pts',(-59.5035171706838,-91.7568310469166,
177.24773698331));
#34130=CARTESIAN_POINT('Ctrl Pts',(-59.7395806933547,-91.7943131744684,
176.501424313155));
#34131=CARTESIAN_POINT('Ctrl Pts',(-59.7840082400886,-91.8181063823523,
176.112536338177));
#34132=CARTESIAN_POINT('Ctrl Pts',(-59.7235636554942,-91.8876608546724,
175.334046855008));
#34133=CARTESIAN_POINT('Ctrl Pts',(-59.6166815717699,-91.9317093374407,
174.952172532456));
#34134=CARTESIAN_POINT('Ctrl Pts',(-59.2652605338654,-92.0319062920826,
174.258968497943));
#34135=CARTESIAN_POINT('Ctrl Pts',(-59.0263023246206,-92.08587485512,173.953143163745));
#34136=CARTESIAN_POINT('Ctrl Pts',(-58.4415336682585,-92.2112437707519,
173.446376314883));
#34137=CARTESIAN_POINT('Ctrl Pts',(-58.0995025750682,-92.2803846238087,
173.252374409362));
#34138=CARTESIAN_POINT('Ctrl Pts',(-57.3671026897501,-92.4212806505717,
173.011983670517));
#34139=CARTESIAN_POINT('Ctrl Pts',(-56.9845499457477,-92.4905300386684,
172.96525589994));
#34140=CARTESIAN_POINT('Ctrl Pts',(-56.216284091542,-92.635377266259,173.022212362854));
#34141=CARTESIAN_POINT('Ctrl Pts',(-55.8380764927768,-92.7083973345374,
173.128234533467));
#34142=CARTESIAN_POINT('Ctrl Pts',(-55.3188346949646,-92.8112758246322,
173.393439625609));
#34143=CARTESIAN_POINT('Ctrl Pts',(-55.1559496924782,-92.8440204616262,
173.49810845369));
#34144=CARTESIAN_POINT('Ctrl Pts',(-55.0045524212243,-92.8749480028505,
173.617797875548));
#34145=CARTESIAN_POINT('Ctrl Pts',(-55.0575554234485,-93.372130747679,173.617797875548));
#34146=CARTESIAN_POINT('Ctrl Pts',(-55.0826501717059,-93.3670043748268,
173.597958839575));
#34147=CARTESIAN_POINT('Ctrl Pts',(-55.1080760854621,-93.3618249067256,
173.57852039083));
#34148=CARTESIAN_POINT('Ctrl Pts',(-55.4528584352249,-93.2917830015913,
173.323717361705));
#34149=CARTESIAN_POINT('Ctrl Pts',(-55.8153492922638,-93.22032977783,173.155314509966));
#34150=CARTESIAN_POINT('Ctrl Pts',(-56.5701409630624,-93.0753202870361,
172.976363563093));
#34151=CARTESIAN_POINT('Ctrl Pts',(-56.9538396838264,-93.0039511914057,
172.961915225107));
#34152=CARTESIAN_POINT('Ctrl Pts',(-57.7201870735368,-92.8618419731353,
173.083405439403));
#34153=CARTESIAN_POINT('Ctrl Pts',(-58.0941464128959,-92.7891688593354,
173.224058494334));
#34154=CARTESIAN_POINT('Ctrl Pts',(-58.7523253532587,-92.6544481586586,
173.638252468771));
#34155=CARTESIAN_POINT('Ctrl Pts',(-59.0332297739802,-92.5940009461163,
173.902819260972));
#34156=CARTESIAN_POINT('Ctrl Pts',(-59.4887090310732,-92.4850559455269,
174.537673954038));
#34157=CARTESIAN_POINT('Ctrl Pts',(-59.6537202371819,-92.4346607096272,
174.905348495639));
#34158=CARTESIAN_POINT('Ctrl Pts',(-59.8268767927802,-92.3516365901475,
175.670963162657));
#34159=CARTESIAN_POINT('Ctrl Pts',(-59.8390186337771,-92.3198066129628,
176.060096237857));
#34160=CARTESIAN_POINT('Ctrl Pts',(-59.7137837922629,-92.2727917671927,
176.837654715681));
#34161=CARTESIAN_POINT('Ctrl Pts',(-59.5713681586131,-92.2551727805481,
177.217655119944));
#34162=CARTESIAN_POINT('Ctrl Pts',(-59.1542349634437,-92.2350681269231,
177.887555270179));
#34163=CARTESIAN_POINT('Ctrl Pts',(-58.8885745411324,-92.2328210251685,
178.17396692491));
#34164=CARTESIAN_POINT('Ctrl Pts',(-58.2519116722656,-92.2403486057468,
178.640023495696));
#34165=CARTESIAN_POINT('Ctrl Pts',(-57.8831575336419,-92.246861193658,178.810341960741));
#34166=CARTESIAN_POINT('Ctrl Pts',(-57.1153094579654,-92.2641363601497,
178.993105557227));
#34167=CARTESIAN_POINT('Ctrl Pts',(-56.7251166733867,-92.2751344100561,
179.009429420874));
#34168=CARTESIAN_POINT('Ctrl Pts',(-55.9451775899093,-92.2979556768727,
178.891589253066));
#34169=CARTESIAN_POINT('Ctrl Pts',(-55.5634757749293,-92.3058508359901,
178.752640123539));
#34170=CARTESIAN_POINT('Ctrl Pts',(-54.8895422164754,-92.3131059527131,
178.34134143223));
#34171=CARTESIAN_POINT('Ctrl Pts',(-54.600921528257,-92.3132467009483,178.077978006958));
#34172=CARTESIAN_POINT('Ctrl Pts',(-54.129746242459,-92.3031699421057,177.444965202739));
#34173=CARTESIAN_POINT('Ctrl Pts',(-53.95615204043,-92.2888815881815,177.077869618163));
#34174=CARTESIAN_POINT('Ctrl Pts',(-53.7660578707382,-92.2445486141228,
176.312747534025));
#34175=CARTESIAN_POINT('Ctrl Pts',(-53.7458319553549,-92.2160493616996,
175.923563743096));
#34176=CARTESIAN_POINT('Ctrl Pts',(-53.8551691600749,-92.1441031926879,
175.145247067551));
#34177=CARTESIAN_POINT('Ctrl Pts',(-53.9891852928614,-92.0970235596548,
174.764521270207));
#34178=CARTESIAN_POINT('Ctrl Pts',(-54.3782657801789,-91.9928589589126,
174.112695179671));
#34179=CARTESIAN_POINT('Ctrl Pts',(-54.6172195876594,-91.9380521560273,
173.840205091023));
#34180=CARTESIAN_POINT('Ctrl Pts',(-54.8985464167762,-91.8805825131934,
173.617797875548));
#34181=CARTESIAN_POINT('Origin',(-54.1598171290174,-67.5719248685924,175.985485069079));
#34182=CARTESIAN_POINT('',(-54.6865344078804,-89.8918515338791,173.617797875547));
#34183=CARTESIAN_POINT('',(-54.739537410104,-90.3890342787078,173.617797875548));
#34184=CARTESIAN_POINT('',(-52.327900808713,-67.7672193871761,173.617797875548));
#34185=CARTESIAN_POINT('Ctrl Pts',(-54.686534407881,-89.891851533879,173.617797875547));
#34186=CARTESIAN_POINT('Ctrl Pts',(-54.4633167153865,-89.9374506013485,
173.794266026801));
#34187=CARTESIAN_POINT('Ctrl Pts',(-54.2662753749012,-89.9814742982852,
174.002644386251));
#34188=CARTESIAN_POINT('Ctrl Pts',(-53.8744147557856,-90.0792998157546,
174.560342096286));
#34189=CARTESIAN_POINT('Ctrl Pts',(-53.7134765841226,-90.1293243049206,
174.926721926365));
#34190=CARTESIAN_POINT('Ctrl Pts',(-53.5458718952793,-90.2087890541603,
175.689958129594));
#34191=CARTESIAN_POINT('Ctrl Pts',(-53.5359469632516,-90.2388267308604,
176.078248986262));
#34192=CARTESIAN_POINT('Ctrl Pts',(-53.6654007924014,-90.2889223883734,
176.851267187356));
#34193=CARTESIAN_POINT('Ctrl Pts',(-53.8083029365153,-90.3065538368161,
177.22775708202));
#34194=CARTESIAN_POINT('Ctrl Pts',(-54.2249191190689,-90.3238154041645,
177.893191928766));
#34195=CARTESIAN_POINT('Ctrl Pts',(-54.4903906452805,-90.3244240736402,
178.178329691486));
#34196=CARTESIAN_POINT('Ctrl Pts',(-55.1249692417654,-90.3206187220871,
178.64074427075));
#34197=CARTESIAN_POINT('Ctrl Pts',(-55.4907054350572,-90.3144920361692,
178.809591114113));
#34198=CARTESIAN_POINT('Ctrl Pts',(-56.2539859372547,-90.2948774807113,
178.992430457108));
#34199=CARTESIAN_POINT('Ctrl Pts',(-56.6430191620045,-90.2822463249235,
179.009465058108));
#34200=CARTESIAN_POINT('Ctrl Pts',(-57.4192658904802,-90.2632843494434,
178.894021241466));
#34201=CARTESIAN_POINT('Ctrl Pts',(-57.7981378905664,-90.2557537741638,
178.757871111041));
#34202=CARTESIAN_POINT('Ctrl Pts',(-58.4703801255018,-90.2459268970991,
178.352709714571));
#34203=CARTESIAN_POINT('Ctrl Pts',(-58.759760035485,-90.2438552899847,178.091790194712));
#34204=CARTESIAN_POINT('Ctrl Pts',(-59.2326888009695,-90.2571726407939,
177.465587105964));
#34205=CARTESIAN_POINT('Ctrl Pts',(-59.4077546669428,-90.2713645633644,
177.103495021403));
#34206=CARTESIAN_POINT('Ctrl Pts',(-59.6043161995092,-90.3123324179346,
176.344807191295));
#34207=CARTESIAN_POINT('Ctrl Pts',(-59.6285073907552,-90.3384712918412,
175.956743027903));
#34208=CARTESIAN_POINT('Ctrl Pts',(-59.5288616190547,-90.4127699722497,
175.181982068486));
#34209=CARTESIAN_POINT('Ctrl Pts',(-59.4012644009517,-90.4592220492257,
174.803380814995));
#34210=CARTESIAN_POINT('Ctrl Pts',(-59.0126446018412,-90.5626595348428,
174.12960818678));
#34211=CARTESIAN_POINT('Ctrl Pts',(-58.7593768324647,-90.6183213238378,
173.838628285224));
#34212=CARTESIAN_POINT('Ctrl Pts',(-58.1489228992904,-90.7470140885838,
173.362985019365));
#34213=CARTESIAN_POINT('Ctrl Pts',(-57.794726357837,-90.8176161826738,173.18648906466));
#34214=CARTESIAN_POINT('Ctrl Pts',(-57.049407235224,-90.9591667760492,172.986630995271));
#34215=CARTESIAN_POINT('Ctrl Pts',(-56.6666652198049,-91.0285802500661,
172.960849429604));
#34216=CARTESIAN_POINT('Ctrl Pts',(-55.9061538922212,-91.172868747317,173.058338296301));
#34217=CARTESIAN_POINT('Ctrl Pts',(-55.5358170768977,-91.2448364349498,
173.183416544522));
#34218=CARTESIAN_POINT('Ctrl Pts',(-55.0759192312235,-91.3366282705884,
173.448860726571));
#34219=CARTESIAN_POINT('Ctrl Pts',(-54.9575343983508,-91.3605221713019,
173.529261695251));
#34220=CARTESIAN_POINT('Ctrl Pts',(-54.8455434145526,-91.3833997683648,
173.617797875547));
#34221=CARTESIAN_POINT('Ctrl Pts',(-54.8985464167762,-91.8805825131934,
173.617797875548));
#34222=CARTESIAN_POINT('Ctrl Pts',(-54.9166810916879,-91.8768779490274,
173.603461231711));
#34223=CARTESIAN_POINT('Ctrl Pts',(-54.9349890694865,-91.8731455836112,
173.589333497864));
#34224=CARTESIAN_POINT('Ctrl Pts',(-55.2706786758864,-91.8048472129455,
173.336533768563));
#34225=CARTESIAN_POINT('Ctrl Pts',(-55.6320124378843,-91.7335359313884,
173.164748325449));
#34226=CARTESIAN_POINT('Ctrl Pts',(-56.3858109203006,-91.5885640570063,
172.979061269994));
#34227=CARTESIAN_POINT('Ctrl Pts',(-56.7695858610019,-91.5169457857638,
172.961300143484));
#34228=CARTESIAN_POINT('Ctrl Pts',(-57.5374706866368,-91.374825024809,173.076344111801));
#34229=CARTESIAN_POINT('Ctrl Pts',(-57.9128873597064,-91.3020142352857,
173.2139861571));
#34230=CARTESIAN_POINT('Ctrl Pts',(-58.5748367120917,-91.1668279668907,
173.623064850725));
#34231=CARTESIAN_POINT('Ctrl Pts',(-58.857963704019,-91.1059167792226,173.885507747618));
#34232=CARTESIAN_POINT('Ctrl Pts',(-59.3187021614947,-90.9965538807659,
174.517108019837));
#34233=CARTESIAN_POINT('Ctrl Pts',(-59.4866569982001,-90.9458616320282,
174.883756248298));
#34234=CARTESIAN_POINT('Ctrl Pts',(-59.6656693259464,-90.8621539735064,
175.648497203549));
#34235=CARTESIAN_POINT('Ctrl Pts',(-59.6806707514033,-90.8298055031703,
176.037719840239));
#34236=CARTESIAN_POINT('Ctrl Pts',(-59.5610573016957,-90.7823250908908,
176.816610699042));
#34237=CARTESIAN_POINT('Ctrl Pts',(-59.421264166161,-90.764442457344,177.19788608769));
#34238=CARTESIAN_POINT('Ctrl Pts',(-59.0085766208076,-90.7438086481022,
177.871104180369));
#34239=CARTESIAN_POINT('Ctrl Pts',(-58.7447412256737,-90.7411661130838,
178.159490981354));
#34240=CARTESIAN_POINT('Ctrl Pts',(-58.1109238709733,-90.7485155107734,
178.630153630412));
#34241=CARTESIAN_POINT('Ctrl Pts',(-57.7430677366468,-90.7549474481067,
178.803055769306));
#34242=CARTESIAN_POINT('Ctrl Pts',(-56.9759778588354,-90.7720903515221,
178.990970442362));
#34243=CARTESIAN_POINT('Ctrl Pts',(-56.5856872827903,-90.7829101058451,
179.009826258095));
#34244=CARTESIAN_POINT('Ctrl Pts',(-55.8046079374573,-90.8059700487964,
178.896911433344));
#34245=CARTESIAN_POINT('Ctrl Pts',(-55.4218044306841,-90.8139969176569,
178.760265658305));
#34246=CARTESIAN_POINT('Ctrl Pts',(-54.7449879083774,-90.8215114762877,
178.352878528531));
#34247=CARTESIAN_POINT('Ctrl Pts',(-54.4546340104405,-90.8216598206604,
178.091135798334));
#34248=CARTESIAN_POINT('Ctrl Pts',(-53.9794754661803,-90.8121172399509,
177.460611953341));
#34249=CARTESIAN_POINT('Ctrl Pts',(-53.8036420816968,-90.7980810670428,
177.094306568579));
#34250=CARTESIAN_POINT('Ctrl Pts',(-53.6090739848902,-90.7541804381832,
176.329858004511));
#34251=CARTESIAN_POINT('Ctrl Pts',(-53.5866342074026,-90.7257509734569,
175.940605797033));
#34252=CARTESIAN_POINT('Ctrl Pts',(-53.6917102782147,-90.6543614750933,
175.161281567195));
#34253=CARTESIAN_POINT('Ctrl Pts',(-53.8237290083727,-90.6075074843315,
174.779591227941));
#34254=CARTESIAN_POINT('Ctrl Pts',(-54.2121538026836,-90.5029429956027,
174.120838580762));
#34255=CARTESIAN_POINT('Ctrl Pts',(-54.4539929001211,-90.4473655123602,
173.843539442958));
#34256=CARTESIAN_POINT('Ctrl Pts',(-54.7395374101039,-90.3890342787078,
173.617797875548));
#34257=CARTESIAN_POINT('Origin',(-54.1598171290174,-67.5719248685924,175.985485069079));
#34258=CARTESIAN_POINT('',(-54.527525401208,-88.4003032993935,173.617797875547));
#34259=CARTESIAN_POINT('',(-54.5805284034317,-88.8974860442222,173.617797875548));
#34260=CARTESIAN_POINT('',(-52.327900808713,-67.7672193871761,173.617797875548));
#34261=CARTESIAN_POINT('Ctrl Pts',(-54.5275254012084,-88.4003032993935,
173.617797875547));
#34262=CARTESIAN_POINT('Ctrl Pts',(-54.278959213732,-88.4510805752748,173.814305666117));
#34263=CARTESIAN_POINT('Ctrl Pts',(-54.0631391385075,-88.4998460783872,
174.050160506599));
#34264=CARTESIAN_POINT('Ctrl Pts',(-53.6710624598621,-88.6006245172416,
174.648595393675));
#34265=CARTESIAN_POINT('Ctrl Pts',(-53.5217286468206,-88.6494022957689,
175.021474411702));
#34266=CARTESIAN_POINT('Ctrl Pts',(-53.3794474284676,-88.7256210554948,
175.791566490734));
#34267=CARTESIAN_POINT('Ctrl Pts',(-53.3826058558834,-88.7548547030929,
176.180234237913));
#34268=CARTESIAN_POINT('Ctrl Pts',(-53.5382939506053,-88.8024794567196,
176.950116833368));
#34269=CARTESIAN_POINT('Ctrl Pts',(-53.694544846128,-88.8186825700164,177.322845741933));
#34270=CARTESIAN_POINT('Ctrl Pts',(-54.1348950035689,-88.8328485434147,
177.974555021883));
#34271=CARTESIAN_POINT('Ctrl Pts',(-54.4103082949843,-88.8329851822358,
178.250309372985));
#34272=CARTESIAN_POINT('Ctrl Pts',(-55.0619731676736,-88.8277023916178,
178.691035708699));
#34273=CARTESIAN_POINT('Ctrl Pts',(-55.4348430505563,-88.8208148853015,
178.847252783794));
#34274=CARTESIAN_POINT('Ctrl Pts',(-56.2056002236782,-88.7998194230701,
179.002367411531));
#34275=CARTESIAN_POINT('Ctrl Pts',(-56.595096367605,-88.7877202098109,179.005175375157));
#34276=CARTESIAN_POINT('Ctrl Pts',(-57.3681199604207,-88.7694646375483,
178.861163165126));
#34277=CARTESIAN_POINT('Ctrl Pts',(-57.7430685887949,-88.7623575781902,
178.710432055626));
#34278=CARTESIAN_POINT('Ctrl Pts',(-58.4005781238326,-88.7534997661608,
178.279269721459));
#34279=CARTESIAN_POINT('Ctrl Pts',(-58.6799123287478,-88.7530699805666,
178.007597618008));
#34280=CARTESIAN_POINT('Ctrl Pts',(-59.1296739375624,-88.7692390572475,
177.362779114218));
#34281=CARTESIAN_POINT('Ctrl Pts',(-59.2912554998927,-88.7848799843777,
176.992817647715));
#34282=CARTESIAN_POINT('Ctrl Pts',(-59.4580244949498,-88.8284055944828,
176.225797860729));
#34283=CARTESIAN_POINT('Ctrl Pts',(-59.4670141404289,-88.8567214239698,
175.837304583598));
#34284=CARTESIAN_POINT('Ctrl Pts',(-59.3368366833603,-88.934676455815,175.065934646549));
#34285=CARTESIAN_POINT('Ctrl Pts',(-59.1936101856561,-88.9828130954779,
174.691427261397));
#34286=CARTESIAN_POINT('Ctrl Pts',(-58.7770321126355,-89.0885970625982,
174.033381480313));
#34287=CARTESIAN_POINT('Ctrl Pts',(-58.5123353943137,-89.1460148183289,
173.753328914884));
#34288=CARTESIAN_POINT('Ctrl Pts',(-57.8819764068814,-89.2772508593794,
173.302601761779));
#34289=CARTESIAN_POINT('Ctrl Pts',(-57.5192586279044,-89.3487873024151,
173.140548522746));
#34290=CARTESIAN_POINT('Ctrl Pts',(-56.7648259432275,-89.4906608863938,
172.972676652572));
#34291=CARTESIAN_POINT('Ctrl Pts',(-56.3816889784975,-89.5606307884222,
172.963324417664));
#34292=CARTESIAN_POINT('Ctrl Pts',(-55.6206076806915,-89.7057586889692,
173.09416500872));
#34293=CARTESIAN_POINT('Ctrl Pts',(-55.2507109162235,-89.7780603762169,
173.238186049348));
#34294=CARTESIAN_POINT('Ctrl Pts',(-54.8390972685506,-89.8608153127105,
173.503077007167));
#34295=CARTESIAN_POINT('Ctrl Pts',(-54.7613681906975,-89.8765644360083,
173.558636887198));
#34296=CARTESIAN_POINT('Ctrl Pts',(-54.686534407881,-89.891851533879,173.617797875547));
#34297=CARTESIAN_POINT('Ctrl Pts',(-54.7395374101039,-90.3890342787078,
173.617797875548));
#34298=CARTESIAN_POINT('Ctrl Pts',(-54.7536254637881,-90.3861563611768,
173.606660349841));
#34299=CARTESIAN_POINT('Ctrl Pts',(-54.7678182303282,-90.3832616402047,
173.595648805531));
#34300=CARTESIAN_POINT('Ctrl Pts',(-55.0982533651628,-90.3159724008806,
173.344078904514));
#34301=CARTESIAN_POINT('Ctrl Pts',(-55.4589009037588,-90.244746248267,173.170330584284));
#34302=CARTESIAN_POINT('Ctrl Pts',(-56.2121090481486,-90.0997986432487,
172.980726626293));
#34303=CARTESIAN_POINT('Ctrl Pts',(-56.595927926668,-90.0280296445997,172.961040933605));
#34304=CARTESIAN_POINT('Ctrl Pts',(-57.364692387148,-89.8859045163428,173.072342018584));
#34305=CARTESIAN_POINT('Ctrl Pts',(-57.740943444431,-89.8130160471777,173.208232122973));
#34306=CARTESIAN_POINT('Ctrl Pts',(-58.4050713366844,-89.677561539593,173.614336496615));
#34307=CARTESIAN_POINT('Ctrl Pts',(-58.6894857142339,-89.6163763313695,
173.875548982126));
#34308=CARTESIAN_POINT('Ctrl Pts',(-59.1532617495717,-89.5067731061024,
174.505256478686));
#34309=CARTESIAN_POINT('Ctrl Pts',(-59.3229162292159,-89.455910265214,174.871300750203));
#34310=CARTESIAN_POINT('Ctrl Pts',(-59.5053156644829,-89.3718080168573,
175.635526450194));
#34311=CARTESIAN_POINT('Ctrl Pts',(-59.5219693261846,-89.3391553739719,
176.024801063651));
#34312=CARTESIAN_POINT('Ctrl Pts',(-59.4056032603791,-89.2914067264333,
176.80445156296));
#34313=CARTESIAN_POINT('Ctrl Pts',(-59.2673278848242,-89.2733722520209,
177.186454382289));
#34314=CARTESIAN_POINT('Ctrl Pts',(-58.8572117329723,-89.2524331345483,
177.861580919718));
#34315=CARTESIAN_POINT('Ctrl Pts',(-58.5944281193864,-89.2495586805081,
178.151106738878));
#34316=CARTESIAN_POINT('Ctrl Pts',(-57.9622569533401,-89.2568053463866,
178.624417870856));
#34317=CARTESIAN_POINT('Ctrl Pts',(-57.5949256922417,-89.2631906837858,
178.798805174538));
#34318=CARTESIAN_POINT('Ctrl Pts',(-56.8282798696182,-89.280257229962,178.989685525946));
#34319=CARTESIAN_POINT('Ctrl Pts',(-56.4379325091458,-89.2909710055577,
179.009998109976));
#34320=CARTESIAN_POINT('Ctrl Pts',(-55.6562050183527,-89.3141679414693,
178.899915840531));
#34321=CARTESIAN_POINT('Ctrl Pts',(-55.2727748448249,-89.3222703955619,
178.764596795762));
#34322=CARTESIAN_POINT('Ctrl Pts',(-54.5943065964784,-89.3299340357216,
178.359461637739));
#34323=CARTESIAN_POINT('Ctrl Pts',(-54.3029571080176,-89.3300837842501,
178.098649388314));
#34324=CARTESIAN_POINT('Ctrl Pts',(-53.8255171030039,-89.3208477620272,
177.469558737649));
#34325=CARTESIAN_POINT('Ctrl Pts',(-53.6484015612722,-89.3069565074131,
177.103712395319));
#34326=CARTESIAN_POINT('Ctrl Pts',(-53.4512680624326,-89.2633042403586,
176.339655732208));
#34327=CARTESIAN_POINT('Ctrl Pts',(-53.4275592631866,-89.2349121908259,
175.950364200724));
#34328=CARTESIAN_POINT('Ctrl Pts',(-53.5301943217796,-89.1638419955626,
175.170468526992));
#34329=CARTESIAN_POINT('Ctrl Pts',(-53.661067303405,-89.117117863704,174.788230851258));
#34330=CARTESIAN_POINT('Ctrl Pts',(-54.0490890144365,-89.0123282517972,
174.125508908105));
#34331=CARTESIAN_POINT('Ctrl Pts',(-54.292569942137,-88.9563104015491,173.845447828985));
#34332=CARTESIAN_POINT('Ctrl Pts',(-54.5805284034317,-88.8974860442222,
173.617797875548));
#34333=CARTESIAN_POINT('Origin',(-54.1598171290174,-67.5719248685924,175.985485069079));
#34334=CARTESIAN_POINT('',(-54.3685163945356,-86.908755064908,173.617797875548));
#34335=CARTESIAN_POINT('',(-54.4215193967595,-87.4059378097366,173.617797875548));
#34336=CARTESIAN_POINT('',(-52.327900808713,-67.7672193871761,173.617797875548));
#34337=CARTESIAN_POINT('Ctrl Pts',(-54.3685163945357,-86.908755064908,173.617797875548));
#34338=CARTESIAN_POINT('Ctrl Pts',(-54.1029134234621,-86.9630126269441,
173.827774355231));
#34339=CARTESIAN_POINT('Ctrl Pts',(-53.8749031255443,-87.0149320416049,
174.082522212409));
#34340=CARTESIAN_POINT('Ctrl Pts',(-53.4839217198981,-87.1175329221976,
174.708627630965));
#34341=CARTESIAN_POINT('Ctrl Pts',(-53.3425096711802,-87.165439707321,175.085665523802));
#34342=CARTESIAN_POINT('Ctrl Pts',(-53.217327784721,-87.2394477467716,175.860123223724));
#34343=CARTESIAN_POINT('Ctrl Pts',(-53.2293355299918,-87.2682568338261,
176.249055654486));
#34344=CARTESIAN_POINT('Ctrl Pts',(-53.4028417589691,-87.3141841401225,
177.016565188295));
#34345=CARTESIAN_POINT('Ctrl Pts',(-53.5681002985076,-87.3294012224974,
177.386475181806));
#34346=CARTESIAN_POINT('Ctrl Pts',(-54.0244567155213,-87.3414536350706,
178.02860024861));
#34347=CARTESIAN_POINT('Ctrl Pts',(-54.3066838638898,-87.3413982130645,
178.297952302799));
#34348=CARTESIAN_POINT('Ctrl Pts',(-54.9699021379563,-87.3350990058782,
178.723581420034));
#34349=CARTESIAN_POINT('Ctrl Pts',(-55.3474236314889,-87.3276908946758,
178.870954732385));
#34350=CARTESIAN_POINT('Ctrl Pts',(-56.1230261659881,-87.3057520135597,
179.006897705685));
#34351=CARTESIAN_POINT('Ctrl Pts',(-56.5128705872014,-87.2941642204602,
178.999870109779));
#34352=CARTESIAN_POINT('Ctrl Pts',(-57.2833550787784,-87.2764084214759,
178.835977058011));
#34353=CARTESIAN_POINT('Ctrl Pts',(-57.655250097498,-87.2696035857755,178.67516561695));
#34354=CARTESIAN_POINT('Ctrl Pts',(-58.3021881708129,-87.2614259727787,
178.226047615204));
#34355=CARTESIAN_POINT('Ctrl Pts',(-58.5745176094255,-87.2623041320782,
177.94683862187));
#34356=CARTESIAN_POINT('Ctrl Pts',(-59.0077172301551,-87.2804824200033,
177.289126552806));
#34357=CARTESIAN_POINT('Ctrl Pts',(-59.1595907756512,-87.2971367709562,
176.913918521583));
#34358=CARTESIAN_POINT('Ctrl Pts',(-59.3052160159744,-87.3424495960633,
176.141379741915));
#34359=CARTESIAN_POINT('Ctrl Pts',(-59.3034448447673,-87.3724845845416,
175.752566156436));
#34360=CARTESIAN_POINT('Ctrl Pts',(-59.1514503037943,-87.4530242277975,
174.98397360187));
#34361=CARTESIAN_POINT('Ctrl Pts',(-58.9971285531111,-87.5023244100845,
174.612779848241));
#34362=CARTESIAN_POINT('Ctrl Pts',(-58.5607371146546,-87.6097336617945,
173.966353225289));
#34363=CARTESIAN_POINT('Ctrl Pts',(-58.2878343094946,-87.6686068793633,
173.694141673873));
#34364=CARTESIAN_POINT('Ctrl Pts',(-57.6433222454351,-87.8016263280554,
173.261740441671));
#34365=CARTESIAN_POINT('Ctrl Pts',(-57.2747814021579,-87.8737669662917,
173.110395606436));
#34366=CARTESIAN_POINT('Ctrl Pts',(-56.5141636936474,-88.0157929314995,
172.965865670225));
#34367=CARTESIAN_POINT('Ctrl Pts',(-56.1307417720863,-88.0863800636285,
172.968487293171));
#34368=CARTESIAN_POINT('Ctrl Pts',(-55.3726400952361,-88.2314813856136,
173.123462718543));
#34369=CARTESIAN_POINT('Ctrl Pts',(-55.0062691489335,-88.3033938284711,
173.279760181978));
#34370=CARTESIAN_POINT('Ctrl Pts',(-54.6285746166461,-88.3797183894738,
173.540528378013));
#34371=CARTESIAN_POINT('Ctrl Pts',(-54.5774011679008,-88.3901146426384,
173.578367827498));
#34372=CARTESIAN_POINT('Ctrl Pts',(-54.5275254012084,-88.4003032993935,
173.617797875547));
#34373=CARTESIAN_POINT('Ctrl Pts',(-54.5805284034317,-88.8974860442222,
173.617797875548));
#34374=CARTESIAN_POINT('Ctrl Pts',(-54.592304347756,-88.89508044602,173.608488223159));
#34375=CARTESIAN_POINT('Ctrl Pts',(-54.604153503143,-88.8926630974012,173.599266555514));
#34376=CARTESIAN_POINT('Ctrl Pts',(-54.9315971883393,-88.8259488965967,
173.348420700598));
#34377=CARTESIAN_POINT('Ctrl Pts',(-55.291848201925,-88.7547722417383,173.173552135254));
#34378=CARTESIAN_POINT('Ctrl Pts',(-56.0447147782708,-88.6098392974242,
172.981710015181));
#34379=CARTESIAN_POINT('Ctrl Pts',(-56.4285586273302,-88.537982258094,172.960925148545));
#34380=CARTESIAN_POINT('Ctrl Pts',(-57.1978210124498,-88.3958554029432,
173.070089317494));
#34381=CARTESIAN_POINT('Ctrl Pts',(-57.5745445588047,-88.3229233273283,
173.204978017596));
#34382=CARTESIAN_POINT('Ctrl Pts',(-58.239912727543,-88.1873163601604,173.609382874055));
#34383=CARTESIAN_POINT('Ctrl Pts',(-58.5250611020044,-88.1259731967198,
173.869893773846));
#34384=CARTESIAN_POINT('Ctrl Pts',(-58.9905661098442,-88.0162335199632,
174.498519613728));
#34385=CARTESIAN_POINT('Ctrl Pts',(-59.1611878212844,-87.9652738946288,
174.86421645565));
#34386=CARTESIAN_POINT('Ctrl Pts',(-59.3455168063876,-87.8809471158559,
175.62814538344));
#34387=CARTESIAN_POINT('Ctrl Pts',(-59.363111134507,-87.8481198021688,176.017449655811));
#34388=CARTESIAN_POINT('Ctrl Pts',(-59.2485936583136,-87.8002186934163,
176.797529305977));
#34389=CARTESIAN_POINT('Ctrl Pts',(-59.1111831652141,-87.7820979358716,
177.179943240195));
#34390=CARTESIAN_POINT('Ctrl Pts',(-58.7025318440207,-87.7609851429597,
177.856153465695));
#34391=CARTESIAN_POINT('Ctrl Pts',(-58.4403461617647,-87.757977536504,178.146327034948));
#34392=CARTESIAN_POINT('Ctrl Pts',(-57.8091128610305,-87.7651657876644,
178.621141802717));
#34393=CARTESIAN_POINT('Ctrl Pts',(-57.4420823604527,-87.7715245954983,
178.796372126317));
#34394=CARTESIAN_POINT('Ctrl Pts',(-56.6756912855874,-87.7885476910923,
178.988937440833));
#34395=CARTESIAN_POINT('Ctrl Pts',(-56.2853115113751,-87.7992001763368,
179.010077390318));
#34396=CARTESIAN_POINT('Ctrl Pts',(-55.5032184787108,-87.8224748083139,
178.901603419635));
#34397=CARTESIAN_POINT('Ctrl Pts',(-55.1194347368525,-87.8306201261721,
178.7670383405));
#34398=CARTESIAN_POINT('Ctrl Pts',(-54.4400306868328,-87.8383683735314,
178.363182624418));
#34399=CARTESIAN_POINT('Ctrl Pts',(-54.1481162878296,-87.8385179630927,
178.102898192409));
#34400=CARTESIAN_POINT('Ctrl Pts',(-53.6693839012453,-87.8294557922013,
177.474621870949));
#34401=CARTESIAN_POINT('Ctrl Pts',(-53.4915421823287,-87.8156467834496,
177.109037647409));
#34402=CARTESIAN_POINT('Ctrl Pts',(-53.2929545172073,-87.7721354430938,
176.345204975317));
#34403=CARTESIAN_POINT('Ctrl Pts',(-53.268526519972,-87.7437637642731,175.955891126618));
#34404=CARTESIAN_POINT('Ctrl Pts',(-53.3697786896165,-87.6728745941867,
175.175673567676));
#34405=CARTESIAN_POINT('Ctrl Pts',(-53.5000020944734,-87.6262242224846,
174.793127496324));
#34406=CARTESIAN_POINT('Ctrl Pts',(-53.8877865868758,-87.5213083526867,
174.128156458117));
#34407=CARTESIAN_POINT('Ctrl Pts',(-54.1321940868959,-87.465041387852,173.846528411968));
#34408=CARTESIAN_POINT('Ctrl Pts',(-54.4215193967595,-87.4059378097366,
173.617797875548));
#34409=CARTESIAN_POINT('Origin',(-54.1598171290174,-67.5719248685924,175.985485069079));
#34410=CARTESIAN_POINT('',(-54.2095073878632,-85.4172068304224,173.617797875548));
#34411=CARTESIAN_POINT('',(-54.2625103900873,-85.914389575251,173.617797875548));
#34412=CARTESIAN_POINT('',(-52.327900808713,-67.7672193871761,173.617797875548));
#34413=CARTESIAN_POINT('Ctrl Pts',(-54.2095073878633,-85.4172068304224,
173.617797875548));
#34414=CARTESIAN_POINT('Ctrl Pts',(-53.9332619774107,-85.473638437472,173.836187897997));
#34415=CARTESIAN_POINT('Ctrl Pts',(-53.6978124997361,-85.5275145906288,
174.102912189541));
#34416=CARTESIAN_POINT('Ctrl Pts',(-53.3080240280004,-85.631186385472,174.746408240766));
#34417=CARTESIAN_POINT('Ctrl Pts',(-53.1716090248673,-85.6785357557079,
175.12595808378));
#34418=CARTESIAN_POINT('Ctrl Pts',(-53.0571443781225,-85.7511505542224,
175.903045422152));
#34419=CARTESIAN_POINT('Ctrl Pts',(-53.0747085639042,-85.7797413584373,
176.29214731336));
#34420=CARTESIAN_POINT('Ctrl Pts',(-53.2594265255084,-85.8245925543852,
177.058062082337));
#34421=CARTESIAN_POINT('Ctrl Pts',(-53.4303247636375,-85.8391830097732,
177.426089782173));
#34422=CARTESIAN_POINT('Ctrl Pts',(-53.8967058701507,-85.8499009319195,
178.062075923266));
#34423=CARTESIAN_POINT('Ctrl Pts',(-54.1832488382114,-85.8497779723597,
178.32738366672));
#34424=CARTESIAN_POINT('Ctrl Pts',(-54.8537139825916,-85.842833703405,178.74335647834));
#34425=CARTESIAN_POINT('Ctrl Pts',(-55.2340772721629,-85.8350966284344,
178.885055963083));
#34426=CARTESIAN_POINT('Ctrl Pts',(-56.0126295423935,-85.8125617841953,
179.008790586575));
#34427=CARTESIAN_POINT('Ctrl Pts',(-56.4027069366073,-85.8013603685799,
178.995495185527));
#34428=CARTESIAN_POINT('Ctrl Pts',(-57.1714392733414,-85.7839277598787,
178.818886663266));
#34429=CARTESIAN_POINT('Ctrl Pts',(-57.5412436559841,-85.7773192886942,
178.651662075905));
#34430=CARTESIAN_POINT('Ctrl Pts',(-58.1812837764483,-85.769579214134,178.191119255375));
#34431=CARTESIAN_POINT('Ctrl Pts',(-58.4491221618275,-85.7713660718236,
177.907062514141));
#34432=CARTESIAN_POINT('Ctrl Pts',(-58.8715335140524,-85.790840307223,177.241132176311));
#34433=CARTESIAN_POINT('Ctrl Pts',(-59.017059928142,-85.8081444246837,176.862674162691));
#34434=CARTESIAN_POINT('Ctrl Pts',(-59.1489804595095,-85.85460350698,176.086729179939));
#34435=CARTESIAN_POINT('Ctrl Pts',(-59.1402390484174,-85.8858301162748,
175.697701855906));
#34436=CARTESIAN_POINT('Ctrl Pts',(-58.974034668921,-85.968040490002,174.931077916915));
#34437=CARTESIAN_POINT('Ctrl Pts',(-58.8125265331801,-86.0180796985493,
174.56221435483));
#34438=CARTESIAN_POINT('Ctrl Pts',(-58.363303890959,-86.1265245857877,173.923525340057));
#34439=CARTESIAN_POINT('Ctrl Pts',(-58.0850332582311,-86.1864369832083,
173.656442059579));
#34440=CARTESIAN_POINT('Ctrl Pts',(-57.4313372083917,-86.3206019885938,
173.236218802077));
#34441=CARTESIAN_POINT('Ctrl Pts',(-57.0591320567907,-86.393106152254,173.092020404767));
#34442=CARTESIAN_POINT('Ctrl Pts',(-56.294637190197,-86.5351951521233,172.962917148004));
#34443=CARTESIAN_POINT('Ctrl Pts',(-55.9110292620967,-86.6062870231821,
172.973455605913));
#34444=CARTESIAN_POINT('Ctrl Pts',(-55.1551026662993,-86.7513341797469,
173.144467091908));
#34445=CARTESIAN_POINT('Ctrl Pts',(-54.7912855834294,-86.8229474419353,
173.308872270221));
#34446=CARTESIAN_POINT('Ctrl Pts',(-54.4356971143808,-86.8950569693321,
173.56585347481));
#34447=CARTESIAN_POINT('Ctrl Pts',(-54.4018159408511,-86.9019526101287,
173.591472411333));
#34448=CARTESIAN_POINT('Ctrl Pts',(-54.3685163945357,-86.908755064908,173.617797875548));
#34449=CARTESIAN_POINT('Ctrl Pts',(-54.4215193967595,-87.4059378097366,
173.617797875548));
#34450=CARTESIAN_POINT('Ctrl Pts',(-54.4319874202367,-87.4037993945264,
173.609522219933));
#34451=CARTESIAN_POINT('Ctrl Pts',(-54.4425133166328,-87.401651689743,173.601316073085));
#34452=CARTESIAN_POINT('Ctrl Pts',(-54.7682682986267,-87.3352622732361,
173.350886654411));
#34453=CARTESIAN_POINT('Ctrl Pts',(-55.1282935773606,-87.2641138943975,
173.175384803604));
#34454=CARTESIAN_POINT('Ctrl Pts',(-55.8809655577316,-87.1191894994919,
172.982276537438));
#34455=CARTESIAN_POINT('Ctrl Pts',(-56.2648234871258,-87.0472820411832,
172.960870028795));
#34456=CARTESIAN_POINT('Ctrl Pts',(-57.0343660410513,-86.9051544556821,
173.068825910744));
#34457=CARTESIAN_POINT('Ctrl Pts',(-57.4113554997123,-86.8321979622416,
173.203148010723));
#34458=CARTESIAN_POINT('Ctrl Pts',(-58.0774238349211,-86.6965050095272,
173.606591451899));
#34459=CARTESIAN_POINT('Ctrl Pts',(-58.3629869156974,-86.6350720497216,
173.866705931947));
#34460=CARTESIAN_POINT('Ctrl Pts',(-58.8294678567425,-86.5252554612533,
174.494719841926));
#34461=CARTESIAN_POINT('Ctrl Pts',(-59.0006354631639,-86.4742413068587,
174.860219401169));
#34462=CARTESIAN_POINT('Ctrl Pts',(-59.1860541207935,-86.3897878119418,
175.623979691486));
#34463=CARTESIAN_POINT('Ctrl Pts',(-59.2041794913773,-86.3568614115411,
176.01330072742));
#34464=CARTESIAN_POINT('Ctrl Pts',(-59.0907055295616,-86.308874314158,176.79362158147));
#34465=CARTESIAN_POINT('Ctrl Pts',(-58.9537835370001,-86.2907048997491,
177.176266632583));
#34466=CARTESIAN_POINT('Ctrl Pts',(-58.5459594382781,-86.2694941077165,
177.853087725861));
#34467=CARTESIAN_POINT('Ctrl Pts',(-58.2841110305906,-86.2664109768285,
178.14362674106));
#34468=CARTESIAN_POINT('Ctrl Pts',(-57.6534073895263,-86.2735662744409,
178.619289013214));
#34469=CARTESIAN_POINT('Ctrl Pts',(-57.286547293649,-86.2799101059405,178.79499443983));
#34470=CARTESIAN_POINT('Ctrl Pts',(-56.5203006495415,-86.2969086792263,
178.988509859046));
#34471=CARTESIAN_POINT('Ctrl Pts',(-56.1299025507582,-86.3075262609867,
179.010116242818));
#34472=CARTESIAN_POINT('Ctrl Pts',(-55.3476042608382,-86.3308446599301,
178.902548818617));
#34473=CARTESIAN_POINT('Ctrl Pts',(-54.9636219411715,-86.339014121752,178.768408933986));
#34474=CARTESIAN_POINT('Ctrl Pts',(-54.28369105841,-86.3468100467483,178.365274651518));
#34475=CARTESIAN_POINT('Ctrl Pts',(-53.9914583566946,-86.3469592427903,
178.105287575512));
#34476=CARTESIAN_POINT('Ctrl Pts',(-53.5119984547237,-86.3379949994304,
177.477470446987));
#34477=CARTESIAN_POINT('Ctrl Pts',(-53.3337479942983,-86.3242323378271,
177.112034440454));
#34478=CARTESIAN_POINT('Ctrl Pts',(-53.1343414415493,-86.2808004043142,
176.348328493555));
#34479=CARTESIAN_POINT('Ctrl Pts',(-53.1095084810868,-86.2524399309787,
175.959002069361));
#34480=CARTESIAN_POINT('Ctrl Pts',(-53.209982146529,-86.1816527120886,175.178603891707));
#34481=CARTESIAN_POINT('Ctrl Pts',(-53.3398397165186,-86.1350439249261,
174.795884743041));
#34482=CARTESIAN_POINT('Ctrl Pts',(-53.7274878481633,-86.0300573849754,
174.129647447484));
#34483=CARTESIAN_POINT('Ctrl Pts',(-53.9724158334711,-85.9736502956349,
173.84713655172));
#34484=CARTESIAN_POINT('Ctrl Pts',(-54.2625103900873,-85.914389575251,173.617797875548));
#34485=CARTESIAN_POINT('Origin',(-54.1598171290174,-67.5719248685924,175.985485069079));
#34486=CARTESIAN_POINT('',(-54.050498381191,-83.9256585959369,173.617797875548));
#34487=CARTESIAN_POINT('',(-54.1035013834151,-84.4228413407654,173.617797875548));
#34488=CARTESIAN_POINT('',(-52.327900808713,-67.7672193871761,173.617797875548));
#34489=CARTESIAN_POINT('Ctrl Pts',(-54.050498381191,-83.9256585959369,173.617797875548));
#34490=CARTESIAN_POINT('Ctrl Pts',(-53.7679065572478,-83.9833866528051,
173.841205151976));
#34491=CARTESIAN_POINT('Ctrl Pts',(-53.5280851485867,-84.0384247724667,
174.115135380727));
#34492=CARTESIAN_POINT('Ctrl Pts',(-53.1391948368034,-84.1427101835225,
174.769037761665));
#34493=CARTESIAN_POINT('Ctrl Pts',(-53.0057771809645,-84.1897223073407,
175.150053949138));
#34494=CARTESIAN_POINT('Ctrl Pts',(-52.8977174976408,-84.2615016781384,
175.928674036426));
#34495=CARTESIAN_POINT('Ctrl Pts',(-52.9186069647449,-84.2899794092634,
176.317878307109));
#34496=CARTESIAN_POINT('Ctrl Pts',(-53.1100418741121,-84.3341829233429,
177.082799875532));
#34497=CARTESIAN_POINT('Ctrl Pts',(-53.2843075286004,-84.3483957778167,
177.449660036152));
#34498=CARTESIAN_POINT('Ctrl Pts',(-53.7566771132667,-84.3583125141355,
178.081928347658));
#34499=CARTESIAN_POINT('Ctrl Pts',(-54.0458168038138,-84.3581688027116,
178.344806348492));
#34500=CARTESIAN_POINT('Ctrl Pts',(-54.7206146471591,-84.3508360098067,
178.75493492402));
#34501=CARTESIAN_POINT('Ctrl Pts',(-55.1026477851618,-84.3429013946851,
178.893195176074));
#34502=CARTESIAN_POINT('Ctrl Pts',(-55.8829299011184,-84.3200086326902,
179.009561251224));
#34503=CARTESIAN_POINT('Ctrl Pts',(-56.2731518250052,-84.3090631467957,
178.992479748983));
#34504=CARTESIAN_POINT('Ctrl Pts',(-57.0407748322682,-84.2918274973282,
178.808175263482));
#34505=CARTESIAN_POINT('Ctrl Pts',(-57.4092621611192,-84.2853389965204,
178.637083382537));
#34506=CARTESIAN_POINT('Ctrl Pts',(-58.0450756540518,-84.2778646839619,
178.169648162453));
#34507=CARTESIAN_POINT('Ctrl Pts',(-58.3101903712652,-84.280229093688,177.882646086267));
#34508=CARTESIAN_POINT('Ctrl Pts',(-58.7259964278775,-84.3004918881376,
177.21175299148));
#34509=CARTESIAN_POINT('Ctrl Pts',(-58.8676293943606,-84.3181897297269,
176.831369667309));
#34510=CARTESIAN_POINT('Ctrl Pts',(-58.991185174051,-84.3653438008588,176.053410903082));
#34511=CARTESIAN_POINT('Ctrl Pts',(-58.9781892577483,-84.3973275787765,
175.66425113474));
#34512=CARTESIAN_POINT('Ctrl Pts',(-58.8032846239125,-84.4805559295001,
174.898895026642));
#34513=CARTESIAN_POINT('Ctrl Pts',(-58.6373939973216,-84.5310401060385,
174.531524492106));
#34514=CARTESIAN_POINT('Ctrl Pts',(-58.1803437281115,-84.6401101784401,
173.897638942517));
#34515=CARTESIAN_POINT('Ctrl Pts',(-57.8987762263253,-84.7006946036871,
173.633705756515));
#34516=CARTESIAN_POINT('Ctrl Pts',(-57.2394712011691,-84.8355545270622,
173.221035260935));
#34517=CARTESIAN_POINT('Ctrl Pts',(-56.8650748640176,-84.9082691861619,
173.081278690915));
#34518=CARTESIAN_POINT('Ctrl Pts',(-56.0982663102263,-85.0503823778178,
172.96170957192));
#34519=CARTESIAN_POINT('Ctrl Pts',(-55.7145448066483,-85.1218243504424,
172.977144954069));
#34520=CARTESIAN_POINT('Ctrl Pts',(-54.9600460210043,-85.266823182249,173.158102082311));
#34521=CARTESIAN_POINT('Ctrl Pts',(-54.5978967227242,-85.3382347224806,
173.327513253623));
#34522=CARTESIAN_POINT('Ctrl Pts',(-54.255829777542,-85.4077563100731,173.581734482978));
#34523=CARTESIAN_POINT('Ctrl Pts',(-54.2325291387492,-85.4125039309337,
173.599597679264));
#34524=CARTESIAN_POINT('Ctrl Pts',(-54.2095073878633,-85.4172068304224,
173.617797875548));
#34525=CARTESIAN_POINT('Ctrl Pts',(-54.2625103900873,-85.914389575251,173.617797875548));
#34526=CARTESIAN_POINT('Ctrl Pts',(-54.272242730254,-85.9124014459457,173.610103825594));
#34527=CARTESIAN_POINT('Ctrl Pts',(-54.2820251050254,-85.910405284795,173.602469849516));
#34528=CARTESIAN_POINT('Ctrl Pts',(-54.6068313405509,-85.8441983922685,
173.352276841814));
#34529=CARTESIAN_POINT('Ctrl Pts',(-54.9667291943884,-85.7730660057973,
173.17641891249));
#34530=CARTESIAN_POINT('Ctrl Pts',(-55.7192912802216,-85.6281465011847,
172.982598442595));
#34531=CARTESIAN_POINT('Ctrl Pts',(-56.1031571149052,-85.556210487934,172.96084231474));
#34532=CARTESIAN_POINT('Ctrl Pts',(-56.8728567841258,-85.4140825697339,
173.068118723903));
#34533=CARTESIAN_POINT('Ctrl Pts',(-57.2499953804115,-85.3411124208112,
173.202122083087));
#34534=CARTESIAN_POINT('Ctrl Pts',(-57.9164570917249,-85.2053711845814,
173.605024735824));
#34535=CARTESIAN_POINT('Ctrl Pts',(-58.2022532786323,-85.1438875755383,
173.864916380031));
#34536=CARTESIAN_POINT('Ctrl Pts',(-58.6692824949556,-85.0340278130821,
174.492586073101));
#34537=CARTESIAN_POINT('Ctrl Pts',(-58.8407567608416,-84.9829830568063,
174.857974428286));
#34538=CARTESIAN_POINT('Ctrl Pts',(-59.0267877573062,-84.8984583802647,
175.621639622987));
#34539=CARTESIAN_POINT('Ctrl Pts',(-59.0452114899296,-84.865476157542,176.010970083441));
#34540=CARTESIAN_POINT('Ctrl Pts',(-58.9323237898062,-84.8174407740576,
176.791426117773));
#34541=CARTESIAN_POINT('Ctrl Pts',(-58.7956763323207,-84.7992440391595,
177.174200711645));
#34542=CARTESIAN_POINT('Ctrl Pts',(-58.3883170860243,-84.7779782022207,
177.851364725428));
#34543=CARTESIAN_POINT('Ctrl Pts',(-58.1266580846683,-84.7748525265982,
178.142108989257));
#34544=CARTESIAN_POINT('Ctrl Pts',(-57.4962520903143,-84.7819893171045,
178.618246995242));
#34545=CARTESIAN_POINT('Ctrl Pts',(-57.1294879282161,-84.7883247345141,
178.79421909619));
#34546=CARTESIAN_POINT('Ctrl Pts',(-56.3633226256829,-84.8053095324604,
178.988267968054));
#34547=CARTESIAN_POINT('Ctrl Pts',(-55.9729142234731,-84.8159074086289,
179.01013620997));
#34548=CARTESIAN_POINT('Ctrl Pts',(-55.1905009603469,-84.8392503674809,
178.903077677773));
#34549=CARTESIAN_POINT('Ctrl Pts',(-54.8064073951959,-84.8474333771942,
178.769176542408));
#34550=CARTESIAN_POINT('Ctrl Pts',(-54.1261809785311,-84.855256062124,178.366447318394));
#34551=CARTESIAN_POINT('Ctrl Pts',(-53.8337696343528,-84.8554049414776,
178.10662711442));
#34552=CARTESIAN_POINT('Ctrl Pts',(-53.3539016423839,-84.8464956488437,
177.479067812005));
#34553=CARTESIAN_POINT('Ctrl Pts',(-53.1754219176799,-84.8327590004161,
177.1137151551));
#34554=CARTESIAN_POINT('Ctrl Pts',(-52.9755559264343,-84.7893716329479,
176.350080493459));
#34555=CARTESIAN_POINT('Ctrl Pts',(-52.9504957729693,-84.7610173627157,
175.960747011359));
#34556=CARTESIAN_POINT('Ctrl Pts',(-53.050532734403,-84.6902873469128,175.180247700522));
#34557=CARTESIAN_POINT('Ctrl Pts',(-53.1801850405792,-84.64370190587,174.797431632577));
#34558=CARTESIAN_POINT('Ctrl Pts',(-53.5677557922408,-84.5386758518192,
174.130483990877));
#34559=CARTESIAN_POINT('Ctrl Pts',(-53.8129753877958,-84.4821901958128,
173.847477632404));
#34560=CARTESIAN_POINT('Ctrl Pts',(-54.1035013834151,-84.4228413407654,
173.617797875548));
#34561=CARTESIAN_POINT('Origin',(-54.1598171290174,-67.5719248685924,175.985485069079));
#34562=CARTESIAN_POINT('',(-53.8914893745187,-82.4341103614513,173.617797875548));
#34563=CARTESIAN_POINT('',(-53.9444923767428,-82.9312931062798,173.617797875548));
#34564=CARTESIAN_POINT('',(-52.327900808713,-67.7672193871761,173.617797875548));
#34565=CARTESIAN_POINT('Ctrl Pts',(-53.8914893745187,-82.4341103614513,
173.617797875548));
#34566=CARTESIAN_POINT('Ctrl Pts',(-53.6052173838758,-82.4925902053654,
173.844114563889));
#34567=CARTESIAN_POINT('Ctrl Pts',(-53.3628827650752,-82.548300455384,174.122245324128));
#34568=CARTESIAN_POINT('Ctrl Pts',(-52.9745773142937,-82.6529330761562,
174.782193804106));
#34569=CARTESIAN_POINT('Ctrl Pts',(-52.8429036775367,-82.6997479866898,
175.164049452677));
#34570=CARTESIAN_POINT('Ctrl Pts',(-52.7385630731543,-82.7710413119158,
175.943546295482));
#34571=CARTESIAN_POINT('Ctrl Pts',(-52.7613851386593,-82.7994593074702,
176.332810341507));
#34572=CARTESIAN_POINT('Ctrl Pts',(-52.9567259886705,-82.8432851590703,
177.09714129416));
#34573=CARTESIAN_POINT('Ctrl Pts',(-53.1329457267273,-82.8572777035077,
177.463308860173));
#34574=CARTESIAN_POINT('Ctrl Pts',(-53.6087916933352,-82.8667279618698,
178.093401456761));
#34575=CARTESIAN_POINT('Ctrl Pts',(-53.8994453490787,-82.8665789681866,
178.354863996896));
#34576=CARTESIAN_POINT('Ctrl Pts',(-54.5767595142852,-82.8590195272374,
178.761573480636));
#34577=CARTESIAN_POINT('Ctrl Pts',(-54.9597521761209,-82.8509698951223,
178.897820073131));
#34578=CARTESIAN_POINT('Ctrl Pts',(-55.7410271945383,-82.82786869725,179.00988231131));
#34579=CARTESIAN_POINT('Ctrl Pts',(-56.1313348213151,-82.8170805779664,
178.990588066779));
#34580=CARTESIAN_POINT('Ctrl Pts',(-56.8982916580408,-82.7999606351723,
178.801780992175));
#34581=CARTESIAN_POINT('Ctrl Pts',(-57.2659904558858,-82.7935427075112,
178.62843176922));
#34582=CARTESIAN_POINT('Ctrl Pts',(-57.8993130645951,-82.7862242116862,
178.156971903279));
#34583=CARTESIAN_POINT('Ctrl Pts',(-58.162832051056,-82.7889362062128,177.868242504181));
#34584=CARTESIAN_POINT('Ctrl Pts',(-58.5747467536174,-82.8096618354097,
177.194450000255));
#34585=CARTESIAN_POINT('Ctrl Pts',(-58.714083785481,-82.8275901558622,176.812955208202));
#34586=CARTESIAN_POINT('Ctrl Pts',(-58.8327209080309,-82.8751512680903,
176.033835190665));
#34587=CARTESIAN_POINT('Ctrl Pts',(-58.8172227638605,-82.9075908303593,
175.644596944486));
#34588=CARTESIAN_POINT('Ctrl Pts',(-58.6371924350539,-82.9914171440261,
174.880010087987));
#34589=CARTESIAN_POINT('Ctrl Pts',(-58.4687265318774,-83.0421607578069,
174.513542586584));
#34590=CARTESIAN_POINT('Ctrl Pts',(-58.0070747818638,-83.1515959942863,
173.882510394372));
#34591=CARTESIAN_POINT('Ctrl Pts',(-57.723561004971,-83.2125891039599,173.620437149146));
#34592=CARTESIAN_POINT('Ctrl Pts',(-57.0609567057928,-83.3478560739444,
173.212251191466));
#34593=CARTESIAN_POINT('Ctrl Pts',(-56.6852885925139,-83.4206903615588,
173.075134902459));
#34594=CARTESIAN_POINT('Ctrl Pts',(-55.9171386449002,-83.5628126136344,
172.961214764093));
#34595=CARTESIAN_POINT('Ctrl Pts',(-55.5333504855745,-83.6344756760652,
172.979553669503));
#34596=CARTESIAN_POINT('Ctrl Pts',(-54.7797281985092,-83.7794404514502,
173.166416362847));
#34597=CARTESIAN_POINT('Ctrl Pts',(-54.4185993701294,-83.8507263819771,
173.338791269425));
#34598=CARTESIAN_POINT('Ctrl Pts',(-54.0844894249589,-83.9187214986427,
173.591226869333));
#34599=CARTESIAN_POINT('Ctrl Pts',(-54.0674184433917,-83.9222021537111,
173.604421462315));
#34600=CARTESIAN_POINT('Ctrl Pts',(-54.050498381191,-83.9256585959369,173.617797875548));
#34601=CARTESIAN_POINT('Ctrl Pts',(-54.1035013834151,-84.4228413407654,
173.617797875548));
#34602=CARTESIAN_POINT('Ctrl Pts',(-54.1128212346228,-84.4209374749952,
173.610429925032));
#34603=CARTESIAN_POINT('Ctrl Pts',(-54.1221869743567,-84.4190262427001,
173.603117059851));
#34604=CARTESIAN_POINT('Ctrl Pts',(-54.4464616129933,-84.3529216380611,
173.353057288645));
#34605=CARTESIAN_POINT('Ctrl Pts',(-54.8062878786021,-84.281798245904,173.17699975264));
#34606=CARTESIAN_POINT('Ctrl Pts',(-55.5587882099357,-84.1368815088752,
172.982779952793));
#34607=CARTESIAN_POINT('Ctrl Pts',(-55.9426584723413,-84.0649294238171,
172.960827811178));
#34608=CARTESIAN_POINT('Ctrl Pts',(-56.7124460848245,-83.9228013436527,
173.067723300916));
#34609=CARTESIAN_POINT('Ctrl Pts',(-57.0896681643246,-83.8498235631671,
173.201547934183));
#34610=CARTESIAN_POINT('Ctrl Pts',(-57.7563502935406,-83.7140552807198,
173.604147370507));
#34611=CARTESIAN_POINT('Ctrl Pts',(-58.0422771302896,-83.6525432291579,
173.863914118319));
#34612=CARTESIAN_POINT('Ctrl Pts',(-58.509613547136,-83.5426592870856,174.491390807906));
#34613=CARTESIAN_POINT('Ctrl Pts',(-58.6812596282787,-83.4915973946548,
174.856716738244));
#34614=CARTESIAN_POINT('Ctrl Pts',(-58.8676337722894,-83.4070328370076,
175.620328538552));
#34615=CARTESIAN_POINT('Ctrl Pts',(-58.8862246860382,-83.3740192878531,
176.009664281697));
#34616=CARTESIAN_POINT('Ctrl Pts',(-58.7736654764938,-83.3259568564042,
176.790195955194));
#34617=CARTESIAN_POINT('Ctrl Pts',(-58.6371718724744,-83.3077448183863,
177.173043038668));
#34618=CARTESIAN_POINT('Ctrl Pts',(-58.2300731230129,-83.2864481429317,
177.850399109429));
#34619=CARTESIAN_POINT('Ctrl Pts',(-57.9685202237763,-83.283298593099,178.141258356762));
#34620=CARTESIAN_POINT('Ctrl Pts',(-57.3382810288697,-83.2904250159173,
178.61766279528));
#34621=CARTESIAN_POINT('Ctrl Pts',(-56.9715706818997,-83.2967557187476,
178.793784240335));
#34622=CARTESIAN_POINT('Ctrl Pts',(-56.2054510184505,-83.3137327987006,
178.988131909377));
#34623=CARTESIAN_POINT('Ctrl Pts',(-55.8150368404808,-83.3243196033431,
179.010146813958));
#34624=CARTESIAN_POINT('Ctrl Pts',(-55.0325592640291,-83.3476763143398,
178.903373289319));
#34625=CARTESIAN_POINT('Ctrl Pts',(-54.6484034664701,-83.3558669099257,
178.769605887138));
#34626=CARTESIAN_POINT('Ctrl Pts',(-53.9680115988919,-83.36370458063,178.367103543302));
#34627=CARTESIAN_POINT('Ctrl Pts',(-53.6755002168483,-83.3638532525733,
178.107376781389));
#34628=CARTESIAN_POINT('Ctrl Pts',(-53.1954037669401,-83.3549747287394,
177.479961893673));
#34629=CARTESIAN_POINT('Ctrl Pts',(-53.0167956993358,-83.3412526478882,
177.114655963443));
#34630=CARTESIAN_POINT('Ctrl Pts',(-52.8166724744574,-83.2978902369778,
176.351061271843));
#34631=CARTESIAN_POINT('Ctrl Pts',(-52.7914851224319,-83.2695394135183,
175.961723837377));
#34632=CARTESIAN_POINT('Ctrl Pts',(-52.8912776032413,-83.1988414259702,
175.181167967157));
#34633=CARTESIAN_POINT('Ctrl Pts',(-53.0208149813474,-83.1522690608241,
174.798297693757));
#34634=CARTESIAN_POINT('Ctrl Pts',(-53.4083421346692,-83.0472209258735,
174.130952367036));
#34635=CARTESIAN_POINT('Ctrl Pts',(-53.6537248706633,-82.9906912972542,
173.847668562182));
#34636=CARTESIAN_POINT('Ctrl Pts',(-53.9444923767429,-82.9312931062798,
173.617797875548));
#34637=CARTESIAN_POINT('Origin',(-54.1598171290174,-67.5719248685924,175.985485069079));
#34638=CARTESIAN_POINT('',(-53.7324803678465,-80.9425621269657,173.617797875548));
#34639=CARTESIAN_POINT('',(-53.7854833700705,-81.4397448717942,173.617797875548));
#34640=CARTESIAN_POINT('',(-52.327900808713,-67.7672193871761,173.617797875548));
#34641=CARTESIAN_POINT('Ctrl Pts',(-53.7324803678465,-80.9425621269657,
173.617797875548));
#34642=CARTESIAN_POINT('Ctrl Pts',(-53.4441088643015,-81.0014708608545,
173.845774365835));
#34643=CARTESIAN_POINT('Ctrl Pts',(-53.2003477048595,-81.0575640078217,
174.126308725592));
#34644=CARTESIAN_POINT('Ctrl Pts',(-52.8123969930906,-81.1623918656509,
174.789710194828));
#34645=CARTESIAN_POINT('Ctrl Pts',(-52.6817202418458,-81.2090937257845,
175.172041179413));
#34646=CARTESIAN_POINT('Ctrl Pts',(-52.5795030176814,-81.2801092351177,
175.952034250505));
#34647=CARTESIAN_POINT('Ctrl Pts',(-52.6034290990334,-81.3084950668171,
176.34133252214));
#34648=CARTESIAN_POINT('Ctrl Pts',(-52.8010019068039,-81.3521047705371,
177.105321657696));
#34649=CARTESIAN_POINT('Ctrl Pts',(-52.978336875166,-81.3659711860284,177.471088959042));
#34650=CARTESIAN_POINT('Ctrl Pts',(-53.4561673771093,-81.375154693423,178.099933745925));
#34651=CARTESIAN_POINT('Ctrl Pts',(-53.7476874832628,-81.3750049200971,
178.36058656955));
#34652=CARTESIAN_POINT('Ctrl Pts',(-54.4264384758535,-81.367315727599,178.765335428131));
#34653=CARTESIAN_POINT('Ctrl Pts',(-54.8099755898715,-81.3592003256552,
178.900426843859));
#34654=CARTESIAN_POINT('Ctrl Pts',(-55.5918136536326,-81.335979920787,179.010023446643));
#34655=CARTESIAN_POINT('Ctrl Pts',(-55.9821707892603,-81.3252845681812,
178.989461036256));
#34656=CARTESIAN_POINT('Ctrl Pts',(-56.7487398844479,-81.3082311356992,
178.798071949872));
#34657=CARTESIAN_POINT('Ctrl Pts',(-57.1159805326535,-81.301853804198,178.623430055959));
#34658=CARTESIAN_POINT('Ctrl Pts',(-57.7478687290417,-81.2946247716651,
178.149664851699));
#34659=CARTESIAN_POINT('Ctrl Pts',(-58.0104718390867,-81.2975393219991,
177.859943506638));
#34660=CARTESIAN_POINT('Ctrl Pts',(-58.4201460168419,-81.3185308603792,
177.184489728788));
#34661=CARTESIAN_POINT('Ctrl Pts',(-58.5581604568431,-81.3365913849285,
176.802362616119));
#34662=CARTESIAN_POINT('Ctrl Pts',(-58.6739686579132,-81.3843860597891,
176.02258235797));
#34663=CARTESIAN_POINT('Ctrl Pts',(-58.6570311332583,-81.4170912985052,
175.633298799305));
#34664=CARTESIAN_POINT('Ctrl Pts',(-58.4740495100569,-81.5012613123642,
174.869162393817));
#34665=CARTESIAN_POINT('Ctrl Pts',(-58.3041031171488,-81.5521533857258,
174.503222692046));
#34666=CARTESIAN_POINT('Ctrl Pts',(-57.8398053009967,-81.661797816338,173.873841296063));
#34667=CARTESIAN_POINT('Ctrl Pts',(-57.555169507049,-81.723030541439,173.612840443946));
#34668=CARTESIAN_POINT('Ctrl Pts',(-56.8906673356877,-81.8585310762853,
173.207248459729));
#34669=CARTESIAN_POINT('Ctrl Pts',(-56.5142735001098,-81.9314327519905,
173.071660243962));
#34670=CARTESIAN_POINT('Ctrl Pts',(-55.7453585609871,-82.073558459601,172.961003554594));
#34671=CARTESIAN_POINT('Ctrl Pts',(-55.3615321434295,-82.1453538554173,
172.981020677109));
#34672=CARTESIAN_POINT('Ctrl Pts',(-54.6084266529547,-82.2902971011637,
173.171299416638));
#34673=CARTESIAN_POINT('Ctrl Pts',(-54.2478983250722,-82.3615083960981,
173.345385584072));
#34674=CARTESIAN_POINT('Ctrl Pts',(-53.9183659285772,-82.428624144687,173.596738821088));
#34675=CARTESIAN_POINT('Ctrl Pts',(-53.9048803387418,-82.4313748458465,
173.607211444546));
#34676=CARTESIAN_POINT('Ctrl Pts',(-53.8914893745187,-82.4341103614513,
173.617797875548));
#34677=CARTESIAN_POINT('Ctrl Pts',(-53.9444923767429,-82.9312931062798,
173.617797875548));
#34678=CARTESIAN_POINT('Ctrl Pts',(-53.9535813647071,-82.9294364014157,
173.61061243749));
#34679=CARTESIAN_POINT('Ctrl Pts',(-53.962713998754,-82.9275726898846,173.603479387289));
#34680=CARTESIAN_POINT('Ctrl Pts',(-54.2866912226434,-82.8615253180011,
173.353494400607));
#34681=CARTESIAN_POINT('Ctrl Pts',(-54.6464773768003,-82.7904069684609,
173.177325161358));
#34682=CARTESIAN_POINT('Ctrl Pts',(-55.3989431018931,-82.6454917884509,
172.982881861345));
#34683=CARTESIAN_POINT('Ctrl Pts',(-55.7828158409426,-82.5735306890303,
172.960820018304));
#34684=CARTESIAN_POINT('Ctrl Pts',(-56.5526526269826,-82.431402525919,173.067502330347));
#34685=CARTESIAN_POINT('Ctrl Pts',(-56.929921387865,-82.3584204819804,173.201226930041));
#34686=CARTESIAN_POINT('Ctrl Pts',(-57.5967268363666,-82.2226370702945,
173.603656660308));
#34687=CARTESIAN_POINT('Ctrl Pts',(-57.8827267800039,-82.1611090861183,
173.863353519765));
#34688=CARTESIAN_POINT('Ctrl Pts',(-58.3502350657911,-82.05121161974,174.490722186914));
#34689=CARTESIAN_POINT('Ctrl Pts',(-58.5219772698673,-82.0001401433687,
174.856013155927));
#34690=CARTESIAN_POINT('Ctrl Pts',(-58.7085434103299,-81.9155532742003,
175.619595048659));
#34691=CARTESIAN_POINT('Ctrl Pts',(-58.7272278590927,-81.8825221835531,
176.008933747952));
#34692=CARTESIAN_POINT('Ctrl Pts',(-58.6148524315187,-81.8344446217895,
176.789507706957));
#34693=CARTESIAN_POINT('Ctrl Pts',(-58.4784449131681,-81.8162240236186,
177.172395316719));
#34694=CARTESIAN_POINT('Ctrl Pts',(-58.071491915452,-81.7949100960382,177.849858811396));
#34695=CARTESIAN_POINT('Ctrl Pts',(-57.8099983698264,-81.7917471779939,
178.140782382714));
#34696=CARTESIAN_POINT('Ctrl Pts',(-57.1798525023496,-81.7988678010176,
178.617335843328));
#34697=CARTESIAN_POINT('Ctrl Pts',(-56.8131722829807,-81.8051958661488,
178.793540818343));
#34698=CARTESIAN_POINT('Ctrl Pts',(-56.0470781729116,-81.8221686282478,
178.988055624169));
#34699=CARTESIAN_POINT('Ctrl Pts',(-55.6566607627439,-81.832749229207,179.010152563904));
#34700=CARTESIAN_POINT('Ctrl Pts',(-54.8741472383782,-81.8561136313191,
178.903538452364));
#34701=CARTESIAN_POINT('Ctrl Pts',(-54.4899566546963,-81.8643084693757,
178.769845857466));
#34702=CARTESIAN_POINT('Ctrl Pts',(-53.8094722657113,-81.8721545216685,
178.367470422246));
#34703=CARTESIAN_POINT('Ctrl Pts',(-53.516904933227,-81.8723030682003,178.107795920391));
#34704=CARTESIAN_POINT('Ctrl Pts',(-53.0366807297978,-81.8634417521832,
177.480461813644));
#34705=CARTESIAN_POINT('Ctrl Pts',(-52.8580008943164,-81.8497278190171,
177.115182033494));
#34706=CARTESIAN_POINT('Ctrl Pts',(-52.6577338152889,-81.80637936614,176.351609712819));
#34707=CARTESIAN_POINT('Ctrl Pts',(-52.6324753305221,-81.7780304620221,
175.962270067826));
#34708=CARTESIAN_POINT('Ctrl Pts',(-52.7304634711916,-81.7085331365265,
175.194744828215));
#34709=CARTESIAN_POINT('Ctrl Pts',(-52.853204470837,-81.6638200595933,174.823815050375));
#34710=CARTESIAN_POINT('Ctrl Pts',(-53.2319768749049,-81.5596848723498,
174.151181362769));
#34711=CARTESIAN_POINT('Ctrl Pts',(-53.4843155844065,-81.5012676392086,
173.85589066183));
#34712=CARTESIAN_POINT('Ctrl Pts',(-53.7854833700705,-81.4397448717942,
173.617797875548));
#34713=CARTESIAN_POINT('Origin',(-54.1598171290174,-67.5719248685924,175.985485069079));
#34714=CARTESIAN_POINT('',(-53.5734713611743,-79.4510138924801,173.617797875548));
#34715=CARTESIAN_POINT('',(-53.626474363399,-79.9481966373084,173.617797875547));
#34716=CARTESIAN_POINT('',(-52.327900808713,-67.7672193871761,173.617797875548));
#34717=CARTESIAN_POINT('Ctrl Pts',(-53.5734713611743,-79.4510138924801,
173.617797875548));
#34718=CARTESIAN_POINT('Ctrl Pts',(-53.2839132390089,-79.5101650296565,
173.846712465284));
#34719=CARTESIAN_POINT('Ctrl Pts',(-53.0393481398622,-79.5664744087806,
174.128607631233));
#34720=CARTESIAN_POINT('Ctrl Pts',(-52.6516046998443,-79.6714116962577,
174.793961864577));
#34721=CARTESIAN_POINT('Ctrl Pts',(-52.5214919950192,-79.7180494879704,
175.176560354536));
#34722=CARTESIAN_POINT('Ctrl Pts',(-52.4204754219013,-79.7889078080589,
175.956832618298));
#34723=CARTESIAN_POINT('Ctrl Pts',(-52.4450259653416,-79.8172760758686,
176.346150271794));
#34724=CARTESIAN_POINT('Ctrl Pts',(-52.6438614285247,-79.860763390992,177.109944641201));
#34725=CARTESIAN_POINT('Ctrl Pts',(-52.8218268486073,-79.874558377363,177.475484060112));
#34726=CARTESIAN_POINT('Ctrl Pts',(-53.3007794039409,-79.8835909170627,
178.103621475286));
#34727=CARTESIAN_POINT('Ctrl Pts',(-53.5927901083991,-79.8834414234718,
178.36381593597));
#34728=CARTESIAN_POINT('Ctrl Pts',(-54.2723535909397,-79.8756787511857,
178.767453415344));
#34729=CARTESIAN_POINT('Ctrl Pts',(-54.6561974632848,-79.8675261277388,
178.901889875769));
#34730=CARTESIAN_POINT('Ctrl Pts',(-55.4383526524422,-79.8442382527869,
179.010089588121));
#34731=CARTESIAN_POINT('Ctrl Pts',(-55.8287379663228,-79.8335962998503,
178.988808533618));
#34732=CARTESIAN_POINT('Ctrl Pts',(-56.5950854101889,-79.8165806206824,
178.795955809325));
#34733=CARTESIAN_POINT('Ctrl Pts',(-56.9620644246878,-79.8102263419449,
178.620581746196));
#34734=CARTESIAN_POINT('Ctrl Pts',(-57.5931375642539,-79.8030480581929,
178.145510578597));
#34735=CARTESIAN_POINT('Ctrl Pts',(-57.8552212288729,-79.8060784772914,
177.855226475813));
#34736=CARTESIAN_POINT('Ctrl Pts',(-58.2636224073494,-79.8272209100588,
177.178831445985));
#34737=CARTESIAN_POINT('Ctrl Pts',(-58.4008851895586,-79.8453563861565,
176.796347544831));
#34738=CARTESIAN_POINT('Ctrl Pts',(-58.5150870864485,-79.8932835052345,
176.016194870104));
#34739=CARTESIAN_POINT('Ctrl Pts',(-58.4973321640642,-79.9261407476775,
175.626885529689));
#34740=CARTESIAN_POINT('Ctrl Pts',(-58.3126736753222,-80.0105058501583,
174.863007516469));
#34741=CARTESIAN_POINT('Ctrl Pts',(-58.1418868667774,-80.0614819741624,
174.497370248303));
#34742=CARTESIAN_POINT('Ctrl Pts',(-57.6760867130961,-80.171244919223,173.868929365769));
#34743=CARTESIAN_POINT('Ctrl Pts',(-57.3908129515967,-80.2326151907151,
173.608538322025));
#34744=CARTESIAN_POINT('Ctrl Pts',(-56.7252330417196,-80.3682481674656,
173.204424060083));
#34745=CARTESIAN_POINT('Ctrl Pts',(-56.3484290168544,-80.4411876425926,
173.069706610886));
#34746=CARTESIAN_POINT('Ctrl Pts',(-55.5790818340909,-80.5833147372578,
172.960907698141));
#34747=CARTESIAN_POINT('Ctrl Pts',(-55.195233725635,-80.6551869693247,172.981880472418));
#34748=CARTESIAN_POINT('Ctrl Pts',(-54.4424258627393,-80.8001173490269,
173.174105292471));
#34749=CARTESIAN_POINT('Ctrl Pts',(-54.0822429708766,-80.8712854782209,
173.349165306176));
#34750=CARTESIAN_POINT('Ctrl Pts',(-53.7553099800293,-80.9379014713065,
173.599885811165));
#34751=CARTESIAN_POINT('Ctrl Pts',(-53.7438609810889,-80.9402372872754,
173.608800758175));
#34752=CARTESIAN_POINT('Ctrl Pts',(-53.7324803678465,-80.9425621269657,
173.617797875548));
#34753=CARTESIAN_POINT('Ctrl Pts',(-53.7854833700706,-81.4397448717942,
173.617797875548));
#34754=CARTESIAN_POINT('Ctrl Pts',(-53.9889618015743,-81.3981781544653,
173.456934898128));
#34755=CARTESIAN_POINT('Ctrl Pts',(-54.2123585900196,-81.3534994634441,
173.323874911151));
#34756=CARTESIAN_POINT('Ctrl Pts',(-54.6917335852962,-81.2593823460045,
173.118281881145));
#34757=CARTESIAN_POINT('Ctrl Pts',(-54.9461396249263,-81.2102817144208,
173.047748606547));
#34758=CARTESIAN_POINT('Ctrl Pts',(-55.5874558779449,-81.0884917717835,
172.960269003438));
#34759=CARTESIAN_POINT('Ctrl Pts',(-55.9750991573887,-81.0181626840939,
172.98415968872));
#34760=CARTESIAN_POINT('Ctrl Pts',(-56.7208832908939,-80.8766330037567,
173.181471212417));
#34761=CARTESIAN_POINT('Ctrl Pts',(-57.0716022776453,-80.8068275275108,
173.353704705639));
#34762=CARTESIAN_POINT('Ctrl Pts',(-57.6860825729975,-80.6776159103853,
173.824415648272));
#34763=CARTESIAN_POINT('Ctrl Pts',(-57.9444428979215,-80.62098075888,174.117898114428));
#34764=CARTESIAN_POINT('Ctrl Pts',(-58.3350117146376,-80.5174025421943,
174.790286529534));
#34765=CARTESIAN_POINT('Ctrl Pts',(-58.4629707254976,-80.4713762772148,
175.162936279234));
#34766=CARTESIAN_POINT('Ctrl Pts',(-58.5690745277377,-80.3963014210774,
175.93701510357));
#34767=CARTESIAN_POINT('Ctrl Pts',(-58.546706106472,-80.3695014870016,176.330943217721));
#34768=CARTESIAN_POINT('Ctrl Pts',(-58.3523161121012,-80.3283656642969,
177.089978636783));
#34769=CARTESIAN_POINT('Ctrl Pts',(-58.1818671708559,-80.3141833564527,
177.447651021712));
#34770=CARTESIAN_POINT('Ctrl Pts',(-57.7141277145983,-80.3002271684866,
178.078024798891));
#34771=CARTESIAN_POINT('Ctrl Pts',(-57.4215969455131,-80.3021327782118,
178.34472730544));
#34772=CARTESIAN_POINT('Ctrl Pts',(-56.7505584155294,-80.311891303891,178.751512130253));
#34773=CARTESIAN_POINT('Ctrl Pts',(-56.3784811663972,-80.3192356354569,
178.887589492959));
#34774=CARTESIAN_POINT('Ctrl Pts',(-55.6030346372377,-80.3380289180745,
179.009816582222));
#34775=CARTESIAN_POINT('Ctrl Pts',(-55.2072753458979,-80.3508412085372,
178.994676671652));
#34776=CARTESIAN_POINT('Ctrl Pts',(-54.4437534306365,-80.370537894246,178.81366465606));
#34777=CARTESIAN_POINT('Ctrl Pts',(-54.0833029169573,-80.376674369447,178.649699500036));
#34778=CARTESIAN_POINT('Ctrl Pts',(-53.4444712725212,-80.380852101205,178.192798229079));
#34779=CARTESIAN_POINT('Ctrl Pts',(-53.1725998370387,-80.3803569578552,
177.903982650869));
#34780=CARTESIAN_POINT('Ctrl Pts',(-52.7546772649625,-80.3632874874759,
177.239578072511));
#34781=CARTESIAN_POINT('Ctrl Pts',(-52.6122887632239,-80.3462085271098,
176.870632974855));
#34782=CARTESIAN_POINT('Ctrl Pts',(-52.4758197014113,-80.2967821838551,
176.098561826864));
#34783=CARTESIAN_POINT('Ctrl Pts',(-52.4837668759432,-80.2663549462667,
175.702774135099));
#34784=CARTESIAN_POINT('Ctrl Pts',(-52.6498828822117,-80.187098197252,174.939374482983));
#34785=CARTESIAN_POINT('Ctrl Pts',(-52.8057763387706,-80.1382515106677,
174.579036605884));
#34786=CARTESIAN_POINT('Ctrl Pts',(-53.1935668659987,-80.0406506942216,
174.016094875201));
#34787=CARTESIAN_POINT('Ctrl Pts',(-53.3960518932188,-79.995267501839,173.799961873686));
#34788=CARTESIAN_POINT('Ctrl Pts',(-53.6264743633996,-79.9481966373083,
173.617797875547));
#34789=CARTESIAN_POINT('Origin',(-54.1598171290174,-67.5719248685924,175.985485069079));
#34790=CARTESIAN_POINT('',(-53.4144623545021,-77.9594656579945,173.617797875548));
#34791=CARTESIAN_POINT('',(-53.4674653567265,-78.4566484028229,173.617797875548));
#34792=CARTESIAN_POINT('',(-52.327900808713,-67.7672193871761,173.617797875548));
#34793=CARTESIAN_POINT('Ctrl Pts',(-53.4144623545021,-77.9594656579945,
173.617797875548));
#34794=CARTESIAN_POINT('Ctrl Pts',(-53.1242371104778,-78.0187530752943,
173.847239868644));
#34795=CARTESIAN_POINT('Ctrl Pts',(-52.8792207699447,-78.075183965081,174.129900821861));
#34796=CARTESIAN_POINT('Ctrl Pts',(-52.4915960091567,-78.1801824835191,
174.796353277051));
#34797=CARTESIAN_POINT('Ctrl Pts',(-52.3618006095129,-78.2267842006455,
175.179101795173));
#34798=CARTESIAN_POINT('Ctrl Pts',(-52.2614592207656,-78.2975540938532,
175.959530619911));
#34799=CARTESIAN_POINT('Ctrl Pts',(-52.286360995377,-78.3259126820135,176.348859181655));
#34800=CARTESIAN_POINT('Ctrl Pts',(-52.4859067048768,-78.3693311182812,
177.112543551467));
#34801=CARTESIAN_POINT('Ctrl Pts',(-52.6642266105073,-78.3830859016589,
177.47795432728));
#34802=CARTESIAN_POINT('Ctrl Pts',(-53.1438101229382,-78.3920335019309,
178.1056933791));
#34803=CARTESIAN_POINT('Ctrl Pts',(-53.4360969282526,-78.3918843945314,
178.365629915207));
#34804=CARTESIAN_POINT('Ctrl Pts',(-54.1161173271656,-78.384080365151,178.76864153432));
#34805=CARTESIAN_POINT('Ctrl Pts',(-54.5001333540368,-78.3759068000259,
178.902709120172));
#34806=CARTESIAN_POINT('Ctrl Pts',(-55.282466481728,-78.352580962601,179.010122429603));
#34807=CARTESIAN_POINT('Ctrl Pts',(-55.6728676995625,-78.341969340023,178.988436745572));
#34808=CARTESIAN_POINT('Ctrl Pts',(-56.43908973001,-78.3249749377774,178.794759781836));
#34809=CARTESIAN_POINT('Ctrl Pts',(-56.8059207939449,-78.3186336538946,
178.618973592585));
#34810=CARTESIAN_POINT('Ctrl Pts',(-57.4365343189338,-78.3114839603943,
178.143167246289));
#34811=CARTESIAN_POINT('Ctrl Pts',(-57.6983253719169,-78.3145799643806,
177.852566080781));
#34812=CARTESIAN_POINT('Ctrl Pts',(-58.1060087301422,-78.3358074239231,
177.175641136799));
#34813=CARTESIAN_POINT('Ctrl Pts',(-58.2428476053164,-78.3539851116537,
176.792956839626));
#34814=CARTESIAN_POINT('Ctrl Pts',(-58.3561440580827,-78.4019868309526,
176.012595030349));
#34815=CARTESIAN_POINT('Ctrl Pts',(-58.3379283501955,-78.4349301216162,
175.623271141334));
#34816=CARTESIAN_POINT('Ctrl Pts',(-58.1523242988494,-78.5194051697063,
174.859539617395));
#34817=CARTESIAN_POINT('Ctrl Pts',(-57.9810638392148,-78.5704285923116,
174.494073700727));
#34818=CARTESIAN_POINT('Ctrl Pts',(-57.5144168893062,-78.6802582557992,
173.866163980835));
#34819=CARTESIAN_POINT('Ctrl Pts',(-57.2287832373442,-78.741706536025,173.606116962053));
#34820=CARTESIAN_POINT('Ctrl Pts',(-56.5625957961499,-78.8774141099415,
173.202837211976));
#34821=CARTESIAN_POINT('Ctrl Pts',(-56.1855611619529,-78.9503747427818,
173.068611589101));
#34822=CARTESIAN_POINT('Ctrl Pts',(-55.4159710145938,-79.0925024349185,
172.960861390174));
#34823=CARTESIAN_POINT('Ctrl Pts',(-55.0321106912169,-79.1644185217348,
172.982373728683));
#34824=CARTESIAN_POINT('Ctrl Pts',(-54.2794719416634,-79.3093414425798,
173.175697571081));
#34825=CARTESIAN_POINT('Ctrl Pts',(-53.9194851988895,-79.3804849873277,
173.35130721382));
#34826=CARTESIAN_POINT('Ctrl Pts',(-53.5940174791467,-79.4468191431629,
173.601665238008));
#34827=CARTESIAN_POINT('Ctrl Pts',(-53.5837166999884,-79.4489209674498,
173.609698266689));
#34828=CARTESIAN_POINT('Ctrl Pts',(-53.5734713611743,-79.4510138924801,
173.617797875548));
#34829=CARTESIAN_POINT('Ctrl Pts',(-53.6264743633996,-79.9481966373083,
173.617797875547));
#34830=CARTESIAN_POINT('Ctrl Pts',(-53.6999737117029,-79.93318213866,173.559691844755));
#34831=CARTESIAN_POINT('Ctrl Pts',(-53.776270499172,-79.9177210304295,173.50505611858));
#34832=CARTESIAN_POINT('Ctrl Pts',(-54.1795502188484,-79.8366199055185,
173.244539735607));
#34833=CARTESIAN_POINT('Ctrl Pts',(-54.5413081342879,-79.7658574063917,
173.101336271712));
#34834=CARTESIAN_POINT('Ctrl Pts',(-55.3013069703931,-79.6207715002734,
172.963199457707));
#34835=CARTESIAN_POINT('Ctrl Pts',(-55.6925578511268,-79.5492764327622,
172.970579437118));
#34836=CARTESIAN_POINT('Ctrl Pts',(-56.4470856128977,-79.4074351507114,
173.137245239642));
#34837=CARTESIAN_POINT('Ctrl Pts',(-56.8031387705855,-79.3373110297835,
173.293926614045));
#34838=CARTESIAN_POINT('Ctrl Pts',(-57.4378982890236,-79.2055351033221,
173.738598285689));
#34839=CARTESIAN_POINT('Ctrl Pts',(-57.7099586638791,-79.1466440388984,
174.023299217339));
#34840=CARTESIAN_POINT('Ctrl Pts',(-58.1273347811811,-79.0408141444312,
174.680630840406));
#34841=CARTESIAN_POINT('Ctrl Pts',(-58.2694808619301,-78.9935235758121,
175.046227733694));
#34842=CARTESIAN_POINT('Ctrl Pts',(-58.4071426369151,-78.9147025687063,
175.816384421502));
#34843=CARTESIAN_POINT('Ctrl Pts',(-58.4000992516212,-78.8854639848545,
176.213783222893));
#34844=CARTESIAN_POINT('Ctrl Pts',(-58.2342698188388,-78.8418741891221,
176.980833984601));
#34845=CARTESIAN_POINT('Ctrl Pts',(-58.0783142710071,-78.8263922169384,
177.343338609313));
#34846=CARTESIAN_POINT('Ctrl Pts',(-57.634822831167,-78.8094892647114,177.992661649254));
#34847=CARTESIAN_POINT('Ctrl Pts',(-57.3503804359288,-78.809722498661,178.272316899594));
#34848=CARTESIAN_POINT('Ctrl Pts',(-56.693447818481,-78.8185517444044,178.70406324853));
#34849=CARTESIAN_POINT('Ctrl Pts',(-56.3280374921874,-78.8254273005829,
178.853306571911));
#34850=CARTESIAN_POINT('Ctrl Pts',(-55.5563426567283,-78.8434784329005,
179.005080249419));
#34851=CARTESIAN_POINT('Ctrl Pts',(-55.1572953278909,-78.8558300002763,
179.004377698217));
#34852=CARTESIAN_POINT('Ctrl Pts',(-54.3865591713871,-78.8768532596877,
178.849971682348));
#34853=CARTESIAN_POINT('Ctrl Pts',(-54.0218103706171,-78.8836857661521,
178.699515970368));
#34854=CARTESIAN_POINT('Ctrl Pts',(-53.3655931673347,-78.8893936985532,
178.265350298767));
#34855=CARTESIAN_POINT('Ctrl Pts',(-53.0816890567742,-78.8893726976383,
177.984174318144));
#34856=CARTESIAN_POINT('Ctrl Pts',(-52.6354814370726,-78.8751014359724,
177.324848622603));
#34857=CARTESIAN_POINT('Ctrl Pts',(-52.4789479421949,-78.8589289835916,
176.952204682775));
#34858=CARTESIAN_POINT('Ctrl Pts',(-52.3227023685931,-78.8113571019577,
176.182393342189));
#34859=CARTESIAN_POINT('Ctrl Pts',(-52.3192666697951,-78.7821382059785,
175.79371741212));
#34860=CARTESIAN_POINT('Ctrl Pts',(-52.4610116599005,-78.7059885439742,
175.023485227097));
#34861=CARTESIAN_POINT('Ctrl Pts',(-52.6100980541892,-78.6572377292065,
174.650472971694));
#34862=CARTESIAN_POINT('Ctrl Pts',(-53.0021555360266,-78.5564000261094,
174.051172062114));
#34863=CARTESIAN_POINT('Ctrl Pts',(-53.2183638889226,-78.5075350261465,
173.814728840144));
#34864=CARTESIAN_POINT('Ctrl Pts',(-53.4674653567269,-78.4566484028228,
173.617797875547));
#34865=CARTESIAN_POINT('Origin',(-54.1598171290174,-67.5719248685924,175.985485069079));
#34866=CARTESIAN_POINT('',(-53.2554533478299,-76.4679174235089,173.617797875548));
#34867=CARTESIAN_POINT('',(-53.308456350054,-76.9651001683374,173.617797875548));
#34868=CARTESIAN_POINT('',(-52.327900808713,-67.7672193871761,173.617797875548));
#34869=CARTESIAN_POINT('Ctrl Pts',(-53.2554533478299,-76.4679174235089,
173.617797875548));
#34870=CARTESIAN_POINT('Ctrl Pts',(-52.964854160848,-76.5272812301394,173.847535494952));
#34871=CARTESIAN_POINT('Ctrl Pts',(-52.7195851171509,-76.5837802128976,
174.130625928072));
#34872=CARTESIAN_POINT('Ctrl Pts',(-52.3320275568318,-76.6888129616136,
174.79769408723));
#34873=CARTESIAN_POINT('Ctrl Pts',(-52.2024100784284,-76.7353944404665,
175.180526586134));
#34874=CARTESIAN_POINT('Ctrl Pts',(-52.1024472067462,-76.8061147504361,
175.961043041675));
#34875=CARTESIAN_POINT('Ctrl Pts',(-52.1275459070151,-76.8344679741608,
176.350377721454));
#34876=CARTESIAN_POINT('Ctrl Pts',(-52.3274898508707,-76.8778477790918,
177.114000274915));
#34877=CARTESIAN_POINT('Ctrl Pts',(-52.5060084703274,-76.8915800131688,
177.479338776243));
#34878=CARTESIAN_POINT('Ctrl Pts',(-52.9859456966574,-76.9004799817596,
178.106854319571));
#34879=CARTESIAN_POINT('Ctrl Pts',(-53.27838735513,-76.9003311629783,178.366646207626));
#34880=CARTESIAN_POINT('Ctrl Pts',(-53.9586639114936,-76.8925039369739,
178.769306684473));
#34881=CARTESIAN_POINT('Ctrl Pts',(-54.342776339663,-76.8843186284663,178.90316729765));
#34882=CARTESIAN_POINT('Ctrl Pts',(-55.1252090968815,-76.8609715022402,
179.010139467056));
#34883=CARTESIAN_POINT('Ctrl Pts',(-55.5156192488589,-76.8503769782809,
178.988226784107));
#34884=CARTESIAN_POINT('Ctrl Pts',(-56.2817707281885,-76.8333945188046,
178.794087373533));
#34885=CARTESIAN_POINT('Ctrl Pts',(-56.6485185898549,-76.8270605298348,
178.618070017813));
#34886=CARTESIAN_POINT('Ctrl Pts',(-57.278874048408,-76.8199268807342,178.141851277279));
#34887=CARTESIAN_POINT('Ctrl Pts',(-57.5405009006074,-76.8230597871527,
177.85107217373));
#34888=CARTESIAN_POINT('Ctrl Pts',(-57.9477812230071,-76.8443349679731,
177.173849963172));
#34889=CARTESIAN_POINT('Ctrl Pts',(-58.0843820674067,-76.8625363398498,
176.791053398886));
#34890=CARTESIAN_POINT('Ctrl Pts',(-58.1971702400539,-76.9105799190036,
176.010574439175));
#34891=CARTESIAN_POINT('Ctrl Pts',(-58.1786958545423,-76.9435716294713,
175.621242378299));
#34892=CARTESIAN_POINT('Ctrl Pts',(-57.9925608932288,-77.028108389584,174.857593352838));
#34893=CARTESIAN_POINT('Ctrl Pts',(-57.8210345692386,-77.0791583386423,
174.492223902628));
#34894=CARTESIAN_POINT('Ctrl Pts',(-57.353912275556,-77.189025428004,173.864612676414));
#34895=CARTESIAN_POINT('Ctrl Pts',(-57.0680765066293,-77.2505176499002,
173.604758870934));
#34896=CARTESIAN_POINT('Ctrl Pts',(-56.4015480124462,-77.3862670812936,
173.201948072434));
#34897=CARTESIAN_POINT('Ctrl Pts',(-56.0243841159366,-77.4592395439619,
173.067998854454));
#34898=CARTESIAN_POINT('Ctrl Pts',(-55.2546577944142,-77.6013675130901,
172.960837842604));
#34899=CARTESIAN_POINT('Ctrl Pts',(-54.8707906180679,-77.6733083903765,
172.982653350642));
#34900=CARTESIAN_POINT('Ctrl Pts',(-54.1182472292829,-77.8182270585414,
173.176594790565));
#34901=CARTESIAN_POINT('Ctrl Pts',(-53.7583710511103,-77.8893567224248,
173.352513190678));
#34902=CARTESIAN_POINT('Ctrl Pts',(-53.4337258810389,-77.9555326246257,
173.602665888411));
#34903=CARTESIAN_POINT('Ctrl Pts',(-53.4240697378998,-77.957503054946,173.610202612074));
#34904=CARTESIAN_POINT('Ctrl Pts',(-53.4144623545021,-77.9594656579945,
173.617797875548));
#34905=CARTESIAN_POINT('Ctrl Pts',(-53.4674653567269,-78.4566484028228,
173.617797875547));
#34906=CARTESIAN_POINT('Ctrl Pts',(-53.5168179472732,-78.4465666208594,
173.578781432379));
#34907=CARTESIAN_POINT('Ctrl Pts',(-53.5674413657633,-78.4362815284313,
173.541322215379));
#34908=CARTESIAN_POINT('Ctrl Pts',(-53.9444328009459,-78.3600907305088,
173.280660874177));
#34909=CARTESIAN_POINT('Ctrl Pts',(-54.3107257198566,-78.2881872354447,
173.12410691606));
#34910=CARTESIAN_POINT('Ctrl Pts',(-55.0687611470599,-78.1430871762328,
172.968625444015));
#34911=CARTESIAN_POINT('Ctrl Pts',(-55.4521889847661,-78.0724852575809,
172.965753553128));
#34912=CARTESIAN_POINT('Ctrl Pts',(-56.2129318446134,-77.9304568434933,
173.109795658303));
#34913=CARTESIAN_POINT('Ctrl Pts',(-56.5815908099749,-77.8583042744884,
173.260915312004));
#34914=CARTESIAN_POINT('Ctrl Pts',(-57.2263953545785,-77.7252481987439,
173.692932254402));
#34915=CARTESIAN_POINT('Ctrl Pts',(-57.4994685573361,-77.6663430468716,
173.964981012495));
#34916=CARTESIAN_POINT('Ctrl Pts',(-57.9362689244949,-77.5589005834618,
174.611163636346));
#34917=CARTESIAN_POINT('Ctrl Pts',(-58.0908197218222,-77.5095766684115,
174.982285367976));
#34918=CARTESIAN_POINT('Ctrl Pts',(-58.2432661406676,-77.4289837410822,
175.75081726355));
#34919=CARTESIAN_POINT('Ctrl Pts',(-58.2452594066001,-77.3989117255198,
176.13963758963));
#34920=CARTESIAN_POINT('Ctrl Pts',(-58.1000707945399,-77.3535622345091,
176.912286950257));
#34921=CARTESIAN_POINT('Ctrl Pts',(-57.9483988300908,-77.3368870941246,
177.287600354543));
#34922=CARTESIAN_POINT('Ctrl Pts',(-57.515542273888,-77.318667441005,177.945575933969));
#34923=CARTESIAN_POINT('Ctrl Pts',(-57.2433564915632,-77.3177610601279,
178.224939813528));
#34924=CARTESIAN_POINT('Ctrl Pts',(-56.5966376496724,-77.3259246927055,
178.674424369112));
#34925=CARTESIAN_POINT('Ctrl Pts',(-56.2248079189572,-77.3327232769949,
178.835441600731));
#34926=CARTESIAN_POINT('Ctrl Pts',(-55.454377979819,-77.3504687699554,178.999741818441));
#34927=CARTESIAN_POINT('Ctrl Pts',(-55.0645262168849,-77.3620449013272,
179.006970374376));
#34928=CARTESIAN_POINT('Ctrl Pts',(-54.2888274410951,-77.384002955326,178.871418979044));
#34929=CARTESIAN_POINT('Ctrl Pts',(-53.9112133437184,-77.3914216495637,
178.72422716204));
#34930=CARTESIAN_POINT('Ctrl Pts',(-53.2477613019418,-77.3977415730732,
178.29890725331));
#34931=CARTESIAN_POINT('Ctrl Pts',(-52.9653954550316,-77.3977998128993,
178.029685296235));
#34932=CARTESIAN_POINT('Ctrl Pts',(-52.5087154904175,-77.3857903409056,
177.38775671557));
#34933=CARTESIAN_POINT('Ctrl Pts',(-52.3432748923029,-77.3705933748417,
177.01790606498));
#34934=CARTESIAN_POINT('Ctrl Pts',(-52.1694074351774,-77.3247006426295,
176.250446686407));
#34935=CARTESIAN_POINT('Ctrl Pts',(-52.1572205391053,-77.2958991705948,
175.861508827493));
#34936=CARTESIAN_POINT('Ctrl Pts',(-52.2820566190224,-77.2219359945378,
175.086965003283));
#34937=CARTESIAN_POINT('Ctrl Pts',(-52.4233078023374,-77.1740470586507,
174.70984491892));
#34938=CARTESIAN_POINT('Ctrl Pts',(-52.8142567922122,-77.0714107626084,
174.083178867424));
#34939=CARTESIAN_POINT('Ctrl Pts',(-53.0425095453552,-77.0194279689487,
173.828046178147));
#34940=CARTESIAN_POINT('Ctrl Pts',(-53.3084563500542,-76.9651001683373,
173.617797875548));
#34941=CARTESIAN_POINT('Origin',(-54.1598171290174,-67.5719248685924,175.985485069079));
#34942=CARTESIAN_POINT('',(-53.0964443411576,-74.9763691890233,173.617797875548));
#34943=CARTESIAN_POINT('',(-53.1494473433817,-75.4735519338518,173.617797875548));
#34944=CARTESIAN_POINT('',(-52.327900808713,-67.7672193871761,173.617797875548));
#34945=CARTESIAN_POINT('Ctrl Pts',(-53.0964443411576,-74.9763691890233,
173.617797875548));
#34946=CARTESIAN_POINT('Ctrl Pts',(-52.8056358972556,-75.0357757428049,
173.847700926202));
#34947=CARTESIAN_POINT('Ctrl Pts',(-52.5602255146313,-75.0923128245866,
174.131031767172));
#34948=CARTESIAN_POINT('Ctrl Pts',(-52.1727057716636,-75.1973646996916,
174.798444507892));
#34949=CARTESIAN_POINT('Ctrl Pts',(-52.0431878765506,-75.2439348478614,
175.181323966111));
#34950=CARTESIAN_POINT('Ctrl Pts',(-51.9434368386618,-75.3146274058711,
175.96188941981));
#34951=CARTESIAN_POINT('Ctrl Pts',(-51.9686457532674,-75.3429776468977,
176.351227524336));
#34952=CARTESIAN_POINT('Ctrl Pts',(-52.1688125846985,-75.3863358268145,
177.114815436015));
#34953=CARTESIAN_POINT('Ctrl Pts',(-52.3474424077776,-75.4000554379297,
177.480113440793));
#34954=CARTESIAN_POINT('Ctrl Pts',(-52.8275775842746,-75.4089287456145,
178.107503842801));
#34955=CARTESIAN_POINT('Ctrl Pts',(-53.1201059261585,-75.4087801109735,
178.367214763405));
#34956=CARTESIAN_POINT('Ctrl Pts',(-53.8005258401282,-75.4009398996325,
178.769678639605));
#34957=CARTESIAN_POINT('Ctrl Pts',(-54.1846921836614,-75.3927480180389,
178.903423366868));
#34958=CARTESIAN_POINT('Ctrl Pts',(-54.9671806584076,-75.3693889756646,
179.010148570594));
#34959=CARTESIAN_POINT('Ctrl Pts',(-55.3575958159887,-75.3588040506301,
178.988108799899));
#34960=CARTESIAN_POINT('Ctrl Pts',(-56.1237077357375,-75.3418282794223,
178.793710469574));
#34961=CARTESIAN_POINT('Ctrl Pts',(-56.4904089525644,-75.3354983760722,
178.617563704924));
#34962=CARTESIAN_POINT('Ctrl Pts',(-57.1206198606809,-75.3283737112098,
178.141114095079));
#34963=CARTESIAN_POINT('Ctrl Pts',(-57.3821547693695,-75.3315273120711,
177.850235350799));
#34964=CARTESIAN_POINT('Ctrl Pts',(-57.789209342569,-75.3528292167029,177.172846718022));
#34965=CARTESIAN_POINT('Ctrl Pts',(-57.9256768548506,-75.3710438494031,
176.789987348856));
#34966=CARTESIAN_POINT('Ctrl Pts',(-58.0381803604521,-75.4191108669956,
176.009442856234));
#34967=CARTESIAN_POINT('Ctrl Pts',(-58.0195610965447,-75.4521297317918,
175.620106217133));
#34968=CARTESIAN_POINT('Ctrl Pts',(-57.833128759881,-75.536701052086,174.856503479113));
#34969=CARTESIAN_POINT('Ctrl Pts',(-57.6614535438247,-75.5877658496395,
174.491188142736));
#34970=CARTESIAN_POINT('Ctrl Pts',(-57.1940650337145,-75.6976538911716,
173.863744191349));
#34971=CARTESIAN_POINT('Ctrl Pts',(-56.9081160393018,-75.7591707703788,
173.603998625641));
#34972=CARTESIAN_POINT('Ctrl Pts',(-56.2413965323488,-75.8949436386513,
173.201450622004));
#34973=CARTESIAN_POINT('Ctrl Pts',(-55.8641603018969,-75.9679227118515,
173.067656305598));
#34974=CARTESIAN_POINT('Ctrl Pts',(-55.0943577828536,-76.1100508177383,
172.960825424802));
#34975=CARTESIAN_POINT('Ctrl Pts',(-54.7104867697401,-76.1820056333181,
172.982810813907));
#34976=CARTESIAN_POINT('Ctrl Pts',(-53.957996923227,-76.3269218990717,173.177098349728));
#34977=CARTESIAN_POINT('Ctrl Pts',(-53.5981828107927,-76.3980437636204,
173.353189740603));
#34978=CARTESIAN_POINT('Ctrl Pts',(-53.273998317967,-76.4641310215298,173.603226863128));
#34979=CARTESIAN_POINT('Ctrl Pts',(-53.2647032314016,-76.4660278507767,
173.610485239014));
#34980=CARTESIAN_POINT('Ctrl Pts',(-53.2554533478299,-76.4679174235089,
173.617797875548));
#34981=CARTESIAN_POINT('Ctrl Pts',(-53.3084563500542,-76.9651001683373,
173.617797875548));
#34982=CARTESIAN_POINT('Ctrl Pts',(-53.3414229337293,-76.9583657314007,
173.591735640026));
#34983=CARTESIAN_POINT('Ctrl Pts',(-53.3749596317192,-76.9515399503452,
173.56636582625));
#34984=CARTESIAN_POINT('Ctrl Pts',(-53.7301077748267,-76.8795145806819,
173.309469127448));
#34985=CARTESIAN_POINT('Ctrl Pts',(-54.0938718360162,-76.8079076592926,
173.144901510774));
#34986=CARTESIAN_POINT('Ctrl Pts',(-54.8497531287336,-76.6628618909532,
172.973567856788));
#34987=CARTESIAN_POINT('Ctrl Pts',(-55.2333647594788,-76.5917591200613,
172.962870625489));
#34988=CARTESIAN_POINT('Ctrl Pts',(-55.9979356555131,-76.449669159368,173.091664639894));
#34989=CARTESIAN_POINT('Ctrl Pts',(-56.370212759963,-76.3771579986217,173.235719256923));
#34990=CARTESIAN_POINT('Ctrl Pts',(-57.0240915397078,-76.2429702970415,
173.655697855252));
#34991=CARTESIAN_POINT('Ctrl Pts',(-57.3024693488843,-76.1830364554036,
173.922678738022));
#34992=CARTESIAN_POINT('Ctrl Pts',(-57.7519471011078,-76.0745711136206,
174.561212200496));
#34993=CARTESIAN_POINT('Ctrl Pts',(-57.9135980924168,-76.0245173319119,
174.930027958775));
#34994=CARTESIAN_POINT('Ctrl Pts',(-58.0800856430789,-75.9422737661782,
175.696611382092));
#34995=CARTESIAN_POINT('Ctrl Pts',(-58.0889656779772,-75.9110228409928,
176.085642999832));
#34996=CARTESIAN_POINT('Ctrl Pts',(-57.9573177126399,-75.8645410572794,
176.861654377664));
#34997=CARTESIAN_POINT('Ctrl Pts',(-57.811917941177,-75.8472240756098,177.240175824889));
#34998=CARTESIAN_POINT('Ctrl Pts',(-57.3897215767072,-75.827724116012,177.906268510214));
#34999=CARTESIAN_POINT('Ctrl Pts',(-57.1219721450795,-75.8259187101642,
178.190421383545));
#35000=CARTESIAN_POINT('Ctrl Pts',(-56.4820695582827,-75.8336501094147,
178.651189752466));
#35001=CARTESIAN_POINT('Ctrl Pts',(-56.1123076095985,-75.8402546725227,
178.818540918871));
#35002=CARTESIAN_POINT('Ctrl Pts',(-55.3436109484019,-75.8576808596364,
178.995400987715));
#35003=CARTESIAN_POINT('Ctrl Pts',(-54.9535288706714,-75.8688741717095,
179.0088202237));
#35004=CARTESIAN_POINT('Ctrl Pts',(-54.1749194025281,-75.8914207477598,
178.885326689875));
#35005=CARTESIAN_POINT('Ctrl Pts',(-53.7945009370796,-75.8991642982313,
178.743739561927));
#35006=CARTESIAN_POINT('Ctrl Pts',(-53.1238935414248,-75.9061212888656,
178.327957775593));
#35007=CARTESIAN_POINT('Ctrl Pts',(-52.8372655166408,-75.9062451634505,
178.062729660632));
#35008=CARTESIAN_POINT('Ctrl Pts',(-52.3706877393788,-75.8955535058313,
177.426865015712));
#35009=CARTESIAN_POINT('Ctrl Pts',(-52.1996788877483,-75.8809754128322,
177.058875146964));
#35010=CARTESIAN_POINT('Ctrl Pts',(-52.0147405618912,-75.8361454299697,
176.292992512181));
#35011=CARTESIAN_POINT('Ctrl Pts',(-51.9970672433361,-75.8075585443191,
175.903887271424));
#35012=CARTESIAN_POINT('Ctrl Pts',(-52.1081627696099,-75.7369779784704,
175.148234780903));
#35013=CARTESIAN_POINT('Ctrl Pts',(-52.2331062331624,-75.6927206684859,
174.788194676274));
#35014=CARTESIAN_POINT('Ctrl Pts',(-52.6089003750333,-75.5904952622481,
174.13606474324));
#35015=CARTESIAN_POINT('Ctrl Pts',(-52.8560409607083,-75.5334891963958,
173.849754766321));
#35016=CARTESIAN_POINT('Ctrl Pts',(-53.1494473433817,-75.4735519338518,
173.617797875548));
#35017=CARTESIAN_POINT('Origin',(-54.1598171290174,-67.5719248685924,175.985485069079));
#35018=CARTESIAN_POINT('',(-52.9374353344854,-73.4848209545377,173.617797875548));
#35019=CARTESIAN_POINT('',(-52.9904383367094,-73.9820036993662,173.617797875548));
#35020=CARTESIAN_POINT('',(-52.327900808713,-67.7672193871761,173.617797875548));
#35021=CARTESIAN_POINT('Ctrl Pts',(-52.9374353344854,-73.4848209545377,
173.617797875548));
#35022=CARTESIAN_POINT('Ctrl Pts',(-52.6465099007733,-73.5442514070801,
173.847793414281));
#35023=CARTESIAN_POINT('Ctrl Pts',(-52.4010205221672,-73.6008097872557,
174.131258683427));
#35024=CARTESIAN_POINT('Ctrl Pts',(-52.0135219882289,-73.705872346413,174.798864081555));
#35025=CARTESIAN_POINT('Ctrl Pts',(-51.8840597734408,-73.7524361582106,
175.181769782186));
#35026=CARTESIAN_POINT('Ctrl Pts',(-51.7844271714147,-73.8231131991743,
175.962362617006));
#35027=CARTESIAN_POINT('Ctrl Pts',(-51.8096977087126,-73.8514617786658,
176.351702636564));
#35028=CARTESIAN_POINT('Ctrl Pts',(-52.0099891621526,-73.8948078664141,
177.115271165447));
#35029=CARTESIAN_POINT('Ctrl Pts',(-52.1886811574383,-73.9085204189799,
177.480546513429));
#35030=CARTESIAN_POINT('Ctrl Pts',(-52.6689270066302,-73.9173788192747,
178.107866931419));
#35031=CARTESIAN_POINT('Ctrl Pts',(-52.9615038196731,-73.9172302946619,
178.367532578133));
#35032=CARTESIAN_POINT('Ctrl Pts',(-53.642003885008,-73.9093828221344,178.769886508089));
#35033=CARTESIAN_POINT('Ctrl Pts',(-54.0262003616248,-73.9011872652275,
178.903566426416));
#35034=CARTESIAN_POINT('Ctrl Pts',(-54.8087199756404,-73.8778215599148,
179.010153525356));
#35035=CARTESIAN_POINT('Ctrl Pts',(-55.1991379336217,-73.8672420109574,
178.988042684565));
#35036=CARTESIAN_POINT('Ctrl Pts',(-55.9652277118067,-73.850269980588,178.793499556595));
#35037=CARTESIAN_POINT('Ctrl Pts',(-56.3319028241094,-73.8439423624653,
178.617280427587));
#35038=CARTESIAN_POINT('Ctrl Pts',(-56.9620328749772,-73.8368227222785,
178.140701715233));
#35039=CARTESIAN_POINT('Ctrl Pts',(-57.223516362575,-73.8399879066131,177.849767243461));
#35040=CARTESIAN_POINT('Ctrl Pts',(-57.6304446591832,-73.8613047578019,
177.17228554571));
#35041=CARTESIAN_POINT('Ctrl Pts',(-57.7668375880929,-73.8795268065409,
176.789391070126));
#35042=CARTESIAN_POINT('Ctrl Pts',(-57.8791818703731,-73.9276069322545,
176.008809947372));
#35043=CARTESIAN_POINT('Ctrl Pts',(-57.8604815702442,-73.9606409967141,
175.619470747061));
#35044=CARTESIAN_POINT('Ctrl Pts',(-57.673882891374,-74.0452316469215,174.855893925201));
#35045=CARTESIAN_POINT('Ctrl Pts',(-57.5021243977001,-74.0963047472366,
174.490608883617));
#35046=CARTESIAN_POINT('Ctrl Pts',(-57.0345869856321,-74.2062045053082,
173.863258525876));
#35047=CARTESIAN_POINT('Ctrl Pts',(-56.748574651833,-74.2677351909695,173.603573511167));
#35048=CARTESIAN_POINT('Ctrl Pts',(-56.0817483044874,-74.4035211664158,
173.201172545343));
#35049=CARTESIAN_POINT('Ctrl Pts',(-55.7044716343725,-74.4765039324346,
173.067464901129));
#35050=CARTESIAN_POINT('Ctrl Pts',(-54.934626516975,-74.6186321090574,172.960818720527));
#35051=CARTESIAN_POINT('Ctrl Pts',(-54.5507533582519,-74.6905947377381,
172.982899157147));
#35052=CARTESIAN_POINT('Ctrl Pts',(-53.7982935018327,-74.8355096532683,
173.177380339521));
#35053=CARTESIAN_POINT('Ctrl Pts',(-53.4385141495588,-74.9066271474933,
173.353568511));
#35054=CARTESIAN_POINT('Ctrl Pts',(-53.1145873281588,-74.9726648198379,
173.603540806818));
#35055=CARTESIAN_POINT('Ctrl Pts',(-53.105494198882,-74.9745204777121,173.610643372498));
#35056=CARTESIAN_POINT('Ctrl Pts',(-53.0964443411576,-74.9763691890233,
173.617797875548));
#35057=CARTESIAN_POINT('Ctrl Pts',(-53.1494473433817,-75.4735519338518,
173.617797875548));
#35058=CARTESIAN_POINT('Ctrl Pts',(-53.4038504347735,-75.4215822911269,
173.416675631565));
#35059=CARTESIAN_POINT('Ctrl Pts',(-53.6890542096037,-75.3648165529217,
173.259278878347));
#35060=CARTESIAN_POINT('Ctrl Pts',(-54.3016794488769,-75.2455619498074,
173.043135222439));
#35061=CARTESIAN_POINT('Ctrl Pts',(-54.6254322052276,-75.1838147802994,
172.986935943668));
#35062=CARTESIAN_POINT('Ctrl Pts',(-55.3316413974426,-75.0517503870613,
172.983856638115));
#35063=CARTESIAN_POINT('Ctrl Pts',(-55.7083574319068,-74.9829291078777,
173.0563943681));
#35064=CARTESIAN_POINT('Ctrl Pts',(-56.4238106814297,-74.8430437902404,
173.34623381907));
#35065=CARTESIAN_POINT('Ctrl Pts',(-56.7541499010389,-74.7749851769342,
173.564937836107));
#35066=CARTESIAN_POINT('Ctrl Pts',(-57.3030913686338,-74.6543682606874,
174.112287546155));
#35067=CARTESIAN_POINT('Ctrl Pts',(-57.5195038293576,-74.6026874586522,
174.432397356868));
#35068=CARTESIAN_POINT('Ctrl Pts',(-57.8237513008106,-74.5067034561762,
175.148939465042));
#35069=CARTESIAN_POINT('Ctrl Pts',(-57.9048085027795,-74.4652282828169,
175.540226350866));
#35070=CARTESIAN_POINT('Ctrl Pts',(-57.9108912239646,-74.4023961896717,
176.322079499261));
#35071=CARTESIAN_POINT('Ctrl Pts',(-57.8402282212688,-74.381365088574,176.70498371168));
#35072=CARTESIAN_POINT('Ctrl Pts',(-57.5539522654626,-74.3484013270949,
177.434334602834));
#35073=CARTESIAN_POINT('Ctrl Pts',(-57.3372981970406,-74.3386738447082,
177.772220279817));
#35074=CARTESIAN_POINT('Ctrl Pts',(-56.7934819174716,-74.3343764047435,
178.337326110435));
#35075=CARTESIAN_POINT('Ctrl Pts',(-56.474676243902,-74.339838461472,178.561989840184));
#35076=CARTESIAN_POINT('Ctrl Pts',(-55.7595098992864,-74.3526661832745,
178.883184739858));
#35077=CARTESIAN_POINT('Ctrl Pts',(-55.368510085521,-74.3615362269356,178.972859944194));
#35078=CARTESIAN_POINT('Ctrl Pts',(-54.5849379680645,-74.3827096517394,
178.995331361022));
#35079=CARTESIAN_POINT('Ctrl Pts',(-54.2001311788535,-74.3952408085493,
178.931996815635));
#35080=CARTESIAN_POINT('Ctrl Pts',(-53.4650579362335,-74.4102619637419,
178.659863551114));
#35081=CARTESIAN_POINT('Ctrl Pts',(-53.123406503473,-74.4138837139738,178.449958816363));
#35082=CARTESIAN_POINT('Ctrl Pts',(-52.5482581730315,-74.4127488661628,
177.917040578791));
#35083=CARTESIAN_POINT('Ctrl Pts',(-52.3177323071135,-74.4088585779677,
177.602070757164));
#35084=CARTESIAN_POINT('Ctrl Pts',(-51.9829683279186,-74.3812775381616,
176.89381178252));
#35085=CARTESIAN_POINT('Ctrl Pts',(-51.8855522842931,-74.3588762395479,
176.505737024407));
#35086=CARTESIAN_POINT('Ctrl Pts',(-51.8465724378342,-74.3004934140384,
175.724870075675));
#35087=CARTESIAN_POINT('Ctrl Pts',(-51.9017164538028,-74.2661673311796,
175.339801118751));
#35088=CARTESIAN_POINT('Ctrl Pts',(-52.1563832812566,-74.1758245781323,
174.604064259488));
#35089=CARTESIAN_POINT('Ctrl Pts',(-52.3570212774142,-74.1216643244169,
174.261723152778));
#35090=CARTESIAN_POINT('Ctrl Pts',(-52.7320292384492,-74.0361458916242,
173.840973054109));
#35091=CARTESIAN_POINT('Ctrl Pts',(-52.8567013290755,-74.0093235894973,
173.723525706652));
#35092=CARTESIAN_POINT('Ctrl Pts',(-52.9904383367094,-73.9820036993662,
173.617797875548));
#35093=CARTESIAN_POINT('Origin',(-54.1598171290174,-67.5719248685924,175.985485069079));
#35094=CARTESIAN_POINT('',(-52.7784263278132,-71.9932727200521,173.617797875548));
#35095=CARTESIAN_POINT('',(-52.8314293300373,-72.4904554648806,173.617797875548));
#35096=CARTESIAN_POINT('',(-52.327900808713,-67.7672193871761,173.617797875548));
#35097=CARTESIAN_POINT('Ctrl Pts',(-52.7784263278132,-71.9932727200521,
173.617797875548));
#35098=CARTESIAN_POINT('Ctrl Pts',(-52.4874355225081,-72.0527165267496,
173.847845094791));
#35099=CARTESIAN_POINT('Ctrl Pts',(-52.2419020096117,-72.1092868075074,
174.131385486844));
#35100=CARTESIAN_POINT('Ctrl Pts',(-51.854415347595,-72.2143553338943,174.799098541648));
#35101=CARTESIAN_POINT('Ctrl Pts',(-51.7249842477566,-72.2609156045222,
175.182018902505));
#35102=CARTESIAN_POINT('Ctrl Pts',(-51.6254178270345,-72.3315839743407,
175.962627033479));
#35103=CARTESIAN_POINT('Ctrl Pts',(-51.6507227993994,-72.3599316272761,
176.351968123227));
#35104=CARTESIAN_POINT('Ctrl Pts',(-51.8510838928015,-72.4032709574674,
177.115525816536));
#35105=CARTESIAN_POINT('Ctrl Pts',(-52.0298106290951,-72.4169795654191,
177.480788499263));
#35106=CARTESIAN_POINT('Ctrl Pts',(-52.5101183213077,-72.4258296351316,
178.108069805027));
#35107=CARTESIAN_POINT('Ctrl Pts',(-52.8027222218384,-72.4256811742122,
178.367710151333));
#35108=CARTESIAN_POINT('Ctrl Pts',(-53.4832670754377,-72.4178296438271,
178.770002635437));
#35109=CARTESIAN_POINT('Ctrl Pts',(-53.8674803868508,-72.4096320330776,
178.903646333472));
#35110=CARTESIAN_POINT('Ctrl Pts',(-54.6500173974771,-72.386262604351,179.010156251863));
#35111=CARTESIAN_POINT('Ctrl Pts',(-55.0404369208613,-72.3756860624331,
178.988005692624));
#35112=CARTESIAN_POINT('Ctrl Pts',(-55.8065143189993,-72.3587161228737,
178.793381641246));
#35113=CARTESIAN_POINT('Ctrl Pts',(-56.1731748362746,-72.352389782025,178.617122071665));
#35114=CARTESIAN_POINT('Ctrl Pts',(-56.8032596922529,-72.3452729501008,
178.140471210068));
#35115=CARTESIAN_POINT('Ctrl Pts',(-57.0647144411369,-72.3484446113575,
177.849505592283));
#35116=CARTESIAN_POINT('Ctrl Pts',(-57.4715721561285,-72.369769816264,177.17197188452));
#35117=CARTESIAN_POINT('Ctrl Pts',(-57.6079233964997,-72.3879960096499,
176.789057794065));
#35118=CARTESIAN_POINT('Ctrl Pts',(-57.7201786848776,-72.4360834612763,
176.00845620547));
#35119=CARTESIAN_POINT('Ctrl Pts',(-57.701433091218,-72.4691260247665,175.61911557349));
#35120=CARTESIAN_POINT('Ctrl Pts',(-57.5147414361687,-72.5537274787296,
174.855553244988));
#35121=CARTESIAN_POINT('Ctrl Pts',(-57.3429363973152,-72.6048052188926,
174.490285144426));
#35122=CARTESIAN_POINT('Ctrl Pts',(-56.8753157606339,-72.7147115247956,
173.862987108372));
#35123=CARTESIAN_POINT('Ctrl Pts',(-56.5892680221202,-72.7762499318678,
173.603335939967));
#35124=CARTESIAN_POINT('Ctrl Pts',(-55.9223819587286,-72.9120432326736,
173.201017172362));
#35125=CARTESIAN_POINT('Ctrl Pts',(-55.5450826918185,-72.9850280612433,
173.06735798104));
#35126=CARTESIAN_POINT('Ctrl Pts',(-54.7752137718068,-73.127156275602,172.960815048826));
#35127=CARTESIAN_POINT('Ctrl Pts',(-54.39133941398,-73.1991232765269,172.982948618528));
#35128=CARTESIAN_POINT('Ctrl Pts',(-53.6388963329757,-73.3440374353567,
173.177538054862));
#35129=CARTESIAN_POINT('Ctrl Pts',(-53.2791364230434,-73.4151524844253,
173.353780326124));
#35130=CARTESIAN_POINT('Ctrl Pts',(-52.9553536206288,-73.4811624409117,
173.603716331819));
#35131=CARTESIAN_POINT('Ctrl Pts',(-52.9463733724799,-73.4829950858397,
173.610731773291));
#35132=CARTESIAN_POINT('Ctrl Pts',(-52.9374353344854,-73.4848209545377,
173.617797875548));
#35133=CARTESIAN_POINT('Ctrl Pts',(-52.9904383367094,-73.9820036993662,
173.617797875548));
#35134=CARTESIAN_POINT('Ctrl Pts',(-53.1553110450625,-73.9483233863585,
173.487455241368));
#35135=CARTESIAN_POINT('Ctrl Pts',(-53.3337275237714,-73.9125044170173,
173.374987996813));
#35136=CARTESIAN_POINT('Ctrl Pts',(-53.8734962529804,-73.805818482098,173.111112646691));
#35137=CARTESIAN_POINT('Ctrl Pts',(-54.2541774238143,-73.7324815471996,
173.01171038204));
#35138=CARTESIAN_POINT('Ctrl Pts',(-55.0234181079905,-73.5877606109365,
172.96879303946));
#35139=CARTESIAN_POINT('Ctrl Pts',(-55.4044453970555,-73.5187067413993,
173.02228372683));
#35140=CARTESIAN_POINT('Ctrl Pts',(-56.132592882784,-73.3780446152237,173.275564729262));
#35141=CARTESIAN_POINT('Ctrl Pts',(-56.4717530818814,-73.3091527358298,
173.476042168944));
#35142=CARTESIAN_POINT('Ctrl Pts',(-57.0473596050972,-73.1849874493357,
173.993471152876));
#35143=CARTESIAN_POINT('Ctrl Pts',(-57.2804732945259,-73.1316967319038,
174.303002885404));
#35144=CARTESIAN_POINT('Ctrl Pts',(-57.6198344451369,-73.0325627744389,
175.002350201893));
#35145=CARTESIAN_POINT('Ctrl Pts',(-57.7201522302408,-72.9891532290938,
175.386808070376));
#35146=CARTESIAN_POINT('Ctrl Pts',(-57.7666314066635,-72.9213105141303,
176.166353229708));
#35147=CARTESIAN_POINT('Ctrl Pts',(-57.7154678118553,-72.8983119303155,
176.553704035339));
#35148=CARTESIAN_POINT('Ctrl Pts',(-57.4665697516579,-72.8619727200906,
177.295849974148));
#35149=CARTESIAN_POINT('Ctrl Pts',(-57.2685877852196,-72.850385520672,177.642568170487));
#35150=CARTESIAN_POINT('Ctrl Pts',(-56.7553577051062,-72.8421268131452,
178.235012179866));
#35151=CARTESIAN_POINT('Ctrl Pts',(-56.4473243401806,-72.846490506357,178.476861972734));
#35152=CARTESIAN_POINT('Ctrl Pts',(-55.7498624927776,-72.8580546688818,
178.833885088967));
#35153=CARTESIAN_POINT('Ctrl Pts',(-55.3660396770667,-72.8663023543203,
178.943181382324));
#35154=CARTESIAN_POINT('Ctrl Pts',(-54.5850133533515,-72.8865093358843,
179.007121977488));
#35155=CARTESIAN_POINT('Ctrl Pts',(-54.1956965410825,-72.8995083972586,
178.963761237945));
#35156=CARTESIAN_POINT('Ctrl Pts',(-53.4480085814119,-72.9165114886649,
178.729766400635));
#35157=CARTESIAN_POINT('Ctrl Pts',(-53.0977170435069,-72.9212088575917,
178.538985461051));
#35158=CARTESIAN_POINT('Ctrl Pts',(-52.4951376818609,-72.9223107963204,
178.037530682304));
#35159=CARTESIAN_POINT('Ctrl Pts',(-52.2472698728753,-72.920192371099,177.733541985202));
#35160=CARTESIAN_POINT('Ctrl Pts',(-51.8767232141554,-72.897074960845,177.043400876252));
#35161=CARTESIAN_POINT('Ctrl Pts',(-51.7597509275285,-72.876924531648,176.662840230563));
#35162=CARTESIAN_POINT('Ctrl Pts',(-51.6791019803236,-72.822305760216,175.884920756758));
#35163=CARTESIAN_POINT('Ctrl Pts',(-51.7141846959403,-72.7899769925759,
175.495274507088));
#35164=CARTESIAN_POINT('Ctrl Pts',(-51.9307601176331,-72.7043542823012,
174.746958074078));
#35165=CARTESIAN_POINT('Ctrl Pts',(-52.1122334186126,-72.6524143093864,
174.396133406655));
#35166=CARTESIAN_POINT('Ctrl Pts',(-52.496335077636,-72.5612400686153,173.915224673226));
#35167=CARTESIAN_POINT('Ctrl Pts',(-52.6559452899231,-72.5263034682156,
173.756529459893));
#35168=CARTESIAN_POINT('Ctrl Pts',(-52.8314293300374,-72.4904554648806,
173.617797875548));
#35169=CARTESIAN_POINT('Origin',(-54.1598171290174,-67.5719248685924,175.985485069079));
#35170=CARTESIAN_POINT('',(-52.6194173211409,-70.5017244855665,173.617797875548));
#35171=CARTESIAN_POINT('',(-52.6724203233655,-70.9989072303948,173.617797875547));
#35172=CARTESIAN_POINT('',(-52.327900808713,-67.7672193871761,173.617797875548));
#35173=CARTESIAN_POINT('Ctrl Pts',(-52.6194173211409,-70.5017244855665,
173.617797875548));
#35174=CARTESIAN_POINT('Ctrl Pts',(-52.3283899981591,-70.5611757521207,
173.847873964397));
#35175=CARTESIAN_POINT('Ctrl Pts',(-52.0828318333189,-70.6177526805768,
174.131456323592));
#35176=CARTESIAN_POINT('Ctrl Pts',(-51.6953518096301,-70.7228245394826,
174.799229518335));
#35177=CARTESIAN_POINT('Ctrl Pts',(-51.5659380917167,-70.7693828317876,
175.182158067545));
#35178=CARTESIAN_POINT('Ctrl Pts',(-51.4664086415161,-70.8400463575936,
175.962774742001));
#35179=CARTESIAN_POINT('Ctrl Pts',(-51.4917328503677,-70.8683934935249,
176.352116429609));
#35180=CARTESIAN_POINT('Ctrl Pts',(-51.6921328469686,-70.9117290486146,
177.115668068469));
#35181=CARTESIAN_POINT('Ctrl Pts',(-51.8708789903038,-70.9254354529018,
177.480923674582));
#35182=CARTESIAN_POINT('Ctrl Pts',(-52.3512212294813,-70.9342808688144,
178.108183129553));
#35183=CARTESIAN_POINT('Ctrl Pts',(-52.643840262403,-70.9341324441656,178.36780934192));
#35184=CARTESIAN_POINT('Ctrl Pts',(-53.3244101358798,-70.9262786468521,
178.77006749819));
#35185=CARTESIAN_POINT('Ctrl Pts',(-53.7086328505657,-70.9180798887446,
178.903690960978));
#35186=CARTESIAN_POINT('Ctrl Pts',(-54.4911795781716,-70.8947083799637,
179.010157761786));
#35187=CARTESIAN_POINT('Ctrl Pts',(-54.8815999762017,-70.8841335187636,
178.987985013315));
#35188=CARTESIAN_POINT('Ctrl Pts',(-55.6476704562077,-70.8671647473231,
178.793315752586));
#35189=CARTESIAN_POINT('Ctrl Pts',(-56.0143228178515,-70.8608391200856,
178.617033590719));
#35190=CARTESIAN_POINT('Ctrl Pts',(-56.6443824229989,-70.8537238570835,
178.140342422428));
#35191=CARTESIAN_POINT('Ctrl Pts',(-56.9058211161949,-70.8568991378029,
177.849359403895));
#35192=CARTESIAN_POINT('Ctrl Pts',(-57.3126393966221,-70.8782290098234,
177.17179664023));
#35193=CARTESIAN_POINT('Ctrl Pts',(-57.448967345067,-70.896457518701,176.788871593169));
#35194=CARTESIAN_POINT('Ctrl Pts',(-57.5611729127472,-70.9445490631288,
176.008258572745));
#35195=CARTESIAN_POINT('Ctrl Pts',(-57.5424020135795,-70.9775963761197,
175.61891714085));
#35196=CARTESIAN_POINT('Ctrl Pts',(-57.355658411896,-71.0622038660495,174.855362912306));
#35197=CARTESIAN_POINT('Ctrl Pts',(-57.1838273685927,-71.1132841982438,
174.490104279311));
#35198=CARTESIAN_POINT('Ctrl Pts',(-56.7161602346341,-71.2231941621447,
173.862835478345));
#35199=CARTESIAN_POINT('Ctrl Pts',(-56.4300927147269,-71.2847368846005,
173.603203220681));
#35200=CARTESIAN_POINT('Ctrl Pts',(-55.7631732880258,-71.420534277891,173.200930381758));
#35201=CARTESIAN_POINT('Ctrl Pts',(-55.385861398193,-71.4935202583481,173.067298263967));
#35202=CARTESIAN_POINT('Ctrl Pts',(-54.6159791817969,-71.6356484932274,
172.960813021029));
#35203=CARTESIAN_POINT('Ctrl Pts',(-54.2321041540749,-71.7076179385728,
172.98297627877));
#35204=CARTESIAN_POINT('Ctrl Pts',(-53.4796704495815,-71.8525316740027,
173.177626202615));
#35205=CARTESIAN_POINT('Ctrl Pts',(-53.1199214064205,-71.9236453561953,
173.353898701391));
#35206=CARTESIAN_POINT('Ctrl Pts',(-52.7962190670824,-71.989639827505,173.603814414118));
#35207=CARTESIAN_POINT('Ctrl Pts',(-52.7873018860386,-71.9914596147653,
173.610781167625));
#35208=CARTESIAN_POINT('Ctrl Pts',(-52.7784263278132,-71.9932727200521,
173.617797875548));
#35209=CARTESIAN_POINT('Ctrl Pts',(-52.8314293300374,-72.4904554648806,
173.617797875548));
#35210=CARTESIAN_POINT('Ctrl Pts',(-52.9562042748654,-72.4649663512528,
173.519155139882));
#35211=CARTESIAN_POINT('Ctrl Pts',(-53.0888728652022,-72.4382244869968,
173.430644439586));
#35212=CARTESIAN_POINT('Ctrl Pts',(-53.5678939714476,-72.3428470269725,
173.164685182053));
#35213=CARTESIAN_POINT('Ctrl Pts',(-53.9408870073599,-72.2705175725099,
173.045737100393));
#35214=CARTESIAN_POINT('Ctrl Pts',(-54.7068403761519,-72.1254929997893,
172.961040170675));
#35215=CARTESIAN_POINT('Ctrl Pts',(-55.0923870636032,-72.0556883697972,
172.994380514604));
#35216=CARTESIAN_POINT('Ctrl Pts',(-55.8328164429564,-71.914391705921,173.209428337053));
#35217=CARTESIAN_POINT('Ctrl Pts',(-56.1801273911734,-71.8448288729157,
173.390642971781));
#35218=CARTESIAN_POINT('Ctrl Pts',(-56.7825455499323,-71.7171656222667,
173.876277011709));
#35219=CARTESIAN_POINT('Ctrl Pts',(-57.0329394139578,-71.6617018875866,
174.174835645679));
#35220=CARTESIAN_POINT('Ctrl Pts',(-57.4076029540624,-71.5594843653007,
174.855845912787));
#35221=CARTESIAN_POINT('Ctrl Pts',(-57.5270451576265,-71.5142434180066,
175.232397895274));
#35222=CARTESIAN_POINT('Ctrl Pts',(-57.6145373411043,-71.4414046018991,
176.008453264421));
#35223=CARTESIAN_POINT('Ctrl Pts',(-57.5831660846008,-71.4159054217256,
176.400326411267));
#35224=CARTESIAN_POINT('Ctrl Pts',(-57.3718410495929,-71.3762438522241,
177.154339528067));
#35225=CARTESIAN_POINT('Ctrl Pts',(-57.1928125044782,-71.3628521244282,
177.508852862468));
#35226=CARTESIAN_POINT('Ctrl Pts',(-56.7108278926429,-71.3506558158484,
178.127690347984));
#35227=CARTESIAN_POINT('Ctrl Pts',(-56.4134978759637,-71.3534304841221,
178.386691236702));
#35228=CARTESIAN_POINT('Ctrl Pts',(-55.7341769742953,-71.3637454216852,
178.778320887476));
#35229=CARTESIAN_POINT('Ctrl Pts',(-55.3583039876754,-71.3713694275508,
178.906310809509));
#35230=CARTESIAN_POINT('Ctrl Pts',(-54.5856989608393,-71.3904835507265,
179.010054932807));
#35231=CARTESIAN_POINT('Ctrl Pts',(-54.1968324650935,-71.4032549324752,
178.98747721674));
#35232=CARTESIAN_POINT('Ctrl Pts',(-53.4366145322674,-71.422326711838,178.793849110096));
#35233=CARTESIAN_POINT('Ctrl Pts',(-53.0737837008178,-71.4281550162257,
178.6201435409));
#35234=CARTESIAN_POINT('Ctrl Pts',(-52.4459767551618,-71.4313829597214,
178.14933536471));
#35235=CARTESIAN_POINT('Ctrl Pts',(-52.1844055279917,-71.4305258825894,
177.860501800465));
#35236=CARTESIAN_POINT('Ctrl Pts',(-51.7772182332885,-71.4120470745932,
177.189773111793));
#35237=CARTESIAN_POINT('Ctrl Pts',(-51.6396120902311,-71.3938596575389,
176.811926665257));
#35238=CARTESIAN_POINT('Ctrl Pts',(-51.5205195801389,-71.3427973554989,
176.037787112913));
#35239=CARTESIAN_POINT('Ctrl Pts',(-51.5356336824963,-71.3123817412031,
175.649640414745));
#35240=CARTESIAN_POINT('Ctrl Pts',(-51.7132874414347,-71.2316383216106,
174.889256332101));
#35241=CARTESIAN_POINT('Ctrl Pts',(-51.8787843813605,-71.1811339473371,
174.525567559822));
#35242=CARTESIAN_POINT('Ctrl Pts',(-52.2699480870556,-71.0845630084185,
173.983931897263));
#35243=CARTESIAN_POINT('Ctrl Pts',(-52.459297511381,-71.0424441085624,173.78628536505));
#35244=CARTESIAN_POINT('Ctrl Pts',(-52.672420323366,-70.9989072303947,173.617797875547));
#35245=CARTESIAN_POINT('Origin',(-54.1598171290174,-67.5719248685924,175.985485069079));
#35246=CARTESIAN_POINT('',(-52.4604083144687,-69.0101762510808,173.617797875548));
#35247=CARTESIAN_POINT('',(-52.5134113166933,-69.5073589959092,173.617797875547));
#35248=CARTESIAN_POINT('',(-52.327900808713,-67.7672193871761,173.617797875548));
#35249=CARTESIAN_POINT('Ctrl Pts',(-52.4604083144687,-69.0101762510809,
173.617797875548));
#35250=CARTESIAN_POINT('Ctrl Pts',(-52.1693605954265,-69.0696316841567,
173.847890088814));
#35251=CARTESIAN_POINT('Ctrl Pts',(-51.9237886625342,-69.1262123254704,
174.131495888427));
#35252=CARTESIAN_POINT('Ctrl Pts',(-51.5363123485411,-69.2312860454002,
174.799302673213));
#35253=CARTESIAN_POINT('Ctrl Pts',(-51.4069083390629,-69.2778432327096,
175.182235795486));
#35254=CARTESIAN_POINT('Ctrl Pts',(-51.3073995380121,-69.3485040529588,
175.962857241318));
#35255=CARTESIAN_POINT('Ctrl Pts',(-51.3327344910843,-69.3768509003128,
176.352199262857));
#35256=CARTESIAN_POINT('Ctrl Pts',(-51.5331562164762,-69.4201843468438,
177.11574751968));
#35257=CARTESIAN_POINT('Ctrl Pts',(-51.7119131991822,-69.4338895202854,
177.480999172827));
#35258=CARTESIAN_POINT('Ctrl Pts',(-52.192274733854,-69.44273233687,178.108246422932));
#35259=CARTESIAN_POINT('Ctrl Pts',(-52.4849022188737,-69.4425839326948,
178.367864740911));
#35260=CARTESIAN_POINT('Ctrl Pts',(-53.1654860667179,-69.4347288691997,
178.770103723224));
#35261=CARTESIAN_POINT('Ctrl Pts',(-53.5497140330834,-69.4265294702486,
178.903715883489));
#35262=CARTESIAN_POINT('Ctrl Pts',(-54.3322661875416,-69.4031567996751,
179.010158601014));
#35263=CARTESIAN_POINT('Ctrl Pts',(-54.722687074142,-69.3925828774908,178.987973458713));
#35264=CARTESIAN_POINT('Ctrl Pts',(-55.4887536894349,-69.3756147585238,
178.793278946101));
#35265=CARTESIAN_POINT('Ctrl Pts',(-55.8554014951372,-69.369289529889,178.616984165394));
#35266=CARTESIAN_POINT('Ctrl Pts',(-56.4854469957362,-69.3621751432259,
178.140270483872));
#35267=CARTESIAN_POINT('Ctrl Pts',(-56.7468767208699,-69.3653524459278,
177.849277745933));
#35268=CARTESIAN_POINT('Ctrl Pts',(-57.1536729740576,-69.3866849248342,
177.171698753104));
#35269=CARTESIAN_POINT('Ctrl Pts',(-57.2899879121142,-69.4049147270426,
176.788767586683));
#35270=CARTESIAN_POINT('Ctrl Pts',(-57.4021657072611,-69.4530085575371,
176.008148181518));
#35271=CARTESIAN_POINT('Ctrl Pts',(-57.383380673139,-69.4860585238073,175.618806302801));
#35272=CARTESIAN_POINT('Ctrl Pts',(-57.1966080552522,-69.5706693852312,
174.855256599452));
#35273=CARTESIAN_POINT('Ctrl Pts',(-57.0247624866957,-69.6217511651833,
174.490003255593));
#35274=CARTESIAN_POINT('Ctrl Pts',(-56.5570693807535,-69.7316631722538,
173.862750785456));
#35275=CARTESIAN_POINT('Ctrl Pts',(-56.2709908112683,-69.7932083056091,
173.603129091057));
#35276=CARTESIAN_POINT('Ctrl Pts',(-55.6040527487679,-69.9290079847868,
173.200881908029));
#35277=CARTESIAN_POINT('Ctrl Pts',(-55.2267338087179,-70.0019946085126,
173.067264913663));
#35278=CARTESIAN_POINT('Ctrl Pts',(-54.4568441659993,-70.1441228546788,
172.960811895719));
#35279=CARTESIAN_POINT('Ctrl Pts',(-54.0729687641061,-70.2160936659234,
172.982991737176));
#35280=CARTESIAN_POINT('Ctrl Pts',(-53.320540298346,-70.3610071646567,173.177675449537));
#35281=CARTESIAN_POINT('Ctrl Pts',(-52.9607973264131,-70.4321200831111,
173.353964833173));
#35282=CARTESIAN_POINT('Ctrl Pts',(-52.6371399314,-70.4981059047316,173.603869205298));
#35283=CARTESIAN_POINT('Ctrl Pts',(-52.6282579780116,-70.4999185099531,
173.610808759424));
#35284=CARTESIAN_POINT('Ctrl Pts',(-52.6194173211409,-70.5017244855665,
173.617797875548));
#35285=CARTESIAN_POINT('Ctrl Pts',(-52.672420323366,-70.9989072303948,173.617797875547));
#35286=CARTESIAN_POINT('Ctrl Pts',(-52.7572963079739,-70.9815687044678,
173.550697871411));
#35287=CARTESIAN_POINT('Ctrl Pts',(-52.8458825851797,-70.9636387281008,
173.488241353861));
#35288=CARTESIAN_POINT('Ctrl Pts',(-53.2713381202172,-70.8782721564819,
173.222237068703));
#35289=CARTESIAN_POINT('Ctrl Pts',(-53.6425444100623,-70.8058346859752,
173.083175461064));
#35290=CARTESIAN_POINT('Ctrl Pts',(-54.4047250023173,-70.660714632616,172.962042479254));
#35291=CARTESIAN_POINT('Ctrl Pts',(-54.7877460202482,-70.5909436825598,
172.976234072482));
#35292=CARTESIAN_POINT('Ctrl Pts',(-55.5395694398728,-70.4491514401287,
173.153536028243));
#35293=CARTESIAN_POINT('Ctrl Pts',(-55.8998399007808,-70.3778776500482,
173.31987650022));
#35294=CARTESIAN_POINT('Ctrl Pts',(-56.5243924397598,-70.2473793664142,
173.777972980736));
#35295=CARTESIAN_POINT('Ctrl Pts',(-56.7857429943176,-70.1905084931426,
174.061223877771));
#35296=CARTESIAN_POINT('Ctrl Pts',(-57.1941771340838,-70.0854016611449,
174.723930962653));
#35297=CARTESIAN_POINT('Ctrl Pts',(-57.3328464299732,-70.0377507510437,
175.099700802466));
#35298=CARTESIAN_POINT('Ctrl Pts',(-57.4540999137606,-69.9608596798413,
175.872121592076));
#35299=CARTESIAN_POINT('Ctrl Pts',(-57.440685526587,-69.9332079842681,176.260487022286));
#35300=CARTESIAN_POINT('Ctrl Pts',(-57.265232808692,-69.8904230715712,177.025146062232));
#35301=CARTESIAN_POINT('Ctrl Pts',(-57.0996962488948,-69.8752020352117,
177.392871258399));
#35302=CARTESIAN_POINT('Ctrl Pts',(-56.643161561418,-69.8598616367307,178.032318363389));
#35303=CARTESIAN_POINT('Ctrl Pts',(-56.3609216026066,-69.8607946766598,
178.300873260204));
#35304=CARTESIAN_POINT('Ctrl Pts',(-55.699097194158,-69.8699336606263,178.724542927165));
#35305=CARTESIAN_POINT('Ctrl Pts',(-55.3229577642767,-69.8771644924136,
178.871069286089));
#35306=CARTESIAN_POINT('Ctrl Pts',(-54.5489509145704,-69.8956257066586,
179.006822433305));
#35307=CARTESIAN_POINT('Ctrl Pts',(-54.1595932969062,-69.9079035694343,
178.999913816536));
#35308=CARTESIAN_POINT('Ctrl Pts',(-53.390934444243,-69.9285028947367,178.836805075672));
#35309=CARTESIAN_POINT('Ctrl Pts',(-53.0200722271393,-69.9351719522811,
178.676926097263));
#35310=CARTESIAN_POINT('Ctrl Pts',(-52.3732877871734,-69.9400296677875,
178.229928690249));
#35311=CARTESIAN_POINT('Ctrl Pts',(-52.1007298406361,-69.9397809636524,
177.951484677003));
#35312=CARTESIAN_POINT('Ctrl Pts',(-51.6671509552613,-69.9247271768927,
177.295800718053));
#35313=CARTESIAN_POINT('Ctrl Pts',(-51.5147101621089,-69.9081124020225,
176.921947998387));
#35314=CARTESIAN_POINT('Ctrl Pts',(-51.3665292113395,-69.8597771442516,
176.151124637624));
#35315=CARTESIAN_POINT('Ctrl Pts',(-51.3671074059843,-69.8303354798373,
175.762566408402));
#35316=CARTESIAN_POINT('Ctrl Pts',(-51.5166173378049,-69.7531866990917,
174.994383443823));
#35317=CARTESIAN_POINT('Ctrl Pts',(-51.6692798777348,-69.7040476858894,
174.623318326548));
#35318=CARTESIAN_POINT('Ctrl Pts',(-52.0615192928287,-69.60408144752,174.036545486382));
#35319=CARTESIAN_POINT('Ctrl Pts',(-52.2720672179397,-69.5566609384186,
173.808596133728));
#35320=CARTESIAN_POINT('Ctrl Pts',(-52.5134113166937,-69.5073589959092,
173.617797875547));
#35321=CARTESIAN_POINT('Origin',(-54.1598171290174,-67.5719248685924,175.985485069079));
#35322=CARTESIAN_POINT('',(-52.327900808713,-67.7672193871761,173.617797875548));
#35323=CARTESIAN_POINT('',(-52.3544023100207,-68.0158107614237,173.617797875548));
#35324=CARTESIAN_POINT('',(-52.327900808713,-67.7672193871761,173.617797875548));
#35325=CARTESIAN_POINT('',(-51.2061722201484,-67.8868031488672,176.406000729814));
#35326=CARTESIAN_POINT('Origin',(-54.1598171290174,-67.5719248685924,175.985485069079));
#35327=CARTESIAN_POINT('Ctrl Pts',(-51.2061722201484,-67.8868031488672,
176.406000729814));
#35328=CARTESIAN_POINT('Ctrl Pts',(-51.2442093398032,-67.9036864730888,
176.660526215341));
#35329=CARTESIAN_POINT('Ctrl Pts',(-51.3146528258394,-67.9173738079232,
176.909358579104));
#35330=CARTESIAN_POINT('Ctrl Pts',(-51.5152351703733,-67.9375181701368,
177.37953524706));
#35331=CARTESIAN_POINT('Ctrl Pts',(-51.6435890877445,-67.944011203737,177.599420545134));
#35332=CARTESIAN_POINT('Ctrl Pts',(-52.0333006391845,-67.9511839361311,
178.108281770286));
#35333=CARTESIAN_POINT('Ctrl Pts',(-52.3259328445715,-67.951035543457,178.36789567938));
#35334=CARTESIAN_POINT('Ctrl Pts',(-53.0065244967854,-67.9431797728178,
178.770123953217));
#35335=CARTESIAN_POINT('Ctrl Pts',(-53.3907553959908,-67.9349800159672,
178.903729801116));
#35336=CARTESIAN_POINT('Ctrl Pts',(-54.1733105811054,-67.911606696553,179.010159068422));
#35337=CARTESIAN_POINT('Ctrl Pts',(-54.563731740578,-67.9010332988762,178.987967004301));
#35338=CARTESIAN_POINT('Ctrl Pts',(-55.3297961972899,-67.8840655443144,
178.793258388745));
#35339=CARTESIAN_POINT('Ctrl Pts',(-55.6964414583606,-67.8777405382994,
178.616956560589));
#35340=CARTESIAN_POINT('Ctrl Pts',(-56.3264790815166,-67.8706266410668,
178.140230305713));
#35341=CARTESIAN_POINT('Ctrl Pts',(-56.5879037980432,-67.8738050731258,
177.84923213953));
#35342=CARTESIAN_POINT('Ctrl Pts',(-56.9946877489435,-67.8951390079691,
177.171644082906));
#35343=CARTESIAN_POINT('Ctrl Pts',(-57.130995420637,-67.9133695324918,176.788709499035));
#35344=CARTESIAN_POINT('Ctrl Pts',(-57.2431577048249,-67.9614646397378,
176.008086528225));
#35345=CARTESIAN_POINT('Ctrl Pts',(-57.22436477632,-67.9945160879726,175.618744399953));
#35346=CARTESIAN_POINT('Ctrl Pts',(-57.0375759527826,-68.0791288323693,
174.855197224174));
#35347=CARTESIAN_POINT('Ctrl Pts',(-56.8657222718961,-68.1302114208706,
174.489946834556));
#35348=CARTESIAN_POINT('Ctrl Pts',(-56.3980146606145,-68.2401245690258,
173.862703485486));
#35349=CARTESIAN_POINT('Ctrl Pts',(-56.1119299198568,-68.3016710490094,
173.603087690757));
#35350=CARTESIAN_POINT('Ctrl Pts',(-55.444981449255,-68.4374720048378,173.200854837005));
#35351=CARTESIAN_POINT('Ctrl Pts',(-55.0676585718396,-68.5104589877847,
173.067246289364));
#35352=CARTESIAN_POINT('Ctrl Pts',(-54.2977647817229,-68.6525872401999,
172.960811269529));
#35353=CARTESIAN_POINT('Ctrl Pts',(-53.9138891708593,-68.7245588144605,
172.983000373254));
#35354=CARTESIAN_POINT('Ctrl Pts',(-53.161463631333,-68.8694721809371,173.17770295711));
#35355=CARTESIAN_POINT('Ctrl Pts',(-52.8017240506071,-68.9405846727686,
173.354001771142));
#35356=CARTESIAN_POINT('Ctrl Pts',(-52.4780917569963,-69.0065656635003,
173.603899807813));
#35357=CARTESIAN_POINT('Ctrl Pts',(-52.4692294783172,-69.0083742575158,
173.61082416993));
#35358=CARTESIAN_POINT('Ctrl Pts',(-52.4604083144687,-69.0101762510809,
173.617797875548));
#35359=CARTESIAN_POINT('Ctrl Pts',(-52.5134113166937,-69.5073589959092,
173.617797875547));
#35360=CARTESIAN_POINT('Ctrl Pts',(-52.5703612089117,-69.4957252318083,
173.572775269671));
#35361=CARTESIAN_POINT('Ctrl Pts',(-52.6289988502732,-69.4838216535598,
173.529829711882));
#35362=CARTESIAN_POINT('Ctrl Pts',(-53.0162333713195,-69.4056840337388,
173.267698507262));
#35363=CARTESIAN_POINT('Ctrl Pts',(-53.3836428075408,-69.3336537771499,
173.114872837393));
#35364=CARTESIAN_POINT('Ctrl Pts',(-54.1426249695377,-69.1885382308423,
172.966739412117));
#35365=CARTESIAN_POINT('Ctrl Pts',(-54.5259666435685,-69.1181436387083,
172.967504561822));
#35366=CARTESIAN_POINT('Ctrl Pts',(-55.2848741247798,-68.9761537624689,
173.118636662349));
#35367=CARTESIAN_POINT('Ctrl Pts',(-55.6518019210303,-68.9041773926925,
173.273023636635));
#35368=CARTESIAN_POINT('Ctrl Pts',(-56.292342357894,-68.7716562328909,173.710620541039));
#35369=CARTESIAN_POINT('Ctrl Pts',(-56.5629347183278,-68.7132091635555,
173.985039489163));
#35370=CARTESIAN_POINT('Ctrl Pts',(-56.993771235524,-68.6062523998265,174.63476376294));
#35371=CARTESIAN_POINT('Ctrl Pts',(-57.1449816641965,-68.557275753891,175.006921289638));
#35372=CARTESIAN_POINT('Ctrl Pts',(-57.2908442705036,-68.4774601691156,
175.776324389069));
#35373=CARTESIAN_POINT('Ctrl Pts',(-57.2895986238276,-68.4479219665201,
176.165046908302));
#35374=CARTESIAN_POINT('Ctrl Pts',(-57.1380431293144,-68.403108095657,176.936070273677));
#35375=CARTESIAN_POINT('Ctrl Pts',(-56.983436033436,-68.3867366680171,177.309835220954));
#35376=CARTESIAN_POINT('Ctrl Pts',(-56.5455811494487,-68.3691207015494,
177.963957333703));
#35377=CARTESIAN_POINT('Ctrl Pts',(-56.2712967053373,-68.3686210341301,
178.241059727161));
#35378=CARTESIAN_POINT('Ctrl Pts',(-55.6213846585,-68.3769887926366,178.685182361705));
#35379=CARTESIAN_POINT('Ctrl Pts',(-55.248611689035,-68.3838784978415,178.843189229673));
#35380=CARTESIAN_POINT('Ctrl Pts',(-54.4773946674087,-68.4017743316973,
179.001538701538));
#35381=CARTESIAN_POINT('Ctrl Pts',(-54.0876493921661,-68.4135161851992,
179.005828413077));
#35382=CARTESIAN_POINT('Ctrl Pts',(-53.3133690550624,-68.4351934355329,
178.86454982639));
#35383=CARTESIAN_POINT('Ctrl Pts',(-52.9371189732991,-68.4424571388153,
178.714706823925));
#35384=CARTESIAN_POINT('Ctrl Pts',(-52.2770947901846,-68.4484738928266,
178.284867845583));
#35385=CARTESIAN_POINT('Ctrl Pts',(-51.9967593790322,-68.4484865578345,
178.013740507156));
#35386=CARTESIAN_POINT('Ctrl Pts',(-51.5448249819886,-68.4358481303952,
177.36894097706));
#35387=CARTESIAN_POINT('Ctrl Pts',(-51.3820548446593,-68.4203568417544,
176.998229323375));
#35388=CARTESIAN_POINT('Ctrl Pts',(-51.2134814210369,-68.3739580476686,
176.230043037157));
#35389=CARTESIAN_POINT('Ctrl Pts',(-51.2039210351969,-68.3450410563414,
175.841184499056));
#35390=CARTESIAN_POINT('Ctrl Pts',(-51.3338285231955,-68.2704205523978,
175.067912287805));
#35391=CARTESIAN_POINT('Ctrl Pts',(-51.4774363099468,-68.2222707731338,
174.692005191722));
#35392=CARTESIAN_POINT('Ctrl Pts',(-51.8688199864617,-68.1201595974737,
174.073557295704));
#35393=CARTESIAN_POINT('Ctrl Pts',(-52.0935008498987,-68.0691078954907,
173.824057504042));
#35394=CARTESIAN_POINT('Ctrl Pts',(-52.354402310021,-68.0158107614237,173.617797875547));
#35395=CARTESIAN_POINT('Origin',(-54.1598171290174,-67.5719248685924,175.985485069079));
#35396=CARTESIAN_POINT('',(-55.2910412295901,-67.4513288218828,173.209554841606));
#35397=CARTESIAN_POINT('Origin',(-54.1598171290174,-67.5719248685924,175.985485069079));
#35398=CARTESIAN_POINT('',(-52.706375385453,-66.9726216402874,174.209719673931));
#35399=CARTESIAN_POINT('',(-52.327900808713,-67.7672193871761,173.617797875548));
#35400=CARTESIAN_POINT('Origin',(-54.0803126256813,-66.8261507513496,175.985485069079));
#35401=CARTESIAN_POINT('Origin',(-54.1598171290174,-67.5719248685924,175.985485069079));
#35402=CARTESIAN_POINT('Origin',(-67.1996360619082,-123.504780015625,174.720045501779));
#35403=CARTESIAN_POINT('',(-67.5442983916463,-127.490702460407,175.213634544043));
#35404=CARTESIAN_POINT('',(-67.378281909146,-127.50840092658,174.285183152721));
#35405=CARTESIAN_POINT('Ctrl Pts',(-67.5442983916463,-127.490702460407,
175.213634544043));
#35406=CARTESIAN_POINT('Ctrl Pts',(-67.5304234891054,-127.360552056844,
175.213634544043));
#35407=CARTESIAN_POINT('Ctrl Pts',(-67.4911232584415,-127.242343176682,
175.210516120998));
#35408=CARTESIAN_POINT('Ctrl Pts',(-67.3976318102772,-127.064966904856,
175.187583073578));
#35409=CARTESIAN_POINT('Ctrl Pts',(-67.3485764499634,-126.998815494605,
175.171030834297));
#35410=CARTESIAN_POINT('Ctrl Pts',(-67.2614371723049,-126.906024647463,
175.122511770945));
#35411=CARTESIAN_POINT('Ctrl Pts',(-67.2236083564389,-126.872997757826,
175.095959464675));
#35412=CARTESIAN_POINT('Ctrl Pts',(-67.1587175920526,-126.825313378244,
175.031998610409));
#35413=CARTESIAN_POINT('Ctrl Pts',(-67.1319329002808,-126.808954737066,
174.998533042655));
#35414=CARTESIAN_POINT('Ctrl Pts',(-67.0934708749846,-126.789346268891,
174.932406978357));
#35415=CARTESIAN_POINT('Ctrl Pts',(-67.0799671384498,-126.783835828759,
174.902724578504));
#35416=CARTESIAN_POINT('Ctrl Pts',(-67.0658545717287,-126.779903311541,
174.859846346238));
#35417=CARTESIAN_POINT('Ctrl Pts',(-67.0624952310764,-126.779206031814,
174.848108401062));
#35418=CARTESIAN_POINT('Ctrl Pts',(-67.0577545525741,-126.778661978635,
174.828612174569));
#35419=CARTESIAN_POINT('Ctrl Pts',(-67.0560975302196,-126.778598171298,
174.820956534739));
#35420=CARTESIAN_POINT('Ctrl Pts',(-67.053284270024,-126.778764593349,174.806117475444));
#35421=CARTESIAN_POINT('Ctrl Pts',(-67.0520995699636,-126.778972273436,
174.798946406207));
#35422=CARTESIAN_POINT('Ctrl Pts',(-67.0497682417782,-126.779748480161,
174.782376171418));
#35423=CARTESIAN_POINT('Ctrl Pts',(-67.0487395242194,-126.780404802314,
174.772964425168));
#35424=CARTESIAN_POINT('Ctrl Pts',(-67.0464880300302,-126.783095278756,
174.744041184592));
#35425=CARTESIAN_POINT('Ctrl Pts',(-67.0462281439738,-126.785837729554,
174.724538074904));
#35426=CARTESIAN_POINT('Ctrl Pts',(-67.0493621086417,-126.79773925412,174.662248799475));
#35427=CARTESIAN_POINT('Ctrl Pts',(-67.0575397367902,-126.810420103395,
174.620975896735));
#35428=CARTESIAN_POINT('Ctrl Pts',(-67.0834419506324,-126.845331488276,
174.543860152732));
#35429=CARTESIAN_POINT('Ctrl Pts',(-67.1008154234339,-126.867155779968,
174.50915449495));
#35430=CARTESIAN_POINT('Ctrl Pts',(-67.1455893123903,-126.926226076948,
174.439800207307));
#35431=CARTESIAN_POINT('Ctrl Pts',(-67.1735543698667,-126.965002079791,
174.408765925659));
#35432=CARTESIAN_POINT('Ctrl Pts',(-67.2372224196924,-127.066221558354,
174.350903316986));
#35433=CARTESIAN_POINT('Ctrl Pts',(-67.2736593363266,-127.133754028887,
174.327643511702));
#35434=CARTESIAN_POINT('Ctrl Pts',(-67.3393575884572,-127.299090717255,
174.293845322914));
#35435=CARTESIAN_POINT('Ctrl Pts',(-67.3666704557199,-127.399482298509,
174.285183152721));
#35436=CARTESIAN_POINT('Ctrl Pts',(-67.378281909146,-127.50840092658,174.285183152721));
#35437=CARTESIAN_POINT('',(-67.9083119313868,-132.480228374865,174.285183152721));
#35438=CARTESIAN_POINT('',(-67.4842879135942,-128.502766416237,174.285183152721));
#35439=CARTESIAN_POINT('',(-68.0743284138871,-132.462529908692,175.213634544043));
#35440=CARTESIAN_POINT('Ctrl Pts',(-67.9083119313868,-132.480228374865,
174.285183152721));
#35441=CARTESIAN_POINT('Ctrl Pts',(-67.9221868339278,-132.61037877843,174.285183152721));
#35442=CARTESIAN_POINT('Ctrl Pts',(-67.9114244081542,-132.733924672231,
174.297355020201));
#35443=CARTESIAN_POINT('Ctrl Pts',(-67.8699924093024,-132.925684684914,
174.344687930061));
#35444=CARTESIAN_POINT('Ctrl Pts',(-67.8443212202638,-132.999802444567,
174.374753888159));
#35445=CARTESIAN_POINT('Ctrl Pts',(-67.8002951023317,-133.106576399184,
174.446993199403));
#35446=CARTESIAN_POINT('Ctrl Pts',(-67.7816024584963,-133.145628854038,
174.483766974752));
#35447=CARTESIAN_POINT('Ctrl Pts',(-67.7540846388161,-133.203164606054,
174.564439207132));
#35448=CARTESIAN_POINT('Ctrl Pts',(-67.7444947926817,-133.223401015987,
174.604482828893));
#35449=CARTESIAN_POINT('Ctrl Pts',(-67.7361912381367,-133.247995007409,
174.679066086809));
#35450=CARTESIAN_POINT('Ctrl Pts',(-67.7352352888166,-133.255046946657,
174.711363409076));
#35451=CARTESIAN_POINT('Ctrl Pts',(-67.7379709489151,-133.260192318128,
174.756299066962));
#35452=CARTESIAN_POINT('Ctrl Pts',(-67.7391038286292,-133.261126953466,
174.768439650388));
#35453=CARTESIAN_POINT('Ctrl Pts',(-67.7416282991207,-133.261907269226,
174.78833666097));
#35454=CARTESIAN_POINT('Ctrl Pts',(-67.7427762424715,-133.262025347786,
174.796084363802));
#35455=CARTESIAN_POINT('Ctrl Pts',(-67.7453070065055,-133.261889041713,
174.810974510343));
#35456=CARTESIAN_POINT('Ctrl Pts',(-67.7466640942182,-133.26166298395,174.818114404605));
#35457=CARTESIAN_POINT('Ctrl Pts',(-67.7501112910221,-133.260767818176,
174.834482843182));
#35458=CARTESIAN_POINT('Ctrl Pts',(-67.7522957860694,-133.259988282421,
174.843685576008));
#35459=CARTESIAN_POINT('Ctrl Pts',(-67.7597044638537,-133.256748015752,
174.871676179795));
#35460=CARTESIAN_POINT('Ctrl Pts',(-67.7656627036566,-133.253398082375,
174.890148786256));
#35461=CARTESIAN_POINT('Ctrl Pts',(-67.7876797926514,-133.238815287458,
174.947889688046));
#35462=CARTESIAN_POINT('Ctrl Pts',(-67.8068751667408,-133.223216293268,
174.984212394924));
#35463=CARTESIAN_POINT('Ctrl Pts',(-67.8501756899867,-133.180927434277,
175.048813358858));
#35464=CARTESIAN_POINT('Ctrl Pts',(-67.8736483858866,-133.154748668112,
175.07613230277));
#35465=CARTESIAN_POINT('Ctrl Pts',(-67.9266051867934,-133.085259626664,
175.127812750604));
#35466=CARTESIAN_POINT('Ctrl Pts',(-67.9550417444708,-133.040470834833,
175.148647236133));
#35467=CARTESIAN_POINT('Ctrl Pts',(-68.0127093306509,-132.92631616684,175.184567232953));
#35468=CARTESIAN_POINT('Ctrl Pts',(-68.0403368828129,-132.851953995925,
175.196241474271));
#35469=CARTESIAN_POINT('Ctrl Pts',(-68.0784333077652,-132.675552101541,
175.211269198035));
#35470=CARTESIAN_POINT('Ctrl Pts',(-68.0859398673133,-132.571448536764,
175.213634544043));
#35471=CARTESIAN_POINT('Ctrl Pts',(-68.0743284138871,-132.462529908693,
175.213634544043));
#35472=CARTESIAN_POINT('',(-67.6503043960945,-128.485067950064,175.213634544043));
#35473=CARTESIAN_POINT('Origin',(-67.297435265312,-123.494353967156,176.440911705352));
#35474=CARTESIAN_POINT('',(-67.5269456805235,-127.492552375344,176.901057832219));
#35475=CARTESIAN_POINT('',(-67.5866943482154,-127.486182768194,175.959630076611));
#35476=CARTESIAN_POINT('Ctrl Pts',(-67.5269456805235,-127.492552375344,
176.901057832219));
#35477=CARTESIAN_POINT('Ctrl Pts',(-67.5130707779826,-127.362401971781,
176.901057832219));
#35478=CARTESIAN_POINT('Ctrl Pts',(-67.4752797181248,-127.244032203929,
176.891676686497));
#35479=CARTESIAN_POINT('Ctrl Pts',(-67.3893884463034,-127.065845702528,
176.851661970524));
#35480=CARTESIAN_POINT('Ctrl Pts',(-67.3454787971686,-126.999145725087,
176.825595328984));
#35481=CARTESIAN_POINT('Ctrl Pts',(-67.2721049050013,-126.904887395887,
176.760103849711));
#35482=CARTESIAN_POINT('Ctrl Pts',(-67.2415803914411,-126.871081818825,
176.726158942161));
#35483=CARTESIAN_POINT('Ctrl Pts',(-67.1936285768875,-126.821591634024,
176.649824498254));
#35484=CARTESIAN_POINT('Ctrl Pts',(-67.1755270558813,-126.804307308831,
176.611372500654));
#35485=CARTESIAN_POINT('Ctrl Pts',(-67.1538458843564,-126.782909889533,
176.538512682906));
#35486=CARTESIAN_POINT('Ctrl Pts',(-67.1477766927268,-126.776606877245,
176.506619146556));
#35487=CARTESIAN_POINT('Ctrl Pts',(-67.1442611725493,-126.771544644068,
176.461728312898));
#35488=CARTESIAN_POINT('Ctrl Pts',(-67.1437894619215,-126.770539523688,
176.449549727278));
#35489=CARTESIAN_POINT('Ctrl Pts',(-67.1438227876615,-126.769486529762,
176.429505701555));
#35490=CARTESIAN_POINT('Ctrl Pts',(-67.144034970312,-126.769223452683,176.421679822394));
#35491=CARTESIAN_POINT('Ctrl Pts',(-67.1448342594165,-126.769004752843,
176.406598273492));
#35492=CARTESIAN_POINT('Ctrl Pts',(-67.1453907133999,-126.769026814277,
176.399348394079));
#35493=CARTESIAN_POINT('Ctrl Pts',(-67.1470719186259,-126.769375258133,
176.382685188959));
#35494=CARTESIAN_POINT('Ctrl Pts',(-67.1483144553802,-126.769789449402,
176.373285479704));
#35495=CARTESIAN_POINT('Ctrl Pts',(-67.153018674885,-126.771738400295,176.34459865966));
#35496=CARTESIAN_POINT('Ctrl Pts',(-67.1574157570097,-126.773984387172,
176.325530857575));
#35497=CARTESIAN_POINT('Ctrl Pts',(-67.1753189387193,-126.784311414529,
176.265495447643));
#35498=CARTESIAN_POINT('Ctrl Pts',(-67.1931220500515,-126.79596612299,176.227046168864));
#35499=CARTESIAN_POINT('Ctrl Pts',(-67.2367380042605,-126.828989104805,
176.157449483168));
#35500=CARTESIAN_POINT('Ctrl Pts',(-67.2619379655662,-126.849979040534,
176.127332967841));
#35501=CARTESIAN_POINT('Ctrl Pts',(-67.3221104066357,-126.907407748984,
176.069150160125));
#35502=CARTESIAN_POINT('Ctrl Pts',(-67.3567758945455,-126.945469441177,
176.044688741343));
#35503=CARTESIAN_POINT('Ctrl Pts',(-67.4326940953435,-127.045382971805,
176.0010905983));
#35504=CARTESIAN_POINT('Ctrl Pts',(-67.4738260419191,-127.112414920779,
175.985464248772));
#35505=CARTESIAN_POINT('Ctrl Pts',(-67.5461859605276,-127.277041430993,
175.964087796028));
#35506=CARTESIAN_POINT('Ctrl Pts',(-67.5750828947892,-127.377264140122,
175.959630076611));
#35507=CARTESIAN_POINT('Ctrl Pts',(-67.5866943482154,-127.486182768194,
175.959630076611));
#35508=CARTESIAN_POINT('',(-68.1167243704562,-132.458010216479,175.959630076611));
#35509=CARTESIAN_POINT('',(-67.6927003526636,-128.480548257851,175.959630076611));
#35510=CARTESIAN_POINT('',(-68.0569757027642,-132.46437982363,176.901057832219));
#35511=CARTESIAN_POINT('Ctrl Pts',(-68.1167243704562,-132.458010216479,
175.959630076611));
#35512=CARTESIAN_POINT('Ctrl Pts',(-68.1305992729972,-132.588160620043,
175.959630076611));
#35513=CARTESIAN_POINT('Ctrl Pts',(-68.1176279830643,-132.711941993521,
175.96575292391));
#35514=CARTESIAN_POINT('Ctrl Pts',(-68.0667100701608,-132.904713268018,
175.996986227033));
#35515=CARTESIAN_POINT('Ctrl Pts',(-68.0348487653193,-132.979490935371,
176.01818933525));
#35516=CARTESIAN_POINT('Ctrl Pts',(-67.9752240480408,-133.087927804889,
176.07514399223));
#35517=CARTESIAN_POINT('Ctrl Pts',(-67.9484371380331,-133.127843162595,
176.105410233963));
#35518=CARTESIAN_POINT('Ctrl Pts',(-67.9026888335392,-133.187322406088,
176.175730319761));
#35519=CARTESIAN_POINT('Ctrl Pts',(-67.8839074332612,-133.2085386971,176.211814902049));
#35520=CARTESIAN_POINT('Ctrl Pts',(-67.858169412698,-133.234991319078,176.281631009657));
#35521=CARTESIAN_POINT('Ctrl Pts',(-67.8495768248006,-133.242857375017,
176.312583445894));
#35522=CARTESIAN_POINT('Ctrl Pts',(-67.8415564306939,-133.249149413727,
176.356733820306));
#35523=CARTESIAN_POINT('Ctrl Pts',(-67.8397705625796,-133.250395207083,
176.36876749803));
#35524=CARTESIAN_POINT('Ctrl Pts',(-67.8374900543234,-133.251687765679,
176.388667283164));
#35525=CARTESIAN_POINT('Ctrl Pts',(-67.8367616776014,-133.252005872494,
176.396460029218));
#35526=CARTESIAN_POINT('Ctrl Pts',(-67.8356759440695,-133.252255109224,
176.411523192025));
#35527=CARTESIAN_POINT('Ctrl Pts',(-67.8352942870893,-133.252214413261,
176.418784291187));
#35528=CARTESIAN_POINT('Ctrl Pts',(-67.834744546255,-133.251745347742,176.435520121956));
#35529=CARTESIAN_POINT('Ctrl Pts',(-67.8346739405432,-133.251206220794,
176.444995054306));
#35530=CARTESIAN_POINT('Ctrl Pts',(-67.8351989832514,-133.248699795614,
176.474017526598));
#35531=CARTESIAN_POINT('Ctrl Pts',(-67.8365798970763,-133.245837835766,
176.493456202671));
#35532=CARTESIAN_POINT('Ctrl Pts',(-67.8441792890309,-133.232792063676,
176.555128554074));
#35533=CARTESIAN_POINT('Ctrl Pts',(-67.8541317546755,-133.218178425277,
176.595359388534));
#35534=CARTESIAN_POINT('Ctrl Pts',(-67.8806857394292,-133.177674859172,
176.669460093496));
#35535=CARTESIAN_POINT('Ctrl Pts',(-67.8969028272927,-133.152269589298,
176.702235057584));
#35536=CARTESIAN_POINT('Ctrl Pts',(-67.9358269946965,-133.084276520331,
176.766778609521));
#35537=CARTESIAN_POINT('Ctrl Pts',(-67.9583514108175,-133.040118002288,
176.794910894109));
#35538=CARTESIAN_POINT('Ctrl Pts',(-68.0054646756924,-132.927088495458,
176.846406095349));
#35539=CARTESIAN_POINT('Ctrl Pts',(-68.0292925855365,-132.853131391799,
176.866202042985));
#35540=CARTESIAN_POINT('Ctrl Pts',(-68.0621780150446,-132.677285024345,
176.894333910976));
#35541=CARTESIAN_POINT('Ctrl Pts',(-68.0685871561905,-132.573298451701,
176.901057832219));
#35542=CARTESIAN_POINT('Ctrl Pts',(-68.0569757027643,-132.46437982363,176.901057832219));
#35543=CARTESIAN_POINT('',(-67.6329516849716,-128.486917865001,176.901057832219));
#35544=CARTESIAN_POINT('Origin',(-66.9828828246889,-123.527887358818,178.135310168233));
#35545=CARTESIAN_POINT('',(-67.1085457489275,-127.537156603338,178.535271359373));
#35546=CARTESIAN_POINT('',(-67.390587191423,-127.507089101279,177.635579598685));
#35547=CARTESIAN_POINT('Ctrl Pts',(-67.1085457489275,-127.537156603338,
178.535271359373));
#35548=CARTESIAN_POINT('Ctrl Pts',(-67.0946708463865,-127.407006199774,
178.535271359373));
#35549=CARTESIAN_POINT('Ctrl Pts',(-67.0598354263899,-127.288321340966,
178.520172689065));
#35550=CARTESIAN_POINT('Ctrl Pts',(-66.9853883610814,-127.108914810696,
178.465401814383));
#35551=CARTESIAN_POINT('Ctrl Pts',(-66.9487390141347,-127.041440836536,
178.431335669042));
#35552=CARTESIAN_POINT('Ctrl Pts',(-66.892769389307,-126.945327096161,178.352677900572));
#35553=CARTESIAN_POINT('Ctrl Pts',(-66.8710961252085,-126.910577916772,
178.313313146384));
#35554=CARTESIAN_POINT('Ctrl Pts',(-66.842535554338,-126.859020495843,178.229041393252));
#35555=CARTESIAN_POINT('Ctrl Pts',(-66.8340514938727,-126.840710885103,
178.187837656138));
#35556=CARTESIAN_POINT('Ctrl Pts',(-66.8302659677143,-126.81740567045,178.112478432712));
#35557=CARTESIAN_POINT('Ctrl Pts',(-66.8319414646711,-126.810277022617,
178.080227296269));
#35558=CARTESIAN_POINT('Ctrl Pts',(-66.8391939933177,-126.804066843496,
178.0359327533));
#35559=CARTESIAN_POINT('Ctrl Pts',(-66.8416308614233,-126.802751649191,
178.024021302365));
#35560=CARTESIAN_POINT('Ctrl Pts',(-66.8464298257885,-126.801190606348,
178.00459436333));
#35561=CARTESIAN_POINT('Ctrl Pts',(-66.848497409127,-126.800729731161,177.99705305649));
#35562=CARTESIAN_POINT('Ctrl Pts',(-66.8528619779962,-126.800130948679,
177.982605502784));
#35563=CARTESIAN_POINT('Ctrl Pts',(-66.855127745491,-126.799970785872,177.975698149833));
#35564=CARTESIAN_POINT('Ctrl Pts',(-66.860727011093,-126.799901538316,177.959910379297));
#35565=CARTESIAN_POINT('Ctrl Pts',(-66.8641719392271,-126.80008093995,177.951068983973));
#35566=CARTESIAN_POINT('Ctrl Pts',(-66.8755734916867,-126.801315910406,
177.92428575817));
#35567=CARTESIAN_POINT('Ctrl Pts',(-66.884388630013,-126.803090902975,177.906761415035));
#35568=CARTESIAN_POINT('Ctrl Pts',(-66.9160955160124,-126.811946363234,
177.852468910406));
#35569=CARTESIAN_POINT('Ctrl Pts',(-66.9425724814864,-126.822676380895,
177.819077787913));
#35570=CARTESIAN_POINT('Ctrl Pts',(-67.001598157425,-126.854056583422,177.761044866923));
#35571=CARTESIAN_POINT('Ctrl Pts',(-67.0333051181494,-126.87435282954,177.737267756454));
#35572=CARTESIAN_POINT('Ctrl Pts',(-67.105770211174,-126.930471059166,177.693637801963));
#35573=CARTESIAN_POINT('Ctrl Pts',(-67.1453773011662,-126.968005943563,
177.677170854792));
#35574=CARTESIAN_POINT('Ctrl Pts',(-67.2297952103285,-127.067013348492,
177.650370942981));
#35575=CARTESIAN_POINT('Ctrl Pts',(-67.2736692454281,-127.13375297251,177.643286195844));
#35576=CARTESIAN_POINT('Ctrl Pts',(-67.3495412883826,-127.298005066807,
177.635573800874));
#35577=CARTESIAN_POINT('Ctrl Pts',(-67.3789757379969,-127.398170473209,
177.635579598685));
#35578=CARTESIAN_POINT('Ctrl Pts',(-67.390587191423,-127.507089101279,177.635579598685));
#35579=CARTESIAN_POINT('',(-67.9206172136638,-132.478916549564,177.635579598685));
#35580=CARTESIAN_POINT('',(-67.4965931958712,-128.501454590936,177.635579598685));
#35581=CARTESIAN_POINT('',(-67.6385757711683,-132.508984051623,178.535271359373));
#35582=CARTESIAN_POINT('Ctrl Pts',(-67.9206172136638,-132.478916549564,
177.635579598685));
#35583=CARTESIAN_POINT('Ctrl Pts',(-67.9344921162048,-132.609066953128,
177.635579598685));
#35584=CARTESIAN_POINT('Ctrl Pts',(-67.9208156163139,-132.732923506699,
177.635297588174));
#35585=CARTESIAN_POINT('Ctrl Pts',(-67.8645186117248,-132.926268228307,
177.64861611851));
#35586=CARTESIAN_POINT('Ctrl Pts',(-67.8287561325003,-133.001461786913,
177.659724129265));
#35587=CARTESIAN_POINT('Ctrl Pts',(-67.7576233297767,-133.111125495223,
177.698084134341));
#35588=CARTESIAN_POINT('Ctrl Pts',(-67.7245259380598,-133.151713592439,
177.720083878501));
#35589=CARTESIAN_POINT('Ctrl Pts',(-67.6635403652347,-133.212817230535,
177.775965069934));
#35590=CARTESIAN_POINT('Ctrl Pts',(-67.6367766223592,-133.234884492597,
177.805993507988));
#35591=CARTESIAN_POINT('Ctrl Pts',(-67.5952451752651,-133.263020799357,
177.866985006884));
#35592=CARTESIAN_POINT('Ctrl Pts',(-67.5795578944418,-133.271643196961,
177.894793714006));
#35593=CARTESIAN_POINT('Ctrl Pts',(-67.5612808692556,-133.279028661068,
177.935592945663));
#35594=CARTESIAN_POINT('Ctrl Pts',(-67.5566865068749,-133.280573858676,
177.946820364077));
#35595=CARTESIAN_POINT('Ctrl Pts',(-67.5497399835682,-133.282363845649,
177.965566420584));
#35596=CARTESIAN_POINT('Ctrl Pts',(-67.5471790904136,-133.282877310959,
177.972951323785));
#35597=CARTESIAN_POINT('Ctrl Pts',(-67.5425407759596,-133.283505276549,
177.987312086586));
#35598=CARTESIAN_POINT('Ctrl Pts',(-67.5404420562521,-133.283647630945,
177.994272401957));
#35599=CARTESIAN_POINT('Ctrl Pts',(-67.5359240942179,-133.283601604317,
178.010402999268));
#35600=CARTESIAN_POINT('Ctrl Pts',(-67.5335991423078,-133.283302805735,
178.019599482513));
#35601=CARTESIAN_POINT('Ctrl Pts',(-67.527195024967,-133.281535075309,178.047967142713));
#35602=CARTESIAN_POINT('Ctrl Pts',(-67.5239017286705,-133.279171417488,
178.067242183202));
#35603=CARTESIAN_POINT('Ctrl Pts',(-67.5165668194536,-133.267717741678,
178.129261811322));
#35604=CARTESIAN_POINT('Ctrl Pts',(-67.5166149524489,-133.254159971309,
178.171062703501));
#35605=CARTESIAN_POINT('Ctrl Pts',(-67.524648395552,-133.215630818677,178.250356685862));
#35606=CARTESIAN_POINT('Ctrl Pts',(-67.5325223561117,-133.191114981914,
178.286682908347));
#35607=CARTESIAN_POINT('Ctrl Pts',(-67.5547606554873,-133.124900737955,
178.360338527753));
#35608=CARTESIAN_POINT('Ctrl Pts',(-67.5698080890573,-133.081539316205,
178.394133665277));
#35609=CARTESIAN_POINT('Ctrl Pts',(-67.6029673336494,-132.969997401164,
178.458211357017));
#35610=CARTESIAN_POINT('Ctrl Pts',(-67.6211733118579,-132.896639632977,
178.484978542452));
#35611=CARTESIAN_POINT('Ctrl Pts',(-67.6458808109757,-132.721665087537,
178.524579632757));
#35612=CARTESIAN_POINT('Ctrl Pts',(-67.6501872245945,-132.617902679695,
178.535271359373));
#35613=CARTESIAN_POINT('Ctrl Pts',(-67.6385757711684,-132.508984051624,
178.535271359373));
#35614=CARTESIAN_POINT('',(-67.2145517533757,-128.531522092995,178.535271359373));
#35615=CARTESIAN_POINT('Origin',(-66.2742593845362,-123.603431351777,179.704768610648));
#35616=CARTESIAN_POINT('',(-66.313414480061,-127.621922908787,180.021300575431));
#35617=CARTESIAN_POINT('',(-66.8013574739011,-127.569904925748,179.215631624547));
#35618=CARTESIAN_POINT('Ctrl Pts',(-66.3134144800609,-127.621922908787,
180.021300575431));
#35619=CARTESIAN_POINT('Ctrl Pts',(-66.2995395775199,-127.491772505223,
180.021300575431));
#35620=CARTESIAN_POINT('Ctrl Pts',(-66.2689344953941,-127.372636664135,
180.001361860373));
#35621=CARTESIAN_POINT('Ctrl Pts',(-66.2091105710828,-127.19167120934,179.935017911137));
#35622=CARTESIAN_POINT('Ctrl Pts',(-66.1814141749603,-127.123242790809,
179.894932062535));
#35623=CARTESIAN_POINT('Ctrl Pts',(-66.1454762265654,-127.024993539896,
179.807679308462));
#35624=CARTESIAN_POINT('Ctrl Pts',(-66.133686756639,-126.989190682016,179.765182444064));
#35625=CARTESIAN_POINT('Ctrl Pts',(-66.1258427747035,-126.935424734301,
179.677870949684));
#35626=CARTESIAN_POINT('Ctrl Pts',(-66.1273515327055,-126.916049822352,
179.636310084488));
#35627=CARTESIAN_POINT('Ctrl Pts',(-66.1415364136483,-126.890828842243,
179.562831059531));
#35628=CARTESIAN_POINT('Ctrl Pts',(-66.1508166497229,-126.882889478414,
179.532096641817));
#35629=CARTESIAN_POINT('Ctrl Pts',(-66.1683824296169,-126.875579837807,
179.490972627369));
#35630=CARTESIAN_POINT('Ctrl Pts',(-66.173579789141,-126.873970356674,179.480020561352));
#35631=CARTESIAN_POINT('Ctrl Pts',(-66.1828590649194,-126.871931682703,
179.462339732087));
#35632=CARTESIAN_POINT('Ctrl Pts',(-66.1866604154849,-126.871285976346,
179.455521270909));
#35633=CARTESIAN_POINT('Ctrl Pts',(-66.1943357934833,-126.870334239492,
179.442547351705));
#35634=CARTESIAN_POINT('Ctrl Pts',(-66.1981796948696,-126.870005837069,
179.436383955464));
#35635=CARTESIAN_POINT('Ctrl Pts',(-66.2073748443838,-126.869553244264,
179.422389147348));
#35636=CARTESIAN_POINT('Ctrl Pts',(-66.2128253059833,-126.869518842632,
179.414619895715));
#35637=CARTESIAN_POINT('Ctrl Pts',(-66.2302765860103,-126.870108871711,
179.391296807883));
#35638=CARTESIAN_POINT('Ctrl Pts',(-66.2430141071915,-126.871465712063,
179.376334374823));
#35639=CARTESIAN_POINT('Ctrl Pts',(-66.28675696361,-126.879038057464,179.330940058521));
#35640=CARTESIAN_POINT('Ctrl Pts',(-66.3204520613092,-126.888998574006,
179.304547662982));
#35641=CARTESIAN_POINT('Ctrl Pts',(-66.3916878833257,-126.919077093387,
179.261451169124));
#35642=CARTESIAN_POINT('Ctrl Pts',(-66.4282041912291,-126.938860630965,
179.245395302747));
#35643=CARTESIAN_POINT('Ctrl Pts',(-66.509141631801,-126.994075651739,179.218853815848));
#35644=CARTESIAN_POINT('Ctrl Pts',(-66.5516443075739,-127.031301847347,
179.211338339403));
#35645=CARTESIAN_POINT('Ctrl Pts',(-66.6403175103417,-127.129855609551,
179.202894172283));
#35646=CARTESIAN_POINT('Ctrl Pts',(-66.6848213323291,-127.196528094079,
179.204762767289));
#35647=CARTESIAN_POINT('Ctrl Pts',(-66.7608518455908,-127.360763294379,
179.211162646458));
#35648=CARTESIAN_POINT('Ctrl Pts',(-66.7897460204748,-127.460986297676,
179.215631624547));
#35649=CARTESIAN_POINT('Ctrl Pts',(-66.8013574739011,-127.569904925748,
179.215631624547));
#35650=CARTESIAN_POINT('',(-67.3313874961418,-132.541732374034,179.215631624547));
#35651=CARTESIAN_POINT('',(-66.9073634783493,-128.564270415405,179.215631624547));
#35652=CARTESIAN_POINT('',(-66.8434445023017,-132.593750357073,180.021300575431));
#35653=CARTESIAN_POINT('Ctrl Pts',(-67.3313874961418,-132.541732374034,
179.215631624547));
#35654=CARTESIAN_POINT('Ctrl Pts',(-67.3452623986828,-132.671882777597,
179.215631624547));
#35655=CARTESIAN_POINT('Ctrl Pts',(-67.3324253272744,-132.795649842484,
179.208961145653));
#35656=CARTESIAN_POINT('Ctrl Pts',(-67.2751686666225,-132.989096869839,
179.203590878629));
#35657=CARTESIAN_POINT('Ctrl Pts',(-67.2380206765098,-133.064438133162,
179.203958234714));
#35658=CARTESIAN_POINT('Ctrl Pts',(-67.1601391103383,-133.174821304745,
179.221494243823));
#35659=CARTESIAN_POINT('Ctrl Pts',(-67.1228817636348,-133.215852880954,
179.233948945246));
#35660=CARTESIAN_POINT('Ctrl Pts',(-67.0505376736116,-133.278167412868,
179.272143630587));
#35661=CARTESIAN_POINT('Ctrl Pts',(-67.0174647044214,-133.300907280607,
179.294370780736));
#35662=CARTESIAN_POINT('Ctrl Pts',(-66.9626987268264,-133.330454476737,
179.342993066701));
#35663=CARTESIAN_POINT('Ctrl Pts',(-66.9408710164934,-133.33973148515,179.36604190373));
#35664=CARTESIAN_POINT('Ctrl Pts',(-66.9134328614723,-133.348093586901,
179.401118889585));
#35665=CARTESIAN_POINT('Ctrl Pts',(-66.9063034778645,-133.349909034709,
179.410887551941));
#35666=CARTESIAN_POINT('Ctrl Pts',(-66.8951010750377,-133.352152726872,
179.427390427158));
#35667=CARTESIAN_POINT('Ctrl Pts',(-66.890857968285,-133.35284552739,179.433938303775));
#35668=CARTESIAN_POINT('Ctrl Pts',(-66.8829374526434,-133.353823397555,
179.446762071235));
#35669=CARTESIAN_POINT('Ctrl Pts',(-66.8792431416185,-133.354135852645,
179.453017094585));
#35670=CARTESIAN_POINT('Ctrl Pts',(-66.871016293415,-133.354485218061,179.467605006754));
#35671=CARTESIAN_POINT('Ctrl Pts',(-66.8665687642743,-133.354412700393,
179.475988574717));
#35672=CARTESIAN_POINT('Ctrl Pts',(-66.853592659507,-133.353345587733,179.502052797526));
#35673=CARTESIAN_POINT('Ctrl Pts',(-66.8457999170483,-133.351461600934,
179.520044007139));
#35674=CARTESIAN_POINT('Ctrl Pts',(-66.8238820298286,-133.341562568005,
179.578806556624));
#35675=CARTESIAN_POINT('Ctrl Pts',(-66.8139400097828,-133.329069814694,
179.619748190606));
#35676=CARTESIAN_POINT('Ctrl Pts',(-66.8027552546388,-133.29258945039,179.699627172334));
#35677=CARTESIAN_POINT('Ctrl Pts',(-66.8016834408603,-133.269027292937,
179.737393505205));
#35678=CARTESIAN_POINT('Ctrl Pts',(-66.8055523596816,-133.204771347669,
179.815880595208));
#35679=CARTESIAN_POINT('Ctrl Pts',(-66.8119925047541,-133.162327520377,
179.853374535115));
#35680=CARTESIAN_POINT('Ctrl Pts',(-66.8286089870249,-133.052549174321,
179.926310754825));
#35681=CARTESIAN_POINT('Ctrl Pts',(-66.8396974705112,-132.979950178623,
179.958493566535));
#35682=CARTESIAN_POINT('Ctrl Pts',(-66.8537353758802,-132.806113083157,
180.00726240773));
#35683=CARTESIAN_POINT('Ctrl Pts',(-66.8550559557278,-132.702668985143,
180.021300575431));
#35684=CARTESIAN_POINT('Ctrl Pts',(-66.8434445023018,-132.593750357073,
180.021300575431));
#35685=CARTESIAN_POINT('',(-66.4194204845091,-128.616288398444,180.021300575431));
#35686=CARTESIAN_POINT('Origin',(-65.2127475634542,-123.716595603752,181.058075812673));
#35687=CARTESIAN_POINT('',(-65.1877620130857,-127.741924982132,181.272782863852));
#35688=CARTESIAN_POINT('',(-65.8532490850691,-127.67097961421,180.607959273711));
#35689=CARTESIAN_POINT('Ctrl Pts',(-65.1877620130857,-127.741924982132,
181.272782863852));
#35690=CARTESIAN_POINT('Ctrl Pts',(-65.1738871105448,-127.611774578569,
181.272782863852));
#35691=CARTESIAN_POINT('Ctrl Pts',(-65.1485412124394,-127.492078073329,
181.24916286969));
#35692=CARTESIAN_POINT('Ctrl Pts',(-65.1056695198069,-127.309305397378,
181.175101515076));
#35693=CARTESIAN_POINT('Ctrl Pts',(-65.0880984101856,-127.23979755566,181.131325607029));
#35694=CARTESIAN_POINT('Ctrl Pts',(-65.073655379095,-127.139256802958,181.04054868027));
#35695=CARTESIAN_POINT('Ctrl Pts',(-65.0722078378599,-127.102351426386,
180.997389468952));
#35696=CARTESIAN_POINT('Ctrl Pts',(-65.0852018172639,-127.046364012776,
180.912112460012));
#35697=CARTESIAN_POINT('Ctrl Pts',(-65.096498005373,-127.025945695389,180.872609833152));
#35698=CARTESIAN_POINT('Ctrl Pts',(-65.1276836804105,-126.998912317049,
180.805281340509));
#35699=CARTESIAN_POINT('Ctrl Pts',(-65.143986746339,-126.990224272638,180.777849814166));
#35700=CARTESIAN_POINT('Ctrl Pts',(-65.1708116112281,-126.981927551713,
180.74228630648));
#35701=CARTESIAN_POINT('Ctrl Pts',(-65.1784609451284,-126.98005667373,180.732930119647));
#35702=CARTESIAN_POINT('Ctrl Pts',(-65.1916748256948,-126.977598544601,
180.718022945683));
#35703=CARTESIAN_POINT('Ctrl Pts',(-65.1969875497771,-126.97679171573,180.712323594346));
#35704=CARTESIAN_POINT('Ctrl Pts',(-65.2075268540773,-126.975534665199,
180.70157730667));
#35705=CARTESIAN_POINT('Ctrl Pts',(-65.2127259943301,-126.975061785259,
180.696516061323));
#35706=CARTESIAN_POINT('Ctrl Pts',(-65.2249858715883,-126.974282472001,
180.68512754301));
#35707=CARTESIAN_POINT('Ctrl Pts',(-65.2321284544224,-126.97406767894,180.678881955732));
#35708=CARTESIAN_POINT('Ctrl Pts',(-65.2546302684554,-126.974119287352,
180.660374458958));
#35709=CARTESIAN_POINT('Ctrl Pts',(-65.2705665445107,-126.975135119064,
180.648843498197));
#35710=CARTESIAN_POINT('Ctrl Pts',(-65.3238781506254,-126.98168737182,180.614985522884));
#35711=CARTESIAN_POINT('Ctrl Pts',(-65.3629161670252,-126.991078297533,
180.597125684394));
#35712=CARTESIAN_POINT('Ctrl Pts',(-65.4424529501596,-127.020271879,180.571470229243));
#35713=CARTESIAN_POINT('Ctrl Pts',(-65.4818014512254,-127.039753485866,
180.564068715551));
#35714=CARTESIAN_POINT('Ctrl Pts',(-65.5668985528937,-127.094525058977,
180.556158190988));
#35715=CARTESIAN_POINT('Ctrl Pts',(-65.6100825172251,-127.131678624674,
180.558030957443));
#35716=CARTESIAN_POINT('Ctrl Pts',(-65.6985192966362,-127.230257591184,
180.568433279314));
#35717=CARTESIAN_POINT('Ctrl Pts',(-65.741504002952,-127.297092023592,180.579146620513));
#35718=CARTESIAN_POINT('Ctrl Pts',(-65.8143301227709,-127.461668833645,
180.599286836105));
#35719=CARTESIAN_POINT('Ctrl Pts',(-65.841637631643,-127.562060986139,180.607959273711));
#35720=CARTESIAN_POINT('Ctrl Pts',(-65.8532490850691,-127.67097961421,180.607959273711));
#35721=CARTESIAN_POINT('',(-66.3832791073098,-132.642807062495,180.607959273711));
#35722=CARTESIAN_POINT('',(-65.9592550895172,-128.665345103867,180.607959273711));
#35723=CARTESIAN_POINT('',(-65.7177920353265,-132.713752430417,181.272782863852));
#35724=CARTESIAN_POINT('Ctrl Pts',(-66.3832791073099,-132.642807062495,
180.607959273711));
#35725=CARTESIAN_POINT('Ctrl Pts',(-66.3971540098509,-132.772957466059,
180.607959273711));
#35726=CARTESIAN_POINT('Ctrl Pts',(-66.3866522208333,-132.896475574241,
180.595287990419));
#35727=CARTESIAN_POINT('Ctrl Pts',(-66.3329111114629,-133.089547820342,
180.571541026436));
#35728=CARTESIAN_POINT('Ctrl Pts',(-66.2969737948129,-133.164760017786,
180.56114637845));
#35729=CARTESIAN_POINT('Ctrl Pts',(-66.217495000793,-133.275313464528,180.556839262484));
#35730=CARTESIAN_POINT('Ctrl Pts',(-66.1784699872881,-133.316533485828,
180.559025099194));
#35731=CARTESIAN_POINT('Ctrl Pts',(-66.0993062469322,-133.379575038029,
180.577313542163));
#35732=CARTESIAN_POINT('Ctrl Pts',(-66.0619638370107,-133.402770056673,
180.590447643233));
#35733=CARTESIAN_POINT('Ctrl Pts',(-65.9972913677529,-133.433373350998,
180.623874965741));
#35734=CARTESIAN_POINT('Ctrl Pts',(-65.9706343507697,-133.443165195765,
180.640824418047));
#35735=CARTESIAN_POINT('Ctrl Pts',(-65.9356629787224,-133.45233038878,180.668140611184));
#35736=CARTESIAN_POINT('Ctrl Pts',(-65.9264193731475,-133.454371226774,
180.675882798333));
#35737=CARTESIAN_POINT('Ctrl Pts',(-65.9116185625805,-133.456998533243,
180.689183405137));
#35738=CARTESIAN_POINT('Ctrl Pts',(-65.905941309204,-133.457844223372,180.694513716381));
#35739=CARTESIAN_POINT('Ctrl Pts',(-65.8951997217115,-133.459122838643,
180.705055217748));
#35740=CARTESIAN_POINT('Ctrl Pts',(-65.8901240207468,-133.45958255913,180.710241429858));
#35741=CARTESIAN_POINT('Ctrl Pts',(-65.8786631683877,-133.460276690995,
180.722438860454));
#35742=CARTESIAN_POINT('Ctrl Pts',(-65.8723481874574,-133.460403256164,
180.729522290637));
#35743=CARTESIAN_POINT('Ctrl Pts',(-65.8535392079069,-133.459957966925,
180.751768318165));
#35744=CARTESIAN_POINT('Ctrl Pts',(-65.8416832747013,-133.458507143405,
180.767430113195));
#35745=CARTESIAN_POINT('Ctrl Pts',(-65.8063812423218,-133.450034949769,
180.819520518261));
#35746=CARTESIAN_POINT('Ctrl Pts',(-65.7869438402254,-133.438554467622,
180.857223515098));
#35747=CARTESIAN_POINT('Ctrl Pts',(-65.7569601220642,-133.404078198369,
180.933045220123));
#35748=CARTESIAN_POINT('Ctrl Pts',(-65.7468597828011,-133.381478542051,
180.970056821388));
#35749=CARTESIAN_POINT('Ctrl Pts',(-65.7317433701701,-133.319246559955,
181.048813997606));
#35750=CARTESIAN_POINT('Ctrl Pts',(-65.7289461451197,-133.277787498032,
181.087827728394));
#35751=CARTESIAN_POINT('Ctrl Pts',(-65.7273925282462,-133.169946205937,
181.165383688096));
#35752=CARTESIAN_POINT('Ctrl Pts',(-65.7302815968463,-133.098221322645,
181.201111778045));
#35753=CARTESIAN_POINT('Ctrl Pts',(-65.7317783231141,-132.925721200658,
181.256214102347));
#35754=CARTESIAN_POINT('Ctrl Pts',(-65.7294034887527,-132.822671058489,
181.272782863852));
#35755=CARTESIAN_POINT('Ctrl Pts',(-65.7177920353265,-132.713752430418,
181.272782863852));
#35756=CARTESIAN_POINT('',(-65.2937680175338,-128.736290471789,181.272782863852));
#35757=CARTESIAN_POINT('Origin',(-63.8600385700458,-123.860803419755,182.116582478797));
#35758=CARTESIAN_POINT('',(-63.7970071778021,-127.890188739059,182.216986622987));
#35759=CARTESIAN_POINT('',(-64.6013626382522,-127.804439073161,181.731645524111));
#35760=CARTESIAN_POINT('Ctrl Pts',(-63.7970071778021,-127.890188739059,
182.216986622987));
#35761=CARTESIAN_POINT('Ctrl Pts',(-63.7831322752611,-127.760038335495,
182.216986622987));
#35762=CARTESIAN_POINT('Ctrl Pts',(-63.7637687626661,-127.639704067992,
182.191058057925));
#35763=CARTESIAN_POINT('Ctrl Pts',(-63.7391931903102,-127.454980903388,
182.113583474664));
#35764=CARTESIAN_POINT('Ctrl Pts',(-63.732331258019,-127.384331391819,182.068661603829));
#35765=CARTESIAN_POINT('Ctrl Pts',(-63.7395971786405,-127.281476319828,
181.979636129405));
#35766=CARTESIAN_POINT('Ctrl Pts',(-63.7483486653117,-127.243483658743,
181.93832282765));
#35767=CARTESIAN_POINT('Ctrl Pts',(-63.7810909518899,-127.185390943651,
181.860036293941));
#35768=CARTESIAN_POINT('Ctrl Pts',(-63.801400371884,-127.164011755529,181.824887654503));
#35769=CARTESIAN_POINT('Ctrl Pts',(-63.8476292036524,-127.13537467618,181.767622581437));
#35770=CARTESIAN_POINT('Ctrl Pts',(-63.8699650488265,-127.126043497198,
181.745088167067));
#35771=CARTESIAN_POINT('Ctrl Pts',(-63.9044567280937,-127.116929442638,
181.717151987942));
#35772=CARTESIAN_POINT('Ctrl Pts',(-63.9141070194901,-127.114845249218,
181.709935427865));
#35773=CARTESIAN_POINT('Ctrl Pts',(-63.9304811332893,-127.112050218114,
181.698668259966));
#35774=CARTESIAN_POINT('Ctrl Pts',(-63.9369950016434,-127.111115339238,
181.694419244055));
#35775=CARTESIAN_POINT('Ctrl Pts',(-63.9497849084295,-127.109618359446,
181.686525123085));
#35776=CARTESIAN_POINT('Ctrl Pts',(-63.9560376309646,-127.109033160596,
181.682860169817));
#35777=CARTESIAN_POINT('Ctrl Pts',(-63.9706529689686,-127.108002739486,
181.674739800591));
#35778=CARTESIAN_POINT('Ctrl Pts',(-63.9790759208733,-127.107651450528,
181.670380848498));
#35779=CARTESIAN_POINT('Ctrl Pts',(-64.0053355566674,-127.107302450035,
181.657764531226));
#35780=CARTESIAN_POINT('Ctrl Pts',(-64.0235610596089,-127.108074234866,
181.65033518029));
#35781=CARTESIAN_POINT('Ctrl Pts',(-64.0834180937468,-127.113928701266,
181.629981248421));
#35782=CARTESIAN_POINT('Ctrl Pts',(-64.1256133043086,-127.122983048988,
181.621691915876));
#35783=CARTESIAN_POINT('Ctrl Pts',(-64.2090594419135,-127.151759867151,
181.614968501231));
#35784=CARTESIAN_POINT('Ctrl Pts',(-64.2490983853533,-127.171167868247,
181.616651489296));
#35785=CARTESIAN_POINT('Ctrl Pts',(-64.3338007172831,-127.225981526449,
181.627831658004));
#35786=CARTESIAN_POINT('Ctrl Pts',(-64.3754120789359,-127.263302742097,
181.638983828978));
#35787=CARTESIAN_POINT('Ctrl Pts',(-64.4591344581,-127.362384295172,181.667628094705));
#35788=CARTESIAN_POINT('Ctrl Pts',(-64.4985394316644,-127.429600351007,
181.686563561648));
#35789=CARTESIAN_POINT('Ctrl Pts',(-64.5649845219845,-127.594857421434,
181.71927363754));
#35790=CARTESIAN_POINT('Ctrl Pts',(-64.589751184826,-127.69552044509,181.731645524111));
#35791=CARTESIAN_POINT('Ctrl Pts',(-64.6013626382522,-127.804439073161,
181.731645524111));
#35792=CARTESIAN_POINT('',(-65.1313926604929,-132.776266521447,181.731645524111));
#35793=CARTESIAN_POINT('',(-64.7073686427003,-128.798804562818,181.731645524111));
#35794=CARTESIAN_POINT('',(-64.3270372000429,-132.862016187344,182.216986622987));
#35795=CARTESIAN_POINT('Ctrl Pts',(-65.131392660493,-132.776266521447,181.731645524111));
#35796=CARTESIAN_POINT('Ctrl Pts',(-65.1452675630339,-132.90641692501,181.731645524111));
#35797=CARTESIAN_POINT('Ctrl Pts',(-65.1384611921918,-133.029541076926,
181.71370984535));
#35798=CARTESIAN_POINT('Ctrl Pts',(-65.0925065303848,-133.221783235699,
181.672966271636));
#35799=CARTESIAN_POINT('Ctrl Pts',(-65.0603057116076,-133.296597097505,
181.652413718737));
#35800=CARTESIAN_POINT('Ctrl Pts',(-64.9844740504155,-133.406761735521,
181.62651379162));
#35801=CARTESIAN_POINT('Ctrl Pts',(-64.946176388664,-133.447904216264,181.618303730733));
#35802=CARTESIAN_POINT('Ctrl Pts',(-64.8651281981303,-133.511146663444,
181.6156230735));
#35803=CARTESIAN_POINT('Ctrl Pts',(-64.8258042574373,-133.534552926507,
181.618900819278));
#35804=CARTESIAN_POINT('Ctrl Pts',(-64.7551290646409,-133.565796151265,
181.635190503848));
#35805=CARTESIAN_POINT('Ctrl Pts',(-64.7252345256159,-133.575933137511,
181.645055530873));
#35806=CARTESIAN_POINT('Ctrl Pts',(-64.6847956525423,-133.585681202663,
181.663023413437));
#35807=CARTESIAN_POINT('Ctrl Pts',(-64.6739814951562,-133.587889471973,
181.668289177604));
#35808=CARTESIAN_POINT('Ctrl Pts',(-64.6564488750106,-133.590808007593,
181.67761453307));
#35809=CARTESIAN_POINT('Ctrl Pts',(-64.6496688893713,-133.59177125635,181.681417500627));
#35810=CARTESIAN_POINT('Ctrl Pts',(-64.6367313098051,-133.593283979047,
181.689064102161));
#35811=CARTESIAN_POINT('Ctrl Pts',(-64.6305687016405,-133.593859571103,
181.692880099232));
#35812=CARTESIAN_POINT('Ctrl Pts',(-64.6165366757052,-133.594827807249,
181.701978177925));
#35813=CARTESIAN_POINT('Ctrl Pts',(-64.608717897936,-133.595114687207,181.707349807114));
#35814=CARTESIAN_POINT('Ctrl Pts',(-64.5851541417277,-133.595176288926,
181.724484781102));
#35815=CARTESIAN_POINT('Ctrl Pts',(-64.5699074110674,-133.594086947069,
181.73690695495));
#35816=CARTESIAN_POINT('Ctrl Pts',(-64.5231979042389,-133.586830866421,
181.779297910596));
#35817=CARTESIAN_POINT('Ctrl Pts',(-64.4953117281725,-133.576251080024,
181.811571109155));
#35818=CARTESIAN_POINT('Ctrl Pts',(-64.4480408096231,-133.543617741827,
181.878929055582));
#35819=CARTESIAN_POINT('Ctrl Pts',(-64.4293538988126,-133.521933471402,
181.913034945508));
#35820=CARTESIAN_POINT('Ctrl Pts',(-64.3957395622863,-133.461673491576,
181.98748512713));
#35821=CARTESIAN_POINT('Ctrl Pts',(-64.3836117278628,-133.421209134949,
182.025751312574));
#35822=CARTESIAN_POINT('Ctrl Pts',(-64.3633166551382,-133.315365807257,
182.103419741796));
#35823=CARTESIAN_POINT('Ctrl Pts',(-64.3574009088777,-133.244579576053,
182.140616723261));
#35824=CARTESIAN_POINT('Ctrl Pts',(-64.3452137184365,-133.073538251009,
182.19885018387));
#35825=CARTESIAN_POINT('Ctrl Pts',(-64.3386486534692,-132.970934815416,
182.216986622987));
#35826=CARTESIAN_POINT('Ctrl Pts',(-64.327037200043,-132.862016187345,182.216986622987));
#35827=CARTESIAN_POINT('',(-63.9030131822503,-128.884554228716,182.216986622987));
#35828=CARTESIAN_POINT('Origin',(-62.2947469341107,-124.027673965694,182.8187720491));
#35829=CARTESIAN_POINT('',(-62.2219755900488,-128.058097628933,182.799038162395));
#35830=CARTESIAN_POINT('',(-63.1184532233173,-127.962527123954,182.521385815309));
#35831=CARTESIAN_POINT('Ctrl Pts',(-62.2219755900488,-128.058097628933,
182.799038162395));
#35832=CARTESIAN_POINT('Ctrl Pts',(-62.2081006875078,-127.927947225369,
182.799038162395));
#35833=CARTESIAN_POINT('Ctrl Pts',(-62.1950950874127,-127.806935161917,
182.772307900389));
#35834=CARTESIAN_POINT('Ctrl Pts',(-62.1890962199225,-127.620231596466,
182.69592262965));
#35835=CARTESIAN_POINT('Ctrl Pts',(-62.1929049773309,-127.548444518085,
182.652465491875));
#35836=CARTESIAN_POINT('Ctrl Pts',(-62.220832238708,-127.443386809133,182.570365306765));
#35837=CARTESIAN_POINT('Ctrl Pts',(-62.2390471220705,-127.404385286736,
182.533298893505));
#35838=CARTESIAN_POINT('Ctrl Pts',(-62.2893003618264,-127.344425787048,
182.466552563806));
#35839=CARTESIAN_POINT('Ctrl Pts',(-62.3173249992075,-127.322224105207,
182.437800622955));
#35840=CARTESIAN_POINT('Ctrl Pts',(-62.3757650967539,-127.292285223344,
182.393927007362));
#35841=CARTESIAN_POINT('Ctrl Pts',(-62.402793067364,-127.282453832442,182.377599323219));
#35842=CARTESIAN_POINT('Ctrl Pts',(-62.442913723009,-127.272739691394,182.358914021841));
#35843=CARTESIAN_POINT('Ctrl Pts',(-62.4539976666445,-127.270502661067,
182.354256488759));
#35844=CARTESIAN_POINT('Ctrl Pts',(-62.4725739808559,-127.267472860686,
182.34728413377));
#35845=CARTESIAN_POINT('Ctrl Pts',(-62.4799089580962,-127.266450446118,
182.344732390644));
#35846=CARTESIAN_POINT('Ctrl Pts',(-62.4942053467175,-127.264792865297,
182.340149213999));
#35847=CARTESIAN_POINT('Ctrl Pts',(-62.5011487645808,-127.264134033711,
182.338093546571));
#35848=CARTESIAN_POINT('Ctrl Pts',(-62.517273405508,-127.262942710826,182.333713252777));
#35849=CARTESIAN_POINT('Ctrl Pts',(-62.52649056392,-127.262506754149,182.331494262321));
#35850=CARTESIAN_POINT('Ctrl Pts',(-62.5549969182946,-127.261918238445,
182.32550233905));
#35851=CARTESIAN_POINT('Ctrl Pts',(-62.5744690785897,-127.262557121273,
182.32260636481));
#35852=CARTESIAN_POINT('Ctrl Pts',(-62.6374678225912,-127.268076660412,
182.316939372924));
#35853=CARTESIAN_POINT('Ctrl Pts',(-62.6804510181273,-127.277047003671,
182.318702292201));
#35854=CARTESIAN_POINT('Ctrl Pts',(-62.7631877060839,-127.305899453907,
182.331301658482));
#35855=CARTESIAN_POINT('Ctrl Pts',(-62.8017352151081,-127.325466451876,
182.341971339155));
#35856=CARTESIAN_POINT('Ctrl Pts',(-62.8815112890473,-127.380805282091,
182.371592450366));
#35857=CARTESIAN_POINT('Ctrl Pts',(-62.9193875507362,-127.41852468435,182.391375902221));
#35858=CARTESIAN_POINT('Ctrl Pts',(-62.9941915365654,-127.518556997735,
182.436597411196));
#35859=CARTESIAN_POINT('Ctrl Pts',(-63.0281642013553,-127.586352173978,
182.462654543372));
#35860=CARTESIAN_POINT('Ctrl Pts',(-63.0854224683637,-127.752588621146,
182.506033488849));
#35861=CARTESIAN_POINT('Ctrl Pts',(-63.106841769891,-127.853608495882,182.521385815309));
#35862=CARTESIAN_POINT('Ctrl Pts',(-63.1184532233173,-127.962527123954,
182.521385815309));
#35863=CARTESIAN_POINT('',(-63.6484832455581,-132.93435457224,182.521385815309));
#35864=CARTESIAN_POINT('',(-63.2244592277655,-128.956892613612,182.521385815309));
#35865=CARTESIAN_POINT('',(-62.7520056122895,-133.029925077219,182.799038162395));
#35866=CARTESIAN_POINT('Ctrl Pts',(-63.6484832455581,-132.93435457224,182.521385815309));
#35867=CARTESIAN_POINT('Ctrl Pts',(-63.662358148099,-133.064504975803,182.521385815309));
#35868=CARTESIAN_POINT('Ctrl Pts',(-63.6603925669443,-133.187113067197,
182.499228097533));
#35869=CARTESIAN_POINT('Ctrl Pts',(-63.6260427289545,-133.37811807422,182.443855782497));
#35870=CARTESIAN_POINT('Ctrl Pts',(-63.5998870807864,-133.452287480453,
182.414339764355));
#35871=CARTESIAN_POINT('Ctrl Pts',(-63.532734954993,-133.561526822008,182.368352235708));
#35872=CARTESIAN_POINT('Ctrl Pts',(-63.4976173925097,-133.602330282924,
182.35022341612));
#35873=CARTESIAN_POINT('Ctrl Pts',(-63.4197294693475,-133.665235824488,
182.32672944874));
#35874=CARTESIAN_POINT('Ctrl Pts',(-63.3808270672087,-133.688597148725,
182.319960348555));
#35875=CARTESIAN_POINT('Ctrl Pts',(-63.3084017754703,-133.720026945723,
182.31816569793));
#35876=CARTESIAN_POINT('Ctrl Pts',(-63.2770496520254,-133.730319320205,
182.320372980161));
#35877=CARTESIAN_POINT('Ctrl Pts',(-63.2335267452168,-133.740396163958,
182.327948324127));
#35878=CARTESIAN_POINT('Ctrl Pts',(-63.2217769809352,-133.742704175214,
182.330431638238));
#35879=CARTESIAN_POINT('Ctrl Pts',(-63.2025379122063,-133.745804629654,
182.335239786608));
#35880=CARTESIAN_POINT('Ctrl Pts',(-63.19505069546,-133.746843273971,182.337294395826));
#35881=CARTESIAN_POINT('Ctrl Pts',(-63.1806698266776,-133.748509860941,
182.341601704837));
#35882=CARTESIAN_POINT('Ctrl Pts',(-63.1737779611485,-133.749163196705,
182.343825714991));
#35883=CARTESIAN_POINT('Ctrl Pts',(-63.1579870194791,-133.750318945019,
182.349295694518));
#35884=CARTESIAN_POINT('Ctrl Pts',(-63.1491154950279,-133.750718054807,
182.352643343149));
#35885=CARTESIAN_POINT('Ctrl Pts',(-63.1221513906236,-133.751142156361,
182.363671441191));
#35886=CARTESIAN_POINT('Ctrl Pts',(-63.1043833166242,-133.750321606548,
182.372132062266));
#35887=CARTESIAN_POINT('Ctrl Pts',(-63.0489059670074,-133.744000236518,
182.402359960234));
#35888=CARTESIAN_POINT('Ctrl Pts',(-63.0141086370849,-133.734157225295,
182.427327759524));
#35889=CARTESIAN_POINT('Ctrl Pts',(-62.9520669500268,-133.703098549704,
182.482307348343));
#35890=CARTESIAN_POINT('Ctrl Pts',(-62.9257344419335,-133.682229351028,
182.511525416577));
#35891=CARTESIAN_POINT('Ctrl Pts',(-62.8751846211686,-133.623774806967,
182.577341829662));
#35892=CARTESIAN_POINT('Ctrl Pts',(-62.8541751992229,-133.584257286906,
182.612636578157));
#35893=CARTESIAN_POINT('Ctrl Pts',(-62.8156564992323,-133.480356719631,
182.685903670104));
#35894=CARTESIAN_POINT('Ctrl Pts',(-62.8008422419721,-133.41051912915,182.722407789729));
#35895=CARTESIAN_POINT('Ctrl Pts',(-62.7746236567139,-133.240973644535,
182.780388069585));
#35896=CARTESIAN_POINT('Ctrl Pts',(-62.7636170657158,-133.13884370529,182.799038162395));
#35897=CARTESIAN_POINT('Ctrl Pts',(-62.7520056122896,-133.029925077219,
182.799038162395));
#35898=CARTESIAN_POINT('',(-62.3279815944969,-129.05246311859,182.799038162395));
#35899=CARTESIAN_POINT('Origin',(-60.6078417159259,-124.207509331988,183.123835818113));
#35900=CARTESIAN_POINT('',(-60.554202360699,-128.235893397398,182.985110762277));
#35901=CARTESIAN_POINT('',(-61.490702145304,-128.136056263704,182.931283312168));
#35902=CARTESIAN_POINT('Ctrl Pts',(-60.554202360699,-128.235893397398,182.985110762277));
#35903=CARTESIAN_POINT('Ctrl Pts',(-60.5403274581581,-128.105742993835,
182.985110762277));
#35904=CARTESIAN_POINT('Ctrl Pts',(-60.533685798788,-127.984052491785,182.959132268995));
#35905=CARTESIAN_POINT('Ctrl Pts',(-60.5454646101901,-127.79545370699,182.888275545063));
#35906=CARTESIAN_POINT('Ctrl Pts',(-60.5592854279688,-127.722599276085,
182.848808711235));
#35907=CARTESIAN_POINT('Ctrl Pts',(-60.6056256571204,-127.615578621755,
182.778405179778));
#35908=CARTESIAN_POINT('Ctrl Pts',(-60.6320183277418,-127.575705292601,
182.747739820219));
#35909=CARTESIAN_POINT('Ctrl Pts',(-60.6965274937305,-127.514226015934,
182.696412748599));
#35910=CARTESIAN_POINT('Ctrl Pts',(-60.7305209536102,-127.491388017738,
182.675728464628));
#35911=CARTESIAN_POINT('Ctrl Pts',(-60.7976307515994,-127.460524887886,
182.647796081573));
#35912=CARTESIAN_POINT('Ctrl Pts',(-60.8277375045609,-127.450365278217,
182.63862403331));
#35913=CARTESIAN_POINT('Ctrl Pts',(-60.8711221629394,-127.440303172671,
182.630275531477));
#35914=CARTESIAN_POINT('Ctrl Pts',(-60.8829891348988,-127.437982666293,
182.628447704284));
#35915=CARTESIAN_POINT('Ctrl Pts',(-60.9026816328099,-127.434833873273,
182.626175370134));
#35916=CARTESIAN_POINT('Ctrl Pts',(-60.9104099636905,-127.433769524579,
182.625469197828));
#35917=CARTESIAN_POINT('Ctrl Pts',(-60.9253811622503,-127.43204000451,182.624463323074));
#35918=CARTESIAN_POINT('Ctrl Pts',(-60.9326122477846,-127.431350505628,
182.624136409406));
#35919=CARTESIAN_POINT('Ctrl Pts',(-60.9493123186159,-127.430097838071,
182.623750757796));
#35920=CARTESIAN_POINT('Ctrl Pts',(-60.9587913645781,-127.429633962431,
182.623800688638));
#35921=CARTESIAN_POINT('Ctrl Pts',(-60.9879027632329,-127.428980944964,
182.624781388169));
#35922=CARTESIAN_POINT('Ctrl Pts',(-61.0075065601553,-127.42960579445,182.626587094122));
#35923=CARTESIAN_POINT('Ctrl Pts',(-61.0700607111023,-127.435172730178,
182.635936387187));
#35924=CARTESIAN_POINT('Ctrl Pts',(-61.1114168876027,-127.444316524536,
182.647649103826));
#35925=CARTESIAN_POINT('Ctrl Pts',(-61.1888665524268,-127.473732606759,
182.678839021662));
#35926=CARTESIAN_POINT('Ctrl Pts',(-61.2238274269927,-127.493681963924,
182.697875311885));
#35927=CARTESIAN_POINT('Ctrl Pts',(-61.2944320508974,-127.549998531986,
182.744215894284));
#35928=CARTESIAN_POINT('Ctrl Pts',(-61.3266277857702,-127.588323516354,
182.771480884706));
#35929=CARTESIAN_POINT('Ctrl Pts',(-61.3888276897839,-127.689699509069,
182.830651527203));
#35930=CARTESIAN_POINT('Ctrl Pts',(-61.4158311758153,-127.758237646329,
182.862315978803));
#35931=CARTESIAN_POINT('Ctrl Pts',(-61.461630730476,-127.925695668786,182.913842767231));
#35932=CARTESIAN_POINT('Ctrl Pts',(-61.4790906918778,-128.027137635632,
182.931283312168));
#35933=CARTESIAN_POINT('Ctrl Pts',(-61.490702145304,-128.136056263704,182.931283312168));
#35934=CARTESIAN_POINT('',(-62.0207321675448,-133.107883711989,182.931283312168));
#35935=CARTESIAN_POINT('',(-61.5967081497522,-129.130421753361,182.931283312168));
#35936=CARTESIAN_POINT('',(-61.0842323829398,-133.207720845684,182.985110762277));
#35937=CARTESIAN_POINT('Ctrl Pts',(-62.0207321675448,-133.107883711989,
182.931283312168));
#35938=CARTESIAN_POINT('Ctrl Pts',(-62.0346070700858,-133.238034115553,
182.931283312168));
#35939=CARTESIAN_POINT('Ctrl Pts',(-62.0383463210293,-133.360034033732,
182.906191281395));
#35940=CARTESIAN_POINT('Ctrl Pts',(-62.0187452529312,-133.549466723349,
182.839408262717));
#35941=CARTESIAN_POINT('Ctrl Pts',(-62.000592124765,-133.622783007485,182.802644143018));
#35942=CARTESIAN_POINT('Ctrl Pts',(-61.9466475138939,-133.730614339712,
182.739241640849));
#35943=CARTESIAN_POINT('Ctrl Pts',(-61.9169779823828,-133.770837004128,
182.712247643659));
#35944=CARTESIAN_POINT('Ctrl Pts',(-61.8471113808894,-133.832887419213,
182.669305750119));
#35945=CARTESIAN_POINT('Ctrl Pts',(-61.8110090883418,-133.85595023306,182.652883199469));
#35946=CARTESIAN_POINT('Ctrl Pts',(-61.7411880316488,-133.887102401203,
182.633108512221));
#35947=CARTESIAN_POINT('Ctrl Pts',(-61.7102429709135,-133.897351380082,
182.627529770437));
#35948=CARTESIAN_POINT('Ctrl Pts',(-61.6661987304834,-133.907483801481,
182.62427232435));
#35949=CARTESIAN_POINT('Ctrl Pts',(-61.6542026782984,-133.909818068673,
182.623828867216));
#35950=CARTESIAN_POINT('Ctrl Pts',(-61.6343816945794,-133.912980559139,
182.623840376381));
#35951=CARTESIAN_POINT('Ctrl Pts',(-61.6266238495805,-133.914048054236,
182.624027220841));
#35952=CARTESIAN_POINT('Ctrl Pts',(-61.6116362731618,-133.915779320293,
182.624744912186));
#35953=CARTESIAN_POINT('Ctrl Pts',(-61.6044151818927,-133.91646775372,182.625247684036));
#35954=CARTESIAN_POINT('Ctrl Pts',(-61.5877798041175,-133.917713524565,
182.62677166907));
#35955=CARTESIAN_POINT('Ctrl Pts',(-61.5783677649524,-133.918170256832,
182.627900783973));
#35956=CARTESIAN_POINT('Ctrl Pts',(-61.549555356689,-133.918791399926,182.632181093098));
#35957=CARTESIAN_POINT('Ctrl Pts',(-61.5302819247756,-133.918131331324,
182.636188460856));
#35958=CARTESIAN_POINT('Ctrl Pts',(-61.4691859191854,-133.912408947559,
182.65249656559));
#35959=CARTESIAN_POINT('Ctrl Pts',(-61.4294167066618,-133.903095972238,
182.668707927871));
#35960=CARTESIAN_POINT('Ctrl Pts',(-61.35597910635,-133.873252177133,182.708113945222));
#35961=CARTESIAN_POINT('Ctrl Pts',(-61.3233863095623,-133.853050367057,
182.730746143841));
#35962=CARTESIAN_POINT('Ctrl Pts',(-61.2584476730013,-133.79612976689,182.784103777694));
#35963=CARTESIAN_POINT('Ctrl Pts',(-61.2295218509685,-133.757456187967,
182.814375886748));
#35964=CARTESIAN_POINT('Ctrl Pts',(-61.1743564432734,-133.655330270948,
182.878983624352));
#35965=CARTESIAN_POINT('Ctrl Pts',(-61.1510671279891,-133.586396178273,
182.912673395392));
#35966=CARTESIAN_POINT('Ctrl Pts',(-61.1112851234711,-133.418296644768,
182.967030891378));
#35967=CARTESIAN_POINT('Ctrl Pts',(-61.0958438363661,-133.316639473756,
182.985110762277));
#35968=CARTESIAN_POINT('Ctrl Pts',(-61.0842323829398,-133.207720845684,
182.985110762277));
#35969=CARTESIAN_POINT('',(-60.6602083651472,-129.230258887056,182.985110762277));
#35970=CARTESIAN_POINT('Origin',(-58.8973597151212,-124.389858140823,183.01404458844));
#35971=CARTESIAN_POINT('',(-58.8906124077336,-128.413243200653,182.764390559475));
#35972=CARTESIAN_POINT('',(-59.8127083802321,-128.314941609559,182.937516262089));
#35973=CARTESIAN_POINT('Ctrl Pts',(-58.8906124077336,-128.413243200653,
182.764390559475));
#35974=CARTESIAN_POINT('Ctrl Pts',(-58.8767375051926,-128.28309279709,182.764390559475));
#35975=CARTESIAN_POINT('Ctrl Pts',(-58.8760959656698,-128.160762642177,
182.740673610517));
#35976=CARTESIAN_POINT('Ctrl Pts',(-58.9038202559127,-127.97046396281,182.679463368635));
#35977=CARTESIAN_POINT('Ctrl Pts',(-58.9264126401748,-127.896674424315,
182.646280507681));
#35978=CARTESIAN_POINT('Ctrl Pts',(-58.9878473693628,-127.788044595435,
182.591665227216));
#35979=CARTESIAN_POINT('Ctrl Pts',(-59.02065695454,-127.747487180319,182.569183080593));
#35980=CARTESIAN_POINT('Ctrl Pts',(-59.0953385172016,-127.684923458206,
182.536258209888));
#35981=CARTESIAN_POINT('Ctrl Pts',(-59.1332075184236,-127.661672301411,
182.524843678197));
#35982=CARTESIAN_POINT('Ctrl Pts',(-59.2049416000455,-127.630316192029,
182.514475856253));
#35983=CARTESIAN_POINT('Ctrl Pts',(-59.2363348646342,-127.620019431626,
182.512992489976));
#35984=CARTESIAN_POINT('Ctrl Pts',(-59.2804288601208,-127.609881706005,
182.515465972269));
#35985=CARTESIAN_POINT('Ctrl Pts',(-59.2923827297318,-127.607551935757,
182.516574077638));
#35986=CARTESIAN_POINT('Ctrl Pts',(-59.3120405261043,-127.604406842153,
182.519133824127));
#35987=CARTESIAN_POINT('Ctrl Pts',(-59.3197115950904,-127.603348597959,
182.52031426281));
#35988=CARTESIAN_POINT('Ctrl Pts',(-59.3344867141845,-127.601639981271,
182.52294414773));
#35989=CARTESIAN_POINT('Ctrl Pts',(-59.3415857215319,-127.600964562806,
182.524364986856));
#35990=CARTESIAN_POINT('Ctrl Pts',(-59.3578939073577,-127.599753672809,
182.527996390102));
#35991=CARTESIAN_POINT('Ctrl Pts',(-59.3670873019613,-127.599320249513,
182.530312340441));
#35992=CARTESIAN_POINT('Ctrl Pts',(-59.3951269076186,-127.59878149234,182.538208668082));
#35993=CARTESIAN_POINT('Ctrl Pts',(-59.4137396701984,-127.599511992707,
182.544611113162));
#35994=CARTESIAN_POINT('Ctrl Pts',(-59.4722887633093,-127.605505894358,
182.568433344249));
#35995=CARTESIAN_POINT('Ctrl Pts',(-59.5096974731965,-127.61507051503,182.589415157732));
#35996=CARTESIAN_POINT('Ctrl Pts',(-59.5775898039698,-127.645505472915,
182.637382982469));
#35997=CARTESIAN_POINT('Ctrl Pts',(-59.6070772861928,-127.66603833027,182.66367956225));
#35998=CARTESIAN_POINT('Ctrl Pts',(-59.6647982793581,-127.723728379444,
182.724046469628));
#35999=CARTESIAN_POINT('Ctrl Pts',(-59.6896981921335,-127.76283114719,182.757208456479));
#36000=CARTESIAN_POINT('Ctrl Pts',(-59.7363408292674,-127.86586564849,182.82688944983));
#36001=CARTESIAN_POINT('Ctrl Pts',(-59.7552432898956,-127.935267409179,
182.862320998025));
#36002=CARTESIAN_POINT('Ctrl Pts',(-59.7879781818845,-128.104118211964,
182.919001079751));
#36003=CARTESIAN_POINT('Ctrl Pts',(-59.801096926806,-128.206022981489,182.937516262089));
#36004=CARTESIAN_POINT('Ctrl Pts',(-59.8127083802321,-128.314941609559,
182.937516262089));
#36005=CARTESIAN_POINT('',(-60.3427384024728,-133.286769057844,182.937516262089));
#36006=CARTESIAN_POINT('',(-59.9187143846802,-129.309307099216,182.937516262089));
#36007=CARTESIAN_POINT('',(-59.4206424299744,-133.385070648939,182.764390559475));
#36008=CARTESIAN_POINT('Ctrl Pts',(-60.3427384024729,-133.286769057844,
182.937516262089));
#36009=CARTESIAN_POINT('Ctrl Pts',(-60.3566133050138,-133.416919461408,
182.937516262089));
#36010=CARTESIAN_POINT('Ctrl Pts',(-60.3665898863617,-133.538254438495,
182.910948175941));
#36011=CARTESIAN_POINT('Ctrl Pts',(-60.3640243893328,-133.725871022423,
182.836635639919));
#36012=CARTESIAN_POINT('Ctrl Pts',(-60.3553660531873,-133.798175098296,
182.79476001567));
#36013=CARTESIAN_POINT('Ctrl Pts',(-60.3183893640027,-133.90419753671,182.717627262946));
#36014=CARTESIAN_POINT('Ctrl Pts',(-60.2961191754112,-133.943631381737,
182.683336881151));
#36015=CARTESIAN_POINT('Ctrl Pts',(-60.2386687798237,-134.004358146321,
182.623442688217));
#36016=CARTESIAN_POINT('Ctrl Pts',(-60.2075824357135,-134.026886226554,
182.598321106052));
#36017=CARTESIAN_POINT('Ctrl Pts',(-60.144568599377,-134.057312699529,182.561715615124));
#36018=CARTESIAN_POINT('Ctrl Pts',(-60.1158715914763,-134.067322020956,
182.548675065521));
#36019=CARTESIAN_POINT('Ctrl Pts',(-60.0738990155605,-134.077233589078,
182.534774140307));
#36020=CARTESIAN_POINT('Ctrl Pts',(-60.0623603078181,-134.079519100297,
182.531429684044));
#36021=CARTESIAN_POINT('Ctrl Pts',(-60.0431157614817,-134.082620138686,
182.526643885133));
#36022=CARTESIAN_POINT('Ctrl Pts',(-60.0355396190153,-134.083668263079,
182.524952106114));
#36023=CARTESIAN_POINT('Ctrl Pts',(-60.020817176179,-134.085371264126,182.522038470182));
#36024=CARTESIAN_POINT('Ctrl Pts',(-60.0136860241933,-134.086050109424,
182.520790784457));
#36025=CARTESIAN_POINT('Ctrl Pts',(-59.9971697655067,-134.087283181378,
182.518280206525));
#36026=CARTESIAN_POINT('Ctrl Pts',(-59.9877608563466,-134.087739579966,
182.517125167646));
#36027=CARTESIAN_POINT('Ctrl Pts',(-59.9587596052638,-134.088380854966,
182.514408931845));
#36028=CARTESIAN_POINT('Ctrl Pts',(-59.9390842867924,-134.087763630156,
182.513730152639));
#36029=CARTESIAN_POINT('Ctrl Pts',(-59.8758453479046,-134.082269697397,
182.51517069637));
#36030=CARTESIAN_POINT('Ctrl Pts',(-59.8333324717794,-134.073249214946,
182.521683476191));
#36031=CARTESIAN_POINT('Ctrl Pts',(-59.7525361025255,-134.044189913774,
182.54322578758));
#36032=CARTESIAN_POINT('Ctrl Pts',(-59.715432150855,-134.024469022947,182.557956815466));
#36033=CARTESIAN_POINT('Ctrl Pts',(-59.6394875926139,-133.96872172756,182.595754718354));
#36034=CARTESIAN_POINT('Ctrl Pts',(-59.6040706303263,-133.930740147556,
182.619244883024));
#36035=CARTESIAN_POINT('Ctrl Pts',(-59.5348028806321,-133.830117634411,
182.671438499415));
#36036=CARTESIAN_POINT('Ctrl Pts',(-59.5039544998657,-133.761989388618,
182.700355994833));
#36037=CARTESIAN_POINT('Ctrl Pts',(-59.4518653082704,-133.595201883477,
182.747931646866));
#36038=CARTESIAN_POINT('Ctrl Pts',(-59.4322538834007,-133.493989277011,
182.764390559475));
#36039=CARTESIAN_POINT('Ctrl Pts',(-59.4206424299744,-133.385070648939,
182.764390559475));
#36040=CARTESIAN_POINT('',(-58.9966184121818,-129.40760869031,182.764390559475));
#36041=CARTESIAN_POINT('Origin',(-57.2627079282344,-124.564122942241,182.495779027277));
#36042=CARTESIAN_POINT('',(-57.3278875323155,-128.579840112772,182.14970500989));
#36043=CARTESIAN_POINT('',(-58.1819908264683,-128.488786995442,182.539722428676));
#36044=CARTESIAN_POINT('Ctrl Pts',(-57.3278875323155,-128.579840112772,
182.14970500989));
#36045=CARTESIAN_POINT('Ctrl Pts',(-57.3140126297744,-128.449689709208,
182.14970500989));
#36046=CARTESIAN_POINT('Ctrl Pts',(-57.3186586840651,-128.32679586147,182.129627948123));
#36047=CARTESIAN_POINT('Ctrl Pts',(-57.3595695598265,-128.135091403988,
182.081621505058));
#36048=CARTESIAN_POINT('Ctrl Pts',(-57.3891832451256,-128.060553347895,
182.056651084241));
#36049=CARTESIAN_POINT('Ctrl Pts',(-57.4615167691348,-127.950761634673,
182.020998096351));
#36050=CARTESIAN_POINT('Ctrl Pts',(-57.4986094684153,-127.909747610979,
182.008005743306));
#36051=CARTESIAN_POINT('Ctrl Pts',(-57.5787887154705,-127.846597798979,
181.995396547325));
#36052=CARTESIAN_POINT('Ctrl Pts',(-57.6182147445026,-127.823180652617,
181.993915139005));
#36053=CARTESIAN_POINT('Ctrl Pts',(-57.6902589463901,-127.791791482344,
182.001714418298));
#36054=CARTESIAN_POINT('Ctrl Pts',(-57.7210716845023,-127.781556609941,
182.008005941864));
#36055=CARTESIAN_POINT('Ctrl Pts',(-57.7632791273821,-127.771620003432,
182.021157658483));
#36056=CARTESIAN_POINT('Ctrl Pts',(-57.7746187137944,-127.769355719877,
182.025137297357));
#36057=CARTESIAN_POINT('Ctrl Pts',(-57.7930929401046,-127.766336802749,
182.032380361324));
#36058=CARTESIAN_POINT('Ctrl Pts',(-57.8002594595197,-127.76533234691,182.035378808189));
#36059=CARTESIAN_POINT('Ctrl Pts',(-57.8139790051779,-127.763736261403,
182.041491613433));
#36060=CARTESIAN_POINT('Ctrl Pts',(-57.8205338643875,-127.763118852765,
182.044577631346));
#36061=CARTESIAN_POINT('Ctrl Pts',(-57.8355056252227,-127.7620504346,182.052015045491));
#36062=CARTESIAN_POINT('Ctrl Pts',(-57.843882430576,-127.761704065173,182.056462420712));
#36063=CARTESIAN_POINT('Ctrl Pts',(-57.8692356946754,-127.761451689958,
182.070815470603));
#36064=CARTESIAN_POINT('Ctrl Pts',(-57.8857923472572,-127.762401385387,
182.081442567973));
#36065=CARTESIAN_POINT('Ctrl Pts',(-57.9370086771498,-127.769177008587,
182.118353275601));
#36066=CARTESIAN_POINT('Ctrl Pts',(-57.9683788852572,-127.779385373891,
182.147384799195));
#36067=CARTESIAN_POINT('Ctrl Pts',(-58.0229990085785,-127.81123523776,182.209342815215));
#36068=CARTESIAN_POINT('Ctrl Pts',(-58.0454444342418,-127.832518825392,
182.24137142292));
#36069=CARTESIAN_POINT('Ctrl Pts',(-58.0873183657515,-127.891898277211,
182.312256350047));
#36070=CARTESIAN_POINT('Ctrl Pts',(-58.1037311678091,-127.931905827661,
182.349388079189));
#36071=CARTESIAN_POINT('Ctrl Pts',(-58.1327674848055,-128.036817280314,
182.425529817342));
#36072=CARTESIAN_POINT('Ctrl Pts',(-58.1429078755347,-128.107153136193,
182.462669309337));
#36073=CARTESIAN_POINT('Ctrl Pts',(-58.1617314252332,-128.277486981004,
182.521208644037));
#36074=CARTESIAN_POINT('Ctrl Pts',(-58.1703793730421,-128.379868367371,
182.539722428676));
#36075=CARTESIAN_POINT('Ctrl Pts',(-58.1819908264683,-128.488786995442,
182.539722428676));
#36076=CARTESIAN_POINT('',(-58.712020848709,-133.460614443727,182.539722428676));
#36077=CARTESIAN_POINT('',(-58.2879968309164,-129.483152485099,182.539722428676));
#36078=CARTESIAN_POINT('',(-57.8579175545562,-133.551667561058,182.14970500989));
#36079=CARTESIAN_POINT('Ctrl Pts',(-58.712020848709,-133.460614443727,182.539722428676));
#36080=CARTESIAN_POINT('Ctrl Pts',(-58.72589575125,-133.590764847291,182.539722428676));
#36081=CARTESIAN_POINT('Ctrl Pts',(-58.7422796703366,-133.711416759368,
182.513222327751));
#36082=CARTESIAN_POINT('Ctrl Pts',(-58.7580465000861,-133.897078994785,
182.435699048863));
#36083=CARTESIAN_POINT('Ctrl Pts',(-58.7598234251794,-133.968270602094,
182.391145579132));
#36084=CARTESIAN_POINT('Ctrl Pts',(-58.7425889505126,-134.072188388545,
182.304765251075));
#36085=CARTESIAN_POINT('Ctrl Pts',(-58.7292393938724,-134.110671234608,
182.265171317025));
#36086=CARTESIAN_POINT('Ctrl Pts',(-58.6878785036726,-134.169682750425,
182.191805657483));
#36087=CARTESIAN_POINT('Ctrl Pts',(-58.6637324381542,-134.191470950593,
182.159445018846));
#36088=CARTESIAN_POINT('Ctrl Pts',(-58.6113331965825,-134.220765836851,
182.108136102317));
#36089=CARTESIAN_POINT('Ctrl Pts',(-58.5865945829816,-134.230353167,182.088391614236));
#36090=CARTESIAN_POINT('Ctrl Pts',(-58.549166272102,-134.239780286109,182.064655081141));
#36091=CARTESIAN_POINT('Ctrl Pts',(-58.5387619619532,-134.241944862965,
182.058603993391));
#36092=CARTESIAN_POINT('Ctrl Pts',(-58.5212187049274,-134.244864532549,
182.049299019641));
#36093=CARTESIAN_POINT('Ctrl Pts',(-58.5142660358884,-134.245846190509,
182.045826937191));
#36094=CARTESIAN_POINT('Ctrl Pts',(-58.5006651592581,-134.247429625105,
182.039451303911));
#36095=CARTESIAN_POINT('Ctrl Pts',(-58.4940378846398,-134.248054753709,
182.036525671569));
#36096=CARTESIAN_POINT('Ctrl Pts',(-58.4785973774569,-134.249173143366,
182.030126436336));
#36097=CARTESIAN_POINT('Ctrl Pts',(-58.469735061115,-134.249571271508,182.026754370336));
#36098=CARTESIAN_POINT('Ctrl Pts',(-58.4422154031119,-134.250054598787,
182.017199447361));
#36099=CARTESIAN_POINT('Ctrl Pts',(-58.4232650256236,-134.249360090425,
182.01187396937));
#36100=CARTESIAN_POINT('Ctrl Pts',(-58.361483415609,-134.243710796672,181.998363232933));
#36101=CARTESIAN_POINT('Ctrl Pts',(-58.318614546638,-134.234728265437,181.994798931204));
#36102=CARTESIAN_POINT('Ctrl Pts',(-58.2349242176556,-134.205977479706,
181.997225575798));
#36103=CARTESIAN_POINT('Ctrl Pts',(-58.1953204168388,-134.186523089499,
182.003199319155));
#36104=CARTESIAN_POINT('Ctrl Pts',(-58.1123924551955,-134.13152027157,182.023240814352));
#36105=CARTESIAN_POINT('Ctrl Pts',(-58.0722868539636,-134.094038531801,
182.03858387165));
#36106=CARTESIAN_POINT('Ctrl Pts',(-57.9922807048315,-133.994560803777,
182.07533006356));
#36107=CARTESIAN_POINT('Ctrl Pts',(-57.9552285565356,-133.927093921049,
182.097794703633));
#36108=CARTESIAN_POINT('Ctrl Pts',(-57.8928036590256,-133.761408271211,
182.135823587746));
#36109=CARTESIAN_POINT('Ctrl Pts',(-57.8695290079825,-133.660586189129,
182.14970500989));
#36110=CARTESIAN_POINT('Ctrl Pts',(-57.8579175545563,-133.551667561058,
182.14970500989));
#36111=CARTESIAN_POINT('',(-57.4338935367636,-129.57420560243,182.14970500989));
#36112=CARTESIAN_POINT('Origin',(-60.6261834003547,-128.228219737673,175.985485069079));
#36113=CARTESIAN_POINT('',(-56.8563447552978,-127.624443285184,171.250110682016));
#36114=CARTESIAN_POINT('Origin',(-60.5201773959065,-127.233854248016,175.985485069079));
#36115=CARTESIAN_POINT('',(-56.3517119863112,-128.683906947702,170.460881617506));
#36116=CARTESIAN_POINT('Origin',(-56.9623507597459,-128.618808774841,171.250110682016));
#36117=CARTESIAN_POINT('',(-56.6510041624572,-128.652000402186,170.239324614047));
#36118=CARTESIAN_POINT('Origin',(-60.6261834003547,-128.228219737673,175.985485069079));
#36119=CARTESIAN_POINT('',(-57.4553596229072,-128.566250736288,169.753983515172));
#36120=CARTESIAN_POINT('Ctrl Pts',(-57.4553596229072,-128.566250736288,
169.753983515172));
#36121=CARTESIAN_POINT('Ctrl Pts',(-57.4414847203663,-128.436100332725,
169.753983515172));
#36122=CARTESIAN_POINT('Ctrl Pts',(-57.4350444863886,-128.314388357382,
169.779912080233));
#36123=CARTESIAN_POINT('Ctrl Pts',(-57.4201248720071,-128.128635803146,
169.857386663495));
#36124=CARTESIAN_POINT('Ctrl Pts',(-57.4119384373763,-128.058127492375,
169.90230853433));
#36125=CARTESIAN_POINT('Ctrl Pts',(-57.3831521735925,-127.959115824103,
169.991334008754));
#36126=CARTESIAN_POINT('Ctrl Pts',(-57.3665878576303,-127.923821996711,
170.032647310509));
#36127=CARTESIAN_POINT('Ctrl Pts',(-57.3223344824676,-127.873937533561,
170.110933844218));
#36128=CARTESIAN_POINT('Ctrl Pts',(-57.2979744020772,-127.857320412612,
170.146082483655));
#36129=CARTESIAN_POINT('Ctrl Pts',(-57.2467473469839,-127.839072781895,
170.203347556721));
#36130=CARTESIAN_POINT('Ctrl Pts',(-57.222946314663,-127.834660102289,170.225881971091));
#36131=CARTESIAN_POINT('Ctrl Pts',(-57.1873084187118,-127.833022328976,
170.253818150217));
#36132=CARTESIAN_POINT('Ctrl Pts',(-57.1774356289432,-127.83301942644,170.261034710294));
#36133=CARTESIAN_POINT('Ctrl Pts',(-57.1608402746568,-127.833739160899,
170.272301878193));
#36134=CARTESIAN_POINT('Ctrl Pts',(-57.1542757137794,-127.834198529955,
170.276550894104));
#36135=CARTESIAN_POINT('Ctrl Pts',(-57.1414576649162,-127.835431529319,
170.284445015073));
#36136=CARTESIAN_POINT('Ctrl Pts',(-57.1352220993665,-127.836177665411,
170.288109968341));
#36137=CARTESIAN_POINT('Ctrl Pts',(-57.1207180037226,-127.838251570473,
170.296230337568));
#36138=CARTESIAN_POINT('Ctrl Pts',(-57.1124102960038,-127.839683881607,
170.300589289661));
#36139=CARTESIAN_POINT('Ctrl Pts',(-57.0866672582166,-127.844878713541,
170.313205606933));
#36140=CARTESIAN_POINT('Ctrl Pts',(-57.0690140708695,-127.849475406459,
170.320634957869));
#36141=CARTESIAN_POINT('Ctrl Pts',(-57.0117365199272,-127.867817202192,
170.340988889737));
#36142=CARTESIAN_POINT('Ctrl Pts',(-56.9723984418365,-127.8855635432,170.349278222282));
#36143=CARTESIAN_POINT('Ctrl Pts',(-56.8968943729927,-127.9312855153,170.356001636928));
#36144=CARTESIAN_POINT('Ctrl Pts',(-56.8618468314437,-127.95869823734,170.354318648863));
#36145=CARTESIAN_POINT('Ctrl Pts',(-56.7906038202443,-128.030136710975,
170.343138480155));
#36146=CARTESIAN_POINT('Ctrl Pts',(-56.7577956176336,-128.075391549363,
170.33198630918));
#36147=CARTESIAN_POINT('Ctrl Pts',(-56.6968429788158,-128.189896425913,
170.303342043454));
#36148=CARTESIAN_POINT('Ctrl Pts',(-56.6724939299533,-128.263909086473,
170.284406576511));
#36149=CARTESIAN_POINT('Ctrl Pts',(-56.6423812329264,-128.439459862121,
170.251696500619));
#36150=CARTESIAN_POINT('Ctrl Pts',(-56.6393927090308,-128.543081774113,
170.239324614047));
#36151=CARTESIAN_POINT('Ctrl Pts',(-56.6510041624572,-128.652000402186,
170.239324614047));
#36152=CARTESIAN_POINT('',(-58.1339135773921,-128.493912351392,169.44958432285));
#36153=CARTESIAN_POINT('Origin',(-60.6261834003547,-128.228219737673,175.985485069079));
#36154=CARTESIAN_POINT('',(-59.0303912106606,-128.398341846414,169.171931975764));
#36155=CARTESIAN_POINT('Ctrl Pts',(-59.0303912106606,-128.398341846414,
169.171931975764));
#36156=CARTESIAN_POINT('Ctrl Pts',(-59.0165163081196,-128.26819144285,169.171931975764));
#36157=CARTESIAN_POINT('Ctrl Pts',(-59.0037181616419,-128.147157263456,
169.198662237769));
#36158=CARTESIAN_POINT('Ctrl Pts',(-58.9702218423946,-127.963385110068,
169.27504750851));
#36159=CARTESIAN_POINT('Ctrl Pts',(-58.951364718064,-127.894014366109,169.318504646285));
#36160=CARTESIAN_POINT('Ctrl Pts',(-58.9019171135249,-127.797205334798,
169.400604831394));
#36161=CARTESIAN_POINT('Ctrl Pts',(-58.8758894008713,-127.762920368717,
169.437671244654));
#36162=CARTESIAN_POINT('Ctrl Pts',(-58.8141250725308,-127.714902690165,
169.504417574353));
#36163=CARTESIAN_POINT('Ctrl Pts',(-58.7820497747533,-127.699108062934,
169.533169515204));
#36164=CARTESIAN_POINT('Ctrl Pts',(-58.7186114538819,-127.682162234731,
169.577043130797));
#36165=CARTESIAN_POINT('Ctrl Pts',(-58.6901182961251,-127.678249767044,
169.59337081494));
#36166=CARTESIAN_POINT('Ctrl Pts',(-58.6488514237962,-127.677212080219,
169.612056116318));
#36167=CARTESIAN_POINT('Ctrl Pts',(-58.6375449817886,-127.67736201459,169.6167136494));
#36168=CARTESIAN_POINT('Ctrl Pts',(-58.618747427092,-127.678316518326,169.623686004388));
#36169=CARTESIAN_POINT('Ctrl Pts',(-58.6113617573274,-127.678863423075,
169.626237747514));
#36170=CARTESIAN_POINT('Ctrl Pts',(-58.5970372266283,-127.680257023467,
169.63082092416));
#36171=CARTESIAN_POINT('Ctrl Pts',(-58.5901109657506,-127.681076792296,
169.632876591588));
#36172=CARTESIAN_POINT('Ctrl Pts',(-58.5740975671833,-127.683311599132,
169.637256885382));
#36173=CARTESIAN_POINT('Ctrl Pts',(-58.5649956529573,-127.684828577986,
169.639475875838));
#36174=CARTESIAN_POINT('Ctrl Pts',(-58.5370058965889,-127.690262925132,
169.645467799109));
#36175=CARTESIAN_POINT('Ctrl Pts',(-58.5181060518879,-127.694992520052,
169.648363773348));
#36176=CARTESIAN_POINT('Ctrl Pts',(-58.4576867910827,-127.713669243046,
169.654030765235));
#36177=CARTESIAN_POINT('Ctrl Pts',(-58.4175607280179,-127.731499588516,
169.652267845958));
#36178=CARTESIAN_POINT('Ctrl Pts',(-58.3427661088215,-127.777145928544,
169.639668479677));
#36179=CARTESIAN_POINT('Ctrl Pts',(-58.309210001688,-127.804399653713,169.628998799003));
#36180=CARTESIAN_POINT('Ctrl Pts',(-58.2428932484799,-127.875312955333,
169.599377687793));
#36181=CARTESIAN_POINT('Ctrl Pts',(-58.2138201458332,-127.920169607111,
169.579594235938));
#36182=CARTESIAN_POINT('Ctrl Pts',(-58.1617859003498,-128.033723723348,
169.534372726963));
#36183=CARTESIAN_POINT('Ctrl Pts',(-58.142869160262,-128.1071572635,169.508315594787));
#36184=CARTESIAN_POINT('Ctrl Pts',(-58.1219432865466,-128.28172866241,169.464936649309));
#36185=CARTESIAN_POINT('Ctrl Pts',(-58.122302123966,-128.384993723323,169.44958432285));
#36186=CARTESIAN_POINT('Ctrl Pts',(-58.1339135773921,-128.493912351392,
169.44958432285));
#36187=CARTESIAN_POINT('',(-59.7616646554053,-128.320383211643,169.03968682599));
#36188=CARTESIAN_POINT('Origin',(-60.6261834003547,-128.228219737673,175.985485069079));
#36189=CARTESIAN_POINT('',(-60.6981644400103,-128.220546077948,168.985859375881));
#36190=CARTESIAN_POINT('Ctrl Pts',(-60.6981644400103,-128.220546077948,
168.985859375881));
#36191=CARTESIAN_POINT('Ctrl Pts',(-60.6842895374694,-128.090395674385,
168.985859375881));
#36192=CARTESIAN_POINT('Ctrl Pts',(-60.6651274502667,-127.970039933589,
169.011837869164));
#36193=CARTESIAN_POINT('Ctrl Pts',(-60.6138534521269,-127.788162999541,
169.082694593096));
#36194=CARTESIAN_POINT('Ctrl Pts',(-60.5849842674264,-127.719859608108,
169.122161426924));
#36195=CARTESIAN_POINT('Ctrl Pts',(-60.5171236951126,-127.625013522177,
169.192564958381));
#36196=CARTESIAN_POINT('Ctrl Pts',(-60.4829181952001,-127.591600362852,
169.22323031794));
#36197=CARTESIAN_POINT('Ctrl Pts',(-60.4068979406267,-127.545102461279,
169.27455738956));
#36198=CARTESIAN_POINT('Ctrl Pts',(-60.3688538203507,-127.529944150403,
169.295241673531));
#36199=CARTESIAN_POINT('Ctrl Pts',(-60.2967457990367,-127.513922570189,
169.323174056586));
#36200=CARTESIAN_POINT('Ctrl Pts',(-60.2651738589284,-127.51033832127,169.332346104849));
#36201=CARTESIAN_POINT('Ctrl Pts',(-60.2206429838666,-127.509648598942,
169.340694606682));
#36202=CARTESIAN_POINT('Ctrl Pts',(-60.2085535135348,-127.509882009364,
169.342522433874));
#36203=CARTESIAN_POINT('Ctrl Pts',(-60.1886397751368,-127.510955505739,
169.344794768025));
#36204=CARTESIAN_POINT('Ctrl Pts',(-60.1808607517325,-127.511544344614,
169.34550094033));
#36205=CARTESIAN_POINT('Ctrl Pts',(-60.1658614110955,-127.513009884254,
169.346506815085));
#36206=CARTESIAN_POINT('Ctrl Pts',(-60.1586474825466,-127.513860320379,
169.346833728753));
#36207=CARTESIAN_POINT('Ctrl Pts',(-60.1420586540755,-127.516156471887,
169.347219380362));
#36208=CARTESIAN_POINT('Ctrl Pts',(-60.1326948522994,-127.517701369704,
169.347169449521));
#36209=CARTESIAN_POINT('Ctrl Pts',(-60.104100051651,-127.523200218612,169.34618874999));
#36210=CARTESIAN_POINT('Ctrl Pts',(-60.0850685703232,-127.527943846876,
169.344383044037));
#36211=CARTESIAN_POINT('Ctrl Pts',(-60.0250939025714,-127.54657317328,169.335033750972));
#36212=CARTESIAN_POINT('Ctrl Pts',(-59.9865948585421,-127.564230067651,
169.323321034333));
#36213=CARTESIAN_POINT('Ctrl Pts',(-59.9170872624789,-127.609312775691,
169.292131116497));
#36214=CARTESIAN_POINT('Ctrl Pts',(-59.8871177898037,-127.636184141664,
169.273094826274));
#36215=CARTESIAN_POINT('Ctrl Pts',(-59.8299724866298,-127.706119705437,
169.226754243875));
#36216=CARTESIAN_POINT('Ctrl Pts',(-59.806579910799,-127.750370775105,169.199489253453));
#36217=CARTESIAN_POINT('Ctrl Pts',(-59.7671497471324,-127.862581212014,
169.140318610957));
#36218=CARTESIAN_POINT('Ctrl Pts',(-59.7552021858026,-127.93527179115,169.108654159356));
#36219=CARTESIAN_POINT('Ctrl Pts',(-59.7457350244345,-128.108621614768,
169.057127370928));
#36220=CARTESIAN_POINT('Ctrl Pts',(-59.750053201979,-128.211464583572,169.03968682599));
#36221=CARTESIAN_POINT('Ctrl Pts',(-59.7616646554053,-128.320383211643,
169.03968682599));
#36222=CARTESIAN_POINT('',(-61.4396584204773,-128.141497865788,169.03345387607));
#36223=CARTESIAN_POINT('Origin',(-60.6261834003547,-128.228219737673,175.985485069079));
#36224=CARTESIAN_POINT('',(-62.3617543929757,-128.043196274694,169.206579578684));
#36225=CARTESIAN_POINT('Ctrl Pts',(-62.3617543929757,-128.043196274694,
169.206579578684));
#36226=CARTESIAN_POINT('Ctrl Pts',(-62.3478794904347,-127.913045871129,
169.206579578684));
#36227=CARTESIAN_POINT('Ctrl Pts',(-62.3227172833847,-127.793329783196,
169.230296527642));
#36228=CARTESIAN_POINT('Ctrl Pts',(-62.2554978064046,-127.613152743724,
169.291506769524));
#36229=CARTESIAN_POINT('Ctrl Pts',(-62.2178570552205,-127.545784459879,
169.324689630478));
#36230=CARTESIAN_POINT('Ctrl Pts',(-62.1349019828699,-127.452547548496,
169.379304910943));
#36231=CARTESIAN_POINT('Ctrl Pts',(-62.0942795684017,-127.419818475134,
169.401787057566));
#36232=CARTESIAN_POINT('Ctrl Pts',(-62.0080869171554,-127.374405019007,
169.434711928271));
#36233=CARTESIAN_POINT('Ctrl Pts',(-61.966167255537,-127.35965986673,169.446126459962));
#36234=CARTESIAN_POINT('Ctrl Pts',(-61.8894349505906,-127.344131266045,
169.456494281906));
#36235=CARTESIAN_POINT('Ctrl Pts',(-61.856576498855,-127.340684167861,169.457977648183));
#36236=CARTESIAN_POINT('Ctrl Pts',(-61.8113362866851,-127.340070065608,
169.45550416589));
#36237=CARTESIAN_POINT('Ctrl Pts',(-61.7991599187017,-127.3403127399,169.454396060521));
#36238=CARTESIAN_POINT('Ctrl Pts',(-61.7792808818439,-127.341382536859,
169.451836314032));
#36239=CARTESIAN_POINT('Ctrl Pts',(-61.7715591203334,-127.341965271234,
169.450655875349));
#36240=CARTESIAN_POINT('Ctrl Pts',(-61.756755859161,-127.343409907493,169.448025990428));
#36241=CARTESIAN_POINT('Ctrl Pts',(-61.7496740087988,-127.344246263201,
169.446605151303));
#36242=CARTESIAN_POINT('Ctrl Pts',(-61.7334770653336,-127.346500637149,
169.442973748057));
#36243=CARTESIAN_POINT('Ctrl Pts',(-61.7243989149161,-127.348015082622,
169.440657797718));
#36244=CARTESIAN_POINT('Ctrl Pts',(-61.6968759072649,-127.353399671236,
169.432761470076));
#36245=CARTESIAN_POINT('Ctrl Pts',(-61.6788354602793,-127.358037648619,
169.426359024997));
#36246=CARTESIAN_POINT('Ctrl Pts',(-61.6228658503647,-127.3762400091,169.40253679391));
#36247=CARTESIAN_POINT('Ctrl Pts',(-61.5883142729488,-127.393476077158,
169.381554980426));
#36248=CARTESIAN_POINT('Ctrl Pts',(-61.5283640109359,-127.437539909536,
169.333587155689));
#36249=CARTESIAN_POINT('Ctrl Pts',(-61.5038679306038,-127.463827775318,
169.307290575909));
#36250=CARTESIAN_POINT('Ctrl Pts',(-61.4596062581692,-127.532389857981,
169.24692366853));
#36251=CARTESIAN_POINT('Ctrl Pts',(-61.443509504436,-127.575863144271,169.213761681679));
#36252=CARTESIAN_POINT('Ctrl Pts',(-61.4196366076484,-127.686415072594,
169.144080688328));
#36253=CARTESIAN_POINT('Ctrl Pts',(-61.4157900717221,-127.7582420283,169.108649140134));
#36254=CARTESIAN_POINT('Ctrl Pts',(-61.4193875730265,-127.930199071595,
169.051969058407));
#36255=CARTESIAN_POINT('Ctrl Pts',(-61.4280469670512,-128.032579237718,
169.03345387607));
#36256=CARTESIAN_POINT('Ctrl Pts',(-61.4396584204773,-128.141497865788,
169.03345387607));
#36257=CARTESIAN_POINT('',(-63.0703759742411,-127.967652479905,169.431247709482));
#36258=CARTESIAN_POINT('Origin',(-60.6261834003547,-128.228219737673,175.985485069079));
#36259=CARTESIAN_POINT('',(-63.9244792683939,-127.876599362575,169.821265128268));
#36260=CARTESIAN_POINT('Ctrl Pts',(-63.9244792683939,-127.876599362574,
169.821265128269));
#36261=CARTESIAN_POINT('Ctrl Pts',(-63.9106043658529,-127.746448959011,
169.821265128269));
#36262=CARTESIAN_POINT('Ctrl Pts',(-63.8801545649898,-127.627296563903,
169.841342190036));
#36263=CARTESIAN_POINT('Ctrl Pts',(-63.7997485024906,-127.448525302545,
169.889348633101));
#36264=CARTESIAN_POINT('Ctrl Pts',(-63.7550864502697,-127.3819055363,169.914319053918));
#36265=CARTESIAN_POINT('Ctrl Pts',(-63.6612325830983,-127.289830509258,
169.949972041807));
#36266=CARTESIAN_POINT('Ctrl Pts',(-63.6163270545268,-127.257558044475,
169.962964394853));
#36267=CARTESIAN_POINT('Ctrl Pts',(-63.5246367188867,-127.212730678233,
169.975573590834));
#36268=CARTESIAN_POINT('Ctrl Pts',(-63.4811600294583,-127.198151515523,
169.977054999153));
#36269=CARTESIAN_POINT('Ctrl Pts',(-63.4041176042462,-127.182655975731,
169.969255719861));
#36270=CARTESIAN_POINT('Ctrl Pts',(-63.3718396789871,-127.179146989545,
169.962964196295));
#36271=CARTESIAN_POINT('Ctrl Pts',(-63.3284860194241,-127.178331768181,
169.949812479676));
#36272=CARTESIAN_POINT('Ctrl Pts',(-63.3169239346392,-127.17850895578,169.945832840802));
#36273=CARTESIAN_POINT('Ctrl Pts',(-63.2982284678402,-127.179452576264,
169.938589776834));
#36274=CARTESIAN_POINT('Ctrl Pts',(-63.2910112559024,-127.179981522283,
169.935591329969));
#36275=CARTESIAN_POINT('Ctrl Pts',(-63.2772635681678,-127.181313627362,
169.929478524726));
#36276=CARTESIAN_POINT('Ctrl Pts',(-63.2707258659438,-127.182091973242,
169.926392506813));
#36277=CARTESIAN_POINT('Ctrl Pts',(-63.2558653474691,-127.184203875358,
169.918955092668));
#36278=CARTESIAN_POINT('Ctrl Pts',(-63.2476037863023,-127.185631266962,
169.914507717447));
#36279=CARTESIAN_POINT('Ctrl Pts',(-63.2227671202083,-127.190729473619,
169.900154667556));
#36280=CARTESIAN_POINT('Ctrl Pts',(-63.2067827832207,-127.195148255939,
169.889527570186));
#36281=CARTESIAN_POINT('Ctrl Pts',(-63.1581459365239,-127.212568894871,
169.852616862557));
#36282=CARTESIAN_POINT('Ctrl Pts',(-63.1296328608877,-127.229161218297,
169.823585338963));
#36283=CARTESIAN_POINT('Ctrl Pts',(-63.0829548063272,-127.271810144691,
169.761627322943));
#36284=CARTESIAN_POINT('Ctrl Pts',(-63.0655007825547,-127.297347280196,
169.729598715239));
#36285=CARTESIAN_POINT('Ctrl Pts',(-63.0370861717759,-127.364219960214,
169.658713788112));
#36286=CARTESIAN_POINT('Ctrl Pts',(-63.0294765287605,-127.4067884638,169.621582058969));
#36287=CARTESIAN_POINT('Ctrl Pts',(-63.0232099521103,-127.515463440772,
169.545440320815));
#36288=CARTESIAN_POINT('Ctrl Pts',(-63.0281254860832,-127.586356301289,
169.508300828821));
#36289=CARTESIAN_POINT('Ctrl Pts',(-63.0456343296776,-127.756830302552,
169.449761494122));
#36290=CARTESIAN_POINT('Ctrl Pts',(-63.0587645208149,-127.858733851834,
169.431247709482));
#36291=CARTESIAN_POINT('Ctrl Pts',(-63.0703759742411,-127.967652479905,
169.431247709482));
#36292=CARTESIAN_POINT('',(-64.5590459398891,-127.80895031592,170.209949994551));
#36293=CARTESIAN_POINT('Origin',(-60.6261834003547,-128.228219737673,175.985485069079));
#36294=CARTESIAN_POINT('',(-65.2955191767793,-127.730437348568,170.794192734786));
#36295=CARTESIAN_POINT('Ctrl Pts',(-65.2955191767793,-127.730437348568,
170.794192734786));
#36296=CARTESIAN_POINT('Ctrl Pts',(-65.2816442742383,-127.600286945004,
170.794192734786));
#36297=CARTESIAN_POINT('Ctrl Pts',(-65.2469267013282,-127.481589522909,
170.80946310351));
#36298=CARTESIAN_POINT('Ctrl Pts',(-65.1568593030527,-127.303848224493,
170.841475787782));
#36299=CARTESIAN_POINT('Ctrl Pts',(-65.1073342677368,-127.237746884734,
170.856782578368));
#36300=CARTESIAN_POINT('Ctrl Pts',(-65.0074107092975,-127.146318927332,
170.87140125162));
#36301=CARTESIAN_POINT('Ctrl Pts',(-64.9606047860984,-127.114249057312,
170.874148742754));
#36302=CARTESIAN_POINT('Ctrl Pts',(-64.8684109837781,-127.069475363982,
170.865709463374));
#36303=CARTESIAN_POINT('Ctrl Pts',(-64.8257862688682,-127.054805375097,
170.857171654254));
#36304=CARTESIAN_POINT('Ctrl Pts',(-64.7527659098192,-127.03888105618,170.831658539489));
#36305=CARTESIAN_POINT('Ctrl Pts',(-64.722901811052,-127.035114739964,170.817957766561));
#36306=CARTESIAN_POINT('Ctrl Pts',(-64.6839209542326,-127.033833348613,
170.794892145581));
#36307=CARTESIAN_POINT('Ctrl Pts',(-64.673638633589,-127.033874104805,170.788272255348));
#36308=CARTESIAN_POINT('Ctrl Pts',(-64.6572068205804,-127.034576404671,
170.776766814454));
#36309=CARTESIAN_POINT('Ctrl Pts',(-64.6509121233055,-127.035007004464,
170.772124618239));
#36310=CARTESIAN_POINT('Ctrl Pts',(-64.639018156889,-127.036141490465,170.762884146693));
#36311=CARTESIAN_POINT('Ctrl Pts',(-64.6334050488427,-127.03682126843,170.758312298135));
#36312=CARTESIAN_POINT('Ctrl Pts',(-64.620747827179,-127.038698284386,170.74750110857));
#36313=CARTESIAN_POINT('Ctrl Pts',(-64.6137863359549,-127.039987079847,
170.741180773749));
#36314=CARTESIAN_POINT('Ctrl Pts',(-64.5930944395732,-127.044643426362,
170.721205148696));
#36315=CARTESIAN_POINT('Ctrl Pts',(-64.5801117945996,-127.04874220826,170.706971007307));
#36316=CARTESIAN_POINT('Ctrl Pts',(-64.5417092629567,-127.065071800833,
170.659116939299));
#36317=CARTESIAN_POINT('Ctrl Pts',(-64.5209747884925,-127.080834873406,
170.623722912221));
#36318=CARTESIAN_POINT('Ctrl Pts',(-64.4905124823315,-127.121755092684,
170.5513754796));
#36319=CARTESIAN_POINT('Ctrl Pts',(-64.4812599206048,-127.146417897543,
170.515476230233));
#36320=CARTESIAN_POINT('Ctrl Pts',(-64.4707348287764,-127.211383435322,
170.438192857666));
#36321=CARTESIAN_POINT('Ctrl Pts',(-64.4723103450735,-127.25297273956,170.399249347361));
#36322=CARTESIAN_POINT('Ctrl Pts',(-64.48467592649,-127.359661404002,170.321071945463));
#36323=CARTESIAN_POINT('Ctrl Pts',(-64.4985053552031,-127.429603983786,
170.284382921946));
#36324=CARTESIAN_POINT('Ctrl Pts',(-64.5299637440578,-127.598590870331,
170.227386427625));
#36325=CARTESIAN_POINT('Ctrl Pts',(-64.5474344864629,-127.700031687849,
170.209949994551));
#36326=CARTESIAN_POINT('Ctrl Pts',(-64.5590459398891,-127.80895031592,170.209949994551));
#36327=CARTESIAN_POINT('',(-65.819152230113,-127.674614566746,171.324305384935));
#36328=CARTESIAN_POINT('Origin',(-60.6261834003547,-128.228219737673,175.985485069079));
#36329=CARTESIAN_POINT('',(-66.3951942621838,-127.613204637651,172.068819382192));
#36330=CARTESIAN_POINT('Ctrl Pts',(-66.3951942621838,-127.613204637651,
172.068819382192));
#36331=CARTESIAN_POINT('Ctrl Pts',(-66.3813193596428,-127.483054234087,
172.068819382192));
#36332=CARTESIAN_POINT('Ctrl Pts',(-66.3436018638514,-127.364676623814,
172.078395599549));
#36333=CARTESIAN_POINT('Ctrl Pts',(-66.2479598612561,-127.187529615458,
172.092554064181));
#36334=CARTESIAN_POINT('Ctrl Pts',(-66.1960127796873,-127.121686482012,
172.097307649504));
#36335=CARTESIAN_POINT('Ctrl Pts',(-66.095201381932,-127.030353174215,172.090042423964));
#36336=CARTESIAN_POINT('Ctrl Pts',(-66.0489882276089,-126.998220111072,
172.082385378989));
#36337=CARTESIAN_POINT('Ctrl Pts',(-65.9613144359736,-126.952964554406,
172.053388084489));
#36338=CARTESIAN_POINT('Ctrl Pts',(-65.9219011842493,-126.937952202089,
172.035327244364));
#36339=CARTESIAN_POINT('Ctrl Pts',(-65.8570013299288,-126.921162183116,
171.993583023619));
#36340=CARTESIAN_POINT('Ctrl Pts',(-65.8312440748459,-126.916958049926,
171.973269240452));
#36341=CARTESIAN_POINT('Ctrl Pts',(-65.7988681395039,-126.914972529819,
171.941630205162));
#36342=CARTESIAN_POINT('Ctrl Pts',(-65.7904566887047,-126.914813838786,
171.932754787527));
#36343=CARTESIAN_POINT('Ctrl Pts',(-65.7772370578837,-126.915173698571,
171.917655624111));
#36344=CARTESIAN_POINT('Ctrl Pts',(-65.7722292271653,-126.915467109792,
171.911639466116));
#36345=CARTESIAN_POINT('Ctrl Pts',(-65.7628793984067,-126.916330373721,
171.899808350887));
#36346=CARTESIAN_POINT('Ctrl Pts',(-65.7585175965269,-126.916876754089,
171.894016370906));
#36347=CARTESIAN_POINT('Ctrl Pts',(-65.748802495888,-126.918440120287,171.880459712958));
#36348=CARTESIAN_POINT('Ctrl Pts',(-65.7435489999587,-126.91954683204,171.872633733424));
#36349=CARTESIAN_POINT('Ctrl Pts',(-65.728219422495,-126.923631519533,171.848196443929));
#36350=CARTESIAN_POINT('Ctrl Pts',(-65.7190096041221,-126.927328092909,
171.83118249508));
#36351=CARTESIAN_POINT('Ctrl Pts',(-65.6931481581786,-126.942320721961,
171.775166171184));
#36352=CARTESIAN_POINT('Ctrl Pts',(-65.6814803202524,-126.957117230505,
171.735466612822));
#36353=CARTESIAN_POINT('Ctrl Pts',(-65.6692349030829,-126.996095407713,
171.656934333413));
#36354=CARTESIAN_POINT('Ctrl Pts',(-65.6688665697256,-127.019811094472,
171.619250776266));
#36355=CARTESIAN_POINT('Ctrl Pts',(-65.6772337803267,-127.082762586595,
171.54006038696));
#36356=CARTESIAN_POINT('Ctrl Pts',(-65.6881586964586,-127.123355182348,
171.501568350758));
#36357=CARTESIAN_POINT('Ctrl Pts',(-65.7190994405689,-127.228063610348,
171.425898671551));
#36358=CARTESIAN_POINT('Ctrl Pts',(-65.7414765457023,-127.297094950719,
171.391792349199));
#36359=CARTESIAN_POINT('Ctrl Pts',(-65.7861119859214,-127.464677075554,
171.339651124332));
#36360=CARTESIAN_POINT('Ctrl Pts',(-65.8075407766868,-127.565695938674,
171.324305384935));
#36361=CARTESIAN_POINT('Ctrl Pts',(-65.819152230113,-127.674614566746,171.324305384935));
#36362=CARTESIAN_POINT('',(-66.7774620476251,-127.572452337832,172.709551595863));
#36363=CARTESIAN_POINT('Origin',(-60.6261834003547,-128.228219737673,175.985485069079));
#36364=CARTESIAN_POINT('',(-67.1595954058001,-127.531714368858,173.57106840282));
#36365=CARTESIAN_POINT('Ctrl Pts',(-67.1595954058001,-127.531714368858,
173.57106840282));
#36366=CARTESIAN_POINT('Ctrl Pts',(-67.1457205032591,-127.401563965294,
173.57106840282));
#36367=CARTESIAN_POINT('Ctrl Pts',(-67.1064452783649,-127.28335241935,173.574393933864));
#36368=CARTESIAN_POINT('Ctrl Pts',(-67.0096393786517,-127.106329490205,
173.569875340355));
#36369=CARTESIAN_POINT('Ctrl Pts',(-66.9578519481981,-127.040469336883,
173.563799459316));
#36370=CARTESIAN_POINT('Ctrl Pts',(-66.8613861610659,-126.948672757959,
173.535072563485));
#36371=CARTESIAN_POINT('Ctrl Pts',(-66.8182244895502,-126.916214386363,
173.517455982022));
#36372=CARTESIAN_POINT('Ctrl Pts',(-66.7398314993754,-126.869969434257,
173.469585889759));
#36373=CARTESIAN_POINT('Ctrl Pts',(-66.705802560936,-126.854383078172,173.443051649007));
#36374=CARTESIAN_POINT('Ctrl Pts',(-66.652649715689,-126.836340749551,173.387502344657));
#36375=CARTESIAN_POINT('Ctrl Pts',(-66.6324536466569,-126.831543756775,
173.361756114491));
#36376=CARTESIAN_POINT('Ctrl Pts',(-66.6085308974996,-126.828657070545,
173.32338241062));
#36377=CARTESIAN_POINT('Ctrl Pts',(-66.6024726940923,-126.828247507619,
173.312767272596));
#36378=CARTESIAN_POINT('Ctrl Pts',(-66.5932270935042,-126.828183709231,
173.294951895151));
#36379=CARTESIAN_POINT('Ctrl Pts',(-66.5897956932282,-126.828309062434,
173.287911412611));
#36380=CARTESIAN_POINT('Ctrl Pts',(-66.5835325624315,-126.828843263739,
173.274177235112));
#36381=CARTESIAN_POINT('Ctrl Pts',(-66.5806760573395,-126.829229169412,
173.26750173253));
#36382=CARTESIAN_POINT('Ctrl Pts',(-66.5744709165635,-126.83041835044,173.251987469885));
#36383=CARTESIAN_POINT('Ctrl Pts',(-66.5712340788036,-126.831310072958,
173.243110663121));
#36384=CARTESIAN_POINT('Ctrl Pts',(-66.5621727309781,-126.834726525295,
173.215631915624));
#36385=CARTESIAN_POINT('Ctrl Pts',(-66.5572876108246,-126.837962056948,
173.196826948178));
#36386=CARTESIAN_POINT('Ctrl Pts',(-66.5455451789095,-126.851449504777,
173.135903833527));
#36387=CARTESIAN_POINT('Ctrl Pts',(-66.5437050929278,-126.865198309306,
173.094205937912));
#36388=CARTESIAN_POINT('Ctrl Pts',(-66.5506190059696,-126.902133973911,
173.01405282234));
#36389=CARTESIAN_POINT('Ctrl Pts',(-66.559301348245,-126.924884798181,172.976774988782));
#36390=CARTESIAN_POINT('Ctrl Pts',(-66.5864656928081,-126.985832390242,
172.900279840317));
#36391=CARTESIAN_POINT('Ctrl Pts',(-66.6063608961624,-127.025468693448,
172.864476295449));
#36392=CARTESIAN_POINT('Ctrl Pts',(-66.6547402866562,-127.128318045238,
172.79571198564));
#36393=CARTESIAN_POINT('Ctrl Pts',(-66.6848020900059,-127.196530145439,
172.766170499937));
#36394=CARTESIAN_POINT('Ctrl Pts',(-66.741076285365,-127.36287150122,172.721914802988));
#36395=CARTESIAN_POINT('Ctrl Pts',(-66.7658505941991,-127.463533709763,
172.709551595863));
#36396=CARTESIAN_POINT('Ctrl Pts',(-66.7774620476251,-127.572452337832,
172.709551595863));
#36397=CARTESIAN_POINT('Origin',(-60.6261834003547,-128.228219737673,175.985485069079));
#36398=CARTESIAN_POINT('Origin',(-60.6261834003547,-128.228219737673,175.985485069079));
#36399=CARTESIAN_POINT('Origin',(-60.6261834003547,-128.228219737673,175.985485069079));
#36400=CARTESIAN_POINT('Origin',(-60.6261834003547,-128.228219737673,175.985485069079));
#36401=CARTESIAN_POINT('Origin',(-60.6261834003547,-128.228219737673,175.985485069079));
#36402=CARTESIAN_POINT('Origin',(-60.6261834003547,-128.228219737673,175.985485069079));
#36403=CARTESIAN_POINT('Origin',(-60.6261834003547,-128.228219737673,175.985485069079));
#36404=CARTESIAN_POINT('Origin',(-60.6261834003547,-128.228219737673,175.985485069079));
#36405=CARTESIAN_POINT('Origin',(-60.6261834003547,-128.228219737673,175.985485069079));
#36406=CARTESIAN_POINT('Origin',(-60.6261834003547,-128.228219737673,175.985485069079));
#36407=CARTESIAN_POINT('',(-56.6933208608202,-128.647489159427,181.761020143608));
#36408=CARTESIAN_POINT('Origin',(-60.6261834003547,-128.228219737673,175.985485069079));
#36409=CARTESIAN_POINT('',(-55.9568476239301,-128.726002126779,181.176777403373));
#36410=CARTESIAN_POINT('Ctrl Pts',(-55.9568476239301,-128.726002126779,
181.176777403373));
#36411=CARTESIAN_POINT('Ctrl Pts',(-55.9429727213892,-128.595851723216,
181.176777403373));
#36412=CARTESIAN_POINT('Ctrl Pts',(-55.9518865477261,-128.472502902465,
181.161507034649));
#36413=CARTESIAN_POINT('Ctrl Pts',(-56.0024587592649,-128.279768482043,
181.129494350376));
#36414=CARTESIAN_POINT('Ctrl Pts',(-56.0369354276589,-128.204711999462,
181.11418755979));
#36415=CARTESIAN_POINT('Ctrl Pts',(-56.1153386429352,-128.094273216599,
181.099568886539));
#36416=CARTESIAN_POINT('Ctrl Pts',(-56.1543317368433,-128.053056598142,
181.096821395405));
#36417=CARTESIAN_POINT('Ctrl Pts',(-56.2350144505794,-127.989853113231,
181.105260674785));
#36418=CARTESIAN_POINT('Ctrl Pts',(-56.2735885050927,-127.966526793044,
181.113798483904));
#36419=CARTESIAN_POINT('Ctrl Pts',(-56.3416106408167,-127.935566401895,
181.13931159867));
#36420=CARTESIAN_POINT('Ctrl Pts',(-56.3700095524372,-127.925588859522,
181.153012371598));
#36421=CARTESIAN_POINT('Ctrl Pts',(-56.4078441925729,-127.916118423,181.176077992577));
#36422=CARTESIAN_POINT('Ctrl Pts',(-56.4179040148444,-127.913990570853,
181.182697882811));
#36423=CARTESIAN_POINT('Ctrl Pts',(-56.4341145873676,-127.911212974341,
181.194203323706));
#36424=CARTESIAN_POINT('Ctrl Pts',(-56.4403585921181,-127.910306864729,
181.198845519921));
#36425=CARTESIAN_POINT('Ctrl Pts',(-56.4522244164565,-127.908908398299,
181.208085991466));
#36426=CARTESIAN_POINT('Ctrl Pts',(-56.4578546814881,-127.908389557577,
181.212657840024));
#36427=CARTESIAN_POINT('Ctrl Pts',(-56.4706231455126,-127.907556025573,
181.223469029589));
#36428=CARTESIAN_POINT('Ctrl Pts',(-56.4776998809229,-127.907348252287,
181.22978936441));
#36429=CARTESIAN_POINT('Ctrl Pts',(-56.4989083753106,-127.907537737214,
181.249764989463));
#36430=CARTESIAN_POINT('Ctrl Pts',(-56.5124633358786,-127.908807433066,
181.263999130852));
#36431=CARTESIAN_POINT('Ctrl Pts',(-56.5534453507174,-127.916674102625,
181.31185319886));
#36432=CARTESIAN_POINT('Ctrl Pts',(-56.5770369576528,-127.927711718782,
181.347247225938));
#36433=CARTESIAN_POINT('Ctrl Pts',(-56.6154413325744,-127.961290289766,
181.419594658559));
#36434=CARTESIAN_POINT('Ctrl Pts',(-56.6296852961918,-127.983448208045,
181.455493907926));
#36435=CARTESIAN_POINT('Ctrl Pts',(-56.6536697087511,-128.044734802102,
181.532777280493));
#36436=CARTESIAN_POINT('Ctrl Pts',(-56.6608973514961,-128.0857215519,181.571720790798));
#36437=CARTESIAN_POINT('Ctrl Pts',(-56.671301510426,-128.192619317084,181.649898192696));
#36438=CARTESIAN_POINT('Ctrl Pts',(-56.6725280064147,-128.263905453695,
181.686587216213));
#36439=CARTESIAN_POINT('Ctrl Pts',(-56.6774020108528,-128.435726413225,
181.743583710534));
#36440=CARTESIAN_POINT('Ctrl Pts',(-56.681709407394,-128.538570531355,181.761020143608));
#36441=CARTESIAN_POINT('Ctrl Pts',(-56.6933208608202,-128.647489159427,
181.761020143608));
#36442=CARTESIAN_POINT('',(-55.4332145705962,-128.781824908601,180.646664753224));
#36443=CARTESIAN_POINT('Origin',(-60.6261834003547,-128.228219737673,175.985485069079));
#36444=CARTESIAN_POINT('',(-54.8571725385255,-128.843234837696,179.902150755967));
#36445=CARTESIAN_POINT('Ctrl Pts',(-54.8571725385255,-128.843234837696,
179.902150755967));
#36446=CARTESIAN_POINT('Ctrl Pts',(-54.8432976359846,-128.713084434133,
179.902150755967));
#36447=CARTESIAN_POINT('Ctrl Pts',(-54.8552113852029,-128.58941580156,179.89257453861));
#36448=CARTESIAN_POINT('Ctrl Pts',(-54.9113582010602,-128.396087091074,
179.878416073978));
#36449=CARTESIAN_POINT('Ctrl Pts',(-54.9482569157069,-128.320772402181,
179.873662488655));
#36450=CARTESIAN_POINT('Ctrl Pts',(-55.0275479703008,-128.210238969717,
179.880927714194));
#36451=CARTESIAN_POINT('Ctrl Pts',(-55.0659482953328,-128.169085544381,
179.88858475917));
#36452=CARTESIAN_POINT('Ctrl Pts',(-55.1421109983837,-128.106363922807,
179.917582053669));
#36453=CARTESIAN_POINT('Ctrl Pts',(-55.1774735897115,-128.083379966052,
179.935642893795));
#36454=CARTESIAN_POINT('Ctrl Pts',(-55.2373752207072,-128.053285274958,
179.97738711454));
#36455=CARTESIAN_POINT('Ctrl Pts',(-55.2616672886433,-128.04374554956,179.997700897707));
#36456=CARTESIAN_POINT('Ctrl Pts',(-55.292897007302,-128.034979241794,180.029339932996));
#36457=CARTESIAN_POINT('Ctrl Pts',(-55.3010859597289,-128.033050836872,
180.038215350631));
#36458=CARTESIAN_POINT('Ctrl Pts',(-55.3140843500635,-128.030615680441,
180.053314514049));
#36459=CARTESIAN_POINT('Ctrl Pts',(-55.3190414882579,-128.029846759401,
180.059330672043));
#36460=CARTESIAN_POINT('Ctrl Pts',(-55.3283631749389,-128.028719515043,
180.071161787272));
#36461=CARTESIAN_POINT('Ctrl Pts',(-55.332742133804,-128.028334071918,180.076953767253));
#36462=CARTESIAN_POINT('Ctrl Pts',(-55.3425684768033,-128.027814189671,
180.0905104252));
#36463=CARTESIAN_POINT('Ctrl Pts',(-55.3479372169186,-128.027788500095,
180.098336404735));
#36464=CARTESIAN_POINT('Ctrl Pts',(-55.3637833923889,-128.028549644043,
180.12277369423));
#36465=CARTESIAN_POINT('Ctrl Pts',(-55.3735655263562,-128.030221548417,
180.139787643079));
#36466=CARTESIAN_POINT('Ctrl Pts',(-55.4020064554956,-128.039425181497,
180.195803966976));
#36467=CARTESIAN_POINT('Ctrl Pts',(-55.416531425893,-128.051429361683,180.235503525337));
#36468=CARTESIAN_POINT('Ctrl Pts',(-55.4367189118229,-128.086949974739,
180.314035804746));
#36469=CARTESIAN_POINT('Ctrl Pts',(-55.4420786470709,-128.110055011116,
180.351719361893));
#36470=CARTESIAN_POINT('Ctrl Pts',(-55.4471707572007,-128.17335565083,180.430909751199));
#36471=CARTESIAN_POINT('Ctrl Pts',(-55.4450490001109,-128.215339109112,
180.469401787402));
#36472=CARTESIAN_POINT('Ctrl Pts',(-55.4368779963468,-128.324217110737,
180.545071466608));
#36473=CARTESIAN_POINT('Ctrl Pts',(-55.4295568159153,-128.396414486761,
180.57917778896));
#36474=CARTESIAN_POINT('Ctrl Pts',(-55.4212537689891,-128.569640208002,
180.631319013827));
#36475=CARTESIAN_POINT('Ctrl Pts',(-55.4216031171701,-128.672906280531,
180.646664753224));
#36476=CARTESIAN_POINT('Ctrl Pts',(-55.4332145705962,-128.781824908601,
180.646664753224));
#36477=CARTESIAN_POINT('',(-54.4749047530841,-128.883987137515,179.261418542296));
#36478=CARTESIAN_POINT('Origin',(-60.6261834003547,-128.228219737673,175.985485069079));
#36479=CARTESIAN_POINT('',(-54.0927713949092,-128.924725106489,178.399901735339));
#36480=CARTESIAN_POINT('Ctrl Pts',(-54.0927713949092,-128.924725106489,
178.399901735339));
#36481=CARTESIAN_POINT('Ctrl Pts',(-54.0788964923682,-128.794574702925,
178.399901735339));
#36482=CARTESIAN_POINT('Ctrl Pts',(-54.0923679706893,-128.670740006023,
178.396576204295));
#36483=CARTESIAN_POINT('Ctrl Pts',(-54.1496786836653,-128.477287216329,
178.401094797804));
#36484=CARTESIAN_POINT('Ctrl Pts',(-54.1864177471969,-128.401989547312,
178.407170678843));
#36485=CARTESIAN_POINT('Ctrl Pts',(-54.2613631911669,-128.291919385972,
178.435897574673));
#36486=CARTESIAN_POINT('Ctrl Pts',(-54.2967120333915,-128.251091269091,
178.453514156137));
#36487=CARTESIAN_POINT('Ctrl Pts',(-54.3635939349819,-128.189359042956,
178.5013842484));
#36488=CARTESIAN_POINT('Ctrl Pts',(-54.3935722130247,-128.166949089969,
178.527918489152));
#36489=CARTESIAN_POINT('Ctrl Pts',(-54.4417268349467,-128.138106708523,
178.583467793501));
#36490=CARTESIAN_POINT('Ctrl Pts',(-54.4604577168323,-128.129159842712,
178.609214023668));
#36491=CARTESIAN_POINT('Ctrl Pts',(-54.4832342493068,-128.121294701068,
178.647587727539));
#36492=CARTESIAN_POINT('Ctrl Pts',(-54.4890699543414,-128.119617168039,
178.658202865563));
#36493=CARTESIAN_POINT('Ctrl Pts',(-54.4980943144427,-128.117605669782,
178.676018243009));
#36494=CARTESIAN_POINT('Ctrl Pts',(-54.5014750221949,-128.117004806759,
178.683058725548));
#36495=CARTESIAN_POINT('Ctrl Pts',(-54.5077100109139,-128.116206625025,
178.696792903046));
#36496=CARTESIAN_POINT('Ctrl Pts',(-54.5105836729911,-128.115981656595,
178.703468405629));
#36497=CARTESIAN_POINT('Ctrl Pts',(-54.5169000561279,-128.115835959519,
178.718982668274));
#36498=CARTESIAN_POINT('Ctrl Pts',(-54.520252138074,-128.116025259176,178.727859475038));
#36499=CARTESIAN_POINT('Ctrl Pts',(-54.5298300839057,-128.117454638282,
178.755338222534));
#36500=CARTESIAN_POINT('Ctrl Pts',(-54.5352875196535,-128.119587584378,
178.77414318998));
#36501=CARTESIAN_POINT('Ctrl Pts',(-54.5496094347646,-128.130296398681,
178.835066304632));
#36502=CARTESIAN_POINT('Ctrl Pts',(-54.5543066532175,-128.143348282882,
178.876764200246));
#36503=CARTESIAN_POINT('Ctrl Pts',(-54.5553348089362,-128.18091140854,178.956917315818));
#36504=CARTESIAN_POINT('Ctrl Pts',(-54.5516438685516,-128.204981307407,
178.994195149376));
#36505=CARTESIAN_POINT('Ctrl Pts',(-54.5379388447194,-128.270285847182,
179.070690297841));
#36506=CARTESIAN_POINT('Ctrl Pts',(-54.5268468004073,-128.313225598012,
179.10649384271));
#36507=CARTESIAN_POINT('Ctrl Pts',(-54.5012371502593,-128.423962675849,
179.17525815252));
#36508=CARTESIAN_POINT('Ctrl Pts',(-54.4862312716116,-128.496979292044,
179.204799638222));
#36509=CARTESIAN_POINT('Ctrl Pts',(-54.4662894695462,-128.671445782337,
179.249055335171));
#36510=CARTESIAN_POINT('Ctrl Pts',(-54.4632932996579,-128.775068509443,
179.261418542296));
#36511=CARTESIAN_POINT('Ctrl Pts',(-54.4749047530841,-128.883987137515,
179.261418542296));
#36512=CARTESIAN_POINT('',(-53.8740848915632,-128.948038548767,177.685786985438));
#36513=CARTESIAN_POINT('Origin',(-60.6261834003547,-128.228219737673,175.985485069079));
#36514=CARTESIAN_POINT('',(-53.708068409063,-128.96573701494,176.757335594116));
#36515=CARTESIAN_POINT('Ctrl Pts',(-53.708068409063,-128.96573701494,176.757335594116));
#36516=CARTESIAN_POINT('Ctrl Pts',(-53.694193506522,-128.835586611376,176.757335594116));
#36517=CARTESIAN_POINT('Ctrl Pts',(-53.7076899906135,-128.711749248692,
176.760454017161));
#36518=CARTESIAN_POINT('Ctrl Pts',(-53.7616862520391,-128.518649801677,
176.783387064581));
#36519=CARTESIAN_POINT('Ctrl Pts',(-53.7956932454308,-128.443643389589,
176.799939303861));
#36520=CARTESIAN_POINT('Ctrl Pts',(-53.8613121799281,-128.334567496468,
176.848458367214));
#36521=CARTESIAN_POINT('Ctrl Pts',(-53.891328166503,-128.294307897628,176.875010673484));
#36522=CARTESIAN_POINT('Ctrl Pts',(-53.9447078423048,-128.234015098969,
176.93897152775));
#36523=CARTESIAN_POINT('Ctrl Pts',(-53.9674418736801,-128.212377431075,
176.972437095504));
#36524=CARTESIAN_POINT('Ctrl Pts',(-54.0009056756515,-128.185101189184,
177.038563159802));
#36525=CARTESIAN_POINT('Ctrl Pts',(-54.0129442250395,-128.176867770727,
177.068245559654));
#36526=CARTESIAN_POINT('Ctrl Pts',(-54.0259105750774,-128.170048460072,
177.111123791921));
#36527=CARTESIAN_POINT('Ctrl Pts',(-54.0290474173572,-128.168658643843,
177.122861737096));
#36528=CARTESIAN_POINT('Ctrl Pts',(-54.0335668553725,-128.167127400378,
177.14235796359));
#36529=CARTESIAN_POINT('Ctrl Pts',(-54.0351731852033,-128.166715697895,
177.15001360342));
#36530=CARTESIAN_POINT('Ctrl Pts',(-54.0379583033214,-128.166285295416,
177.164852662714));
#36531=CARTESIAN_POINT('Ctrl Pts',(-54.039160160367,-128.166238552571,177.17202373195));
#36532=CARTESIAN_POINT('Ctrl Pts',(-54.0416027309134,-128.166505829798,
177.188593966742));
#36533=CARTESIAN_POINT('Ctrl Pts',(-54.0427466926584,-128.166930529821,
177.198005712992));
#36534=CARTESIAN_POINT('Ctrl Pts',(-54.0455147848535,-128.16908588482,177.226928953567));
#36535=CARTESIAN_POINT('Ctrl Pts',(-54.0463469865043,-128.171711911772,
177.246432063255));
#36536=CARTESIAN_POINT('Ctrl Pts',(-54.0457925050324,-128.184006649338,
177.308721338684));
#36537=CARTESIAN_POINT('Ctrl Pts',(-54.040472009355,-128.198126488793,177.349994241424));
#36538=CARTESIAN_POINT('Ctrl Pts',(-54.0225118642734,-128.237713894175,
177.427109985427));
#36539=CARTESIAN_POINT('Ctrl Pts',(-54.0101297933627,-128.26271032562,177.461815643209));
#36540=CARTESIAN_POINT('Ctrl Pts',(-53.9788152251371,-128.329892160475,
177.531169930852));
#36541=CARTESIAN_POINT('Ctrl Pts',(-53.9596533267027,-128.373692211668,
177.5622042125));
#36542=CARTESIAN_POINT('Ctrl Pts',(-53.9187550172226,-128.486059162732,
177.620066821173));
#36543=CARTESIAN_POINT('Ctrl Pts',(-53.8973740252904,-128.559755408594,
177.643326626457));
#36544=CARTESIAN_POINT('Ctrl Pts',(-53.8680081664537,-128.7352265663,177.677124815244));
#36545=CARTESIAN_POINT('Ctrl Pts',(-53.8624734381369,-128.839119920695,
177.685786985438));
#36546=CARTESIAN_POINT('Ctrl Pts',(-53.8740848915633,-128.948038548767,
177.685786985438));
#36547=CARTESIAN_POINT('',(-53.6656724524939,-128.970256707153,176.011340061548));
#36548=CARTESIAN_POINT('Origin',(-60.6261834003547,-128.228219737673,175.985485069079));
#36549=CARTESIAN_POINT('',(-53.7254211201858,-128.963887100003,175.06991230594));
#36550=CARTESIAN_POINT('Ctrl Pts',(-53.7254211201858,-128.963887100003,
175.06991230594));
#36551=CARTESIAN_POINT('Ctrl Pts',(-53.7115462176449,-128.833736696439,
175.06991230594));
#36552=CARTESIAN_POINT('Ctrl Pts',(-53.72353353093,-128.710060221445,175.079293451662));
#36553=CARTESIAN_POINT('Ctrl Pts',(-53.7699296160128,-128.517771004004,
175.119308167634));
#36554=CARTESIAN_POINT('Ctrl Pts',(-53.7987908982256,-128.443313159106,
175.145374809174));
#36555=CARTESIAN_POINT('Ctrl Pts',(-53.8506444472315,-128.335704748044,
175.210866288448));
#36556=CARTESIAN_POINT('Ctrl Pts',(-53.8733561315008,-128.296223836628,
175.244811195998));
#36557=CARTESIAN_POINT('Ctrl Pts',(-53.9097968574698,-128.237736843189,
175.321145639904));
#36558=CARTESIAN_POINT('Ctrl Pts',(-53.9238477180795,-128.21702485931,175.359597637505));
#36559=CARTESIAN_POINT('Ctrl Pts',(-53.9405306662796,-128.191537568542,
175.432457455253));
#36560=CARTESIAN_POINT('Ctrl Pts',(-53.9451346707625,-128.184096722242,
175.464350991603));
#36561=CARTESIAN_POINT('Ctrl Pts',(-53.9475039742569,-128.178407127546,
175.509241825261));
#36562=CARTESIAN_POINT('Ctrl Pts',(-53.9477531865121,-128.17732515197,175.521420410881));
#36563=CARTESIAN_POINT('Ctrl Pts',(-53.947498620285,-128.176302849251,175.541464436604));
#36564=CARTESIAN_POINT('Ctrl Pts',(-53.9472357451108,-128.17609041651,175.549290315765));
#36565=CARTESIAN_POINT('Ctrl Pts',(-53.9464083139291,-128.176045135921,
175.564371864667));
#36566=CARTESIAN_POINT('Ctrl Pts',(-53.9458690169309,-128.17618401173,175.57162174408));
#36567=CARTESIAN_POINT('Ctrl Pts',(-53.9442990540655,-128.176879051825,
175.5882849492));
#36568=CARTESIAN_POINT('Ctrl Pts',(-53.9431717614975,-128.177545882733,
175.597684658454));
#36569=CARTESIAN_POINT('Ctrl Pts',(-53.9389841399988,-128.180442763281,
175.626371478498));
#36570=CARTESIAN_POINT('Ctrl Pts',(-53.9351593734685,-128.183565254154,
175.645439280584));
#36571=CARTESIAN_POINT('Ctrl Pts',(-53.9198356749549,-128.197434488929,
175.705474690515));
#36572=CARTESIAN_POINT('Ctrl Pts',(-53.9048896960938,-128.212580469198,
175.743923969295));
#36573=CARTESIAN_POINT('Ctrl Pts',(-53.8692158106455,-128.254056277646,
175.81352065499));
#36574=CARTESIAN_POINT('Ctrl Pts',(-53.8490072512308,-128.279887065054,
175.843637170317));
#36575=CARTESIAN_POINT('Ctrl Pts',(-53.802294130892,-128.348710488441,175.901819978033));
#36576=CARTESIAN_POINT('Ctrl Pts',(-53.7764318020244,-128.393224850283,
175.926281396815));
#36577=CARTESIAN_POINT('Ctrl Pts',(-53.7232833415724,-128.50689774928,175.969879539858));
#36578=CARTESIAN_POINT('Ctrl Pts',(-53.6972073196987,-128.581094516701,
175.985505889386));
#36579=CARTESIAN_POINT('Ctrl Pts',(-53.6611797943829,-128.757275852562,
176.006882342131));
#36580=CARTESIAN_POINT('Ctrl Pts',(-53.6540609990676,-128.861338079082,
176.011340061548));
#36581=CARTESIAN_POINT('Ctrl Pts',(-53.6656724524939,-128.970256707153,
176.011340061548));
#36582=CARTESIAN_POINT('',(-53.8617796092863,-128.949350374068,174.335390539474));
#36583=CARTESIAN_POINT('Origin',(-60.6261834003547,-128.228219737673,175.985485069079));
#36584=CARTESIAN_POINT('',(-54.1438210517818,-128.919282872009,173.435698778786));
#36585=CARTESIAN_POINT('Ctrl Pts',(-54.1438210517818,-128.919282872009,
173.435698778786));
#36586=CARTESIAN_POINT('Ctrl Pts',(-54.1299461492408,-128.789132468445,
173.435698778786));
#36587=CARTESIAN_POINT('Ctrl Pts',(-54.1389778226646,-128.665771084407,
173.450797449094));
#36588=CARTESIAN_POINT('Ctrl Pts',(-54.1739297012356,-128.474701895836,
173.505568323775));
#36589=CARTESIAN_POINT('Ctrl Pts',(-54.1955306812605,-128.401018047657,
173.539634469117));
#36590=CARTESIAN_POINT('Ctrl Pts',(-54.2299799629259,-128.29526504777,173.618292237587));
#36591=CARTESIAN_POINT('Ctrl Pts',(-54.2438403977334,-128.256727738681,
173.657656991775));
#36592=CARTESIAN_POINT('Ctrl Pts',(-54.2608898800193,-128.20030798137,173.741928744907));
#36593=CARTESIAN_POINT('Ctrl Pts',(-54.2653232800882,-128.180621283037,
173.783132482021));
#36594=CARTESIAN_POINT('Ctrl Pts',(-54.2641105829218,-128.157041787624,
173.858491705446));
#36595=CARTESIAN_POINT('Ctrl Pts',(-54.2609698988183,-128.150426576869,
173.890742841889));
#36596=CARTESIAN_POINT('Ctrl Pts',(-54.2525711534886,-128.145884928118,
173.935037384859));
#36597=CARTESIAN_POINT('Ctrl Pts',(-54.2499117870103,-128.145113026467,
173.946948835794));
#36598=CARTESIAN_POINT('Ctrl Pts',(-54.244891582158,-128.144598772664,173.966375774829));
#36599=CARTESIAN_POINT('Ctrl Pts',(-54.242773306296,-128.144584138032,173.973917081669));
#36600=CARTESIAN_POINT('Ctrl Pts',(-54.2383805953492,-128.144918940085,
173.988364635376));
#36601=CARTESIAN_POINT('Ctrl Pts',(-54.2361319848394,-128.145240040135,
173.995271988326));
#36602=CARTESIAN_POINT('Ctrl Pts',(-54.2306439615985,-128.146352771642,
174.011059758862));
#36603=CARTESIAN_POINT('Ctrl Pts',(-54.2273142776506,-128.147254392184,
174.019901154185));
#36604=CARTESIAN_POINT('Ctrl Pts',(-54.2164293231972,-128.150865253171,
174.046684379989));
#36605=CARTESIAN_POINT('Ctrl Pts',(-54.2081865004653,-128.154458738351,
174.064208723124));
#36606=CARTESIAN_POINT('Ctrl Pts',(-54.1790590976617,-128.169799540224,
174.118501227753));
#36607=CARTESIAN_POINT('Ctrl Pts',(-54.1554392646589,-128.185870211294,
174.151892350246));
#36608=CARTESIAN_POINT('Ctrl Pts',(-54.1043556574809,-128.228988799029,
174.209925271236));
#36609=CARTESIAN_POINT('Ctrl Pts',(-54.0776400986473,-128.255513276048,
174.233702381705));
#36610=CARTESIAN_POINT('Ctrl Pts',(-54.0186343263536,-128.325647178259,
174.277332336196));
#36611=CARTESIAN_POINT('Ctrl Pts',(-53.9878303954035,-128.370688347897,
174.293799283367));
#36612=CARTESIAN_POINT('Ctrl Pts',(-53.926182226586,-128.485267372592,174.320599195178));
#36613=CARTESIAN_POINT('Ctrl Pts',(-53.8973641161886,-128.559756464969,
174.327683942315));
#36614=CARTESIAN_POINT('Ctrl Pts',(-53.8578244665285,-128.73631221675,174.335396337284));
#36615=CARTESIAN_POINT('Ctrl Pts',(-53.8501681558601,-128.840431745997,
174.335390539474));
#36616=CARTESIAN_POINT('Ctrl Pts',(-53.8617796092863,-128.949350374068,
174.335390539474));
#36617=CARTESIAN_POINT('',(-54.4510093268082,-128.886534549599,172.755338513612));
#36618=CARTESIAN_POINT('Origin',(-60.6261834003547,-128.228219737673,175.985485069079));
#36619=CARTESIAN_POINT('',(-54.9389523206484,-128.83451656656,171.949669562728));
#36620=CARTESIAN_POINT('Ctrl Pts',(-54.9389523206484,-128.83451656656,171.949669562728));
#36621=CARTESIAN_POINT('Ctrl Pts',(-54.9250774181075,-128.704366162997,
171.949669562728));
#36622=CARTESIAN_POINT('Ctrl Pts',(-54.9298787536602,-128.581455761238,
171.969608277785));
#36623=CARTESIAN_POINT('Ctrl Pts',(-54.9502074912346,-128.391945497192,
172.035952227023));
#36624=CARTESIAN_POINT('Ctrl Pts',(-54.9628555204352,-128.319216093385,
172.076038075624));
#36625=CARTESIAN_POINT('Ctrl Pts',(-54.9772731256675,-128.215598604036,
172.163290829697));
#36626=CARTESIAN_POINT('Ctrl Pts',(-54.9812497663029,-128.178114973438,
172.205787694094));
#36627=CARTESIAN_POINT('Ctrl Pts',(-54.9775826596539,-128.123903742912,
172.293099188475));
#36628=CARTESIAN_POINT('Ctrl Pts',(-54.9720232412554,-128.105282345789,
172.334660053671));
#36629=CARTESIAN_POINT('Ctrl Pts',(-54.9528401369879,-128.083618615832,
172.408139078627));
#36630=CARTESIAN_POINT('Ctrl Pts',(-54.9420947137666,-128.077814121073,
172.438873496341));
#36631=CARTESIAN_POINT('Ctrl Pts',(-54.9233827171895,-128.074371933806,
172.479997510789));
#36632=CARTESIAN_POINT('Ctrl Pts',(-54.9179628592929,-128.073894318983,
172.490949576807));
#36633=CARTESIAN_POINT('Ctrl Pts',(-54.9084623430268,-128.073857696309,
172.508630406072));
#36634=CARTESIAN_POINT('Ctrl Pts',(-54.9046102999379,-128.074027892847,
172.51544886725));
#36635=CARTESIAN_POINT('Ctrl Pts',(-54.8969067798621,-128.074715649273,
172.528422786454));
#36636=CARTESIAN_POINT('Ctrl Pts',(-54.8930800354609,-128.075204988938,
172.534586182696));
#36637=CARTESIAN_POINT('Ctrl Pts',(-54.8839961283079,-128.076701065694,
172.54858099081));
#36638=CARTESIAN_POINT('Ctrl Pts',(-54.8786609108948,-128.077816489503,
172.556350242443));
#36639=CARTESIAN_POINT('Ctrl Pts',(-54.8617262288735,-128.082072291865,
172.579673330276));
#36640=CARTESIAN_POINT('Ctrl Pts',(-54.8495610232867,-128.086083929263,
172.594635763336));
#36641=CARTESIAN_POINT('Ctrl Pts',(-54.808397650064,-128.102707845994,172.640030079638));
#36642=CARTESIAN_POINT('Ctrl Pts',(-54.7775596848358,-128.119548018182,
172.666422475177));
#36643=CARTESIAN_POINT('Ctrl Pts',(-54.7142659315802,-128.163968289064,
172.709518969035));
#36644=CARTESIAN_POINT('Ctrl Pts',(-54.6827410255676,-128.191005474623,
172.725574835412));
#36645=CARTESIAN_POINT('Ctrl Pts',(-54.6152629057264,-128.262042585685,
172.752116322311));
#36646=CARTESIAN_POINT('Ctrl Pts',(-54.5815633889956,-128.307392444113,
172.759631798755));
#36647=CARTESIAN_POINT('Ctrl Pts',(-54.5156599265751,-128.422425111535,
172.768075965875));
#36648=CARTESIAN_POINT('Ctrl Pts',(-54.4862120292892,-128.496981343401,
172.76620737087));
#36649=CARTESIAN_POINT('Ctrl Pts',(-54.4465139093197,-128.673553989176,
172.759807491701));
#36650=CARTESIAN_POINT('Ctrl Pts',(-54.439397873382,-128.777615921527,172.755338513612));
#36651=CARTESIAN_POINT('Ctrl Pts',(-54.4510093268082,-128.886534549599,
172.755338513612));
#36652=CARTESIAN_POINT('',(-55.3991177156403,-128.785459861137,171.363010864448));
#36653=CARTESIAN_POINT('Origin',(-60.6261834003547,-128.228219737673,175.985485069079));
#36654=CARTESIAN_POINT('',(-56.0646047876237,-128.714514493215,170.698187274307));
#36655=CARTESIAN_POINT('Ctrl Pts',(-56.0646047876237,-128.714514493215,
170.698187274307));
#36656=CARTESIAN_POINT('Ctrl Pts',(-56.0507298850827,-128.584364089651,
170.698187274307));
#36657=CARTESIAN_POINT('Ctrl Pts',(-56.0502720366154,-128.462014352045,
170.721807268469));
#36658=CARTESIAN_POINT('Ctrl Pts',(-56.05364854251,-128.274311309154,170.795868623082));
#36659=CARTESIAN_POINT('Ctrl Pts',(-56.0561712852096,-128.202661328533,
170.839644531129));
#36660=CARTESIAN_POINT('Ctrl Pts',(-56.049093973138,-128.101335340974,170.930421457889));
#36661=CARTESIAN_POINT('Ctrl Pts',(-56.042728685082,-128.064954229068,170.973580669207));
#36662=CARTESIAN_POINT('Ctrl Pts',(-56.0182236170934,-128.012964464437,
171.058857678147));
#36663=CARTESIAN_POINT('Ctrl Pts',(-56.0028767685879,-127.995386472752,
171.098360305007));
#36664=CARTESIAN_POINT('Ctrl Pts',(-55.9666928702255,-127.975535141026,
171.16568879765));
#36665=CARTESIAN_POINT('Ctrl Pts',(-55.9489246171503,-127.970479326848,
171.193120323993));
#36666=CARTESIAN_POINT('Ctrl Pts',(-55.9209535355779,-127.968024219901,
171.228683831679));
#36667=CARTESIAN_POINT('Ctrl Pts',(-55.9130817033051,-127.967808001928,
171.238040018512));
#36668=CARTESIAN_POINT('Ctrl Pts',(-55.8996465822519,-127.968190834411,
171.252947192476));
#36669=CARTESIAN_POINT('Ctrl Pts',(-55.894283165646,-127.968522153463,171.258646543812));
#36670=CARTESIAN_POINT('Ctrl Pts',(-55.8837157192689,-127.969515223566,
171.269392831488));
#36671=CARTESIAN_POINT('Ctrl Pts',(-55.878533736002,-127.970149040748,171.274454076834));
#36672=CARTESIAN_POINT('Ctrl Pts',(-55.8663851011032,-127.971971837957,
171.285842595149));
#36673=CARTESIAN_POINT('Ctrl Pts',(-55.8593577624554,-127.973267653194,
171.292088182427));
#36674=CARTESIAN_POINT('Ctrl Pts',(-55.8373725464286,-127.978061876224,
171.310595679201));
#36675=CARTESIAN_POINT('Ctrl Pts',(-55.8220085859679,-127.982414522262,
171.322126639961));
#36676=CARTESIAN_POINT('Ctrl Pts',(-55.771276463049,-128.000058531638,171.355984615275));
#36677=CARTESIAN_POINT('Ctrl Pts',(-55.7350955791204,-128.017468294655,
171.373844453765));
#36678=CARTESIAN_POINT('Ctrl Pts',(-55.6635008647466,-128.06277350345,171.399499908916));
#36679=CARTESIAN_POINT('Ctrl Pts',(-55.6291437655714,-128.090112619721,
171.406901422608));
#36680=CARTESIAN_POINT('Ctrl Pts',(-55.5575059846342,-128.161593178447,
171.414811947171));
#36681=CARTESIAN_POINT('Ctrl Pts',(-55.5231251793449,-128.207015666787,
171.412939180716));
#36682=CARTESIAN_POINT('Ctrl Pts',(-55.4574581402791,-128.3220231299,171.402536858845));
#36683=CARTESIAN_POINT('Ctrl Pts',(-55.4295293586655,-128.396417413887,
171.391823517646));
#36684=CARTESIAN_POINT('Ctrl Pts',(-55.39303563214,-128.572648449912,171.371683302053));
#36685=CARTESIAN_POINT('Ctrl Pts',(-55.3875062622141,-128.676541233066,
171.363010864448));
#36686=CARTESIAN_POINT('Ctrl Pts',(-55.3991177156403,-128.785459861137,
171.363010864448));
#36687=CARTESIAN_POINT('Origin',(-60.6261834003547,-128.228219737673,175.985485069079));
#36688=CARTESIAN_POINT('Origin',(-61.1562134225954,-133.200047185959,175.985485069079));
#36689=CARTESIAN_POINT('',(-64.9260520676523,-133.803823638448,180.720859456143));
#36690=CARTESIAN_POINT('Origin',(-61.2622194270436,-134.194412675616,175.985485069079));
#36691=CARTESIAN_POINT('',(-65.4306848366389,-132.74435997593,181.510088520653));
#36692=CARTESIAN_POINT('Origin',(-64.8200460632041,-132.809458148791,180.720859456143));
#36693=CARTESIAN_POINT('Origin',(-61.1562134225954,-133.200047185959,175.985485069079));
#36694=CARTESIAN_POINT('Origin',(-61.1562134225954,-133.200047185959,175.985485069079));
#36695=CARTESIAN_POINT('Origin',(-61.1562134225954,-133.200047185959,175.985485069079));
#36696=CARTESIAN_POINT('Origin',(-61.1562134225954,-133.200047185959,175.985485069079));
#36697=CARTESIAN_POINT('Origin',(-61.1562134225954,-133.200047185959,175.985485069079));
#36698=CARTESIAN_POINT('',(-67.6896254280408,-132.503541817143,173.57106840282));
#36699=CARTESIAN_POINT('Origin',(-61.1562134225954,-133.200047185959,175.985485069079));
#36700=CARTESIAN_POINT('',(-67.3074920698659,-132.544279786117,172.709551595863));
#36701=CARTESIAN_POINT('Ctrl Pts',(-67.3074920698659,-132.544279786117,
172.709551595863));
#36702=CARTESIAN_POINT('Ctrl Pts',(-67.3213669724068,-132.67443018968,172.709551595863));
#36703=CARTESIAN_POINT('Ctrl Pts',(-67.314188693838,-132.797593989444,172.727065098828));
#36704=CARTESIAN_POINT('Ctrl Pts',(-67.2857981445578,-132.987963696479,
172.787746798755));
#36705=CARTESIAN_POINT('Ctrl Pts',(-67.2682462657113,-133.061215883421,
172.824928282536));
#36706=CARTESIAN_POINT('Ctrl Pts',(-67.2430027271334,-133.165987489591,
172.908253961851));
#36707=CARTESIAN_POINT('Ctrl Pts',(-67.2337177246049,-133.204037027031,
172.94939811266));
#36708=CARTESIAN_POINT('Ctrl Pts',(-67.2263641167085,-133.259423139356,
173.035734114708));
#36709=CARTESIAN_POINT('Ctrl Pts',(-67.2266408565468,-133.278607705306,
173.077409586198));
#36710=CARTESIAN_POINT('Ctrl Pts',(-67.2363995797138,-133.301276137252,
173.152425486572));
#36711=CARTESIAN_POINT('Ctrl Pts',(-67.2431784009463,-133.307503498284,
173.184190691894));
#36712=CARTESIAN_POINT('Ctrl Pts',(-67.2565444356024,-133.311515600807,
173.227300136152));
#36713=CARTESIAN_POINT('Ctrl Pts',(-67.2605366896921,-133.312145407734,
173.2388420587));
#36714=CARTESIAN_POINT('Ctrl Pts',(-67.2677258547293,-133.31242843589,173.257579952797));
#36715=CARTESIAN_POINT('Ctrl Pts',(-67.2706848768904,-133.312353441349,
173.264832344081));
#36716=CARTESIAN_POINT('Ctrl Pts',(-67.2766858774409,-133.31184718488,173.278684113163));
#36717=CARTESIAN_POINT('Ctrl Pts',(-67.2797023422905,-133.311444226428,
173.285287857823));
#36718=CARTESIAN_POINT('Ctrl Pts',(-67.286942905684,-133.310144662432,173.300337630055));
#36719=CARTESIAN_POINT('Ctrl Pts',(-67.291252197792,-133.309138609115,173.308733333975));
#36720=CARTESIAN_POINT('Ctrl Pts',(-67.3050989338295,-133.305212002425,
173.334065357106));
#36721=CARTESIAN_POINT('Ctrl Pts',(-67.3152715979195,-133.301412783262,
173.350498333212));
#36722=CARTESIAN_POINT('Ctrl Pts',(-67.3503518756773,-133.285437365149,
173.400952094059));
#36723=CARTESIAN_POINT('Ctrl Pts',(-67.3775915697648,-133.268980792704,
173.431255729657));
#36724=CARTESIAN_POINT('Ctrl Pts',(-67.4348913803985,-133.22519951615,173.482602579355));
#36725=CARTESIAN_POINT('Ctrl Pts',(-67.4641104955011,-133.198408143308,
173.50287782537));
#36726=CARTESIAN_POINT('Ctrl Pts',(-67.527631169734,-133.127792922386,173.538691689326));
#36727=CARTESIAN_POINT('Ctrl Pts',(-67.5600714357955,-133.082577308493,
173.551017551226));
#36728=CARTESIAN_POINT('Ctrl Pts',(-67.6242802655126,-132.967725300239,
173.569274803976));
#36729=CARTESIAN_POINT('Ctrl Pts',(-67.6536643492743,-132.893175871321,
173.572148874503));
#36730=CARTESIAN_POINT('Ctrl Pts',(-67.6937019906102,-132.716567030299,
173.57319909736));
#36731=CARTESIAN_POINT('Ctrl Pts',(-67.701236881467,-132.612460445214,173.57106840282));
#36732=CARTESIAN_POINT('Ctrl Pts',(-67.6896254280408,-132.503541817143,
173.57106840282));
#36733=CARTESIAN_POINT('',(-66.9252242844245,-132.585032085936,172.068819382192));
#36734=CARTESIAN_POINT('Origin',(-61.1562134225954,-133.200047185959,175.985485069079));
#36735=CARTESIAN_POINT('',(-66.3491822523538,-132.646442015031,171.324305384935));
#36736=CARTESIAN_POINT('Ctrl Pts',(-66.3491822523538,-132.646442015031,
171.324305384935));
#36737=CARTESIAN_POINT('Ctrl Pts',(-66.3630571548947,-132.776592418594,
171.324305384935));
#36738=CARTESIAN_POINT('Ctrl Pts',(-66.3606300089676,-132.899249715877,
171.346142702252));
#36739=CARTESIAN_POINT('Ctrl Pts',(-66.348078523136,-133.087930872927,171.416646592413));
#36740=CARTESIAN_POINT('Ctrl Pts',(-66.3401032840752,-133.160162126088,
171.458782749188));
#36741=CARTESIAN_POINT('Ctrl Pts',(-66.3357347296167,-133.262708319488,
171.548352210971));
#36742=CARTESIAN_POINT('Ctrl Pts',(-66.3366240056125,-133.299673210864,
171.591475588748));
#36743=CARTESIAN_POINT('Ctrl Pts',(-66.3501964657754,-133.352828464529,
171.678457825844));
#36744=CARTESIAN_POINT('Ctrl Pts',(-66.3604414133021,-133.370950352943,
171.719343120144));
#36745=CARTESIAN_POINT('Ctrl Pts',(-66.3878405119482,-133.39173820301,171.790432011517));
#36746=CARTESIAN_POINT('Ctrl Pts',(-66.4020027189591,-133.397178445789,
171.819819021622));
#36747=CARTESIAN_POINT('Ctrl Pts',(-66.4252556497954,-133.400136539126,
171.85859688805));
#36748=CARTESIAN_POINT('Ctrl Pts',(-66.4318817283628,-133.400485562767,
171.868869375135));
#36749=CARTESIAN_POINT('Ctrl Pts',(-66.4433242086511,-133.400315159102,
171.88535917445));
#36750=CARTESIAN_POINT('Ctrl Pts',(-66.4479238150429,-133.400065267322,
171.891694771565));
#36751=CARTESIAN_POINT('Ctrl Pts',(-66.4570471135294,-133.399226153033,
171.903703148721));
#36752=CARTESIAN_POINT('Ctrl Pts',(-66.4615471509932,-133.398665035829,
171.909386958144));
#36753=CARTESIAN_POINT('Ctrl Pts',(-66.4721570532479,-133.3970062778,171.922243425969));
#36754=CARTESIAN_POINT('Ctrl Pts',(-66.4783373532359,-133.395800762543,
171.929344173189));
#36755=CARTESIAN_POINT('Ctrl Pts',(-66.4978024141607,-133.391275204884,
171.95054541056));
#36756=CARTESIAN_POINT('Ctrl Pts',(-66.5115816738262,-133.387091498538,
171.963983731472));
#36757=CARTESIAN_POINT('Ctrl Pts',(-66.5576114470216,-133.369948791058,
172.004218162185));
#36758=CARTESIAN_POINT('Ctrl Pts',(-66.5912293660221,-133.352812257225,
172.026741589352));
#36759=CARTESIAN_POINT('Ctrl Pts',(-66.6589676252424,-133.307918172314,
172.061850232547));
#36760=CARTESIAN_POINT('Ctrl Pts',(-66.692090009718,-133.280710684879,172.073903457065));
#36761=CARTESIAN_POINT('Ctrl Pts',(-66.7620918631791,-133.209404526951,
172.091769365546));
#36762=CARTESIAN_POINT('Ctrl Pts',(-66.7963947234741,-133.163990348069,
172.094870269528));
#36763=CARTESIAN_POINT('Ctrl Pts',(-66.8627515656631,-133.048909347335,
172.094403733039));
#36764=CARTESIAN_POINT('Ctrl Pts',(-66.891746987074,-132.974401352419,172.088310602244));
#36765=CARTESIAN_POINT('Ctrl Pts',(-66.9303432492909,-132.797946172042,
172.075322289057));
#36766=CARTESIAN_POINT('Ctrl Pts',(-66.9368357378507,-132.693950714007,
172.068819382192));
#36767=CARTESIAN_POINT('Ctrl Pts',(-66.9252242844245,-132.585032085936,
172.068819382192));
#36768=CARTESIAN_POINT('',(-65.82554919902,-132.702264796853,170.794192734786));
#36769=CARTESIAN_POINT('Origin',(-61.1562134225954,-133.200047185959,175.985485069079));
#36770=CARTESIAN_POINT('',(-65.0890759621299,-132.780777764206,170.209949994551));
#36771=CARTESIAN_POINT('Ctrl Pts',(-65.0890759621299,-132.780777764206,
170.209949994551));
#36772=CARTESIAN_POINT('Ctrl Pts',(-65.1029508646709,-132.910928167769,
170.209949994551));
#36773=CARTESIAN_POINT('Ctrl Pts',(-65.1061657182635,-133.03298399021,170.234842020713));
#36774=CARTESIAN_POINT('Ctrl Pts',(-65.1113304009609,-133.219776485334,
170.311070671283));
#36775=CARTESIAN_POINT('Ctrl Pts',(-65.1138325717848,-133.290890776603,
170.355712700779));
#36776=CARTESIAN_POINT('Ctrl Pts',(-65.1312182280125,-133.391117825806,
170.446320493482));
#36777=CARTESIAN_POINT('Ctrl Pts',(-65.142457127664,-133.426979378156,170.488916924258));
#36778=CARTESIAN_POINT('Ctrl Pts',(-65.1765013651493,-133.477952203588,
170.571490304949));
#36779=CARTESIAN_POINT('Ctrl Pts',(-65.1962368260823,-133.495062339868,
170.609209317368));
#36780=CARTESIAN_POINT('Ctrl Pts',(-65.2398292034717,-133.514123878235,
170.67223977177));
#36781=CARTESIAN_POINT('Ctrl Pts',(-65.2605943159424,-133.51886020718,170.697540720449));
#36782=CARTESIAN_POINT('Ctrl Pts',(-65.2924160741141,-133.520904806275,
170.729733380401));
#36783=CARTESIAN_POINT('Ctrl Pts',(-65.3012973589557,-133.521013409861,
170.738139432412));
#36784=CARTESIAN_POINT('Ctrl Pts',(-65.3163345879792,-133.520459781964,
170.751422809749));
#36785=CARTESIAN_POINT('Ctrl Pts',(-65.3223089392296,-133.520063333198,
170.75647341082));
#36786=CARTESIAN_POINT('Ctrl Pts',(-65.3340251404624,-133.518947798153,
170.765940512815));
#36787=CARTESIAN_POINT('Ctrl Pts',(-65.3397467261682,-133.518256455745,
170.770374064657));
#36788=CARTESIAN_POINT('Ctrl Pts',(-65.3531061258319,-133.516304582923,
170.780290056899));
#36789=CARTESIAN_POINT('Ctrl Pts',(-65.3607949083432,-133.514938253351,
170.785683177801));
#36790=CARTESIAN_POINT('Ctrl Pts',(-65.3847320441665,-133.509935942631,
170.801521490557));
#36791=CARTESIAN_POINT('Ctrl Pts',(-65.4013004684702,-133.5054548927,170.81118416991));
#36792=CARTESIAN_POINT('Ctrl Pts',(-65.4555296989026,-133.487438068299,
170.838860991624));
#36793=CARTESIAN_POINT('Ctrl Pts',(-65.4934890684829,-133.46983870683,170.852295230642));
#36794=CARTESIAN_POINT('Ctrl Pts',(-65.5674982927985,-133.424276095143,
170.869125280607));
#36795=CARTESIAN_POINT('Ctrl Pts',(-65.602453952989,-133.396873168269,170.87225599403));
#36796=CARTESIAN_POINT('Ctrl Pts',(-65.6744776290023,-133.32535147055,170.871135645376));
#36797=CARTESIAN_POINT('Ctrl Pts',(-65.7083937221736,-133.279978523627,
170.86483137817));
#36798=CARTESIAN_POINT('Ctrl Pts',(-65.7723805110916,-133.165150186405,
170.845668165849));
#36799=CARTESIAN_POINT('Ctrl Pts',(-65.7988646638445,-133.090909909506,
170.830961944344));
#36800=CARTESIAN_POINT('Ctrl Pts',(-65.832720719157,-132.914960066854,170.804689928667));
#36801=CARTESIAN_POINT('Ctrl Pts',(-65.8371606524461,-132.811183424923,
170.794192734786));
#36802=CARTESIAN_POINT('Ctrl Pts',(-65.82554919902,-132.702264796853,170.794192734786));
#36803=CARTESIAN_POINT('',(-64.4545092906346,-132.84842681086,169.821265128268));
#36804=CARTESIAN_POINT('Origin',(-61.1562134225954,-133.200047185959,175.985485069079));
#36805=CARTESIAN_POINT('',(-63.6004059964818,-132.93947992819,169.431247709482));
#36806=CARTESIAN_POINT('Ctrl Pts',(-63.6004059964818,-132.93947992819,169.431247709482));
#36807=CARTESIAN_POINT('Ctrl Pts',(-63.6142808990228,-133.069630331754,
169.431247709482));
#36808=CARTESIAN_POINT('Ctrl Pts',(-63.623700726509,-133.191024662523,169.457747810408));
#36809=CARTESIAN_POINT('Ctrl Pts',(-63.6474290834969,-133.375838145946,
169.535271089296));
#36810=CARTESIAN_POINT('Ctrl Pts',(-63.6607005253255,-133.445804360977,
169.579824559026));
#36811=CARTESIAN_POINT('Ctrl Pts',(-63.6994553431546,-133.543753314789,
169.666204887084));
#36812=CARTESIAN_POINT('Ctrl Pts',(-63.7206177290859,-133.578556957203,
169.705798821133));
#36813=CARTESIAN_POINT('Ctrl Pts',(-63.7734897078701,-133.627522619627,
169.779164480675));
#36814=CARTESIAN_POINT('Ctrl Pts',(-63.8016864337849,-133.643730728531,
169.811525119313));
#36815=CARTESIAN_POINT('Ctrl Pts',(-63.8590838986816,-133.661320552339,
169.862834035842));
#36816=CARTESIAN_POINT('Ctrl Pts',(-63.8852876994291,-133.665477080778,
169.882578523923));
#36817=CARTESIAN_POINT('Ctrl Pts',(-63.9238622269919,-133.666801789542,
169.906315057018));
#36818=CARTESIAN_POINT('Ctrl Pts',(-63.9344890355132,-133.666724308642,
169.912366144767));
#36819=CARTESIAN_POINT('Ctrl Pts',(-63.9522535330249,-133.665879935704,
169.921671118517));
#36820=CARTESIAN_POINT('Ctrl Pts',(-63.9592568945881,-133.665373787563,
169.925143200968));
#36821=CARTESIAN_POINT('Ctrl Pts',(-63.9728859132973,-133.664054333396,
169.931518834248));
#36822=CARTESIAN_POINT('Ctrl Pts',(-63.9794960309314,-133.663268267548,
169.93444446659));
#36823=CARTESIAN_POINT('Ctrl Pts',(-63.9948252957511,-133.66110639394,169.940843701822));
#36824=CARTESIAN_POINT('Ctrl Pts',(-64.0035723679062,-133.659627243622,
169.944215767822));
#36825=CARTESIAN_POINT('Ctrl Pts',(-64.0305754279041,-133.654298084902,
169.953770690797));
#36826=CARTESIAN_POINT('Ctrl Pts',(-64.0489534897979,-133.649624115514,
169.959096168788));
#36827=CARTESIAN_POINT('Ctrl Pts',(-64.1081556166164,-133.631077147135,
169.972606905226));
#36828=CARTESIAN_POINT('Ctrl Pts',(-64.1481673531163,-133.61325898964,169.976171206955));
#36829=CARTESIAN_POINT('Ctrl Pts',(-64.223915613338,-133.567510985108,169.973744562361));
#36830=CARTESIAN_POINT('Ctrl Pts',(-64.258528012264,-133.540144652178,169.967770819004));
#36831=CARTESIAN_POINT('Ctrl Pts',(-64.3279966531765,-133.468895338271,
169.947729323807));
#36832=CARTESIAN_POINT('Ctrl Pts',(-64.3592990953663,-133.423801024004,
169.93238626651));
#36833=CARTESIAN_POINT('Ctrl Pts',(-64.4165355041514,-133.309692322405,
169.8956400746));
#36834=CARTESIAN_POINT('Ctrl Pts',(-64.438531727746,-133.235930488738,169.873175434526));
#36835=CARTESIAN_POINT('Ctrl Pts',(-64.4646242319639,-133.060808292499,
169.835146550413));
#36836=CARTESIAN_POINT('Ctrl Pts',(-64.4661207440609,-132.957345438932,
169.821265128269));
#36837=CARTESIAN_POINT('Ctrl Pts',(-64.4545092906346,-132.84842681086,169.821265128269));
#36838=CARTESIAN_POINT('',(-62.8917844152165,-133.015023722979,169.206579578684));
#36839=CARTESIAN_POINT('Origin',(-61.1562134225954,-133.200047185959,175.985485069079));
#36840=CARTESIAN_POINT('',(-61.969688442718,-133.113325314073,169.03345387607));
#36841=CARTESIAN_POINT('Ctrl Pts',(-61.969688442718,-133.113325314073,169.03345387607));
#36842=CARTESIAN_POINT('Ctrl Pts',(-61.983563345259,-133.243475717636,169.03345387607));
#36843=CARTESIAN_POINT('Ctrl Pts',(-61.9993905104838,-133.364186983395,
169.060021962217));
#36844=CARTESIAN_POINT('Ctrl Pts',(-62.0414511942499,-133.547046118307,
169.134334498239));
#36845=CARTESIAN_POINT('Ctrl Pts',(-62.0651578973172,-133.615899864773,
169.176210122489));
#36846=CARTESIAN_POINT('Ctrl Pts',(-62.1236549296646,-133.711744166623,
169.253342875213));
#36847=CARTESIAN_POINT('Ctrl Pts',(-62.1537379475471,-133.745596810073,
169.287633257008));
#36848=CARTESIAN_POINT('Ctrl Pts',(-62.2226994317192,-133.79284722373,169.347527449942));
#36849=CARTESIAN_POINT('Ctrl Pts',(-62.2578364362259,-133.808315452569,
169.372649032107));
#36850=CARTESIAN_POINT('Ctrl Pts',(-62.3258484958873,-133.824773689661,
169.409254523035));
#36851=CARTESIAN_POINT('Ctrl Pts',(-62.3560106909347,-133.828508226822,
169.422295072638));
#36852=CARTESIAN_POINT('Ctrl Pts',(-62.3991294835324,-133.829348486573,
169.436195997852));
#36853=CARTESIAN_POINT('Ctrl Pts',(-62.4108906896479,-133.82915007131,169.439540454114));
#36854=CARTESIAN_POINT('Ctrl Pts',(-62.4303564764721,-133.828124329566,
169.444326253026));
#36855=CARTESIAN_POINT('Ctrl Pts',(-62.4379833114621,-133.827551714992,
169.446018032044));
#36856=CARTESIAN_POINT('Ctrl Pts',(-62.4527338963768,-133.826112694374,
169.448931667977));
#36857=CARTESIAN_POINT('Ctrl Pts',(-62.4598478913784,-133.825272911833,
169.450179353702));
#36858=CARTESIAN_POINT('Ctrl Pts',(-62.4762529077012,-133.822996355928,
169.452689931634));
#36859=CARTESIAN_POINT('Ctrl Pts',(-62.4855465726741,-133.821458935164,
169.453844970513));
#36860=CARTESIAN_POINT('Ctrl Pts',(-62.5140312257525,-133.815971828722,
169.456561206314));
#36861=CARTESIAN_POINT('Ctrl Pts',(-62.5331342286297,-133.811220575783,
169.45723998552));
#36862=CARTESIAN_POINT('Ctrl Pts',(-62.5937936843215,-133.79251824641,169.455799441789));
#36863=CARTESIAN_POINT('Ctrl Pts',(-62.6334494279754,-133.774738040131,
169.449286661968));
#36864=CARTESIAN_POINT('Ctrl Pts',(-62.7063037284689,-133.72929855104,169.427744350578));
#36865=CARTESIAN_POINT('Ctrl Pts',(-62.7384162782486,-133.70219871873,169.413013322693));
#36866=CARTESIAN_POINT('Ctrl Pts',(-62.800901515759,-133.631693882281,169.375215419805));
#36867=CARTESIAN_POINT('Ctrl Pts',(-62.8275153190044,-133.58709940825,169.351725255135));
#36868=CARTESIAN_POINT('Ctrl Pts',(-62.8740133283526,-133.474135491771,
169.299531638744));
#36869=CARTESIAN_POINT('Ctrl Pts',(-62.8898057844172,-133.40103502117,169.270614143326));
#36870=CARTESIAN_POINT('Ctrl Pts',(-62.9055625827193,-133.227014680234,
169.223038491293));
#36871=CARTESIAN_POINT('Ctrl Pts',(-62.9033958686428,-133.123942351051,
169.206579578684));
#36872=CARTESIAN_POINT('Ctrl Pts',(-62.8917844152165,-133.015023722979,
169.206579578684));
#36873=CARTESIAN_POINT('',(-61.2281944622511,-133.192373526234,168.985859375881));
#36874=CARTESIAN_POINT('Origin',(-61.1562134225954,-133.200047185959,175.985485069079));
#36875=CARTESIAN_POINT('',(-60.2916946776461,-133.292210659929,169.03968682599));
#36876=CARTESIAN_POINT('Ctrl Pts',(-60.2916946776461,-133.292210659929,
169.03968682599));
#36877=CARTESIAN_POINT('Ctrl Pts',(-60.3055695801871,-133.422361063493,
169.03968682599));
#36878=CARTESIAN_POINT('Ctrl Pts',(-60.3276340758163,-133.54240738816,169.064778856764));
#36879=CARTESIAN_POINT('Ctrl Pts',(-60.386730330652,-133.723450417383,169.131561875442));
#36880=CARTESIAN_POINT('Ctrl Pts',(-60.4199318257402,-133.791291955586,
169.168325995141));
#36881=CARTESIAN_POINT('Ctrl Pts',(-60.4953967797734,-133.885327363622,
169.23172849731));
#36882=CARTESIAN_POINT('Ctrl Pts',(-60.5328791405755,-133.918391187683,
169.2587224945));
#36883=CARTESIAN_POINT('Ctrl Pts',(-60.6142568306537,-133.964317950839,
169.301664388039));
#36884=CARTESIAN_POINT('Ctrl Pts',(-60.6544097835976,-133.979251446064,
169.31808693869));
#36885=CARTESIAN_POINT('Ctrl Pts',(-60.7292290636159,-133.994983987987,
169.337861625938));
#36886=CARTESIAN_POINT('Ctrl Pts',(-60.7616393114978,-133.998478867696,
169.343440367722));
#36887=CARTESIAN_POINT('Ctrl Pts',(-60.8068297686094,-133.99909827417,169.346697813809));
#36888=CARTESIAN_POINT('Ctrl Pts',(-60.8190483191676,-133.998851102934,
169.347141270942));
#36889=CARTESIAN_POINT('Ctrl Pts',(-60.8390905433741,-133.997763909113,
169.347129761778));
#36890=CARTESIAN_POINT('Ctrl Pts',(-60.8468990808967,-133.997171923836,
169.346942917318));
#36891=CARTESIAN_POINT('Ctrl Pts',(-60.8619147993941,-133.995704638207,
169.346225225972));
#36892=CARTESIAN_POINT('Ctrl Pts',(-60.8691187336791,-133.994855267537,
169.345722454122));
#36893=CARTESIAN_POINT('Ctrl Pts',(-60.8856428690902,-133.992566012741,
169.344198469089));
#36894=CARTESIAN_POINT('Ctrl Pts',(-60.8949396640679,-133.991028258298,
169.343069354186));
#36895=CARTESIAN_POINT('Ctrl Pts',(-60.9232354743277,-133.985561283762,
169.338789045061));
#36896=CARTESIAN_POINT('Ctrl Pts',(-60.9419365906471,-133.980852874615,
169.334781677302));
#36897=CARTESIAN_POINT('Ctrl Pts',(-61.0004531130408,-133.962378996248,
169.318473572569));
#36898=CARTESIAN_POINT('Ctrl Pts',(-61.0373651930932,-133.944891282839,
169.302262210288));
#36899=CARTESIAN_POINT('Ctrl Pts',(-61.1028607246446,-133.90023628768,169.262856192937));
#36900=CARTESIAN_POINT('Ctrl Pts',(-61.1304621195415,-133.873617374619,
169.240223994317));
#36901=CARTESIAN_POINT('Ctrl Pts',(-61.1819414353715,-133.804285842951,
169.186866360465));
#36902=CARTESIAN_POINT('Ctrl Pts',(-61.2020640983622,-133.760383367837,
169.156594251411));
#36903=CARTESIAN_POINT('Ctrl Pts',(-61.2344597657111,-133.648922855231,
169.091986513806));
#36904=CARTESIAN_POINT('Ctrl Pts',(-61.2426931562934,-133.576628231511,
169.058296742767));
#36905=CARTESIAN_POINT('Ctrl Pts',(-61.2461427675187,-133.403919918941,
169.00393924678));
#36906=CARTESIAN_POINT('Ctrl Pts',(-61.2398059156773,-133.301292154304,
168.985859375881));
#36907=CARTESIAN_POINT('Ctrl Pts',(-61.2281944622511,-133.192373526234,
168.985859375881));
#36908=CARTESIAN_POINT('',(-59.5604212329013,-133.370169294699,169.171931975764));
#36909=CARTESIAN_POINT('Origin',(-61.1562134225954,-133.200047185959,175.985485069079));
#36910=CARTESIAN_POINT('',(-58.6639435996328,-133.465739799678,169.44958432285));
#36911=CARTESIAN_POINT('Ctrl Pts',(-58.6639435996328,-133.465739799678,
169.44958432285));
#36912=CARTESIAN_POINT('Ctrl Pts',(-58.6778185021737,-133.59589020324,169.44958432285));
#36913=CARTESIAN_POINT('Ctrl Pts',(-58.7055878299011,-133.715328354692,
169.471742040625));
#36914=CARTESIAN_POINT('Ctrl Pts',(-58.7794328546285,-133.894799066511,
169.527114355661));
#36915=CARTESIAN_POINT('Ctrl Pts',(-58.8206368697185,-133.961787482618,
169.556630373804));
#36916=CARTESIAN_POINT('Ctrl Pts',(-58.9093093386745,-134.054414881325,
169.602617902451));
#36917=CARTESIAN_POINT('Ctrl Pts',(-58.952239730449,-134.086897908887,169.620746722039));
#36918=CARTESIAN_POINT('Ctrl Pts',(-59.0416387421954,-134.131969545564,
169.644240689419));
#36919=CARTESIAN_POINT('Ctrl Pts',(-59.0845918047307,-134.146604530399,
169.651009789604));
#36920=CARTESIAN_POINT('Ctrl Pts',(-59.162015319794,-134.162059443467,169.652804440229));
#36921=CARTESIAN_POINT('Ctrl Pts',(-59.1948326303858,-134.165510927573,
169.650597157998));
#36922=CARTESIAN_POINT('Ctrl Pts',(-59.2395017538799,-134.166185911693,
169.643021814031));
#36923=CARTESIAN_POINT('Ctrl Pts',(-59.2514740165327,-134.165964996393,
169.64053849992));
#36924=CARTESIAN_POINT('Ctrl Pts',(-59.2709343257464,-134.164939838598,
169.635730351551));
#36925=CARTESIAN_POINT('Ctrl Pts',(-59.2784722350168,-134.164376704101,
169.633675742333));
#36926=CARTESIAN_POINT('Ctrl Pts',(-59.2928812458769,-134.162974097559,
169.629368433322));
#36927=CARTESIAN_POINT('Ctrl Pts',(-59.2997559544205,-134.162159824553,
169.627144423168));
#36928=CARTESIAN_POINT('Ctrl Pts',(-59.3154356537289,-134.159960592287,
169.621674443641));
#36929=CARTESIAN_POINT('Ctrl Pts',(-59.3241919339931,-134.158480460323,
169.61832679501));
#36930=CARTESIAN_POINT('Ctrl Pts',(-59.3506394403934,-134.153210527328,
169.607298696968));
#36931=CARTESIAN_POINT('Ctrl Pts',(-59.3678351987989,-134.148662599391,
169.598838075892));
#36932=CARTESIAN_POINT('Ctrl Pts',(-59.4207330652189,-134.130787707288,
169.568610177924));
#36933=CARTESIAN_POINT('Ctrl Pts',(-59.4526732626702,-134.113830029781,
169.543642378634));
#36934=CARTESIAN_POINT('Ctrl Pts',(-59.5067728809681,-134.07038991511,169.488662789815));
#36935=CARTESIAN_POINT('Ctrl Pts',(-59.5281139871706,-134.044438390648,
169.459444721581));
#36936=CARTESIAN_POINT('Ctrl Pts',(-59.5652044872045,-133.976640802874,
169.393628308496));
#36937=CARTESIAN_POINT('Ctrl Pts',(-59.5774107501079,-133.933582268898,
169.358333560002));
#36938=CARTESIAN_POINT('Ctrl Pts',(-59.5931597097522,-133.823896406549,
169.285066468054));
#36939=CARTESIAN_POINT('Ctrl Pts',(-59.5929180423105,-133.752505280635,
169.248562348429));
#36940=CARTESIAN_POINT('Ctrl Pts',(-59.5828042342757,-133.581242919175,
169.190582068574));
#36941=CARTESIAN_POINT('Ctrl Pts',(-59.5720326863276,-133.479087922771,
169.171931975764));
#36942=CARTESIAN_POINT('Ctrl Pts',(-59.5604212329013,-133.370169294699,
169.171931975764));
#36943=CARTESIAN_POINT('',(-57.985389645148,-133.538078184573,169.753983515172));
#36944=CARTESIAN_POINT('Origin',(-61.1562134225954,-133.200047185959,175.985485069079));
#36945=CARTESIAN_POINT('',(-57.1810341846979,-133.623827850471,170.239324614047));
#36946=CARTESIAN_POINT('Ctrl Pts',(-57.1810341846979,-133.623827850471,
170.239324614047));
#36947=CARTESIAN_POINT('Ctrl Pts',(-57.1949090872389,-133.753978254034,
170.239324614047));
#36948=CARTESIAN_POINT('Ctrl Pts',(-57.2275192046538,-133.872900344965,
170.257260292809));
#36949=CARTESIAN_POINT('Ctrl Pts',(-57.312969053198,-134.051133905033,170.298003866522));
#36950=CARTESIAN_POINT('Ctrl Pts',(-57.3602182388967,-134.117477865566,
170.318556419421));
#36951=CARTESIAN_POINT('Ctrl Pts',(-57.4575702432519,-134.209179967813,
170.344456346538));
#36952=CARTESIAN_POINT('Ctrl Pts',(-57.5036807342943,-134.241323975547,
170.352666407426));
#36953=CARTESIAN_POINT('Ctrl Pts',(-57.5962400134122,-134.286058706608,
170.355347064658));
#36954=CARTESIAN_POINT('Ctrl Pts',(-57.6396146145018,-134.300648752617,
170.352069318881));
#36955=CARTESIAN_POINT('Ctrl Pts',(-57.7152880306234,-134.316290237925,
170.335779634311));
#36956=CARTESIAN_POINT('Ctrl Pts',(-57.7466477567951,-134.319897110267,
170.325914607286));
#36957=CARTESIAN_POINT('Ctrl Pts',(-57.7882328465512,-134.320900872989,
170.307946724722));
#36958=CARTESIAN_POINT('Ctrl Pts',(-57.7992695023101,-134.320779699634,
170.302680960555));
#36959=CARTESIAN_POINT('Ctrl Pts',(-57.8170233629453,-134.319936460658,
170.293355605087));
#36960=CARTESIAN_POINT('Ctrl Pts',(-57.823854041107,-134.319448721722,170.289552637531));
#36961=CARTESIAN_POINT('Ctrl Pts',(-57.8368197627493,-134.318199979453,
170.281906035998));
#36962=CARTESIAN_POINT('Ctrl Pts',(-57.8429652139283,-134.317463450155,
170.278090038927));
#36963=CARTESIAN_POINT('Ctrl Pts',(-57.856885997503,-134.315451730057,170.268991960234));
#36964=CARTESIAN_POINT('Ctrl Pts',(-57.8645895310856,-134.314083827922,
170.263620331045));
#36965=CARTESIAN_POINT('Ctrl Pts',(-57.8876366892889,-134.309176394762,
170.246485357057));
#36966=CARTESIAN_POINT('Ctrl Pts',(-57.902311104355,-134.30489725887,170.234063183208));
#36967=CARTESIAN_POINT('Ctrl Pts',(-57.9464411279872,-134.287957077386,
170.191672227563));
#36968=CARTESIAN_POINT('Ctrl Pts',(-57.9714701715824,-134.271736175052,
170.159399029004));
#36969=CARTESIAN_POINT('Ctrl Pts',(-58.0107990213713,-134.229870722986,
170.092041082576));
#36970=CARTESIAN_POINT('Ctrl Pts',(-58.024494530291,-134.204734270274,170.05793519265));
#36971=CARTESIAN_POINT('Ctrl Pts',(-58.0446495460863,-134.138742118264,
169.983485011029));
#36972=CARTESIAN_POINT('Ctrl Pts',(-58.0479742214678,-134.096630420855,
169.945218825585));
#36973=CARTESIAN_POINT('Ctrl Pts',(-58.045499553846,-133.988887318923,169.867550396363));
#36974=CARTESIAN_POINT('Ctrl Pts',(-58.0363593754047,-133.918444833732,
169.830353414898));
#36975=CARTESIAN_POINT('Ctrl Pts',(-58.0122141725528,-133.748678312699,
169.772119954288));
#36976=CARTESIAN_POINT('Ctrl Pts',(-57.997001098574,-133.646996812643,169.753983515172));
#36977=CARTESIAN_POINT('Ctrl Pts',(-57.985389645148,-133.538078184573,169.753983515172));
#36978=CARTESIAN_POINT('',(-56.5946348098644,-133.6863419415,170.698187274307));
#36979=CARTESIAN_POINT('Origin',(-61.1562134225954,-133.200047185959,175.985485069079));
#36980=CARTESIAN_POINT('',(-55.929147737881,-133.757287309423,171.363010864448));
#36981=CARTESIAN_POINT('Ctrl Pts',(-55.929147737881,-133.757287309423,171.363010864448));
#36982=CARTESIAN_POINT('Ctrl Pts',(-55.9430226404219,-133.887437712986,
171.363010864448));
#36983=CARTESIAN_POINT('Ctrl Pts',(-55.979328176012,-134.00596584765,171.375682147739));
#36984=CARTESIAN_POINT('Ctrl Pts',(-56.0725644721205,-134.183369320388,
171.399429111723));
#36985=CARTESIAN_POINT('Ctrl Pts',(-56.1235501556925,-134.249314945284,
171.409823759709));
#36986=CARTESIAN_POINT('Ctrl Pts',(-56.2245492928744,-134.340628238806,
171.414130875675));
#36987=CARTESIAN_POINT('Ctrl Pts',(-56.2713871356702,-134.372694705983,
171.411945038965));
#36988=CARTESIAN_POINT('Ctrl Pts',(-56.3620619646102,-134.417630332023,
171.393656595996));
#36989=CARTESIAN_POINT('Ctrl Pts',(-56.4034550349283,-134.432431622451,
171.380522494926));
#36990=CARTESIAN_POINT('Ctrl Pts',(-56.4731257275112,-134.448713038192,
171.347095172418));
#36991=CARTESIAN_POINT('Ctrl Pts',(-56.5012479316411,-134.452665052013,
171.330145720112));
#36992=CARTESIAN_POINT('Ctrl Pts',(-56.5373655203723,-134.454251686872,
171.302829526974));
#36993=CARTESIAN_POINT('Ctrl Pts',(-56.5468316243193,-134.454297944833,
171.295087339825));
#36994=CARTESIAN_POINT('Ctrl Pts',(-56.5618536753716,-134.45374593501,171.281786733023));
#36995=CARTESIAN_POINT('Ctrl Pts',(-56.5675816212726,-134.453375754699,
171.276456421779));
#36996=CARTESIAN_POINT('Ctrl Pts',(-56.5783513508432,-134.452361119857,
171.26591492041));
#36997=CARTESIAN_POINT('Ctrl Pts',(-56.5834098948226,-134.451740462127,
171.260728708301));
#36998=CARTESIAN_POINT('Ctrl Pts',(-56.5947595048212,-134.45000284631,171.248531277705));
#36999=CARTESIAN_POINT('Ctrl Pts',(-56.6009592415656,-134.448795258966,
171.241447847521));
#37000=CARTESIAN_POINT('Ctrl Pts',(-56.6192516231093,-134.444394716763,
171.219201819994));
#37001=CARTESIAN_POINT('Ctrl Pts',(-56.6305352407206,-134.440477062534,
171.203540024964));
#37002=CARTESIAN_POINT('Ctrl Pts',(-56.6632577899041,-134.424752994038,
171.151449619898));
#37003=CARTESIAN_POINT('Ctrl Pts',(-56.6798380595294,-134.409432787455,
171.113746623061));
#37004=CARTESIAN_POINT('Ctrl Pts',(-56.7018797089301,-134.369410266444,
171.037924918036));
#37005=CARTESIAN_POINT('Ctrl Pts',(-56.7069886463024,-134.345189199625,
171.00091331677));
#37006=CARTESIAN_POINT('Ctrl Pts',(-56.7086457382025,-134.281169049884,
170.922156140553));
#37007=CARTESIAN_POINT('Ctrl Pts',(-56.7026398042108,-134.240052057771,
170.883142409765));
#37008=CARTESIAN_POINT('Ctrl Pts',(-56.6814236807383,-134.134306920244,
170.805586450063));
#37009=CARTESIAN_POINT('Ctrl Pts',(-56.6634786874364,-134.064803087141,
170.769858360114));
#37010=CARTESIAN_POINT('Ctrl Pts',(-56.6256495678753,-133.896495363049,
170.714756035812));
#37011=CARTESIAN_POINT('Ctrl Pts',(-56.6062462632905,-133.795260569571,
170.698187274307));
#37012=CARTESIAN_POINT('Ctrl Pts',(-56.5946348098644,-133.6863419415,170.698187274307));
#37013=CARTESIAN_POINT('',(-55.4689823428891,-133.806344014845,171.949669562728));
#37014=CARTESIAN_POINT('Origin',(-61.1562134225954,-133.200047185959,175.985485069079));
#37015=CARTESIAN_POINT('',(-54.981039349049,-133.858361997884,172.755338513612));
#37016=CARTESIAN_POINT('Ctrl Pts',(-54.981039349049,-133.858361997884,172.755338513612));
#37017=CARTESIAN_POINT('Ctrl Pts',(-54.9949142515899,-133.988512401447,
172.755338513612));
#37018=CARTESIAN_POINT('Ctrl Pts',(-55.0335550695708,-134.106791579407,
172.762008992506));
#37019=CARTESIAN_POINT('Ctrl Pts',(-55.1303069169609,-134.283820270891,
172.767379259529));
#37020=CARTESIAN_POINT('Ctrl Pts',(-55.1825032739958,-134.349636829908,
172.767011903445));
#37021=CARTESIAN_POINT('Ctrl Pts',(-55.2819051833289,-134.441120398589,
172.749475894336));
#37022=CARTESIAN_POINT('Ctrl Pts',(-55.3269753593235,-134.473375310857,
172.737021192913));
#37023=CARTESIAN_POINT('Ctrl Pts',(-55.4108305379313,-134.519037957184,
172.698826507572));
#37024=CARTESIAN_POINT('Ctrl Pts',(-55.4479541675179,-134.534294398517,
172.676599357423));
#37025=CARTESIAN_POINT('Ctrl Pts',(-55.507718368438,-134.551631912454,172.627977071457));
#37026=CARTESIAN_POINT('Ctrl Pts',(-55.5310112659176,-134.556098762628,
172.604928234429));
#37027=CARTESIAN_POINT('Ctrl Pts',(-55.5595956376216,-134.55848848875,172.569851248574));
#37028=CARTESIAN_POINT('Ctrl Pts',(-55.566947519602,-134.558760136898,172.560082586218));
#37029=CARTESIAN_POINT('Ctrl Pts',(-55.5783711629161,-134.55859174138,172.543579711001));
#37030=CARTESIAN_POINT('Ctrl Pts',(-55.5826649621923,-134.558374450681,
172.537031834384));
#37031=CARTESIAN_POINT('Ctrl Pts',(-55.590613619911,-134.557660560946,172.524208066924));
#37032=CARTESIAN_POINT('Ctrl Pts',(-55.5942907739505,-134.557187168612,
172.517953043574));
#37033=CARTESIAN_POINT('Ctrl Pts',(-55.6024063797937,-134.555794319245,
172.503365131405));
#37034=CARTESIAN_POINT('Ctrl Pts',(-55.6067386647482,-134.554785814737,
172.494981563442));
#37035=CARTESIAN_POINT('Ctrl Pts',(-55.6191981715094,-134.551007095955,
172.468917340633));
#37036=CARTESIAN_POINT('Ctrl Pts',(-55.6264185983737,-134.547522605005,
172.45092613102));
#37037=CARTESIAN_POINT('Ctrl Pts',(-55.6457570023975,-134.533225375801,
172.392163581535));
#37038=CARTESIAN_POINT('Ctrl Pts',(-55.652841889972,-134.518917440383,172.351221947552));
#37039=CARTESIAN_POINT('Ctrl Pts',(-55.6560845763555,-134.480899014423,
172.271342965824));
#37040=CARTESIAN_POINT('Ctrl Pts',(-55.6521649882432,-134.45764044874,172.233576632953));
#37041=CARTESIAN_POINT('Ctrl Pts',(-55.634836748691,-134.395644262171,172.15508954295));
#37042=CARTESIAN_POINT('Ctrl Pts',(-55.6195934445764,-134.355512035427,
172.117595603043));
#37043=CARTESIAN_POINT('Ctrl Pts',(-55.5802072219595,-134.25170395186,172.044659383334));
#37044=CARTESIAN_POINT('Ctrl Pts',(-55.5540628137713,-134.183074231163,
172.012476571624));
#37045=CARTESIAN_POINT('Ctrl Pts',(-55.5036925151093,-134.016103480551,
171.963707730429));
#37046=CARTESIAN_POINT('Ctrl Pts',(-55.4805937963153,-133.915262642916,
171.949669562728));
#37047=CARTESIAN_POINT('Ctrl Pts',(-55.4689823428892,-133.806344014845,
171.949669562728));
#37048=CARTESIAN_POINT('',(-54.6738510740226,-133.891110320294,173.435698778786));
#37049=CARTESIAN_POINT('Origin',(-61.1562134225954,-133.200047185959,175.985485069079));
#37050=CARTESIAN_POINT('',(-54.391809631527,-133.921177822353,174.335390539474));
#37051=CARTESIAN_POINT('Ctrl Pts',(-54.3918096315271,-133.921177822353,
174.335390539474));
#37052=CARTESIAN_POINT('Ctrl Pts',(-54.405684534068,-134.051328225917,174.335390539474));
#37053=CARTESIAN_POINT('Ctrl Pts',(-54.4451647805315,-134.169517915192,
174.335672549985));
#37054=CARTESIAN_POINT('Ctrl Pts',(-54.5409569718588,-134.346648912425,
174.322354019649));
#37055=CARTESIAN_POINT('Ctrl Pts',(-54.5917678180055,-134.412613176158,
174.311246008893));
#37056=CARTESIAN_POINT('Ctrl Pts',(-54.6844209638907,-134.50481620811,174.272886003818));
#37057=CARTESIAN_POINT('Ctrl Pts',(-54.7253311848986,-134.537514599372,
174.250886259657));
#37058=CARTESIAN_POINT('Ctrl Pts',(-54.797827846308,-134.584388139517,174.195005068225));
#37059=CARTESIAN_POINT('Ctrl Pts',(-54.82864224958,-134.600317186527,174.164976630171));
#37060=CARTESIAN_POINT('Ctrl Pts',(-54.8751719199992,-134.619065589833,
174.103985131274));
#37061=CARTESIAN_POINT('Ctrl Pts',(-54.8923243879691,-134.624187050817,
174.076176424152));
#37062=CARTESIAN_POINT('Ctrl Pts',(-54.9117476298381,-134.627553414584,
174.035377192497));
#37063=CARTESIAN_POINT('Ctrl Pts',(-54.9165644905915,-134.628095312931,
174.024149774082));
#37064=CARTESIAN_POINT('Ctrl Pts',(-54.9237322543856,-134.628380622603,
174.005403717575));
#37065=CARTESIAN_POINT('Ctrl Pts',(-54.9263438400637,-134.628342667112,
173.998018814374));
#37066=CARTESIAN_POINT('Ctrl Pts',(-54.9310102965949,-134.627978681951,
173.983658051573));
#37067=CARTESIAN_POINT('Ctrl Pts',(-54.9330918593172,-134.627675390312,
173.976697736202));
#37068=CARTESIAN_POINT('Ctrl Pts',(-54.9374985789908,-134.626677932989,
173.960567138891));
#37069=CARTESIAN_POINT('Ctrl Pts',(-54.9397082867146,-134.625895709395,
173.951370655646));
#37070=CARTESIAN_POINT('Ctrl Pts',(-54.9455958060493,-134.62281760838,173.923002995446));
#37071=CARTESIAN_POINT('Ctrl Pts',(-54.9483167867514,-134.61981278845,173.903727954957));
#37072=CARTESIAN_POINT('Ctrl Pts',(-54.9530722127725,-134.607070202129,
173.841708326837));
#37073=CARTESIAN_POINT('Ctrl Pts',(-54.950166947306,-134.593827283768,173.799907434658));
#37074=CARTESIAN_POINT('Ctrl Pts',(-54.9341914354423,-134.557857646137,
173.720613452297));
#37075=CARTESIAN_POINT('Ctrl Pts',(-54.9213260729919,-134.535552759763,
173.684287229812));
#37076=CARTESIAN_POINT('Ctrl Pts',(-54.8856284528856,-134.475514871886,
173.610631610406));
#37077=CARTESIAN_POINT('Ctrl Pts',(-54.8617778602733,-134.4363002396,173.576836472882));
#37078=CARTESIAN_POINT('Ctrl Pts',(-54.8058488753351,-134.334255725016,
173.512758781142));
#37079=CARTESIAN_POINT('Ctrl Pts',(-54.7725869724248,-134.266384776808,
173.485991595707));
#37080=CARTESIAN_POINT('Ctrl Pts',(-54.7115470800142,-134.100551476174,
173.446390505402));
#37081=CARTESIAN_POINT('Ctrl Pts',(-54.6854625274489,-134.000028948366,
173.435698778786));
#37082=CARTESIAN_POINT('Ctrl Pts',(-54.6738510740226,-133.891110320294,
173.435698778786));
#37083=CARTESIAN_POINT('',(-54.2554511424266,-133.935714548288,175.06991230594));
#37084=CARTESIAN_POINT('Origin',(-61.1562134225954,-133.200047185959,175.985485069079));
#37085=CARTESIAN_POINT('',(-54.1957024747346,-133.942084155439,176.011340061548));
#37086=CARTESIAN_POINT('Ctrl Pts',(-54.1957024747346,-133.942084155439,
176.011340061548));
#37087=CARTESIAN_POINT('Ctrl Pts',(-54.2095773772757,-134.072234559003,
176.011340061548));
#37088=CARTESIAN_POINT('Ctrl Pts',(-54.2483524137813,-134.190499428371,
176.005217214248));
#37089=CARTESIAN_POINT('Ctrl Pts',(-54.3387655134225,-134.368203872713,
175.973983911125));
#37090=CARTESIAN_POINT('Ctrl Pts',(-54.385675185186,-134.434584027699,175.952780802909));
#37091=CARTESIAN_POINT('Ctrl Pts',(-54.4668202456265,-134.528013898444,
175.895826145928));
#37092=CARTESIAN_POINT('Ctrl Pts',(-54.5014199849252,-134.561385029216,
175.865559904196));
#37093=CARTESIAN_POINT('Ctrl Pts',(-54.5586793780035,-134.609882963964,
175.795239818398));
#37094=CARTESIAN_POINT('Ctrl Pts',(-54.581511438678,-134.626662982024,175.75915523611));
#37095=CARTESIAN_POINT('Ctrl Pts',(-54.6122476825661,-134.647095070112,
175.689339128502));
#37096=CARTESIAN_POINT('Ctrl Pts',(-54.6223054576102,-134.652972872761,
175.658386692264));
#37097=CARTESIAN_POINT('Ctrl Pts',(-54.6314720683999,-134.657432661924,
175.614236317853));
#37098=CARTESIAN_POINT('Ctrl Pts',(-54.6334804348868,-134.658273964524,
175.602202640129));
#37099=CARTESIAN_POINT('Ctrl Pts',(-54.6359821836304,-134.659056702573,
175.582302854994));
#37100=CARTESIAN_POINT('Ctrl Pts',(-54.6367612528759,-134.659214105577,
175.57451010894));
#37101=CARTESIAN_POINT('Ctrl Pts',(-54.6378751284851,-134.659228849277,
175.559446946134));
#37102=CARTESIAN_POINT('Ctrl Pts',(-54.63823962848,-134.659108607996,175.552185846972));
#37103=CARTESIAN_POINT('Ctrl Pts',(-54.6386781269537,-134.658534189564,
175.535450016203));
#37104=CARTESIAN_POINT('Ctrl Pts',(-54.6386334884793,-134.657992294335,
175.525975083853));
#37105=CARTESIAN_POINT('Ctrl Pts',(-54.6375918477649,-134.655652888075,
175.496952611561));
#37106=CARTESIAN_POINT('Ctrl Pts',(-54.6356386183457,-134.653146370172,
175.477513935488));
#37107=CARTESIAN_POINT('Ctrl Pts',(-54.6254597431951,-134.64199588013,175.415841584085));
#37108=CARTESIAN_POINT('Ctrl Pts',(-54.6126501450793,-134.629808829799,
175.375610749624));
#37109=CARTESIAN_POINT('Ctrl Pts',(-54.578154091565,-134.595813605642,175.301510044663));
#37110=CARTESIAN_POINT('Ctrl Pts',(-54.5569456018108,-134.574398152378,
175.268735080574));
#37111=CARTESIAN_POINT('Ctrl Pts',(-54.5045621136761,-134.516139089509,
175.204191528638));
#37112=CARTESIAN_POINT('Ctrl Pts',(-54.4732345385129,-134.477721553516,
175.17605924405));
#37113=CARTESIAN_POINT('Ctrl Pts',(-54.4033515332927,-134.37716463072,175.124564042811));
#37114=CARTESIAN_POINT('Ctrl Pts',(-54.3644676987464,-134.309893017983,
175.104768095174));
#37115=CARTESIAN_POINT('Ctrl Pts',(-54.2952498759444,-134.144931539363,
175.076636227182));
#37116=CARTESIAN_POINT('Ctrl Pts',(-54.2670625958527,-134.044633176358,
175.06991230594));
#37117=CARTESIAN_POINT('Ctrl Pts',(-54.2554511424266,-133.935714548288,
175.06991230594));
#37118=CARTESIAN_POINT('',(-54.2380984313038,-133.937564463225,176.757335594116));
#37119=CARTESIAN_POINT('Origin',(-61.1562134225954,-133.200047185959,175.985485069079));
#37120=CARTESIAN_POINT('',(-54.404114913804,-133.919865997052,177.685786985438));
#37121=CARTESIAN_POINT('Ctrl Pts',(-54.404114913804,-133.919865997052,177.685786985438));
#37122=CARTESIAN_POINT('Ctrl Pts',(-54.4179898163449,-134.050016400615,
177.685786985438));
#37123=CARTESIAN_POINT('Ctrl Pts',(-54.454555988691,-134.16851674966,177.673615117958));
#37124=CARTESIAN_POINT('Ctrl Pts',(-54.5354831742812,-134.347232455816,
177.626282208097));
#37125=CARTESIAN_POINT('Ctrl Pts',(-54.5762027302419,-134.414272518502,
177.596216249999));
#37126=CARTESIAN_POINT('Ctrl Pts',(-54.6417491913354,-134.50936530415,177.523976938756));
#37127=CARTESIAN_POINT('Ctrl Pts',(-54.6682546644619,-134.543599337773,
177.487203163407));
#37128=CARTESIAN_POINT('Ctrl Pts',(-54.7072835727268,-134.594040763998,
177.406530931027));
#37129=CARTESIAN_POINT('Ctrl Pts',(-54.7209240792575,-134.611800663137,
177.366487309265));
#37130=CARTESIAN_POINT('Ctrl Pts',(-54.7342258571274,-134.634091381781,
177.291904051349));
#37131=CARTESIAN_POINT('Ctrl Pts',(-54.7366469935942,-134.640783301122,
177.259606729083));
#37132=CARTESIAN_POINT('Ctrl Pts',(-54.7350575501788,-134.646389757523,
177.214671071197));
#37133=CARTESIAN_POINT('Ctrl Pts',(-54.7341471688373,-134.647542218141,
177.202530487771));
#37134=CARTESIAN_POINT('Ctrl Pts',(-54.7318439388331,-134.648837199026,
177.18263347719));
#37135=CARTESIAN_POINT('Ctrl Pts',(-54.7307466880059,-134.649194630286,
177.174885774357));
#37136=CARTESIAN_POINT('Ctrl Pts',(-54.728244066049,-134.649594916787,177.159995627815));
#37137=CARTESIAN_POINT('Ctrl Pts',(-54.7268698213509,-134.649660037307,
177.152855733553));
#37138=CARTESIAN_POINT('Ctrl Pts',(-54.7233113821865,-134.64951171913,177.136487294976));
#37139=CARTESIAN_POINT('Ctrl Pts',(-54.721011642953,-134.649210232709,177.127284562151));
#37140=CARTESIAN_POINT('Ctrl Pts',(-54.7130863671627,-134.647604667936,
177.099293958364));
#37141=CARTESIAN_POINT('Ctrl Pts',(-54.7065558117654,-134.645586123563,
177.080821351903));
#37142=CARTESIAN_POINT('Ctrl Pts',(-54.6819592395746,-134.635972656349,
177.023080450112));
#37143=CARTESIAN_POINT('Ctrl Pts',(-54.659906733014,-134.624770961809,176.986757743235));
#37144=CARTESIAN_POINT('Ctrl Pts',(-54.6086641410077,-134.592561030537,
176.922156779301));
#37145=CARTESIAN_POINT('Ctrl Pts',(-54.5802000432173,-134.571919073564,
176.894837835389));
#37146=CARTESIAN_POINT('Ctrl Pts',(-54.5137839215791,-134.515155983177,
176.843157387555));
#37147=CARTESIAN_POINT('Ctrl Pts',(-54.4765442048596,-134.477368720972,
176.822322902026));
#37148=CARTESIAN_POINT('Ctrl Pts',(-54.3961068783355,-134.377936959341,
176.786402905207));
#37149=CARTESIAN_POINT('Ctrl Pts',(-54.3534234014711,-134.311070413862,
176.774728663888));
#37150=CARTESIAN_POINT('Ctrl Pts',(-54.2789945832238,-134.146664462167,
176.759700940123));
#37151=CARTESIAN_POINT('Ctrl Pts',(-54.2497098847298,-134.046483091295,
176.757335594116));
#37152=CARTESIAN_POINT('Ctrl Pts',(-54.2380984313037,-133.937564463225,
176.757335594116));
#37153=CARTESIAN_POINT('',(-54.62280141715,-133.896552554774,178.399901735339));
#37154=CARTESIAN_POINT('Origin',(-61.1562134225954,-133.200047185959,175.985485069079));
#37155=CARTESIAN_POINT('',(-55.0049347753249,-133.8558145858,179.261418542296));
#37156=CARTESIAN_POINT('Ctrl Pts',(-55.0049347753249,-133.8558145858,179.261418542296));
#37157=CARTESIAN_POINT('Ctrl Pts',(-55.0188096778659,-133.985964989364,
179.261418542296));
#37158=CARTESIAN_POINT('Ctrl Pts',(-55.0517917030077,-134.104847432446,
179.243905039331));
#37159=CARTESIAN_POINT('Ctrl Pts',(-55.119677439025,-134.284953444254,179.183223339405));
#37160=CARTESIAN_POINT('Ctrl Pts',(-55.1522776847934,-134.352859079651,
179.146041855624));
#37161=CARTESIAN_POINT('Ctrl Pts',(-55.1990415665339,-134.449954213742,
179.062716176308));
#37162=CARTESIAN_POINT('Ctrl Pts',(-55.2161393983533,-134.48519116478,179.021572025499));
#37163=CARTESIAN_POINT('Ctrl Pts',(-55.2350040948343,-134.537782230696,
178.935236023451));
#37164=CARTESIAN_POINT('Ctrl Pts',(-55.2387780153924,-134.556593973818,
178.89356055196));
#37165=CARTESIAN_POINT('Ctrl Pts',(-55.2340175155502,-134.580810251938,
178.818544651587));
#37166=CARTESIAN_POINT('Ctrl Pts',(-55.2287038814645,-134.588326749495,
178.786779446265));
#37167=CARTESIAN_POINT('Ctrl Pts',(-55.2164840634913,-134.595066474844,
178.743670002006));
#37168=CARTESIAN_POINT('Ctrl Pts',(-55.2127143077742,-134.596523763874,
178.732128079458));
#37169=CARTESIAN_POINT('Ctrl Pts',(-55.2057463832246,-134.598316032362,
178.713390185362));
#37170=CARTESIAN_POINT('Ctrl Pts',(-55.2028380535871,-134.598866536722,
178.706137794079));
#37171=CARTESIAN_POINT('Ctrl Pts',(-55.1968651951133,-134.599636773621,
178.692286024995));
#37172=CARTESIAN_POINT('Ctrl Pts',(-55.193831573278,-134.59987879483,178.685682280334));
#37173=CARTESIAN_POINT('Ctrl Pts',(-55.1864797675247,-134.600134874874,
178.670632508104));
#37174=CARTESIAN_POINT('Ctrl Pts',(-55.1820552312309,-134.600059906015,
178.662236804185));
#37175=CARTESIAN_POINT('Ctrl Pts',(-55.1676918971867,-134.599140681264,
178.636904781052));
#37176=CARTESIAN_POINT('Ctrl Pts',(-55.1569469175024,-134.597571422677,
178.620471804946));
#37177=CARTESIAN_POINT('Ctrl Pts',(-55.1192871565485,-134.589350578658,
178.570018044099));
#37178=CARTESIAN_POINT('Ctrl Pts',(-55.0891903299897,-134.579006462373,
178.539714408502));
#37179=CARTESIAN_POINT('Ctrl Pts',(-55.0239484505953,-134.548288948664,
178.488367558804));
#37180=CARTESIAN_POINT('Ctrl Pts',(-54.9897379336018,-134.52825959837,178.468092312789));
#37181=CARTESIAN_POINT('Ctrl Pts',(-54.9127579386383,-134.472622687455,
178.432278448833));
#37182=CARTESIAN_POINT('Ctrl Pts',(-54.8715145135347,-134.435262247312,
178.419952586932));
#37183=CARTESIAN_POINT('Ctrl Pts',(-54.7845359434711,-134.336527825942,
178.401695334183));
#37184=CARTESIAN_POINT('Ctrl Pts',(-54.7400959350076,-134.269848538465,
178.398821263656));
#37185=CARTESIAN_POINT('Ctrl Pts',(-54.6637259003796,-134.105649533411,
178.397771040799));
#37186=CARTESIAN_POINT('Ctrl Pts',(-54.6344128705762,-134.005471182846,
178.399901735339));
#37187=CARTESIAN_POINT('Ctrl Pts',(-54.62280141715,-133.896552554774,178.399901735339));
#37188=CARTESIAN_POINT('',(-55.3872025607663,-133.815062285981,179.902150755967));
#37189=CARTESIAN_POINT('Origin',(-61.1562134225954,-133.200047185959,175.985485069079));
#37190=CARTESIAN_POINT('',(-55.963244592837,-133.753652356887,180.646664753224));
#37191=CARTESIAN_POINT('Ctrl Pts',(-55.963244592837,-133.753652356887,180.646664753224));
#37192=CARTESIAN_POINT('Ctrl Pts',(-55.9771194953779,-133.88380276045,180.646664753224));
#37193=CARTESIAN_POINT('Ctrl Pts',(-56.0053503878778,-134.003191706013,
180.624827435906));
#37194=CARTESIAN_POINT('Ctrl Pts',(-56.0573970604472,-134.184986267805,
180.554323545746));
#37195=CARTESIAN_POINT('Ctrl Pts',(-56.0804206664297,-134.253912836984,
180.512187388971));
#37196=CARTESIAN_POINT('Ctrl Pts',(-56.1063095640505,-134.353233383846,
180.422617927188));
#37197=CARTESIAN_POINT('Ctrl Pts',(-56.1132331173457,-134.389554980947,
180.379494549411));
#37198=CARTESIAN_POINT('Ctrl Pts',(-56.1111717457673,-134.444376905523,
180.292512312315));
#37199=CARTESIAN_POINT('Ctrl Pts',(-56.104977458637,-134.464251326181,180.251627018014));
#37200=CARTESIAN_POINT('Ctrl Pts',(-56.0825765833158,-134.490348186181,
180.180538126642));
#37201=CARTESIAN_POINT('Ctrl Pts',(-56.0698795634517,-134.498651801989,
180.151151116536));
#37202=CARTESIAN_POINT('Ctrl Pts',(-56.0477728492981,-134.506445536525,
180.112373250109));
#37203=CARTESIAN_POINT('Ctrl Pts',(-56.0413692691035,-134.50818360884,180.102100763024));
#37204=CARTESIAN_POINT('Ctrl Pts',(-56.0301480293029,-134.51042930915,180.085610963709));
#37205=CARTESIAN_POINT('Ctrl Pts',(-56.0255991154346,-134.51115471075,180.079275366594));
#37206=CARTESIAN_POINT('Ctrl Pts',(-56.0165039590249,-134.512257805468,
180.067266989438));
#37207=CARTESIAN_POINT('Ctrl Pts',(-56.0119867645754,-134.512657985429,
180.061583180014));
#37208=CARTESIAN_POINT('Ctrl Pts',(-56.0012656199609,-134.513273259507,
180.04872671219));
#37209=CARTESIAN_POINT('Ctrl Pts',(-55.9949700757869,-134.513397752587,
180.04162596497));
#37210=CARTESIAN_POINT('Ctrl Pts',(-55.9749884168559,-134.513077478804,
180.020424727599));
#37211=CARTESIAN_POINT('Ctrl Pts',(-55.9606368415963,-134.511892707401,
180.006986406688));
#37212=CARTESIAN_POINT('Ctrl Pts',(-55.9120275852045,-134.504839152748,
179.966751975973));
#37213=CARTESIAN_POINT('Ctrl Pts',(-55.8755525337326,-134.495174997851,
179.944228548807));
#37214=CARTESIAN_POINT('Ctrl Pts',(-55.7998722057521,-134.4655702925,179.909119905611));
#37215=CARTESIAN_POINT('Ctrl Pts',(-55.7617584193857,-134.445957056798,
179.897066681094));
#37216=CARTESIAN_POINT('Ctrl Pts',(-55.6782972451937,-134.391011082889,
179.879200772612));
#37217=CARTESIAN_POINT('Ctrl Pts',(-55.6351912258566,-134.353849207735,
179.876099868631));
#37218=CARTESIAN_POINT('Ctrl Pts',(-55.5460646433215,-134.255343778846,
179.876566405119));
#37219=CARTESIAN_POINT('Ctrl Pts',(-55.5020132972087,-134.188623057366,
179.882659535915));
#37220=CARTESIAN_POINT('Ctrl Pts',(-55.4270846416986,-134.024270391666,
179.895647849101));
#37221=CARTESIAN_POINT('Ctrl Pts',(-55.3988140141925,-133.923980914052,
179.902150755967));
#37222=CARTESIAN_POINT('Ctrl Pts',(-55.3872025607663,-133.815062285981,
179.902150755967));
#37223=CARTESIAN_POINT('',(-56.4868776461708,-133.697829575064,181.176777403373));
#37224=CARTESIAN_POINT('Origin',(-61.1562134225954,-133.200047185959,175.985485069079));
#37225=CARTESIAN_POINT('',(-57.223350883061,-133.619316607712,181.761020143608));
#37226=CARTESIAN_POINT('Ctrl Pts',(-57.223350883061,-133.619316607712,181.761020143608));
#37227=CARTESIAN_POINT('Ctrl Pts',(-57.237225785602,-133.749467011276,181.761020143608));
#37228=CARTESIAN_POINT('Ctrl Pts',(-57.2598146785821,-133.869457431682,
181.736128117445));
#37229=CARTESIAN_POINT('Ctrl Pts',(-57.294145182622,-134.053140655397,181.659899466876));
#37230=CARTESIAN_POINT('Ctrl Pts',(-57.3066913787201,-134.123184186468,
181.61525743738));
#37231=CARTESIAN_POINT('Ctrl Pts',(-57.3108260656547,-134.224823877527,
181.524649644676));
#37232=CARTESIAN_POINT('Ctrl Pts',(-57.3073999952942,-134.262248813655,
181.4820532139));
#37233=CARTESIAN_POINT('Ctrl Pts',(-57.2848668463936,-134.319253166463,
181.39947983321));
#37234=CARTESIAN_POINT('Ctrl Pts',(-57.269182045857,-134.340139339255,181.361760820791));
#37235=CARTESIAN_POINT('Ctrl Pts',(-57.2305878917923,-134.367962510955,
181.298730366389));
#37236=CARTESIAN_POINT('Ctrl Pts',(-57.2112879664683,-134.376970040598,
181.27342941771));
#37237=CARTESIAN_POINT('Ctrl Pts',(-57.1806124249801,-134.385677269376,
181.241236757758));
#37238=CARTESIAN_POINT('Ctrl Pts',(-57.171953638511,-134.387655761746,181.232830705747));
#37239=CARTESIAN_POINT('Ctrl Pts',(-57.1571376499742,-134.390284686288,
181.21954732841));
#37240=CARTESIAN_POINT('Ctrl Pts',(-57.1512139912475,-134.391156644874,
181.214496727339));
#37241=CARTESIAN_POINT('Ctrl Pts',(-57.1395259320919,-134.392536160348,
181.205029625343));
#37242=CARTESIAN_POINT('Ctrl Pts',(-57.1337871894003,-134.393066565513,
181.200596073502));
#37243=CARTESIAN_POINT('Ctrl Pts',(-57.1203165473769,-134.393974954383,
181.19068008126));
#37244=CARTESIAN_POINT('Ctrl Pts',(-57.1125125206794,-134.394260261779,
181.185286960358));
#37245=CARTESIAN_POINT('Ctrl Pts',(-57.0880587868503,-134.394416741058,
181.169448647602));
#37246=CARTESIAN_POINT('Ctrl Pts',(-57.0709180469526,-134.393529313238,
181.15978596825));
#37247=CARTESIAN_POINT('Ctrl Pts',(-57.0141093333233,-134.387349875507,
181.132109146535));
#37248=CARTESIAN_POINT('Ctrl Pts',(-56.9732928312716,-134.378148548247,
181.118674907517));
#37249=CARTESIAN_POINT('Ctrl Pts',(-56.8913415381959,-134.34921236967,181.101844857552));
#37250=CARTESIAN_POINT('Ctrl Pts',(-56.8513944761148,-134.329794573407,
181.098714144129));
#37251=CARTESIAN_POINT('Ctrl Pts',(-56.7659114793704,-134.27506413929,181.099834492783));
#37252=CARTESIAN_POINT('Ctrl Pts',(-56.7231922271569,-134.237861032177,
181.106138759988));
#37253=CARTESIAN_POINT('Ctrl Pts',(-56.6364356978932,-134.139102939774,
181.12530197231));
#37254=CARTESIAN_POINT('Ctrl Pts',(-56.5948956204382,-134.072114500278,
181.140008193814));
#37255=CARTESIAN_POINT('Ctrl Pts',(-56.5247071718325,-133.907256496853,
181.166280209492));
#37256=CARTESIAN_POINT('Ctrl Pts',(-56.498489099597,-133.806748203135,181.176777403373));
#37257=CARTESIAN_POINT('Ctrl Pts',(-56.4868776461708,-133.697829575064,
181.176777403373));
#37258=CARTESIAN_POINT('Origin',(-61.1562134225954,-133.200047185959,175.985485069079));
#37259=CARTESIAN_POINT('Origin',(-61.1562134225954,-133.200047185959,175.985485069079));
#37260=CARTESIAN_POINT('Origin',(-61.1562134225954,-133.200047185959,175.985485069079));
#37261=CARTESIAN_POINT('Origin',(-61.1562134225954,-133.200047185959,175.985485069079));
#37262=CARTESIAN_POINT('Origin',(-61.1562134225954,-133.200047185959,175.985485069079));
#37263=CARTESIAN_POINT('Origin',(-61.1562134225954,-133.200047185959,175.985485069079));
#37264=CARTESIAN_POINT('Origin',(-54.1598171290174,-67.5719248685924,175.985485069079));
#37265=CARTESIAN_POINT('Ctrl Pts',(-52.354402310021,-68.0158107614237,173.617797875547));
#37266=CARTESIAN_POINT('Ctrl Pts',(-52.3922609029376,-68.008076981393,173.587868187509));
#37267=CARTESIAN_POINT('Ctrl Pts',(-52.4308701851704,-68.0002229772944,
173.558852597356));
#37268=CARTESIAN_POINT('Ctrl Pts',(-52.7925027578306,-67.926959058679,173.300747567891));
#37269=CARTESIAN_POINT('Ctrl Pts',(-53.1570390226867,-67.855260286434,173.138568265546));
#37270=CARTESIAN_POINT('Ctrl Pts',(-53.8341366603134,-67.7254283072159,
172.989462193406));
#37271=CARTESIAN_POINT('Ctrl Pts',(-54.1340786807895,-67.6689480666864,
172.970420115031));
#37272=CARTESIAN_POINT('Ctrl Pts',(-54.727201252603,-67.5592649898145,173.023972702883));
#37273=CARTESIAN_POINT('Ctrl Pts',(-55.0168740057393,-67.5050562916733,
173.095494376926));
#37274=CARTESIAN_POINT('Ctrl Pts',(-55.2910412295907,-67.4513288218826,
173.209554841606));
#37275=CARTESIAN_POINT('Origin',(-54.1598171290174,-67.5719248685924,175.985485069079));
#37276=CARTESIAN_POINT('Origin',(-54.1598171290174,-67.5719248685924,175.985485069079));
#37277=CARTESIAN_POINT('',(-67.2656014102483,-128.526079858515,173.57106840282));
#37278=CARTESIAN_POINT('Origin',(-54.1598171290174,-67.5719248685924,175.985485069079));
#37279=CARTESIAN_POINT('Origin',(-54.1598171290174,-67.5719248685924,175.985485069079));
#37280=CARTESIAN_POINT('Origin',(-54.1598171290174,-67.5719248685924,175.985485069079));
#37281=CARTESIAN_POINT('Origin',(-54.1598171290174,-67.5719248685924,175.985485069079));
#37282=CARTESIAN_POINT('Origin',(-54.1598171290174,-67.5719248685924,175.985485069079));
#37283=CARTESIAN_POINT('Origin',(-54.1598171290174,-67.5719248685924,175.985485069079));
#37284=CARTESIAN_POINT('Origin',(-54.1598171290174,-67.5719248685924,175.985485069079));
#37285=CARTESIAN_POINT('Origin',(-54.1598171290174,-67.5719248685924,175.985485069079));
#37286=CARTESIAN_POINT('Origin',(-54.1598171290174,-67.5719248685924,175.985485069079));
#37287=CARTESIAN_POINT('',(-56.7993268652684,-129.641854649084,181.761020143608));
#37288=CARTESIAN_POINT('Origin',(-54.1598171290174,-67.5719248685924,175.985485069079));
#37289=CARTESIAN_POINT('',(-56.0628536283782,-129.720367616436,181.176777403373));
#37290=CARTESIAN_POINT('',(-55.5392205750444,-129.776190398259,180.646664753224));
#37291=CARTESIAN_POINT('Origin',(-54.1598171290174,-67.5719248685924,175.985485069079));
#37292=CARTESIAN_POINT('',(-54.9631785429737,-129.837600327353,179.902150755967));
#37293=CARTESIAN_POINT('',(-54.5809107575323,-129.878352627172,179.261418542296));
#37294=CARTESIAN_POINT('Origin',(-54.1598171290174,-67.5719248685924,175.985485069079));
#37295=CARTESIAN_POINT('',(-54.1987773993573,-129.919090596146,178.399901735339));
#37296=CARTESIAN_POINT('',(-53.9800908960114,-129.942404038424,177.685786985438));
#37297=CARTESIAN_POINT('Origin',(-54.1598171290174,-67.5719248685924,175.985485069079));
#37298=CARTESIAN_POINT('',(-53.8140744135111,-129.960102504597,176.757335594116));
#37299=CARTESIAN_POINT('',(-53.771678456942,-129.96462219681,176.011340061548));
#37300=CARTESIAN_POINT('Origin',(-54.1598171290174,-67.5719248685924,175.985485069079));
#37301=CARTESIAN_POINT('',(-53.831427124634,-129.95825258966,175.06991230594));
#37302=CARTESIAN_POINT('',(-53.9677856137344,-129.943715863725,174.335390539474));
#37303=CARTESIAN_POINT('Origin',(-54.1598171290174,-67.5719248685924,175.985485069079));
#37304=CARTESIAN_POINT('',(-54.2498270562299,-129.913648361666,173.435698778786));
#37305=CARTESIAN_POINT('',(-54.5570153312564,-129.880900039256,172.755338513612));
#37306=CARTESIAN_POINT('Origin',(-54.1598171290174,-67.5719248685924,175.985485069079));
#37307=CARTESIAN_POINT('',(-55.0449583250965,-129.828882056217,171.949669562728));
#37308=CARTESIAN_POINT('',(-55.5051237200884,-129.779825350794,171.363010864448));
#37309=CARTESIAN_POINT('Origin',(-54.1598171290174,-67.5719248685924,175.985485069079));
#37310=CARTESIAN_POINT('',(-56.1706107920718,-129.708879982872,170.698187274307));
#37311=CARTESIAN_POINT('',(-56.7570101669053,-129.646365891843,170.239324614047));
#37312=CARTESIAN_POINT('Origin',(-54.1598171290174,-67.5719248685924,175.985485069079));
#37313=CARTESIAN_POINT('',(-57.5613656273554,-129.560616225945,169.753983515172));
#37314=CARTESIAN_POINT('',(-58.2399195818402,-129.48827784105,169.44958432285));
#37315=CARTESIAN_POINT('Origin',(-54.1598171290174,-67.5719248685924,175.985485069079));
#37316=CARTESIAN_POINT('',(-59.1363972151087,-129.392707336071,169.171931975764));
#37317=CARTESIAN_POINT('',(-59.8676706598535,-129.3147487013,169.03968682599));
#37318=CARTESIAN_POINT('Origin',(-54.1598171290174,-67.5719248685924,175.985485069079));
#37319=CARTESIAN_POINT('',(-60.8041704444585,-129.214911567606,168.985859375881));
#37320=CARTESIAN_POINT('',(-61.5456644249254,-129.135863355445,169.03345387607));
#37321=CARTESIAN_POINT('Origin',(-54.1598171290174,-67.5719248685924,175.985485069079));
#37322=CARTESIAN_POINT('',(-62.4677603974239,-129.037561764351,169.206579578684));
#37323=CARTESIAN_POINT('',(-63.1763819786892,-128.962017969562,169.431247709482));
#37324=CARTESIAN_POINT('Origin',(-54.1598171290174,-67.5719248685924,175.985485069079));
#37325=CARTESIAN_POINT('',(-64.030485272842,-128.870964852232,169.821265128268));
#37326=CARTESIAN_POINT('',(-64.6650519443373,-128.803315805577,170.209949994551));
#37327=CARTESIAN_POINT('Origin',(-54.1598171290174,-67.5719248685924,175.985485069079));
#37328=CARTESIAN_POINT('',(-65.4015251812274,-128.724802838225,170.794192734786));
#37329=CARTESIAN_POINT('',(-65.9251582345612,-128.668980056403,171.324305384935));
#37330=CARTESIAN_POINT('Origin',(-64.79464880995,-126.778167037988,181.510088520653));
#37331=CARTESIAN_POINT('',(-59.0118785952597,-127.394648976958,179.686725372425));
#37332=CARTESIAN_POINT('',(-64.4583706077394,-126.814016540979,175.424797521489));
#37333=CARTESIAN_POINT('Ctrl Pts',(-59.0118785952585,-127.39464897695,179.686725372426));
#37334=CARTESIAN_POINT('Ctrl Pts',(-59.4359949842293,-127.349435336409,
179.865346446743));
#37335=CARTESIAN_POINT('Ctrl Pts',(-59.8876448219349,-127.301286446285,
179.967826141208));
#37336=CARTESIAN_POINT('Ctrl Pts',(-60.7960132539299,-127.204448302721,
180.012144456981));
#37337=CARTESIAN_POINT('Ctrl Pts',(-61.2457410607842,-127.156504313926,
179.956996941234));
#37338=CARTESIAN_POINT('Ctrl Pts',(-62.1463022559178,-127.060498473971,
179.685447946453));
#37339=CARTESIAN_POINT('Ctrl Pts',(-62.5856624257918,-127.013659744544,
179.457395568183));
#37340=CARTESIAN_POINT('Ctrl Pts',(-63.3595262690438,-126.931160688751,
178.851724556864));
#37341=CARTESIAN_POINT('Ctrl Pts',(-63.6872391011354,-126.896224311435,
178.479429252066));
#37342=CARTESIAN_POINT('Ctrl Pts',(-64.1700987222909,-126.844748249885,
177.668306113048));
#37343=CARTESIAN_POINT('Ctrl Pts',(-64.3336854609466,-126.827308810639,
177.243537880892));
#37344=CARTESIAN_POINT('Ctrl Pts',(-64.5140884934819,-126.808076642117,
176.347356701111));
#37345=CARTESIAN_POINT('Ctrl Pts',(-64.5262870428016,-126.806776195262,
175.882015335093));
#37346=CARTESIAN_POINT('Ctrl Pts',(-64.4583706077402,-126.814016540982,
175.424797521489));
#37347=CARTESIAN_POINT('Ctrl Pts',(-64.4583706077523,-126.814016540981,
175.424797521484));
#37348=CARTESIAN_POINT('Ctrl Pts',(-64.340455120303,-126.826587119724,175.127034144718));
#37349=CARTESIAN_POINT('Ctrl Pts',(-64.185525566722,-126.843103645204,174.845600608932));
#37350=CARTESIAN_POINT('Ctrl Pts',(-63.8142461467475,-126.882684511852,
174.337218287797));
#37351=CARTESIAN_POINT('Ctrl Pts',(-63.6016307872636,-126.905350729633,
174.111030744869));
#37352=CARTESIAN_POINT('Ctrl Pts',(-63.1867614231896,-126.949578575542,
173.767005019069));
#37353=CARTESIAN_POINT('Ctrl Pts',(-62.9060963946901,-126.979499342674,
173.561578827361));
#37354=CARTESIAN_POINT('Ctrl Pts',(-62.237164000988,-127.050812004909,173.298981894668));
#37355=CARTESIAN_POINT('Ctrl Pts',(-61.9468760301073,-127.081758641988,
173.232074662412));
#37356=CARTESIAN_POINT('Ctrl Pts',(-61.6514014972809,-127.113258201221,
173.209554841667));
#37357=CARTESIAN_POINT('Ctrl Pts',(-57.5665324870373,-127.548732528291,
176.406000729816));
#37358=CARTESIAN_POINT('Ctrl Pts',(-57.5156929015415,-127.554152367759,
176.69915760637));
#37359=CARTESIAN_POINT('Ctrl Pts',(-57.5087873657294,-127.554888544012,
176.998153402395));
#37360=CARTESIAN_POINT('Ctrl Pts',(-57.5972658161105,-127.545456150086,
177.715327713047));
#37361=CARTESIAN_POINT('Ctrl Pts',(-57.7265253129934,-127.531676224149,
178.039347906201));
#37362=CARTESIAN_POINT('Ctrl Pts',(-57.9549266303152,-127.507327117798,
178.526645640705));
#37363=CARTESIAN_POINT('Ctrl Pts',(-58.1207929492895,-127.48964466006,178.789993473182));
#37364=CARTESIAN_POINT('Ctrl Pts',(-58.5199743484872,-127.447089256016,
179.277750850868));
#37365=CARTESIAN_POINT('Ctrl Pts',(-58.7534704118167,-127.422197015703,
179.498319550967));
#37366=CARTESIAN_POINT('Ctrl Pts',(-59.0118785952414,-127.394648976952,
179.686725372449));
#37367=CARTESIAN_POINT('Origin',(-61.2622194270436,-134.194412675616,175.985485069079));
#37368=CARTESIAN_POINT('Origin',(-54.1598171290174,-67.5719248685924,175.985485069079));
#37369=CARTESIAN_POINT('',(-66.8834680520733,-128.566817827489,172.709551595863));
#37370=CARTESIAN_POINT('',(-66.5012002666319,-128.607570127308,172.068819382192));
#37371=CARTESIAN_POINT('Origin',(-55.9917334493218,-67.3766303500087,178.353172262611));
#37372=CARTESIAN_POINT('',(-52.6515183282542,-67.7327195975386,179.686725372378));
#37373=CARTESIAN_POINT('Ctrl Pts',(-51.2061722201485,-67.8868031488672,
176.406000729815));
#37374=CARTESIAN_POINT('Ctrl Pts',(-51.1553326346522,-67.892222988335,176.699157606371));
#37375=CARTESIAN_POINT('Ctrl Pts',(-51.1484270988405,-67.8929591645877,
176.998153402397));
#37376=CARTESIAN_POINT('Ctrl Pts',(-51.2369055492213,-67.8835267706619,
177.715327713046));
#37377=CARTESIAN_POINT('Ctrl Pts',(-51.3661650461041,-67.8697468447252,
178.0393479062));
#37378=CARTESIAN_POINT('Ctrl Pts',(-51.5945663634263,-67.8453977383736,
178.526645640706));
#37379=CARTESIAN_POINT('Ctrl Pts',(-51.760432682401,-67.8277152806355,178.789993473183));
#37380=CARTESIAN_POINT('Ctrl Pts',(-52.1596140815011,-67.7851598766027,
179.277750850749));
#37381=CARTESIAN_POINT('Ctrl Pts',(-52.3931101446833,-67.760267636305,179.498319550776));
#37382=CARTESIAN_POINT('Ctrl Pts',(-52.6515183282542,-67.7327195975386,
179.686725372378));
#37383=CARTESIAN_POINT('',(-58.0980103408427,-67.1520871615593,175.424797521432));
#37384=CARTESIAN_POINT('Ctrl Pts',(-58.0980103408427,-67.1520871615593,
175.424797521432));
#37385=CARTESIAN_POINT('Ctrl Pts',(-57.9800948533587,-67.164657740306,175.127034144591));
#37386=CARTESIAN_POINT('Ctrl Pts',(-57.8251652997951,-67.1811742657839,
174.845600608881));
#37387=CARTESIAN_POINT('Ctrl Pts',(-57.4538858798669,-67.2207551324268,
174.337218287807));
#37388=CARTESIAN_POINT('Ctrl Pts',(-57.2412705203865,-67.2434213502081,
174.111030744881));
#37389=CARTESIAN_POINT('Ctrl Pts',(-56.8264011563053,-67.2876491961175,
173.767005019072));
#37390=CARTESIAN_POINT('Ctrl Pts',(-56.5457361278046,-67.3175699632491,
173.561578827364));
#37391=CARTESIAN_POINT('Ctrl Pts',(-55.8768037354484,-67.3888826253409,
173.298981895197));
#37392=CARTESIAN_POINT('Ctrl Pts',(-55.5865157635609,-67.4198292625273,
173.232074662357));
#37393=CARTESIAN_POINT('Ctrl Pts',(-55.29104122959,-67.4513288218827,173.209554841606));
#37394=CARTESIAN_POINT('Ctrl Pts',(-52.6515183282542,-67.7327195975386,
179.686725372378));
#37395=CARTESIAN_POINT('Ctrl Pts',(-53.0762789282691,-67.6874372797963,
179.865617762962));
#37396=CARTESIAN_POINT('Ctrl Pts',(-53.5286545057955,-67.6392110209586,
179.968135041463));
#37397=CARTESIAN_POINT('Ctrl Pts',(-54.4383742439024,-67.542228819135,180.012039202549));
#37398=CARTESIAN_POINT('Ctrl Pts',(-54.8887059634283,-67.4942204492149,
179.956466658887));
#37399=CARTESIAN_POINT('Ctrl Pts',(-55.7899722900454,-67.3981394375324,
179.68371381595));
#37400=CARTESIAN_POINT('Ctrl Pts',(-56.2294231124242,-67.3512910439425,
179.454971033449));
#37401=CARTESIAN_POINT('Ctrl Pts',(-57.0028982092043,-67.2688334311204,
178.847994825624));
#37402=CARTESIAN_POINT('Ctrl Pts',(-57.3301960056921,-67.2339412993728,
178.475171130105));
#37403=CARTESIAN_POINT('Ctrl Pts',(-57.8115564772304,-67.1826250571884,
177.664035140268));
#37404=CARTESIAN_POINT('Ctrl Pts',(-57.9743790814683,-67.165267079776,177.239932149216));
#37405=CARTESIAN_POINT('Ctrl Pts',(-58.153780989458,-67.1461416378191,176.345419634447));
#37406=CARTESIAN_POINT('Ctrl Pts',(-58.1657851525024,-67.1448619138401,
175.881061917132));
#37407=CARTESIAN_POINT('Ctrl Pts',(-58.0980103408427,-67.1520871615593,
175.424797521432));
#37408=CARTESIAN_POINT('Ctrl Pts',(-51.0870509156302,-66.8309817211475,
175.613978373734));
#37409=CARTESIAN_POINT('Ctrl Pts',(-50.9439729228075,-66.9405160196288,
176.847054148052));
#37410=CARTESIAN_POINT('Ctrl Pts',(-51.7127157157354,-66.9528441305708,
177.8277821816));
#37411=CARTESIAN_POINT('Ctrl Pts',(-52.4814585086634,-66.9651722415128,
178.808510215148));
#37412=CARTESIAN_POINT('Ctrl Pts',(-53.7175245676945,-66.9276805701509,
178.962393326872));
#37413=CARTESIAN_POINT('Ctrl Pts',(-54.9535906267256,-66.890188898789,179.116276438596));
#37414=CARTESIAN_POINT('Ctrl Pts',(-55.9387308009417,-66.8794476031576,
178.35317198867));
#37415=CARTESIAN_POINT('Ctrl Pts',(-56.9238709751577,-66.8687063075263,
177.590067538743));
#37416=CARTESIAN_POINT('Ctrl Pts',(-57.0868250938145,-66.9456155383557,
176.356991764425));
#37417=CARTESIAN_POINT('Ctrl Pts',(-57.2497792124713,-67.0225247691851,
175.123915990107));
#37418=CARTESIAN_POINT('Ctrl Pts',(-56.5009125453774,-67.1966401875538,
174.143187956559));
#37419=CARTESIAN_POINT('Ctrl Pts',(-55.7520458782835,-67.3707556059225,
173.162459923011));
#37420=CARTESIAN_POINT('Ctrl Pts',(-54.5358559450863,-67.5946908065951,
173.008576811287));
#37421=CARTESIAN_POINT('Ctrl Pts',(-53.3196660118892,-67.8186260072677,
172.854693699562));
#37422=CARTESIAN_POINT('Ctrl Pts',(-52.3544019635072,-68.0158108322098,
173.617798149489));
#37423=CARTESIAN_POINT('Ctrl Pts',(-51.3891379151252,-68.2129956571518,
174.380902599416));
#37424=CARTESIAN_POINT('Ctrl Pts',(-51.2460599223025,-68.3225299556331,
175.613978373734));
#37425=CARTESIAN_POINT('Ctrl Pts',(-51.1029819294797,-68.4320642541144,
176.847054148052));
#37426=CARTESIAN_POINT('Ctrl Pts',(-51.8717247224076,-68.4443923650564,
177.8277821816));
#37427=CARTESIAN_POINT('Ctrl Pts',(-52.6404675153356,-68.4567204759984,
178.808510215148));
#37428=CARTESIAN_POINT('Ctrl Pts',(-53.8765335743667,-68.4192288046365,
178.962393326872));
#37429=CARTESIAN_POINT('Ctrl Pts',(-55.1125996333979,-68.3817371332746,
179.116276438596));
#37430=CARTESIAN_POINT('Ctrl Pts',(-56.0977398076139,-68.3709958376432,
178.35317198867));
#37431=CARTESIAN_POINT('Ctrl Pts',(-57.0828799818299,-68.3602545420119,
177.590067538743));
#37432=CARTESIAN_POINT('Ctrl Pts',(-57.2458341004867,-68.4371637728413,
176.356991764425));
#37433=CARTESIAN_POINT('Ctrl Pts',(-57.4087882191435,-68.5140730036707,
175.123915990107));
#37434=CARTESIAN_POINT('Ctrl Pts',(-56.6599215520496,-68.6881884220394,
174.143187956559));
#37435=CARTESIAN_POINT('Ctrl Pts',(-55.9110548849557,-68.8623038404081,
173.162459923011));
#37436=CARTESIAN_POINT('Ctrl Pts',(-54.6948649517586,-69.0862390410807,
173.008576811287));
#37437=CARTESIAN_POINT('Ctrl Pts',(-53.4786750185615,-69.3101742417533,
172.854693699562));
#37438=CARTESIAN_POINT('Ctrl Pts',(-52.5134109701795,-69.5073590666954,
173.617798149489));
#37439=CARTESIAN_POINT('Ctrl Pts',(-51.5481469217975,-69.7045438916374,
174.380902599416));
#37440=CARTESIAN_POINT('Ctrl Pts',(-51.4050689289747,-69.8140781901187,
175.613978373734));
#37441=CARTESIAN_POINT('Ctrl Pts',(-51.2619909361519,-69.9236124886,176.847054148052));
#37442=CARTESIAN_POINT('Ctrl Pts',(-52.0307337290798,-69.935940599542,177.8277821816));
#37443=CARTESIAN_POINT('Ctrl Pts',(-52.7994765220078,-69.948268710484,178.808510215148));
#37444=CARTESIAN_POINT('Ctrl Pts',(-54.035542581039,-69.9107770391221,178.962393326872));
#37445=CARTESIAN_POINT('Ctrl Pts',(-55.2716086400701,-69.8732853677602,
179.116276438596));
#37446=CARTESIAN_POINT('Ctrl Pts',(-56.2567488142861,-69.8625440721288,
178.35317198867));
#37447=CARTESIAN_POINT('Ctrl Pts',(-57.2418889885021,-69.8518027764975,
177.590067538743));
#37448=CARTESIAN_POINT('Ctrl Pts',(-57.404843107159,-69.9287120073269,176.356991764425));
#37449=CARTESIAN_POINT('Ctrl Pts',(-57.5677972258158,-70.0056212381563,
175.123915990107));
#37450=CARTESIAN_POINT('Ctrl Pts',(-56.8189305587218,-70.179736656525,174.143187956559));
#37451=CARTESIAN_POINT('Ctrl Pts',(-56.0700638916279,-70.3538520748937,
173.162459923011));
#37452=CARTESIAN_POINT('Ctrl Pts',(-54.8538739584308,-70.5777872755663,
173.008576811287));
#37453=CARTESIAN_POINT('Ctrl Pts',(-53.6376840252337,-70.801722476239,172.854693699562));
#37454=CARTESIAN_POINT('Ctrl Pts',(-52.6724199768517,-70.998907301181,173.617798149489));
#37455=CARTESIAN_POINT('Ctrl Pts',(-51.7071559284697,-71.196092126123,174.380902599416));
#37456=CARTESIAN_POINT('Ctrl Pts',(-51.5640779356469,-71.3056264246043,
175.613978373734));
#37457=CARTESIAN_POINT('Ctrl Pts',(-51.4209999428241,-71.4151607230856,
176.847054148052));
#37458=CARTESIAN_POINT('Ctrl Pts',(-52.1897427357521,-71.4274888340276,
177.8277821816));
#37459=CARTESIAN_POINT('Ctrl Pts',(-52.95848552868,-71.4398169449696,178.808510215148));
#37460=CARTESIAN_POINT('Ctrl Pts',(-54.1945515877112,-71.4023252736077,
178.962393326872));
#37461=CARTESIAN_POINT('Ctrl Pts',(-55.4306176467423,-71.3648336022458,
179.116276438596));
#37462=CARTESIAN_POINT('Ctrl Pts',(-56.4157578209583,-71.3540923066144,
178.35317198867));
#37463=CARTESIAN_POINT('Ctrl Pts',(-57.4008979951744,-71.3433510109831,
177.590067538743));
#37464=CARTESIAN_POINT('Ctrl Pts',(-57.5638521138312,-71.4202602418125,
176.356991764425));
#37465=CARTESIAN_POINT('Ctrl Pts',(-57.726806232488,-71.4971694726419,175.123915990107));
#37466=CARTESIAN_POINT('Ctrl Pts',(-56.9779395653941,-71.6712848910106,
174.143187956559));
#37467=CARTESIAN_POINT('Ctrl Pts',(-56.2290728983002,-71.8454003093793,
173.162459923011));
#37468=CARTESIAN_POINT('Ctrl Pts',(-55.012882965103,-72.0693355100519,173.008576811287));
#37469=CARTESIAN_POINT('Ctrl Pts',(-53.7966930319059,-72.2932707107245,
172.854693699562));
#37470=CARTESIAN_POINT('Ctrl Pts',(-52.8314289835239,-72.4904555356666,
173.617798149489));
#37471=CARTESIAN_POINT('Ctrl Pts',(-51.8661649351419,-72.6876403606086,
174.380902599416));
#37472=CARTESIAN_POINT('Ctrl Pts',(-51.7230869423191,-72.7971746590899,
175.613978373734));
#37473=CARTESIAN_POINT('Ctrl Pts',(-51.5800089494964,-72.9067089575712,
176.847054148052));
#37474=CARTESIAN_POINT('Ctrl Pts',(-52.3487517424243,-72.9190370685132,
177.8277821816));
#37475=CARTESIAN_POINT('Ctrl Pts',(-53.1174945353523,-72.9313651794552,
178.808510215148));
#37476=CARTESIAN_POINT('Ctrl Pts',(-54.3535605943834,-72.8938735080933,
178.962393326872));
#37477=CARTESIAN_POINT('Ctrl Pts',(-55.5896266534145,-72.8563818367314,
179.116276438596));
#37478=CARTESIAN_POINT('Ctrl Pts',(-56.5747668276306,-72.8456405411,178.35317198867));
#37479=CARTESIAN_POINT('Ctrl Pts',(-57.5599070018466,-72.8348992454687,
177.590067538743));
#37480=CARTESIAN_POINT('Ctrl Pts',(-57.7228611205034,-72.9118084762981,
176.356991764425));
#37481=CARTESIAN_POINT('Ctrl Pts',(-57.8858152391602,-72.9887177071275,
175.123915990107));
#37482=CARTESIAN_POINT('Ctrl Pts',(-57.1369485720663,-73.1628331254962,
174.143187956559));
#37483=CARTESIAN_POINT('Ctrl Pts',(-56.3880819049724,-73.3369485438649,
173.162459923011));
#37484=CARTESIAN_POINT('Ctrl Pts',(-55.1718919717753,-73.5608837445375,
173.008576811287));
#37485=CARTESIAN_POINT('Ctrl Pts',(-53.9557020385781,-73.7848189452101,
172.854693699562));
#37486=CARTESIAN_POINT('Ctrl Pts',(-52.9904379901961,-73.9820037701522,
173.617798149489));
#37487=CARTESIAN_POINT('Ctrl Pts',(-52.0251739418142,-74.1791885950942,
174.380902599416));
#37488=CARTESIAN_POINT('Ctrl Pts',(-51.8820959489914,-74.2887228935755,
175.613978373734));
#37489=CARTESIAN_POINT('Ctrl Pts',(-51.7390179561686,-74.3982571920568,
176.847054148052));
#37490=CARTESIAN_POINT('Ctrl Pts',(-52.5077607490965,-74.4105853029988,
177.8277821816));
#37491=CARTESIAN_POINT('Ctrl Pts',(-53.2765035420245,-74.4229134139408,
178.808510215148));
#37492=CARTESIAN_POINT('Ctrl Pts',(-54.5125696010556,-74.3854217425789,
178.962393326872));
#37493=CARTESIAN_POINT('Ctrl Pts',(-55.7486356600868,-74.347930071217,179.116276438596));
#37494=CARTESIAN_POINT('Ctrl Pts',(-56.7337758343028,-74.3371887755856,
178.35317198867));
#37495=CARTESIAN_POINT('Ctrl Pts',(-57.7189160085188,-74.3264474799543,
177.590067538743));
#37496=CARTESIAN_POINT('Ctrl Pts',(-57.8818701271756,-74.4033567107837,
176.356991764425));
#37497=CARTESIAN_POINT('Ctrl Pts',(-58.0448242458325,-74.4802659416131,
175.123915990107));
#37498=CARTESIAN_POINT('Ctrl Pts',(-57.2959575787385,-74.6543813599818,
174.143187956559));
#37499=CARTESIAN_POINT('Ctrl Pts',(-56.5470909116446,-74.8284967783505,
173.162459923011));
#37500=CARTESIAN_POINT('Ctrl Pts',(-55.3309009784475,-75.0524319790231,
173.008576811287));
#37501=CARTESIAN_POINT('Ctrl Pts',(-54.1147110452504,-75.2763671796957,
172.854693699562));
#37502=CARTESIAN_POINT('Ctrl Pts',(-53.1494469968684,-75.4735520046378,
173.617798149489));
#37503=CARTESIAN_POINT('Ctrl Pts',(-52.1841829484864,-75.6707368295798,
174.380902599416));
#37504=CARTESIAN_POINT('Ctrl Pts',(-52.0411049556636,-75.7802711280611,
175.613978373734));
#37505=CARTESIAN_POINT('Ctrl Pts',(-51.8980269628408,-75.8898054265424,
176.847054148052));
#37506=CARTESIAN_POINT('Ctrl Pts',(-52.6667697557687,-75.9021335374844,
177.8277821816));
#37507=CARTESIAN_POINT('Ctrl Pts',(-53.4355125486967,-75.9144616484264,
178.808510215148));
#37508=CARTESIAN_POINT('Ctrl Pts',(-54.6715786077279,-75.8769699770645,
178.962393326872));
#37509=CARTESIAN_POINT('Ctrl Pts',(-55.907644666759,-75.8394783057026,179.116276438596));
#37510=CARTESIAN_POINT('Ctrl Pts',(-56.892784840975,-75.8287370100712,178.35317198867));
#37511=CARTESIAN_POINT('Ctrl Pts',(-57.877925015191,-75.8179957144399,177.590067538743));
#37512=CARTESIAN_POINT('Ctrl Pts',(-58.0408791338479,-75.8949049452693,
176.356991764425));
#37513=CARTESIAN_POINT('Ctrl Pts',(-58.2038332525047,-75.9718141760987,
175.123915990107));
#37514=CARTESIAN_POINT('Ctrl Pts',(-57.4549665854108,-76.1459295944674,
174.143187956559));
#37515=CARTESIAN_POINT('Ctrl Pts',(-56.7060999183168,-76.3200450128361,
173.162459923011));
#37516=CARTESIAN_POINT('Ctrl Pts',(-55.4899099851197,-76.5439802135087,
173.008576811287));
#37517=CARTESIAN_POINT('Ctrl Pts',(-54.2737200519226,-76.7679154141813,
172.854693699562));
#37518=CARTESIAN_POINT('Ctrl Pts',(-53.3084560035406,-76.9651002391234,
173.617798149489));
#37519=CARTESIAN_POINT('Ctrl Pts',(-52.3431919551586,-77.1622850640654,
174.380902599416));
#37520=CARTESIAN_POINT('Ctrl Pts',(-52.2001139623358,-77.2718193625467,
175.613978373734));
#37521=CARTESIAN_POINT('Ctrl Pts',(-52.057035969513,-77.381353661028,176.847054148052));
#37522=CARTESIAN_POINT('Ctrl Pts',(-52.825778762441,-77.39368177197,177.8277821816));
#37523=CARTESIAN_POINT('Ctrl Pts',(-53.5945215553689,-77.406009882912,178.808510215148));
#37524=CARTESIAN_POINT('Ctrl Pts',(-54.8305876144001,-77.3685182115501,
178.962393326872));
#37525=CARTESIAN_POINT('Ctrl Pts',(-56.0666536734312,-77.3310265401882,
179.116276438596));
#37526=CARTESIAN_POINT('Ctrl Pts',(-57.0517938476472,-77.3202852445568,
178.35317198867));
#37527=CARTESIAN_POINT('Ctrl Pts',(-58.0369340218633,-77.3095439489255,
177.590067538743));
#37528=CARTESIAN_POINT('Ctrl Pts',(-58.1998881405201,-77.3864531797549,
176.356991764425));
#37529=CARTESIAN_POINT('Ctrl Pts',(-58.3628422591769,-77.4633624105843,
175.123915990107));
#37530=CARTESIAN_POINT('Ctrl Pts',(-57.613975592083,-77.637477828953,174.143187956559));
#37531=CARTESIAN_POINT('Ctrl Pts',(-56.8651089249891,-77.8115932473217,
173.162459923011));
#37532=CARTESIAN_POINT('Ctrl Pts',(-55.6489189917919,-78.0355284479943,
173.008576811287));
#37533=CARTESIAN_POINT('Ctrl Pts',(-54.4327290585948,-78.259463648667,172.854693699562));
#37534=CARTESIAN_POINT('Ctrl Pts',(-53.4674650102128,-78.456648473609,173.617798149489));
#37535=CARTESIAN_POINT('Ctrl Pts',(-52.5022009618309,-78.653833298551,174.380902599416));
#37536=CARTESIAN_POINT('Ctrl Pts',(-52.359122969008,-78.7633675970323,175.613978373734));
#37537=CARTESIAN_POINT('Ctrl Pts',(-52.2160449761853,-78.8729018955136,
176.847054148052));
#37538=CARTESIAN_POINT('Ctrl Pts',(-52.9847877691132,-78.8852300064556,
177.8277821816));
#37539=CARTESIAN_POINT('Ctrl Pts',(-53.7535305620412,-78.8975581173976,
178.808510215148));
#37540=CARTESIAN_POINT('Ctrl Pts',(-54.9895966210723,-78.8600664460357,
178.962393326872));
#37541=CARTESIAN_POINT('Ctrl Pts',(-56.2256626801035,-78.8225747746738,
179.116276438596));
#37542=CARTESIAN_POINT('Ctrl Pts',(-57.2108028543195,-78.8118334790424,
178.35317198867));
#37543=CARTESIAN_POINT('Ctrl Pts',(-58.1959430285355,-78.8010921834111,
177.590067538743));
#37544=CARTESIAN_POINT('Ctrl Pts',(-58.3588971471923,-78.8780014142405,
176.356991764425));
#37545=CARTESIAN_POINT('Ctrl Pts',(-58.5218512658491,-78.9549106450699,
175.123915990107));
#37546=CARTESIAN_POINT('Ctrl Pts',(-57.7729845987552,-79.1290260634386,
174.143187956559));
#37547=CARTESIAN_POINT('Ctrl Pts',(-57.0241179316613,-79.3031414818073,
173.162459923011));
#37548=CARTESIAN_POINT('Ctrl Pts',(-55.8079279984642,-79.5270766824799,
173.008576811287));
#37549=CARTESIAN_POINT('Ctrl Pts',(-54.5917380652671,-79.7510118831525,
172.854693699562));
#37550=CARTESIAN_POINT('Ctrl Pts',(-53.6264740168851,-79.9481967080946,
173.617798149489));
#37551=CARTESIAN_POINT('Ctrl Pts',(-52.6612099685031,-80.1453815330366,
174.380902599416));
#37552=CARTESIAN_POINT('Ctrl Pts',(-52.5181319756803,-80.2549158315179,
175.613978373734));
#37553=CARTESIAN_POINT('Ctrl Pts',(-52.3750539828575,-80.3644501299992,
176.847054148052));
#37554=CARTESIAN_POINT('Ctrl Pts',(-53.1437967757854,-80.3767782409412,
177.8277821816));
#37555=CARTESIAN_POINT('Ctrl Pts',(-53.9125395687134,-80.3891063518832,
178.808510215148));
#37556=CARTESIAN_POINT('Ctrl Pts',(-55.1486056277445,-80.3516146805213,
178.962393326872));
#37557=CARTESIAN_POINT('Ctrl Pts',(-56.3846716867757,-80.3141230091594,
179.116276438596));
#37558=CARTESIAN_POINT('Ctrl Pts',(-57.3698118609917,-80.303381713528,178.35317198867));
#37559=CARTESIAN_POINT('Ctrl Pts',(-58.3549520352077,-80.2926404178967,
177.590067538743));
#37560=CARTESIAN_POINT('Ctrl Pts',(-58.5179061538645,-80.3695496487261,
176.356991764425));
#37561=CARTESIAN_POINT('Ctrl Pts',(-58.6808602725214,-80.4464588795555,
175.123915990107));
#37562=CARTESIAN_POINT('Ctrl Pts',(-57.9319936054274,-80.6205742979242,
174.143187956559));
#37563=CARTESIAN_POINT('Ctrl Pts',(-57.1831269383335,-80.7946897162929,
173.162459923011));
#37564=CARTESIAN_POINT('Ctrl Pts',(-55.9669370051364,-81.0186249169655,
173.008576811287));
#37565=CARTESIAN_POINT('Ctrl Pts',(-54.7507470719393,-81.2425601176382,
172.854693699562));
#37566=CARTESIAN_POINT('Ctrl Pts',(-53.7854830235573,-81.4397449425802,
173.617798149489));
#37567=CARTESIAN_POINT('Ctrl Pts',(-52.8202189751753,-81.6369297675222,
174.380902599416));
#37568=CARTESIAN_POINT('Ctrl Pts',(-52.6771409823525,-81.7464640660035,
175.613978373734));
#37569=CARTESIAN_POINT('Ctrl Pts',(-52.5340629895297,-81.8559983644848,
176.847054148052));
#37570=CARTESIAN_POINT('Ctrl Pts',(-53.3028057824577,-81.8683264754268,
177.8277821816));
#37571=CARTESIAN_POINT('Ctrl Pts',(-54.0715485753856,-81.8806545863688,
178.808510215148));
#37572=CARTESIAN_POINT('Ctrl Pts',(-55.3076146344168,-81.8431629150069,
178.962393326872));
#37573=CARTESIAN_POINT('Ctrl Pts',(-56.5436806934479,-81.805671243645,179.116276438596));
#37574=CARTESIAN_POINT('Ctrl Pts',(-57.5288208676639,-81.7949299480136,
178.35317198867));
#37575=CARTESIAN_POINT('Ctrl Pts',(-58.5139610418799,-81.7841886523823,
177.590067538743));
#37576=CARTESIAN_POINT('Ctrl Pts',(-58.6769151605368,-81.8610978832117,
176.356991764425));
#37577=CARTESIAN_POINT('Ctrl Pts',(-58.8398692791936,-81.9380071140411,
175.123915990107));
#37578=CARTESIAN_POINT('Ctrl Pts',(-58.0910026120997,-82.1121225324098,
174.143187956559));
#37579=CARTESIAN_POINT('Ctrl Pts',(-57.3421359450057,-82.2862379507785,
173.162459923011));
#37580=CARTESIAN_POINT('Ctrl Pts',(-56.1259460118086,-82.5101731514511,
173.008576811287));
#37581=CARTESIAN_POINT('Ctrl Pts',(-54.9097560786115,-82.7341083521237,
172.854693699562));
#37582=CARTESIAN_POINT('Ctrl Pts',(-53.9444920302295,-82.9312931770658,
173.617798149489));
#37583=CARTESIAN_POINT('Ctrl Pts',(-52.9792279818475,-83.1284780020078,
174.380902599416));
#37584=CARTESIAN_POINT('Ctrl Pts',(-52.8361499890247,-83.2380123004891,
175.613978373734));
#37585=CARTESIAN_POINT('Ctrl Pts',(-52.6930719962019,-83.3475465989704,
176.847054148052));
#37586=CARTESIAN_POINT('Ctrl Pts',(-53.4618147891299,-83.3598747099124,
177.8277821816));
#37587=CARTESIAN_POINT('Ctrl Pts',(-54.2305575820579,-83.3722028208544,
178.808510215148));
#37588=CARTESIAN_POINT('Ctrl Pts',(-55.466623641089,-83.3347111494925,178.962393326872));
#37589=CARTESIAN_POINT('Ctrl Pts',(-56.7026897001201,-83.2972194781306,
179.116276438596));
#37590=CARTESIAN_POINT('Ctrl Pts',(-57.6878298743361,-83.2864781824993,
178.35317198867));
#37591=CARTESIAN_POINT('Ctrl Pts',(-58.6729700485522,-83.2757368868679,
177.590067538743));
#37592=CARTESIAN_POINT('Ctrl Pts',(-58.835924167209,-83.3526461176973,176.356991764425));
#37593=CARTESIAN_POINT('Ctrl Pts',(-58.9988782858658,-83.4295553485267,
175.123915990107));
#37594=CARTESIAN_POINT('Ctrl Pts',(-58.2500116187719,-83.6036707668954,
174.143187956559));
#37595=CARTESIAN_POINT('Ctrl Pts',(-57.501144951678,-83.7777861852641,173.162459923011));
#37596=CARTESIAN_POINT('Ctrl Pts',(-56.2849550184808,-84.0017213859367,
173.008576811287));
#37597=CARTESIAN_POINT('Ctrl Pts',(-55.0687650852837,-84.2256565866093,
172.854693699562));
#37598=CARTESIAN_POINT('Ctrl Pts',(-54.1035010369017,-84.4228414115514,
173.617798149489));
#37599=CARTESIAN_POINT('Ctrl Pts',(-53.1382369885197,-84.6200262364934,
174.380902599416));
#37600=CARTESIAN_POINT('Ctrl Pts',(-52.9951589956969,-84.7295605349747,
175.613978373734));
#37601=CARTESIAN_POINT('Ctrl Pts',(-52.8520810028742,-84.839094833456,176.847054148052));
#37602=CARTESIAN_POINT('Ctrl Pts',(-53.6208237958021,-84.851422944398,177.8277821816));
#37603=CARTESIAN_POINT('Ctrl Pts',(-54.3895665887301,-84.86375105534,178.808510215148));
#37604=CARTESIAN_POINT('Ctrl Pts',(-55.6256326477612,-84.8262593839781,
178.962393326872));
#37605=CARTESIAN_POINT('Ctrl Pts',(-56.8616987067924,-84.7887677126162,
179.116276438596));
#37606=CARTESIAN_POINT('Ctrl Pts',(-57.8468388810084,-84.7780264169849,
178.35317198867));
#37607=CARTESIAN_POINT('Ctrl Pts',(-58.8319790552244,-84.7672851213535,
177.590067538743));
#37608=CARTESIAN_POINT('Ctrl Pts',(-58.9949331738812,-84.8441943521829,
176.356991764425));
#37609=CARTESIAN_POINT('Ctrl Pts',(-59.157887292538,-84.9211035830123,175.123915990107));
#37610=CARTESIAN_POINT('Ctrl Pts',(-58.4090206254441,-85.095219001381,174.143187956559));
#37611=CARTESIAN_POINT('Ctrl Pts',(-57.6601539583502,-85.2693344197497,
173.162459923011));
#37612=CARTESIAN_POINT('Ctrl Pts',(-56.4439640251531,-85.4932696204223,
173.008576811287));
#37613=CARTESIAN_POINT('Ctrl Pts',(-55.227774091956,-85.717204821095,172.854693699562));
#37614=CARTESIAN_POINT('Ctrl Pts',(-54.262510043574,-85.914389646037,173.617798149489));
#37615=CARTESIAN_POINT('Ctrl Pts',(-53.297245995192,-86.111574470979,174.380902599416));
#37616=CARTESIAN_POINT('Ctrl Pts',(-53.1541680023692,-86.2211087694603,
175.613978373734));
#37617=CARTESIAN_POINT('Ctrl Pts',(-53.0110900095464,-86.3306430679416,
176.847054148052));
#37618=CARTESIAN_POINT('Ctrl Pts',(-53.7798328024743,-86.3429711788836,
177.8277821816));
#37619=CARTESIAN_POINT('Ctrl Pts',(-54.5485755954023,-86.3552992898256,
178.808510215148));
#37620=CARTESIAN_POINT('Ctrl Pts',(-55.7846416544334,-86.3178076184637,
178.962393326872));
#37621=CARTESIAN_POINT('Ctrl Pts',(-57.0207077134646,-86.2803159471018,
179.116276438596));
#37622=CARTESIAN_POINT('Ctrl Pts',(-58.0058478876806,-86.2695746514704,
178.35317198867));
#37623=CARTESIAN_POINT('Ctrl Pts',(-58.9909880618966,-86.2588333558391,
177.590067538743));
#37624=CARTESIAN_POINT('Ctrl Pts',(-59.1539421805534,-86.3357425866685,
176.356991764425));
#37625=CARTESIAN_POINT('Ctrl Pts',(-59.3168962992103,-86.4126518174979,
175.123915990107));
#37626=CARTESIAN_POINT('Ctrl Pts',(-58.5680296321163,-86.5867672358666,
174.143187956559));
#37627=CARTESIAN_POINT('Ctrl Pts',(-57.8191629650224,-86.7608826542353,
173.162459923011));
#37628=CARTESIAN_POINT('Ctrl Pts',(-56.6029730318253,-86.9848178549079,
173.008576811287));
#37629=CARTESIAN_POINT('Ctrl Pts',(-55.3867830986282,-87.2087530555805,
172.854693699562));
#37630=CARTESIAN_POINT('Ctrl Pts',(-54.4215190502462,-87.4059378805226,
173.617798149489));
#37631=CARTESIAN_POINT('Ctrl Pts',(-53.4562550018642,-87.6031227054646,
174.380902599416));
#37632=CARTESIAN_POINT('Ctrl Pts',(-53.3131770090414,-87.7126570039459,
175.613978373734));
#37633=CARTESIAN_POINT('Ctrl Pts',(-53.1700990162186,-87.8221913024272,
176.847054148052));
#37634=CARTESIAN_POINT('Ctrl Pts',(-53.9388418091466,-87.8345194133692,
177.8277821816));
#37635=CARTESIAN_POINT('Ctrl Pts',(-54.7075846020745,-87.8468475243112,
178.808510215148));
#37636=CARTESIAN_POINT('Ctrl Pts',(-55.9436506611057,-87.8093558529493,
178.962393326872));
#37637=CARTESIAN_POINT('Ctrl Pts',(-57.1797167201368,-87.7718641815874,
179.116276438596));
#37638=CARTESIAN_POINT('Ctrl Pts',(-58.1648568943528,-87.761122885956,178.35317198867));
#37639=CARTESIAN_POINT('Ctrl Pts',(-59.1499970685689,-87.7503815903247,
177.590067538743));
#37640=CARTESIAN_POINT('Ctrl Pts',(-59.3129511872257,-87.8272908211541,
176.356991764425));
#37641=CARTESIAN_POINT('Ctrl Pts',(-59.4759053058825,-87.9042000519835,
175.123915990107));
#37642=CARTESIAN_POINT('Ctrl Pts',(-58.7270386387886,-88.0783154703522,
174.143187956559));
#37643=CARTESIAN_POINT('Ctrl Pts',(-57.9781719716946,-88.2524308887209,
173.162459923011));
#37644=CARTESIAN_POINT('Ctrl Pts',(-56.7619820384975,-88.4763660893935,
173.008576811287));
#37645=CARTESIAN_POINT('Ctrl Pts',(-55.5457921053004,-88.7003012900661,
172.854693699562));
#37646=CARTESIAN_POINT('Ctrl Pts',(-54.5805280569184,-88.8974861150082,
173.617798149489));
#37647=CARTESIAN_POINT('Ctrl Pts',(-53.6152640085364,-89.0946709399502,
174.380902599416));
#37648=CARTESIAN_POINT('Ctrl Pts',(-53.4721860157136,-89.2042052384315,
175.613978373734));
#37649=CARTESIAN_POINT('Ctrl Pts',(-53.3291080228908,-89.3137395369128,
176.847054148052));
#37650=CARTESIAN_POINT('Ctrl Pts',(-54.0978508158188,-89.3260676478548,
177.8277821816));
#37651=CARTESIAN_POINT('Ctrl Pts',(-54.8665936087468,-89.3383957587968,
178.808510215148));
#37652=CARTESIAN_POINT('Ctrl Pts',(-56.1026596677779,-89.3009040874349,
178.962393326872));
#37653=CARTESIAN_POINT('Ctrl Pts',(-57.3387257268091,-89.263412416073,179.116276438596));
#37654=CARTESIAN_POINT('Ctrl Pts',(-58.3238659010251,-89.2526711204416,
178.35317198867));
#37655=CARTESIAN_POINT('Ctrl Pts',(-59.3090060752411,-89.2419298248103,
177.590067538743));
#37656=CARTESIAN_POINT('Ctrl Pts',(-59.4719601938979,-89.3188390556397,
176.356991764425));
#37657=CARTESIAN_POINT('Ctrl Pts',(-59.6349143125547,-89.3957482864691,
175.123915990107));
#37658=CARTESIAN_POINT('Ctrl Pts',(-58.8860476454608,-89.5698637048378,
174.143187956559));
#37659=CARTESIAN_POINT('Ctrl Pts',(-58.1371809783669,-89.7439791232065,
173.162459923011));
#37660=CARTESIAN_POINT('Ctrl Pts',(-56.9209910451698,-89.9679143238791,
173.008576811287));
#37661=CARTESIAN_POINT('Ctrl Pts',(-55.7048011119726,-90.1918495245517,
172.854693699562));
#37662=CARTESIAN_POINT('Ctrl Pts',(-54.7395370635906,-90.3890343494938,
173.617798149489));
#37663=CARTESIAN_POINT('Ctrl Pts',(-53.7742730152086,-90.5862191744358,
174.380902599416));
#37664=CARTESIAN_POINT('Ctrl Pts',(-53.6311950223859,-90.6957534729171,
175.613978373734));
#37665=CARTESIAN_POINT('Ctrl Pts',(-53.4881170295631,-90.8052877713984,
176.847054148052));
#37666=CARTESIAN_POINT('Ctrl Pts',(-54.256859822491,-90.8176158823404,177.8277821816));
#37667=CARTESIAN_POINT('Ctrl Pts',(-55.025602615419,-90.8299439932824,178.808510215148));
#37668=CARTESIAN_POINT('Ctrl Pts',(-56.2616686744501,-90.7924523219205,
178.962393326872));
#37669=CARTESIAN_POINT('Ctrl Pts',(-57.4977347334813,-90.7549606505586,
179.116276438596));
#37670=CARTESIAN_POINT('Ctrl Pts',(-58.4828749076973,-90.7442193549272,
178.35317198867));
#37671=CARTESIAN_POINT('Ctrl Pts',(-59.4680150819133,-90.7334780592959,
177.590067538743));
#37672=CARTESIAN_POINT('Ctrl Pts',(-59.6309692005701,-90.8103872901253,
176.356991764425));
#37673=CARTESIAN_POINT('Ctrl Pts',(-59.793923319227,-90.8872965209547,175.123915990107));
#37674=CARTESIAN_POINT('Ctrl Pts',(-59.045056652133,-91.0614119393234,174.143187956559));
#37675=CARTESIAN_POINT('Ctrl Pts',(-58.2961899850391,-91.2355273576921,
173.162459923011));
#37676=CARTESIAN_POINT('Ctrl Pts',(-57.080000051842,-91.4594625583647,173.008576811287));
#37677=CARTESIAN_POINT('Ctrl Pts',(-55.8638101186449,-91.6833977590373,
172.854693699562));
#37678=CARTESIAN_POINT('Ctrl Pts',(-54.8985460702629,-91.8805825839794,
173.617798149489));
#37679=CARTESIAN_POINT('Ctrl Pts',(-53.9332820218809,-92.0777674089214,
174.380902599416));
#37680=CARTESIAN_POINT('Ctrl Pts',(-53.7902040290581,-92.1873017074027,
175.613978373734));
#37681=CARTESIAN_POINT('Ctrl Pts',(-53.6471260362353,-92.296836005884,176.847054148052));
#37682=CARTESIAN_POINT('Ctrl Pts',(-54.4158688291633,-92.309164116826,177.8277821816));
#37683=CARTESIAN_POINT('Ctrl Pts',(-55.1846116220912,-92.321492227768,178.808510215148));
#37684=CARTESIAN_POINT('Ctrl Pts',(-56.4206776811223,-92.2840005564061,
178.962393326872));
#37685=CARTESIAN_POINT('Ctrl Pts',(-57.6567437401535,-92.2465088850442,
179.116276438596));
#37686=CARTESIAN_POINT('Ctrl Pts',(-58.6418839143695,-92.2357675894128,
178.35317198867));
#37687=CARTESIAN_POINT('Ctrl Pts',(-59.6270240885855,-92.2250262937815,
177.590067538743));
#37688=CARTESIAN_POINT('Ctrl Pts',(-59.7899782072423,-92.3019355246109,
176.356991764425));
#37689=CARTESIAN_POINT('Ctrl Pts',(-59.9529323258992,-92.3788447554403,
175.123915990107));
#37690=CARTESIAN_POINT('Ctrl Pts',(-59.2040656588053,-92.552960173809,174.143187956559));
#37691=CARTESIAN_POINT('Ctrl Pts',(-58.4551989917113,-92.7270755921777,
173.162459923011));
#37692=CARTESIAN_POINT('Ctrl Pts',(-57.2390090585142,-92.9510107928503,
173.008576811287));
#37693=CARTESIAN_POINT('Ctrl Pts',(-56.0228191253171,-93.1749459935229,
172.854693699562));
#37694=CARTESIAN_POINT('Ctrl Pts',(-55.0575550769351,-93.372130818465,173.617798149489));
#37695=CARTESIAN_POINT('Ctrl Pts',(-54.0922910285531,-93.569315643407,174.380902599416));
#37696=CARTESIAN_POINT('Ctrl Pts',(-53.9492130357303,-93.6788499418883,
175.613978373734));
#37697=CARTESIAN_POINT('Ctrl Pts',(-53.8061350429075,-93.7883842403696,
176.847054148052));
#37698=CARTESIAN_POINT('Ctrl Pts',(-54.5748778358355,-93.8007123513116,
177.8277821816));
#37699=CARTESIAN_POINT('Ctrl Pts',(-55.3436206287634,-93.8130404622536,
178.808510215148));
#37700=CARTESIAN_POINT('Ctrl Pts',(-56.5796866877946,-93.7755487908917,
178.962393326872));
#37701=CARTESIAN_POINT('Ctrl Pts',(-57.8157527468257,-93.7380571195298,
179.116276438596));
#37702=CARTESIAN_POINT('Ctrl Pts',(-58.8008929210417,-93.7273158238985,
178.35317198867));
#37703=CARTESIAN_POINT('Ctrl Pts',(-59.7860330952578,-93.7165745282671,
177.590067538743));
#37704=CARTESIAN_POINT('Ctrl Pts',(-59.9489872139146,-93.7934837590965,
176.356991764425));
#37705=CARTESIAN_POINT('Ctrl Pts',(-60.1119413325714,-93.8703929899259,
175.123915990107));
#37706=CARTESIAN_POINT('Ctrl Pts',(-59.3630746654775,-94.0445084082946,
174.143187956559));
#37707=CARTESIAN_POINT('Ctrl Pts',(-58.6142079983836,-94.2186238266633,
173.162459923011));
#37708=CARTESIAN_POINT('Ctrl Pts',(-57.3980180651864,-94.4425590273359,
173.008576811287));
#37709=CARTESIAN_POINT('Ctrl Pts',(-56.1818281319893,-94.6664942280085,
172.854693699562));
#37710=CARTESIAN_POINT('Ctrl Pts',(-55.2165640836073,-94.8636790529506,
173.617798149489));
#37711=CARTESIAN_POINT('Ctrl Pts',(-54.2513000352253,-95.0608638778926,
174.380902599416));
#37712=CARTESIAN_POINT('Ctrl Pts',(-54.1082220424025,-95.1703981763739,
175.613978373734));
#37713=CARTESIAN_POINT('Ctrl Pts',(-53.9651440495798,-95.2799324748552,
176.847054148052));
#37714=CARTESIAN_POINT('Ctrl Pts',(-54.7338868425077,-95.2922605857972,
177.8277821816));
#37715=CARTESIAN_POINT('Ctrl Pts',(-55.5026296354357,-95.3045886967392,
178.808510215148));
#37716=CARTESIAN_POINT('Ctrl Pts',(-56.7386956944668,-95.2670970253773,
178.962393326872));
#37717=CARTESIAN_POINT('Ctrl Pts',(-57.974761753498,-95.2296053540154,179.116276438596));
#37718=CARTESIAN_POINT('Ctrl Pts',(-58.959901927714,-95.218864058384,178.35317198867));
#37719=CARTESIAN_POINT('Ctrl Pts',(-59.94504210193,-95.2081227627527,177.590067538743));
#37720=CARTESIAN_POINT('Ctrl Pts',(-60.1079962205868,-95.2850319935821,
176.356991764425));
#37721=CARTESIAN_POINT('Ctrl Pts',(-60.2709503392436,-95.3619412244115,
175.123915990107));
#37722=CARTESIAN_POINT('Ctrl Pts',(-59.5220836721497,-95.5360566427802,
174.143187956559));
#37723=CARTESIAN_POINT('Ctrl Pts',(-58.7732170050558,-95.7101720611489,
173.162459923011));
#37724=CARTESIAN_POINT('Ctrl Pts',(-57.5570270718587,-95.9341072618215,
173.008576811287));
#37725=CARTESIAN_POINT('Ctrl Pts',(-56.3408371386615,-96.1580424624942,
172.854693699562));
#37726=CARTESIAN_POINT('Ctrl Pts',(-55.3755730902795,-96.3552272874362,
173.617798149489));
#37727=CARTESIAN_POINT('Ctrl Pts',(-54.4103090418976,-96.5524121123782,
174.380902599416));
#37728=CARTESIAN_POINT('Ctrl Pts',(-54.2672310490748,-96.6619464108595,
175.613978373734));
#37729=CARTESIAN_POINT('Ctrl Pts',(-54.124153056252,-96.7714807093408,176.847054148052));
#37730=CARTESIAN_POINT('Ctrl Pts',(-54.8928958491799,-96.7838088202828,
177.8277821816));
#37731=CARTESIAN_POINT('Ctrl Pts',(-55.6616386421079,-96.7961369312248,
178.808510215148));
#37732=CARTESIAN_POINT('Ctrl Pts',(-56.897704701139,-96.7586452598629,178.962393326872));
#37733=CARTESIAN_POINT('Ctrl Pts',(-58.1337707601702,-96.721153588501,179.116276438596));
#37734=CARTESIAN_POINT('Ctrl Pts',(-59.1189109343862,-96.7104122928696,
178.35317198867));
#37735=CARTESIAN_POINT('Ctrl Pts',(-60.1040511086022,-96.6996709972383,
177.590067538743));
#37736=CARTESIAN_POINT('Ctrl Pts',(-60.267005227259,-96.7765802280677,176.356991764425));
#37737=CARTESIAN_POINT('Ctrl Pts',(-60.4299593459159,-96.8534894588971,
175.123915990107));
#37738=CARTESIAN_POINT('Ctrl Pts',(-59.6810926788219,-97.0276048772658,
174.143187956559));
#37739=CARTESIAN_POINT('Ctrl Pts',(-58.932226011728,-97.2017202956345,173.162459923011));
#37740=CARTESIAN_POINT('Ctrl Pts',(-57.7160360785309,-97.4256554963071,
173.008576811287));
#37741=CARTESIAN_POINT('Ctrl Pts',(-56.4998461453338,-97.6495906969797,
172.854693699562));
#37742=CARTESIAN_POINT('Ctrl Pts',(-55.5345820969518,-97.8467755219218,
173.617798149489));
#37743=CARTESIAN_POINT('Ctrl Pts',(-54.5693180485698,-98.0439603468638,
174.380902599416));
#37744=CARTESIAN_POINT('Ctrl Pts',(-54.426240055747,-98.1534946453451,175.613978373734));
#37745=CARTESIAN_POINT('Ctrl Pts',(-54.2831620629242,-98.2630289438264,
176.847054148052));
#37746=CARTESIAN_POINT('Ctrl Pts',(-55.0519048558522,-98.2753570547684,
177.8277821816));
#37747=CARTESIAN_POINT('Ctrl Pts',(-55.8206476487801,-98.2876851657105,
178.808510215148));
#37748=CARTESIAN_POINT('Ctrl Pts',(-57.0567137078113,-98.2501934943485,
178.962393326872));
#37749=CARTESIAN_POINT('Ctrl Pts',(-58.2927797668424,-98.2127018229866,
179.116276438596));
#37750=CARTESIAN_POINT('Ctrl Pts',(-59.2779199410584,-98.2019605273553,
178.35317198867));
#37751=CARTESIAN_POINT('Ctrl Pts',(-60.2630601152744,-98.1912192317239,
177.590067538743));
#37752=CARTESIAN_POINT('Ctrl Pts',(-60.4260142339313,-98.2681284625533,
176.356991764425));
#37753=CARTESIAN_POINT('Ctrl Pts',(-60.5889683525881,-98.3450376933827,
175.123915990107));
#37754=CARTESIAN_POINT('Ctrl Pts',(-59.8401016854942,-98.5191531117514,
174.143187956559));
#37755=CARTESIAN_POINT('Ctrl Pts',(-59.0912350184002,-98.6932685301201,
173.162459923011));
#37756=CARTESIAN_POINT('Ctrl Pts',(-57.8750450852031,-98.9172037307927,
173.008576811287));
#37757=CARTESIAN_POINT('Ctrl Pts',(-56.658855152006,-99.1411389314653,172.854693699562));
#37758=CARTESIAN_POINT('Ctrl Pts',(-55.693591103624,-99.3383237564074,173.617798149489));
#37759=CARTESIAN_POINT('Ctrl Pts',(-54.728327055242,-99.5355085813494,174.380902599416));
#37760=CARTESIAN_POINT('Ctrl Pts',(-54.5852490624192,-99.6450428798307,
175.613978373734));
#37761=CARTESIAN_POINT('Ctrl Pts',(-54.4421710695964,-99.754577178312,176.847054148052));
#37762=CARTESIAN_POINT('Ctrl Pts',(-55.2109138625244,-99.766905289254,177.8277821816));
#37763=CARTESIAN_POINT('Ctrl Pts',(-55.9796566554524,-99.779233400196,178.808510215148));
#37764=CARTESIAN_POINT('Ctrl Pts',(-57.2157227144835,-99.7417417288341,
178.962393326872));
#37765=CARTESIAN_POINT('Ctrl Pts',(-58.4517887735146,-99.7042500574722,
179.116276438596));
#37766=CARTESIAN_POINT('Ctrl Pts',(-59.4369289477306,-99.6935087618409,
178.35317198867));
#37767=CARTESIAN_POINT('Ctrl Pts',(-60.4220691219467,-99.6827674662096,
177.590067538743));
#37768=CARTESIAN_POINT('Ctrl Pts',(-60.5850232406035,-99.7596766970389,
176.356991764425));
#37769=CARTESIAN_POINT('Ctrl Pts',(-60.7479773592603,-99.8365859278683,
175.123915990107));
#37770=CARTESIAN_POINT('Ctrl Pts',(-59.9991106921664,-100.010701346237,
174.143187956559));
#37771=CARTESIAN_POINT('Ctrl Pts',(-59.2502440250725,-100.184816764606,
173.162459923011));
#37772=CARTESIAN_POINT('Ctrl Pts',(-58.0340540918753,-100.408751965278,
173.008576811287));
#37773=CARTESIAN_POINT('Ctrl Pts',(-56.8178641586782,-100.632687165951,
172.854693699562));
#37774=CARTESIAN_POINT('Ctrl Pts',(-55.8526001102962,-100.829871990893,
173.617798149489));
#37775=CARTESIAN_POINT('Ctrl Pts',(-54.8873360619142,-101.027056815835,
174.380902599416));
#37776=CARTESIAN_POINT('Ctrl Pts',(-54.7442580690915,-101.136591114316,
175.613978373734));
#37777=CARTESIAN_POINT('Ctrl Pts',(-54.6011800762687,-101.246125412798,
176.847054148052));
#37778=CARTESIAN_POINT('Ctrl Pts',(-55.3699228691966,-101.25845352374,177.8277821816));
#37779=CARTESIAN_POINT('Ctrl Pts',(-56.1386656621246,-101.270781634682,
178.808510215148));
#37780=CARTESIAN_POINT('Ctrl Pts',(-57.3747317211557,-101.23328996332,178.962393326872));
#37781=CARTESIAN_POINT('Ctrl Pts',(-58.6107977801869,-101.195798291958,
179.116276438596));
#37782=CARTESIAN_POINT('Ctrl Pts',(-59.5959379544029,-101.185056996326,
178.35317198867));
#37783=CARTESIAN_POINT('Ctrl Pts',(-60.5810781286189,-101.174315700695,
177.590067538743));
#37784=CARTESIAN_POINT('Ctrl Pts',(-60.7440322472757,-101.251224931525,
176.356991764425));
#37785=CARTESIAN_POINT('Ctrl Pts',(-60.9069863659325,-101.328134162354,
175.123915990107));
#37786=CARTESIAN_POINT('Ctrl Pts',(-60.1581196988386,-101.502249580723,
174.143187956559));
#37787=CARTESIAN_POINT('Ctrl Pts',(-59.4092530317447,-101.676364999091,
173.162459923011));
#37788=CARTESIAN_POINT('Ctrl Pts',(-58.1930630985476,-101.900300199764,
173.008576811287));
#37789=CARTESIAN_POINT('Ctrl Pts',(-56.9768731653505,-102.124235400437,
172.854693699562));
#37790=CARTESIAN_POINT('Ctrl Pts',(-56.0116091169685,-102.321420225379,
173.617798149489));
#37791=CARTESIAN_POINT('Ctrl Pts',(-55.0463450685865,-102.518605050321,
174.380902599416));
#37792=CARTESIAN_POINT('Ctrl Pts',(-54.9032670757637,-102.628139348802,
175.613978373734));
#37793=CARTESIAN_POINT('Ctrl Pts',(-54.7601890829409,-102.737673647283,
176.847054148052));
#37794=CARTESIAN_POINT('Ctrl Pts',(-55.5289318758688,-102.750001758225,
177.8277821816));
#37795=CARTESIAN_POINT('Ctrl Pts',(-56.2976746687968,-102.762329869167,
178.808510215148));
#37796=CARTESIAN_POINT('Ctrl Pts',(-57.5337407278279,-102.724838197805,
178.962393326872));
#37797=CARTESIAN_POINT('Ctrl Pts',(-58.7698067868591,-102.687346526443,
179.116276438596));
#37798=CARTESIAN_POINT('Ctrl Pts',(-59.7549469610751,-102.676605230812,
178.35317198867));
#37799=CARTESIAN_POINT('Ctrl Pts',(-60.7400871352911,-102.665863935181,
177.590067538743));
#37800=CARTESIAN_POINT('Ctrl Pts',(-60.9030412539479,-102.74277316601,176.356991764425));
#37801=CARTESIAN_POINT('Ctrl Pts',(-61.0659953726048,-102.81968239684,175.123915990107));
#37802=CARTESIAN_POINT('Ctrl Pts',(-60.3171287055108,-102.993797815208,
174.143187956559));
#37803=CARTESIAN_POINT('Ctrl Pts',(-59.5682620384169,-103.167913233577,
173.162459923011));
#37804=CARTESIAN_POINT('Ctrl Pts',(-58.3520721052198,-103.39184843425,173.008576811287));
#37805=CARTESIAN_POINT('Ctrl Pts',(-57.1358821720227,-103.615783634922,
172.854693699562));
#37806=CARTESIAN_POINT('Ctrl Pts',(-56.1706181236407,-103.812968459864,
173.617798149489));
#37807=CARTESIAN_POINT('Ctrl Pts',(-55.2053540752587,-104.010153284806,
174.380902599416));
#37808=CARTESIAN_POINT('Ctrl Pts',(-55.0622760824359,-104.119687583288,
175.613978373734));
#37809=CARTESIAN_POINT('Ctrl Pts',(-54.9191980896131,-104.229221881769,
176.847054148052));
#37810=CARTESIAN_POINT('Ctrl Pts',(-55.6879408825411,-104.241549992711,
177.8277821816));
#37811=CARTESIAN_POINT('Ctrl Pts',(-56.456683675469,-104.253878103653,178.808510215148));
#37812=CARTESIAN_POINT('Ctrl Pts',(-57.6927497345002,-104.216386432291,
178.962393326872));
#37813=CARTESIAN_POINT('Ctrl Pts',(-58.9288157935313,-104.178894760929,
179.116276438596));
#37814=CARTESIAN_POINT('Ctrl Pts',(-59.9139559677473,-104.168153465298,
178.35317198867));
#37815=CARTESIAN_POINT('Ctrl Pts',(-60.8990961419634,-104.157412169666,
177.590067538743));
#37816=CARTESIAN_POINT('Ctrl Pts',(-61.0620502606202,-104.234321400496,
176.356991764425));
#37817=CARTESIAN_POINT('Ctrl Pts',(-61.225004379277,-104.311230631325,175.123915990107));
#37818=CARTESIAN_POINT('Ctrl Pts',(-60.4761377121831,-104.485346049694,
174.143187956559));
#37819=CARTESIAN_POINT('Ctrl Pts',(-59.7272710450891,-104.659461468063,
173.162459923011));
#37820=CARTESIAN_POINT('Ctrl Pts',(-58.511081111892,-104.883396668735,173.008576811287));
#37821=CARTESIAN_POINT('Ctrl Pts',(-57.2948911786949,-105.107331869408,
172.854693699562));
#37822=CARTESIAN_POINT('Ctrl Pts',(-56.3296271303129,-105.30451669435,173.617798149489));
#37823=CARTESIAN_POINT('Ctrl Pts',(-55.3643630819309,-105.501701519292,
174.380902599416));
#37824=CARTESIAN_POINT('Ctrl Pts',(-55.2212850891081,-105.611235817773,
175.613978373734));
#37825=CARTESIAN_POINT('Ctrl Pts',(-55.0782070962854,-105.720770116254,
176.847054148052));
#37826=CARTESIAN_POINT('Ctrl Pts',(-55.8469498892133,-105.733098227196,
177.8277821816));
#37827=CARTESIAN_POINT('Ctrl Pts',(-56.6156926821413,-105.745426338138,
178.808510215148));
#37828=CARTESIAN_POINT('Ctrl Pts',(-57.8517587411724,-105.707934666776,
178.962393326872));
#37829=CARTESIAN_POINT('Ctrl Pts',(-59.0878248002036,-105.670442995415,
179.116276438596));
#37830=CARTESIAN_POINT('Ctrl Pts',(-60.0729649744196,-105.659701699783,
178.35317198867));
#37831=CARTESIAN_POINT('Ctrl Pts',(-61.0581051486356,-105.648960404152,
177.590067538743));
#37832=CARTESIAN_POINT('Ctrl Pts',(-61.2210592672924,-105.725869634981,
176.356991764425));
#37833=CARTESIAN_POINT('Ctrl Pts',(-61.3840133859492,-105.802778865811,
175.123915990107));
#37834=CARTESIAN_POINT('Ctrl Pts',(-60.6351467188553,-105.976894284179,
174.143187956559));
#37835=CARTESIAN_POINT('Ctrl Pts',(-59.8862800517614,-106.151009702548,
173.162459923011));
#37836=CARTESIAN_POINT('Ctrl Pts',(-58.6700901185642,-106.374944903221,
173.008576811287));
#37837=CARTESIAN_POINT('Ctrl Pts',(-57.4539001853671,-106.598880103893,
172.854693699562));
#37838=CARTESIAN_POINT('Ctrl Pts',(-56.4886361369851,-106.796064928835,
173.617798149489));
#37839=CARTESIAN_POINT('Ctrl Pts',(-55.5233720886032,-106.993249753777,
174.380902599416));
#37840=CARTESIAN_POINT('Ctrl Pts',(-55.3802940957804,-107.102784052259,
175.613978373734));
#37841=CARTESIAN_POINT('Ctrl Pts',(-55.2372161029576,-107.21231835074,176.847054148052));
#37842=CARTESIAN_POINT('Ctrl Pts',(-56.0059588958855,-107.224646461682,
177.8277821816));
#37843=CARTESIAN_POINT('Ctrl Pts',(-56.7747016888135,-107.236974572624,
178.808510215148));
#37844=CARTESIAN_POINT('Ctrl Pts',(-58.0107677478446,-107.199482901262,
178.962393326872));
#37845=CARTESIAN_POINT('Ctrl Pts',(-59.2468338068758,-107.1619912299,179.116276438596));
#37846=CARTESIAN_POINT('Ctrl Pts',(-60.2319739810918,-107.151249934269,
178.35317198867));
#37847=CARTESIAN_POINT('Ctrl Pts',(-61.2171141553078,-107.140508638638,
177.590067538743));
#37848=CARTESIAN_POINT('Ctrl Pts',(-61.3800682739646,-107.217417869467,
176.356991764425));
#37849=CARTESIAN_POINT('Ctrl Pts',(-61.5430223926215,-107.294327100296,
175.123915990107));
#37850=CARTESIAN_POINT('Ctrl Pts',(-60.7941557255275,-107.468442518665,
174.143187956559));
#37851=CARTESIAN_POINT('Ctrl Pts',(-60.0452890584336,-107.642557937034,
173.162459923011));
#37852=CARTESIAN_POINT('Ctrl Pts',(-58.8290991252365,-107.866493137706,
173.008576811287));
#37853=CARTESIAN_POINT('Ctrl Pts',(-57.6129091920394,-108.090428338379,
172.854693699562));
#37854=CARTESIAN_POINT('Ctrl Pts',(-56.6476451436574,-108.287613163321,
173.617798149489));
#37855=CARTESIAN_POINT('Ctrl Pts',(-55.6823810952754,-108.484797988263,
174.380902599416));
#37856=CARTESIAN_POINT('Ctrl Pts',(-55.5393031024526,-108.594332286744,
175.613978373734));
#37857=CARTESIAN_POINT('Ctrl Pts',(-55.3962251096298,-108.703866585226,
176.847054148052));
#37858=CARTESIAN_POINT('Ctrl Pts',(-56.1649679025577,-108.716194696168,
177.8277821816));
#37859=CARTESIAN_POINT('Ctrl Pts',(-56.9337106954857,-108.72852280711,178.808510215148));
#37860=CARTESIAN_POINT('Ctrl Pts',(-58.1697767545169,-108.691031135748,
178.962393326872));
#37861=CARTESIAN_POINT('Ctrl Pts',(-59.405842813548,-108.653539464386,179.116276438596));
#37862=CARTESIAN_POINT('Ctrl Pts',(-60.390982987764,-108.642798168754,178.35317198867));
#37863=CARTESIAN_POINT('Ctrl Pts',(-61.37612316198,-108.632056873123,177.590067538743));
#37864=CARTESIAN_POINT('Ctrl Pts',(-61.5390772806369,-108.708966103953,
176.356991764425));
#37865=CARTESIAN_POINT('Ctrl Pts',(-61.7020313992937,-108.785875334782,
175.123915990107));
#37866=CARTESIAN_POINT('Ctrl Pts',(-60.9531647321997,-108.959990753151,
174.143187956559));
#37867=CARTESIAN_POINT('Ctrl Pts',(-60.2042980651058,-109.134106171519,
173.162459923011));
#37868=CARTESIAN_POINT('Ctrl Pts',(-58.9881081319087,-109.358041372192,
173.008576811287));
#37869=CARTESIAN_POINT('Ctrl Pts',(-57.7719181987116,-109.581976572865,
172.854693699562));
#37870=CARTESIAN_POINT('Ctrl Pts',(-56.8066541503296,-109.779161397807,
173.617798149489));
#37871=CARTESIAN_POINT('Ctrl Pts',(-55.8413901019476,-109.976346222749,
174.380902599416));
#37872=CARTESIAN_POINT('Ctrl Pts',(-55.6983121091248,-110.08588052123,175.613978373734));
#37873=CARTESIAN_POINT('Ctrl Pts',(-55.555234116302,-110.195414819711,176.847054148052));
#37874=CARTESIAN_POINT('Ctrl Pts',(-56.32397690923,-110.207742930653,177.8277821816));
#37875=CARTESIAN_POINT('Ctrl Pts',(-57.092719702158,-110.220071041595,178.808510215148));
#37876=CARTESIAN_POINT('Ctrl Pts',(-58.3287857611891,-110.182579370233,
178.962393326872));
#37877=CARTESIAN_POINT('Ctrl Pts',(-59.5648518202202,-110.145087698871,
179.116276438596));
#37878=CARTESIAN_POINT('Ctrl Pts',(-60.5499919944362,-110.13434640324,178.35317198867));
#37879=CARTESIAN_POINT('Ctrl Pts',(-61.5351321686523,-110.123605107609,
177.590067538743));
#37880=CARTESIAN_POINT('Ctrl Pts',(-61.6980862873091,-110.200514338438,
176.356991764425));
#37881=CARTESIAN_POINT('Ctrl Pts',(-61.8610404059659,-110.277423569268,
175.123915990107));
#37882=CARTESIAN_POINT('Ctrl Pts',(-61.112173738872,-110.451538987636,174.143187956559));
#37883=CARTESIAN_POINT('Ctrl Pts',(-60.363307071778,-110.625654406005,173.162459923011));
#37884=CARTESIAN_POINT('Ctrl Pts',(-59.1471171385809,-110.849589606678,
173.008576811287));
#37885=CARTESIAN_POINT('Ctrl Pts',(-57.9309272053838,-111.07352480735,172.854693699562));
#37886=CARTESIAN_POINT('Ctrl Pts',(-56.9656631570018,-111.270709632292,
173.617798149489));
#37887=CARTESIAN_POINT('Ctrl Pts',(-56.0003991086198,-111.467894457234,
174.380902599416));
#37888=CARTESIAN_POINT('Ctrl Pts',(-55.857321115797,-111.577428755716,175.613978373734));
#37889=CARTESIAN_POINT('Ctrl Pts',(-55.7142431229743,-111.686963054197,
176.847054148052));
#37890=CARTESIAN_POINT('Ctrl Pts',(-56.4829859159022,-111.699291165139,
177.8277821816));
#37891=CARTESIAN_POINT('Ctrl Pts',(-57.2517287088302,-111.711619276081,
178.808510215148));
#37892=CARTESIAN_POINT('Ctrl Pts',(-58.4877947678613,-111.674127604719,
178.962393326872));
#37893=CARTESIAN_POINT('Ctrl Pts',(-59.7238608268925,-111.636635933357,
179.116276438596));
#37894=CARTESIAN_POINT('Ctrl Pts',(-60.7090010011085,-111.625894637726,
178.35317198867));
#37895=CARTESIAN_POINT('Ctrl Pts',(-61.6941411753245,-111.615153342094,
177.590067538743));
#37896=CARTESIAN_POINT('Ctrl Pts',(-61.8570952939813,-111.692062572924,
176.356991764425));
#37897=CARTESIAN_POINT('Ctrl Pts',(-62.0200494126381,-111.768971803753,
175.123915990107));
#37898=CARTESIAN_POINT('Ctrl Pts',(-61.2711827455442,-111.943087222122,
174.143187956559));
#37899=CARTESIAN_POINT('Ctrl Pts',(-60.5223160784503,-112.117202640491,
173.162459923011));
#37900=CARTESIAN_POINT('Ctrl Pts',(-59.3061261452532,-112.341137841163,
173.008576811287));
#37901=CARTESIAN_POINT('Ctrl Pts',(-58.0899362120561,-112.565073041836,
172.854693699562));
#37902=CARTESIAN_POINT('Ctrl Pts',(-57.124672163674,-112.762257866778,173.617798149489));
#37903=CARTESIAN_POINT('Ctrl Pts',(-56.1594081152921,-112.95944269172,174.380902599416));
#37904=CARTESIAN_POINT('Ctrl Pts',(-56.0163301224693,-113.068976990201,
175.613978373734));
#37905=CARTESIAN_POINT('Ctrl Pts',(-55.8732521296465,-113.178511288682,
176.847054148052));
#37906=CARTESIAN_POINT('Ctrl Pts',(-56.6419949225744,-113.190839399624,
177.8277821816));
#37907=CARTESIAN_POINT('Ctrl Pts',(-57.4107377155024,-113.203167510566,
178.808510215148));
#37908=CARTESIAN_POINT('Ctrl Pts',(-58.6468037745335,-113.165675839205,
178.962393326872));
#37909=CARTESIAN_POINT('Ctrl Pts',(-59.8828698335647,-113.128184167843,
179.116276438596));
#37910=CARTESIAN_POINT('Ctrl Pts',(-60.8680100077807,-113.117442872211,
178.35317198867));
#37911=CARTESIAN_POINT('Ctrl Pts',(-61.8531501819967,-113.10670157658,177.590067538743));
#37912=CARTESIAN_POINT('Ctrl Pts',(-62.0161043006535,-113.183610807409,
176.356991764425));
#37913=CARTESIAN_POINT('Ctrl Pts',(-62.1790584193104,-113.260520038239,
175.123915990107));
#37914=CARTESIAN_POINT('Ctrl Pts',(-61.4301917522164,-113.434635456607,
174.143187956559));
#37915=CARTESIAN_POINT('Ctrl Pts',(-60.6813250851225,-113.608750874976,
173.162459923011));
#37916=CARTESIAN_POINT('Ctrl Pts',(-59.4651351519254,-113.832686075649,
173.008576811287));
#37917=CARTESIAN_POINT('Ctrl Pts',(-58.2489452187283,-114.056621276321,
172.854693699562));
#37918=CARTESIAN_POINT('Ctrl Pts',(-57.2836811703463,-114.253806101263,
173.617798149489));
#37919=CARTESIAN_POINT('Ctrl Pts',(-56.3184171219643,-114.450990926205,
174.380902599416));
#37920=CARTESIAN_POINT('Ctrl Pts',(-56.1753391291415,-114.560525224687,
175.613978373734));
#37921=CARTESIAN_POINT('Ctrl Pts',(-56.0322611363187,-114.670059523168,
176.847054148052));
#37922=CARTESIAN_POINT('Ctrl Pts',(-56.8010039292467,-114.68238763411,177.8277821816));
#37923=CARTESIAN_POINT('Ctrl Pts',(-57.5697467221746,-114.694715745052,
178.808510215148));
#37924=CARTESIAN_POINT('Ctrl Pts',(-58.8058127812058,-114.65722407369,178.962393326872));
#37925=CARTESIAN_POINT('Ctrl Pts',(-60.0418788402369,-114.619732402328,
179.116276438596));
#37926=CARTESIAN_POINT('Ctrl Pts',(-61.0270190144529,-114.608991106697,
178.35317198867));
#37927=CARTESIAN_POINT('Ctrl Pts',(-62.0121591886689,-114.598249811066,
177.590067538743));
#37928=CARTESIAN_POINT('Ctrl Pts',(-62.1751133073258,-114.675159041895,
176.356991764425));
#37929=CARTESIAN_POINT('Ctrl Pts',(-62.3380674259826,-114.752068272724,
175.123915990107));
#37930=CARTESIAN_POINT('Ctrl Pts',(-61.5892007588887,-114.926183691093,
174.143187956559));
#37931=CARTESIAN_POINT('Ctrl Pts',(-60.8403340917947,-115.100299109462,
173.162459923011));
#37932=CARTESIAN_POINT('Ctrl Pts',(-59.6241441585976,-115.324234310134,
173.008576811287));
#37933=CARTESIAN_POINT('Ctrl Pts',(-58.4079542254005,-115.548169510807,
172.854693699562));
#37934=CARTESIAN_POINT('Ctrl Pts',(-57.4426901770185,-115.745354335749,
173.617798149489));
#37935=CARTESIAN_POINT('Ctrl Pts',(-56.4774261286365,-115.942539160691,
174.380902599416));
#37936=CARTESIAN_POINT('Ctrl Pts',(-56.3343481358137,-116.052073459172,
175.613978373734));
#37937=CARTESIAN_POINT('Ctrl Pts',(-56.1912701429909,-116.161607757654,
176.847054148052));
#37938=CARTESIAN_POINT('Ctrl Pts',(-56.9600129359189,-116.173935868596,
177.8277821816));
#37939=CARTESIAN_POINT('Ctrl Pts',(-57.7287557288468,-116.186263979538,
178.808510215148));
#37940=CARTESIAN_POINT('Ctrl Pts',(-58.964821787878,-116.148772308176,178.962393326872));
#37941=CARTESIAN_POINT('Ctrl Pts',(-60.2008878469091,-116.111280636814,
179.116276438596));
#37942=CARTESIAN_POINT('Ctrl Pts',(-61.1860280211252,-116.100539341182,
178.35317198867));
#37943=CARTESIAN_POINT('Ctrl Pts',(-62.1711681953412,-116.089798045551,
177.590067538743));
#37944=CARTESIAN_POINT('Ctrl Pts',(-62.334122313998,-116.166707276381,176.356991764425));
#37945=CARTESIAN_POINT('Ctrl Pts',(-62.4970764326548,-116.24361650721,175.123915990107));
#37946=CARTESIAN_POINT('Ctrl Pts',(-61.7482097655609,-116.417731925579,
174.143187956559));
#37947=CARTESIAN_POINT('Ctrl Pts',(-60.999343098467,-116.591847343947,173.162459923011));
#37948=CARTESIAN_POINT('Ctrl Pts',(-59.7831531652698,-116.81578254462,173.008576811287));
#37949=CARTESIAN_POINT('Ctrl Pts',(-58.5669632320727,-117.039717745293,
172.854693699562));
#37950=CARTESIAN_POINT('Ctrl Pts',(-57.6016991836907,-117.236902570235,
173.617798149489));
#37951=CARTESIAN_POINT('Ctrl Pts',(-56.6364351353087,-117.434087395177,
174.380902599416));
#37952=CARTESIAN_POINT('Ctrl Pts',(-56.4933571424859,-117.543621693658,
175.613978373734));
#37953=CARTESIAN_POINT('Ctrl Pts',(-56.3502791496632,-117.653155992139,
176.847054148052));
#37954=CARTESIAN_POINT('Ctrl Pts',(-57.1190219425911,-117.665484103081,
177.8277821816));
#37955=CARTESIAN_POINT('Ctrl Pts',(-57.8877647355191,-117.677812214023,
178.808510215148));
#37956=CARTESIAN_POINT('Ctrl Pts',(-59.1238307945502,-117.640320542661,
178.962393326872));
#37957=CARTESIAN_POINT('Ctrl Pts',(-60.3598968535814,-117.602828871299,
179.116276438596));
#37958=CARTESIAN_POINT('Ctrl Pts',(-61.3450370277974,-117.592087575668,
178.35317198867));
#37959=CARTESIAN_POINT('Ctrl Pts',(-62.3301772020134,-117.581346280037,
177.590067538743));
#37960=CARTESIAN_POINT('Ctrl Pts',(-62.4931313206702,-117.658255510866,
176.356991764425));
#37961=CARTESIAN_POINT('Ctrl Pts',(-62.656085439327,-117.735164741696,175.123915990107));
#37962=CARTESIAN_POINT('Ctrl Pts',(-61.9072187722331,-117.909280160064,
174.143187956559));
#37963=CARTESIAN_POINT('Ctrl Pts',(-61.1583521051392,-118.083395578433,
173.162459923011));
#37964=CARTESIAN_POINT('Ctrl Pts',(-59.9421621719421,-118.307330779106,
173.008576811287));
#37965=CARTESIAN_POINT('Ctrl Pts',(-58.725972238745,-118.531265979778,172.854693699562));
#37966=CARTESIAN_POINT('Ctrl Pts',(-57.760708190363,-118.72845080472,173.617798149489));
#37967=CARTESIAN_POINT('Ctrl Pts',(-56.795444141981,-118.925635629662,174.380902599416));
#37968=CARTESIAN_POINT('Ctrl Pts',(-56.6523661491582,-119.035169928144,
175.613978373734));
#37969=CARTESIAN_POINT('Ctrl Pts',(-56.5092881563354,-119.144704226625,
176.847054148052));
#37970=CARTESIAN_POINT('Ctrl Pts',(-57.2780309492633,-119.157032337567,
177.8277821816));
#37971=CARTESIAN_POINT('Ctrl Pts',(-58.0467737421913,-119.169360448509,
178.808510215148));
#37972=CARTESIAN_POINT('Ctrl Pts',(-59.2828398012224,-119.131868777147,
178.962393326872));
#37973=CARTESIAN_POINT('Ctrl Pts',(-60.5189058602536,-119.094377105785,
179.116276438596));
#37974=CARTESIAN_POINT('Ctrl Pts',(-61.5040460344696,-119.083635810154,
178.35317198867));
#37975=CARTESIAN_POINT('Ctrl Pts',(-62.4891862086856,-119.072894514522,
177.590067538743));
#37976=CARTESIAN_POINT('Ctrl Pts',(-62.6521403273424,-119.149803745352,
176.356991764425));
#37977=CARTESIAN_POINT('Ctrl Pts',(-62.8150944459993,-119.226712976181,
175.123915990107));
#37978=CARTESIAN_POINT('Ctrl Pts',(-62.0662277789053,-119.40082839455,174.143187956559));
#37979=CARTESIAN_POINT('Ctrl Pts',(-61.3173611118114,-119.574943812919,
173.162459923011));
#37980=CARTESIAN_POINT('Ctrl Pts',(-60.1011711786143,-119.798879013591,
173.008576811287));
#37981=CARTESIAN_POINT('Ctrl Pts',(-58.8849812454172,-120.022814214264,
172.854693699562));
#37982=CARTESIAN_POINT('Ctrl Pts',(-57.9197171970352,-120.219999039206,
173.617798149489));
#37983=CARTESIAN_POINT('Ctrl Pts',(-56.9544531486532,-120.417183864148,
174.380902599416));
#37984=CARTESIAN_POINT('Ctrl Pts',(-56.8113751558304,-120.526718162629,
175.613978373734));
#37985=CARTESIAN_POINT('Ctrl Pts',(-56.6682971630076,-120.63625246111,176.847054148052));
#37986=CARTESIAN_POINT('Ctrl Pts',(-57.4370399559356,-120.648580572052,
177.8277821816));
#37987=CARTESIAN_POINT('Ctrl Pts',(-58.2057827488635,-120.660908682994,
178.808510215148));
#37988=CARTESIAN_POINT('Ctrl Pts',(-59.4418488078947,-120.623417011633,
178.962393326872));
#37989=CARTESIAN_POINT('Ctrl Pts',(-60.6779148669258,-120.585925340271,
179.116276438596));
#37990=CARTESIAN_POINT('Ctrl Pts',(-61.6630550411418,-120.575184044639,
178.35317198867));
#37991=CARTESIAN_POINT('Ctrl Pts',(-62.6481952153579,-120.564442749008,
177.590067538743));
#37992=CARTESIAN_POINT('Ctrl Pts',(-62.8111493340147,-120.641351979837,
176.356991764425));
#37993=CARTESIAN_POINT('Ctrl Pts',(-62.9741034526715,-120.718261210667,
175.123915990107));
#37994=CARTESIAN_POINT('Ctrl Pts',(-62.2252367855776,-120.892376629035,
174.143187956559));
#37995=CARTESIAN_POINT('Ctrl Pts',(-61.4763701184836,-121.066492047404,
173.162459923011));
#37996=CARTESIAN_POINT('Ctrl Pts',(-60.2601801852865,-121.290427248077,
173.008576811287));
#37997=CARTESIAN_POINT('Ctrl Pts',(-59.0439902520894,-121.514362448749,
172.854693699562));
#37998=CARTESIAN_POINT('Ctrl Pts',(-58.0787262037074,-121.711547273691,
173.617798149489));
#37999=CARTESIAN_POINT('Ctrl Pts',(-57.1134621553254,-121.908732098633,
174.380902599416));
#38000=CARTESIAN_POINT('Ctrl Pts',(-56.9703841625026,-122.018266397115,
175.613978373734));
#38001=CARTESIAN_POINT('Ctrl Pts',(-56.8273061696798,-122.127800695596,
176.847054148052));
#38002=CARTESIAN_POINT('Ctrl Pts',(-57.5960489626078,-122.140128806538,
177.8277821816));
#38003=CARTESIAN_POINT('Ctrl Pts',(-58.3647917555358,-122.15245691748,178.808510215148));
#38004=CARTESIAN_POINT('Ctrl Pts',(-59.6008578145669,-122.114965246118,
178.962393326872));
#38005=CARTESIAN_POINT('Ctrl Pts',(-60.836923873598,-122.077473574756,179.116276438596));
#38006=CARTESIAN_POINT('Ctrl Pts',(-61.8220640478141,-122.066732279125,
178.35317198867));
#38007=CARTESIAN_POINT('Ctrl Pts',(-62.8072042220301,-122.055990983494,
177.590067538743));
#38008=CARTESIAN_POINT('Ctrl Pts',(-62.9701583406869,-122.132900214323,
176.356991764425));
#38009=CARTESIAN_POINT('Ctrl Pts',(-63.1331124593437,-122.209809445152,
175.123915990107));
#38010=CARTESIAN_POINT('Ctrl Pts',(-62.3842457922498,-122.383924863521,
174.143187956559));
#38011=CARTESIAN_POINT('Ctrl Pts',(-61.6353791251559,-122.55804028189,173.162459923011));
#38012=CARTESIAN_POINT('Ctrl Pts',(-60.4191891919588,-122.781975482562,
173.008576811287));
#38013=CARTESIAN_POINT('Ctrl Pts',(-59.2029992587616,-123.005910683235,
172.854693699562));
#38014=CARTESIAN_POINT('Ctrl Pts',(-58.2377352103796,-123.203095508177,
173.617798149489));
#38015=CARTESIAN_POINT('Ctrl Pts',(-57.2724711619977,-123.400280333119,
174.380902599416));
#38016=CARTESIAN_POINT('Ctrl Pts',(-57.1293931691749,-123.5098146316,175.613978373734));
#38017=CARTESIAN_POINT('Ctrl Pts',(-56.9863151763521,-123.619348930082,
176.847054148052));
#38018=CARTESIAN_POINT('Ctrl Pts',(-57.75505796928,-123.631677041024,177.8277821816));
#38019=CARTESIAN_POINT('Ctrl Pts',(-58.523800762208,-123.644005151966,178.808510215148));
#38020=CARTESIAN_POINT('Ctrl Pts',(-59.7598668212391,-123.606513480604,
178.962393326872));
#38021=CARTESIAN_POINT('Ctrl Pts',(-60.9959328802703,-123.569021809242,
179.116276438596));
#38022=CARTESIAN_POINT('Ctrl Pts',(-61.9810730544863,-123.55828051361,178.35317198867));
#38023=CARTESIAN_POINT('Ctrl Pts',(-62.9662132287023,-123.547539217979,
177.590067538743));
#38024=CARTESIAN_POINT('Ctrl Pts',(-63.1291673473591,-123.624448448809,
176.356991764425));
#38025=CARTESIAN_POINT('Ctrl Pts',(-63.292121466016,-123.701357679638,175.123915990107));
#38026=CARTESIAN_POINT('Ctrl Pts',(-62.543254798922,-123.875473098007,174.143187956559));
#38027=CARTESIAN_POINT('Ctrl Pts',(-61.7943881318281,-124.049588516375,
173.162459923011));
#38028=CARTESIAN_POINT('Ctrl Pts',(-60.578198198631,-124.273523717048,173.008576811287));
#38029=CARTESIAN_POINT('Ctrl Pts',(-59.3620082654339,-124.497458917721,
172.854693699562));
#38030=CARTESIAN_POINT('Ctrl Pts',(-58.3967442170519,-124.694643742663,
173.617798149489));
#38031=CARTESIAN_POINT('Ctrl Pts',(-57.4314801686699,-124.891828567605,
174.380902599416));
#38032=CARTESIAN_POINT('Ctrl Pts',(-57.2884021758471,-125.001362866086,
175.613978373734));
#38033=CARTESIAN_POINT('Ctrl Pts',(-57.1453241830243,-125.110897164567,
176.847054148052));
#38034=CARTESIAN_POINT('Ctrl Pts',(-57.9140669759523,-125.123225275509,
177.8277821816));
#38035=CARTESIAN_POINT('Ctrl Pts',(-58.6828097688802,-125.135553386451,
178.808510215148));
#38036=CARTESIAN_POINT('Ctrl Pts',(-59.9188758279114,-125.098061715089,
178.962393326872));
#38037=CARTESIAN_POINT('Ctrl Pts',(-61.1549418869425,-125.060570043727,
179.116276438596));
#38038=CARTESIAN_POINT('Ctrl Pts',(-62.1400820611585,-125.049828748096,
178.35317198867));
#38039=CARTESIAN_POINT('Ctrl Pts',(-63.1252222353745,-125.039087452465,
177.590067538743));
#38040=CARTESIAN_POINT('Ctrl Pts',(-63.2881763540314,-125.115996683294,
176.356991764425));
#38041=CARTESIAN_POINT('Ctrl Pts',(-63.4511304726882,-125.192905914124,
175.123915990107));
#38042=CARTESIAN_POINT('Ctrl Pts',(-62.7022638055942,-125.367021332492,
174.143187956559));
#38043=CARTESIAN_POINT('Ctrl Pts',(-61.9533971385003,-125.541136750861,
173.162459923011));
#38044=CARTESIAN_POINT('Ctrl Pts',(-60.7372072053032,-125.765071951534,
173.008576811287));
#38045=CARTESIAN_POINT('Ctrl Pts',(-59.5210172721061,-125.989007152206,
172.854693699562));
#38046=CARTESIAN_POINT('Ctrl Pts',(-58.5557532237241,-126.186191977148,
173.617798149489));
#38047=CARTESIAN_POINT('Ctrl Pts',(-57.5904891753421,-126.38337680209,174.380902599416));
#38048=CARTESIAN_POINT('Ctrl Pts',(-57.4474111825193,-126.492911100572,
175.613978373734));
#38049=CARTESIAN_POINT('Ctrl Pts',(-57.3043331896965,-126.602445399053,
176.847054148052));
#38050=CARTESIAN_POINT('Ctrl Pts',(-58.0730759826245,-126.614773509995,
177.8277821816));
#38051=CARTESIAN_POINT('Ctrl Pts',(-58.8418187755524,-126.627101620937,
178.808510215148));
#38052=CARTESIAN_POINT('Ctrl Pts',(-60.0778848345836,-126.589609949575,
178.962393326872));
#38053=CARTESIAN_POINT('Ctrl Pts',(-61.3139508936147,-126.552118278213,
179.116276438596));
#38054=CARTESIAN_POINT('Ctrl Pts',(-62.2990910678308,-126.541376982582,
178.35317198867));
#38055=CARTESIAN_POINT('Ctrl Pts',(-63.2842312420468,-126.53063568695,177.590067538743));
#38056=CARTESIAN_POINT('Ctrl Pts',(-63.4471853607036,-126.60754491778,176.356991764425));
#38057=CARTESIAN_POINT('Ctrl Pts',(-63.6101394793604,-126.684454148609,
175.123915990107));
#38058=CARTESIAN_POINT('Ctrl Pts',(-62.8612728122665,-126.858569566978,
174.143187956559));
#38059=CARTESIAN_POINT('Ctrl Pts',(-62.1124061451725,-127.032684985347,
173.162459923011));
#38060=CARTESIAN_POINT('Ctrl Pts',(-60.8962162119754,-127.256620186019,
173.008576811287));
#38061=CARTESIAN_POINT('Ctrl Pts',(-59.6800262787783,-127.480555386692,
172.854693699562));
#38062=CARTESIAN_POINT('Ctrl Pts',(-58.7147622303963,-127.677740211634,
173.617798149489));
#38063=CARTESIAN_POINT('Ctrl Pts',(-57.7494981820143,-127.874925036576,
174.380902599416));
#38064=CARTESIAN_POINT('Ctrl Pts',(-57.6064201891915,-127.984459335057,
175.613978373734));
#38065=CARTESIAN_POINT('Ctrl Pts',(-57.4633421963688,-128.093993633538,
176.847054148052));
#38066=CARTESIAN_POINT('Ctrl Pts',(-58.2320849892967,-128.10632174448,177.8277821816));
#38067=CARTESIAN_POINT('Ctrl Pts',(-59.0008277822247,-128.118649855422,
178.808510215148));
#38068=CARTESIAN_POINT('Ctrl Pts',(-60.2368938412558,-128.081158184061,
178.962393326872));
#38069=CARTESIAN_POINT('Ctrl Pts',(-61.472959900287,-128.043666512699,179.116276438596));
#38070=CARTESIAN_POINT('Ctrl Pts',(-62.458100074503,-128.032925217067,178.35317198867));
#38071=CARTESIAN_POINT('Ctrl Pts',(-63.443240248719,-128.022183921436,177.590067538743));
#38072=CARTESIAN_POINT('Ctrl Pts',(-63.6061943673758,-128.099093152265,
176.356991764425));
#38073=CARTESIAN_POINT('Ctrl Pts',(-63.7691484860326,-128.176002383095,
175.123915990107));
#38074=CARTESIAN_POINT('Ctrl Pts',(-63.0202818189387,-128.350117801463,
174.143187956559));
#38075=CARTESIAN_POINT('Ctrl Pts',(-62.2714151518448,-128.524233219832,
173.162459923011));
#38076=CARTESIAN_POINT('Ctrl Pts',(-61.0552252186477,-128.748168420505,
173.008576811287));
#38077=CARTESIAN_POINT('Ctrl Pts',(-59.8390352854505,-128.972103621177,
172.854693699562));
#38078=CARTESIAN_POINT('Ctrl Pts',(-58.8737712370686,-129.169288446119,
173.617798149489));
#38079=CARTESIAN_POINT('Ctrl Pts',(-57.9085071886866,-129.366473271061,
174.380902599416));
#38080=CARTESIAN_POINT('Ctrl Pts',(-57.7654291958638,-129.476007569543,
175.613978373734));
#38081=CARTESIAN_POINT('Ctrl Pts',(-57.622351203041,-129.585541868024,176.847054148052));
#38082=CARTESIAN_POINT('Ctrl Pts',(-58.3910939959689,-129.597869978966,
177.8277821816));
#38083=CARTESIAN_POINT('Ctrl Pts',(-59.1598367888969,-129.610198089908,
178.808510215148));
#38084=CARTESIAN_POINT('Ctrl Pts',(-60.395902847928,-129.572706418546,178.962393326872));
#38085=CARTESIAN_POINT('Ctrl Pts',(-61.6319689069592,-129.535214747184,
179.116276438596));
#38086=CARTESIAN_POINT('Ctrl Pts',(-62.6171090811752,-129.524473451553,
178.35317198867));
#38087=CARTESIAN_POINT('Ctrl Pts',(-63.6022492553912,-129.513732155922,
177.590067538743));
#38088=CARTESIAN_POINT('Ctrl Pts',(-63.765203374048,-129.590641386751,176.356991764425));
#38089=CARTESIAN_POINT('Ctrl Pts',(-63.9281574927048,-129.66755061758,175.123915990107));
#38090=CARTESIAN_POINT('Ctrl Pts',(-63.1792908256109,-129.841666035949,
174.143187956559));
#38091=CARTESIAN_POINT('Ctrl Pts',(-62.430424158517,-130.015781454318,173.162459923011));
#38092=CARTESIAN_POINT('Ctrl Pts',(-61.2142342253199,-130.23971665499,173.008576811287));
#38093=CARTESIAN_POINT('Ctrl Pts',(-59.9980442921228,-130.463651855663,
172.854693699562));
#38094=CARTESIAN_POINT('Ctrl Pts',(-59.0327802437408,-130.660836680605,
173.617798149489));
#38095=CARTESIAN_POINT('Ctrl Pts',(-58.0675161953588,-130.858021505547,
174.380902599416));
#38096=CARTESIAN_POINT('Ctrl Pts',(-57.924438202536,-130.967555804028,175.613978373734));
#38097=CARTESIAN_POINT('Ctrl Pts',(-57.7813602097132,-131.07709010251,176.847054148052));
#38098=CARTESIAN_POINT('Ctrl Pts',(-58.5501030026412,-131.089418213452,
177.8277821816));
#38099=CARTESIAN_POINT('Ctrl Pts',(-59.3188457955691,-131.101746324394,
178.808510215148));
#38100=CARTESIAN_POINT('Ctrl Pts',(-60.5549118546003,-131.064254653032,
178.962393326872));
#38101=CARTESIAN_POINT('Ctrl Pts',(-61.3544752486066,-131.040002738838,
179.061934368543));
#38102=CARTESIAN_POINT('Ctrl Pts',(-62.0977450155935,-131.026212373353,
178.749339314461));
#38103=CARTESIAN_POINT('Ctrl Pts',(-65.9070979972576,-130.955534979744,
177.14724952928));
#38104=CARTESIAN_POINT('Ctrl Pts',(-69.7164509789216,-130.884857586135,
175.545159744099));
#38105=CARTESIAN_POINT('Ctrl Pts',(-50.1268408042676,-67.1847631435675,
175.490142808619));
#38106=CARTESIAN_POINT('Ctrl Pts',(-49.9327574595315,-67.2997349533242,
177.134243841043));
#38107=CARTESIAN_POINT('Ctrl Pts',(-50.9544351624631,-67.2850985130284,
178.441881219107));
#38108=CARTESIAN_POINT('Ctrl Pts',(-51.9761128653947,-67.2704620727326,
179.74951859717));
#38109=CARTESIAN_POINT('Ctrl Pts',(-53.6208882564639,-67.1893992560316,
179.954696079469));
#38110=CARTESIAN_POINT('Ctrl Pts',(-55.2656636475331,-67.1083364393306,
180.159873561769));
#38111=CARTESIAN_POINT('Ctrl Pts',(-56.5758711921821,-67.0629407902703,
179.142400961866));
#38112=CARTESIAN_POINT('Ctrl Pts',(-57.8860787368312,-67.0175451412101,
178.124928361964));
#38113=CARTESIAN_POINT('Ctrl Pts',(-58.1000382074012,-67.0890168607642,
176.48082732954));
#38114=CARTESIAN_POINT('Ctrl Pts',(-58.3139976779713,-67.1604885803183,
174.836726297116));
#38115=CARTESIAN_POINT('Ctrl Pts',(-57.3121961008737,-67.3615685499248,
173.529088919052));
#38116=CARTESIAN_POINT('Ctrl Pts',(-56.3103945237762,-67.5626485195312,
172.221451540989));
#38117=CARTESIAN_POINT('Ctrl Pts',(-54.685495258541,-67.830154865543,172.016274058689));
#38118=CARTESIAN_POINT('Ctrl Pts',(-53.0605959933058,-68.0976612115547,
171.81109657639));
#38119=CARTESIAN_POINT('Ctrl Pts',(-51.7702645744908,-68.3295003899256,
172.828569176292));
#38120=CARTESIAN_POINT('Ctrl Pts',(-50.4799331556759,-68.5613395682965,
173.846041776195));
#38121=CARTESIAN_POINT('Ctrl Pts',(-50.2858498109398,-68.6763113780532,
175.490142808619));
#38122=CARTESIAN_POINT('Ctrl Pts',(-50.0917664662038,-68.7912831878098,
177.134243841043));
#38123=CARTESIAN_POINT('Ctrl Pts',(-51.1134441691353,-68.776646747514,178.441881219107));
#38124=CARTESIAN_POINT('Ctrl Pts',(-52.1351218720669,-68.7620103072182,
179.74951859717));
#38125=CARTESIAN_POINT('Ctrl Pts',(-53.7798972631361,-68.6809474905172,
179.954696079469));
#38126=CARTESIAN_POINT('Ctrl Pts',(-55.4246726542053,-68.5998846738162,
180.159873561769));
#38127=CARTESIAN_POINT('Ctrl Pts',(-56.7348801988543,-68.5544890247559,
179.142400961866));
#38128=CARTESIAN_POINT('Ctrl Pts',(-58.0450877435034,-68.5090933756957,
178.124928361964));
#38129=CARTESIAN_POINT('Ctrl Pts',(-58.2590472140735,-68.5805650952498,
176.48082732954));
#38130=CARTESIAN_POINT('Ctrl Pts',(-58.4730066846436,-68.6520368148039,
174.836726297116));
#38131=CARTESIAN_POINT('Ctrl Pts',(-57.471205107546,-68.8531167844104,173.529088919052));
#38132=CARTESIAN_POINT('Ctrl Pts',(-56.4694035304484,-69.0541967540168,
172.221451540989));
#38133=CARTESIAN_POINT('Ctrl Pts',(-54.8445042652132,-69.3217031000286,
172.016274058689));
#38134=CARTESIAN_POINT('Ctrl Pts',(-53.2196049999781,-69.5892094460403,
171.81109657639));
#38135=CARTESIAN_POINT('Ctrl Pts',(-51.9292735811631,-69.8210486244112,
172.828569176292));
#38136=CARTESIAN_POINT('Ctrl Pts',(-50.6389421623481,-70.0528878027821,
173.846041776195));
#38137=CARTESIAN_POINT('Ctrl Pts',(-50.444858817612,-70.1678596125387,175.490142808619));
#38138=CARTESIAN_POINT('Ctrl Pts',(-50.250775472876,-70.2828314222954,177.134243841043));
#38139=CARTESIAN_POINT('Ctrl Pts',(-51.2724531758076,-70.2681949819996,
178.441881219107));
#38140=CARTESIAN_POINT('Ctrl Pts',(-52.2941308787392,-70.2535585417038,
179.74951859717));
#38141=CARTESIAN_POINT('Ctrl Pts',(-53.9389062698084,-70.1724957250028,
179.954696079469));
#38142=CARTESIAN_POINT('Ctrl Pts',(-55.5836816608776,-70.0914329083018,
180.159873561769));
#38143=CARTESIAN_POINT('Ctrl Pts',(-56.8938892055266,-70.0460372592415,
179.142400961866));
#38144=CARTESIAN_POINT('Ctrl Pts',(-58.2040967501756,-70.0006416101813,
178.124928361964));
#38145=CARTESIAN_POINT('Ctrl Pts',(-58.4180562207457,-70.0721133297354,
176.48082732954));
#38146=CARTESIAN_POINT('Ctrl Pts',(-58.6320156913158,-70.1435850492895,
174.836726297116));
#38147=CARTESIAN_POINT('Ctrl Pts',(-57.6302141142182,-70.344665018896,173.529088919052));
#38148=CARTESIAN_POINT('Ctrl Pts',(-56.6284125371206,-70.5457449885024,
172.221451540989));
#38149=CARTESIAN_POINT('Ctrl Pts',(-55.0035132718855,-70.8132513345142,
172.016274058689));
#38150=CARTESIAN_POINT('Ctrl Pts',(-53.3786140066503,-71.0807576805259,
171.81109657639));
#38151=CARTESIAN_POINT('Ctrl Pts',(-52.0882825878353,-71.3125968588968,
172.828569176292));
#38152=CARTESIAN_POINT('Ctrl Pts',(-50.7979511690203,-71.5444360372677,
173.846041776195));
#38153=CARTESIAN_POINT('Ctrl Pts',(-50.6038678242842,-71.6594078470244,
175.490142808619));
#38154=CARTESIAN_POINT('Ctrl Pts',(-50.4097844795482,-71.774379656781,177.134243841043));
#38155=CARTESIAN_POINT('Ctrl Pts',(-51.4314621824798,-71.7597432164852,
178.441881219107));
#38156=CARTESIAN_POINT('Ctrl Pts',(-52.4531398854114,-71.7451067761894,
179.74951859717));
#38157=CARTESIAN_POINT('Ctrl Pts',(-54.0979152764806,-71.6640439594884,
179.954696079469));
#38158=CARTESIAN_POINT('Ctrl Pts',(-55.7426906675498,-71.5829811427874,
180.159873561769));
#38159=CARTESIAN_POINT('Ctrl Pts',(-57.0528982121988,-71.5375854937271,
179.142400961866));
#38160=CARTESIAN_POINT('Ctrl Pts',(-58.3631057568478,-71.4921898446669,
178.124928361964));
#38161=CARTESIAN_POINT('Ctrl Pts',(-58.5770652274179,-71.563661564221,176.48082732954));
#38162=CARTESIAN_POINT('Ctrl Pts',(-58.791024697988,-71.6351332837751,174.836726297116));
#38163=CARTESIAN_POINT('Ctrl Pts',(-57.7892231208904,-71.8362132533815,
173.529088919052));
#38164=CARTESIAN_POINT('Ctrl Pts',(-56.7874215437928,-72.037293222988,172.221451540989));
#38165=CARTESIAN_POINT('Ctrl Pts',(-55.1625222785577,-72.3047995689997,
172.016274058689));
#38166=CARTESIAN_POINT('Ctrl Pts',(-53.5376230133225,-72.5723059150115,
171.81109657639));
#38167=CARTESIAN_POINT('Ctrl Pts',(-52.2472915945075,-72.8041450933824,
172.828569176292));
#38168=CARTESIAN_POINT('Ctrl Pts',(-50.9569601756925,-73.0359842717533,
173.846041776195));
#38169=CARTESIAN_POINT('Ctrl Pts',(-50.7628768309565,-73.1509560815099,
175.490142808619));
#38170=CARTESIAN_POINT('Ctrl Pts',(-50.5687934862204,-73.2659278912666,
177.134243841043));
#38171=CARTESIAN_POINT('Ctrl Pts',(-51.590471189152,-73.2512914509708,178.441881219107));
#38172=CARTESIAN_POINT('Ctrl Pts',(-52.6121488920836,-73.236655010675,179.74951859717));
#38173=CARTESIAN_POINT('Ctrl Pts',(-54.2569242831528,-73.155592193974,179.954696079469));
#38174=CARTESIAN_POINT('Ctrl Pts',(-55.901699674222,-73.074529377273,180.159873561769));
#38175=CARTESIAN_POINT('Ctrl Pts',(-57.211907218871,-73.0291337282128,179.142400961866));
#38176=CARTESIAN_POINT('Ctrl Pts',(-58.5221147635201,-72.9837380791525,
178.124928361964));
#38177=CARTESIAN_POINT('Ctrl Pts',(-58.7360742340901,-73.0552097987066,
176.48082732954));
#38178=CARTESIAN_POINT('Ctrl Pts',(-58.9500337046602,-73.1266815182607,
174.836726297116));
#38179=CARTESIAN_POINT('Ctrl Pts',(-57.9482321275626,-73.3277614878671,
173.529088919052));
#38180=CARTESIAN_POINT('Ctrl Pts',(-56.9464305504651,-73.5288414574736,
172.221451540989));
#38181=CARTESIAN_POINT('Ctrl Pts',(-55.3215312852299,-73.7963478034854,
172.016274058689));
#38182=CARTESIAN_POINT('Ctrl Pts',(-53.6966320199948,-74.0638541494971,
171.81109657639));
#38183=CARTESIAN_POINT('Ctrl Pts',(-52.4063006011798,-74.295693327868,172.828569176292));
#38184=CARTESIAN_POINT('Ctrl Pts',(-51.1159691823648,-74.5275325062389,
173.846041776195));
#38185=CARTESIAN_POINT('Ctrl Pts',(-50.9218858376287,-74.6425043159955,
175.490142808619));
#38186=CARTESIAN_POINT('Ctrl Pts',(-50.7278024928926,-74.7574761257522,
177.134243841043));
#38187=CARTESIAN_POINT('Ctrl Pts',(-51.7494801958242,-74.7428396854564,
178.441881219107));
#38188=CARTESIAN_POINT('Ctrl Pts',(-52.7711578987558,-74.7282032451606,
179.74951859717));
#38189=CARTESIAN_POINT('Ctrl Pts',(-54.415933289825,-74.6471404284596,179.954696079469));
#38190=CARTESIAN_POINT('Ctrl Pts',(-56.0607086808942,-74.5660776117586,
180.159873561769));
#38191=CARTESIAN_POINT('Ctrl Pts',(-57.3709162255433,-74.5206819626983,
179.142400961866));
#38192=CARTESIAN_POINT('Ctrl Pts',(-58.6811237701923,-74.4752863136381,
178.124928361964));
#38193=CARTESIAN_POINT('Ctrl Pts',(-58.8950832407624,-74.5467580331922,
176.48082732954));
#38194=CARTESIAN_POINT('Ctrl Pts',(-59.1090427113324,-74.6182297527463,
174.836726297116));
#38195=CARTESIAN_POINT('Ctrl Pts',(-58.1072411342349,-74.8193097223528,
173.529088919052));
#38196=CARTESIAN_POINT('Ctrl Pts',(-57.1054395571373,-75.0203896919592,
172.221451540989));
#38197=CARTESIAN_POINT('Ctrl Pts',(-55.4805402919021,-75.287896037971,172.016274058689));
#38198=CARTESIAN_POINT('Ctrl Pts',(-53.855641026667,-75.5554023839827,171.81109657639));
#38199=CARTESIAN_POINT('Ctrl Pts',(-52.565309607852,-75.7872415623536,172.828569176292));
#38200=CARTESIAN_POINT('Ctrl Pts',(-51.274978189037,-76.0190807407245,173.846041776195));
#38201=CARTESIAN_POINT('Ctrl Pts',(-51.0808948443009,-76.1340525504811,
175.490142808619));
#38202=CARTESIAN_POINT('Ctrl Pts',(-50.8868114995649,-76.2490243602377,
177.134243841043));
#38203=CARTESIAN_POINT('Ctrl Pts',(-51.9084892024965,-76.234387919942,178.441881219107));
#38204=CARTESIAN_POINT('Ctrl Pts',(-52.9301669054281,-76.2197514796462,
179.74951859717));
#38205=CARTESIAN_POINT('Ctrl Pts',(-54.5749422964973,-76.1386886629452,
179.954696079469));
#38206=CARTESIAN_POINT('Ctrl Pts',(-56.2197176875665,-76.0576258462442,
180.159873561769));
#38207=CARTESIAN_POINT('Ctrl Pts',(-57.5299252322155,-76.012230197184,179.142400961866));
#38208=CARTESIAN_POINT('Ctrl Pts',(-58.8401327768645,-75.9668345481237,
178.124928361964));
#38209=CARTESIAN_POINT('Ctrl Pts',(-59.0540922474346,-76.0383062676778,
176.48082732954));
#38210=CARTESIAN_POINT('Ctrl Pts',(-59.2680517180047,-76.1097779872319,
174.836726297116));
#38211=CARTESIAN_POINT('Ctrl Pts',(-58.2662501409071,-76.3108579568383,
173.529088919052));
#38212=CARTESIAN_POINT('Ctrl Pts',(-57.2644485638095,-76.5119379264448,
172.221451540989));
#38213=CARTESIAN_POINT('Ctrl Pts',(-55.6395492985744,-76.7794442724566,
172.016274058689));
#38214=CARTESIAN_POINT('Ctrl Pts',(-54.0146500333392,-77.0469506184683,
171.81109657639));
#38215=CARTESIAN_POINT('Ctrl Pts',(-52.7243186145242,-77.2787897968392,
172.828569176292));
#38216=CARTESIAN_POINT('Ctrl Pts',(-51.4339871957092,-77.5106289752101,
173.846041776195));
#38217=CARTESIAN_POINT('Ctrl Pts',(-51.2399038509732,-77.6256007849667,
175.490142808619));
#38218=CARTESIAN_POINT('Ctrl Pts',(-51.0458205062371,-77.7405725947234,
177.134243841043));
#38219=CARTESIAN_POINT('Ctrl Pts',(-52.0674982091687,-77.7259361544276,
178.441881219107));
#38220=CARTESIAN_POINT('Ctrl Pts',(-53.0891759121003,-77.7112997141318,
179.74951859717));
#38221=CARTESIAN_POINT('Ctrl Pts',(-54.7339513031695,-77.6302368974308,
179.954696079469));
#38222=CARTESIAN_POINT('Ctrl Pts',(-56.3787266942387,-77.5491740807298,
180.159873561769));
#38223=CARTESIAN_POINT('Ctrl Pts',(-57.6889342388877,-77.5037784316696,
179.142400961866));
#38224=CARTESIAN_POINT('Ctrl Pts',(-58.9991417835367,-77.4583827826093,
178.124928361964));
#38225=CARTESIAN_POINT('Ctrl Pts',(-59.2131012541068,-77.5298545021634,
176.48082732954));
#38226=CARTESIAN_POINT('Ctrl Pts',(-59.4270607246769,-77.6013262217175,
174.836726297116));
#38227=CARTESIAN_POINT('Ctrl Pts',(-58.4252591475793,-77.802406191324,173.529088919052));
#38228=CARTESIAN_POINT('Ctrl Pts',(-57.4234575704818,-78.0034861609304,
172.221451540989));
#38229=CARTESIAN_POINT('Ctrl Pts',(-55.7985583052466,-78.2709925069422,
172.016274058689));
#38230=CARTESIAN_POINT('Ctrl Pts',(-54.1736590400114,-78.5384988529539,
171.81109657639));
#38231=CARTESIAN_POINT('Ctrl Pts',(-52.8833276211964,-78.7703380313248,
172.828569176292));
#38232=CARTESIAN_POINT('Ctrl Pts',(-51.5929962023814,-79.0021772096957,
173.846041776195));
#38233=CARTESIAN_POINT('Ctrl Pts',(-51.3989128576454,-79.1171490194523,
175.490142808619));
#38234=CARTESIAN_POINT('Ctrl Pts',(-51.2048295129093,-79.232120829209,177.134243841043));
#38235=CARTESIAN_POINT('Ctrl Pts',(-52.2265072158409,-79.2174843889132,
178.441881219107));
#38236=CARTESIAN_POINT('Ctrl Pts',(-53.2481849187725,-79.2028479486174,
179.74951859717));
#38237=CARTESIAN_POINT('Ctrl Pts',(-54.8929603098417,-79.1217851319164,
179.954696079469));
#38238=CARTESIAN_POINT('Ctrl Pts',(-56.5377357009109,-79.0407223152154,
180.159873561769));
#38239=CARTESIAN_POINT('Ctrl Pts',(-57.8479432455599,-78.9953266661552,
179.142400961866));
#38240=CARTESIAN_POINT('Ctrl Pts',(-59.158150790209,-78.9499310170949,178.124928361964));
#38241=CARTESIAN_POINT('Ctrl Pts',(-59.372110260779,-79.021402736649,176.48082732954));
#38242=CARTESIAN_POINT('Ctrl Pts',(-59.5860697313491,-79.0928744562031,
174.836726297116));
#38243=CARTESIAN_POINT('Ctrl Pts',(-58.5842681542516,-79.2939544258096,
173.529088919052));
#38244=CARTESIAN_POINT('Ctrl Pts',(-57.582466577154,-79.495034395416,172.221451540989));
#38245=CARTESIAN_POINT('Ctrl Pts',(-55.9575673119188,-79.7625407414277,
172.016274058689));
#38246=CARTESIAN_POINT('Ctrl Pts',(-54.3326680466837,-80.0300470874395,
171.81109657639));
#38247=CARTESIAN_POINT('Ctrl Pts',(-53.0423366278687,-80.2618862658104,
172.828569176292));
#38248=CARTESIAN_POINT('Ctrl Pts',(-51.7520052090537,-80.4937254441813,
173.846041776195));
#38249=CARTESIAN_POINT('Ctrl Pts',(-51.5579218643176,-80.6086972539379,
175.490142808619));
#38250=CARTESIAN_POINT('Ctrl Pts',(-51.3638385195816,-80.7236690636945,
177.134243841043));
#38251=CARTESIAN_POINT('Ctrl Pts',(-52.3855162225132,-80.7090326233988,
178.441881219107));
#38252=CARTESIAN_POINT('Ctrl Pts',(-53.4071939254448,-80.694396183103,179.74951859717));
#38253=CARTESIAN_POINT('Ctrl Pts',(-55.0519693165139,-80.613333366402,179.954696079469));
#38254=CARTESIAN_POINT('Ctrl Pts',(-56.6967447075831,-80.532270549701,180.159873561769));
#38255=CARTESIAN_POINT('Ctrl Pts',(-58.0069522522322,-80.4868749006407,
179.142400961866));
#38256=CARTESIAN_POINT('Ctrl Pts',(-59.3171597968812,-80.4414792515805,
178.124928361964));
#38257=CARTESIAN_POINT('Ctrl Pts',(-59.5311192674513,-80.5129509711346,
176.48082732954));
#38258=CARTESIAN_POINT('Ctrl Pts',(-59.7450787380214,-80.5844226906887,
174.836726297116));
#38259=CARTESIAN_POINT('Ctrl Pts',(-58.7432771609238,-80.7855026602952,
173.529088919052));
#38260=CARTESIAN_POINT('Ctrl Pts',(-57.7414755838262,-80.9865826299016,
172.221451540989));
#38261=CARTESIAN_POINT('Ctrl Pts',(-56.116576318591,-81.2540889759133,172.016274058689));
#38262=CARTESIAN_POINT('Ctrl Pts',(-54.4916770533559,-81.5215953219251,
171.81109657639));
#38263=CARTESIAN_POINT('Ctrl Pts',(-53.2013456345409,-81.753434500296,172.828569176292));
#38264=CARTESIAN_POINT('Ctrl Pts',(-51.9110142157259,-81.9852736786669,
173.846041776195));
#38265=CARTESIAN_POINT('Ctrl Pts',(-51.7169308709898,-82.1002454884235,
175.490142808619));
#38266=CARTESIAN_POINT('Ctrl Pts',(-51.5228475262538,-82.2152172981802,
177.134243841043));
#38267=CARTESIAN_POINT('Ctrl Pts',(-52.5445252291854,-82.2005808578844,
178.441881219107));
#38268=CARTESIAN_POINT('Ctrl Pts',(-53.566202932117,-82.1859444175886,179.74951859717));
#38269=CARTESIAN_POINT('Ctrl Pts',(-55.2109783231862,-82.1048816008876,
179.954696079469));
#38270=CARTESIAN_POINT('Ctrl Pts',(-56.8557537142554,-82.0238187841866,
180.159873561769));
#38271=CARTESIAN_POINT('Ctrl Pts',(-58.1659612589044,-81.9784231351264,
179.142400961866));
#38272=CARTESIAN_POINT('Ctrl Pts',(-59.4761688035534,-81.9330274860661,
178.124928361964));
#38273=CARTESIAN_POINT('Ctrl Pts',(-59.6901282741235,-82.0044992056202,
176.48082732954));
#38274=CARTESIAN_POINT('Ctrl Pts',(-59.9040877446936,-82.0759709251743,
174.836726297116));
#38275=CARTESIAN_POINT('Ctrl Pts',(-58.902286167596,-82.2770508947808,173.529088919052));
#38276=CARTESIAN_POINT('Ctrl Pts',(-57.9004845904984,-82.4781308643872,
172.221451540989));
#38277=CARTESIAN_POINT('Ctrl Pts',(-56.2755853252633,-82.745637210399,172.016274058689));
#38278=CARTESIAN_POINT('Ctrl Pts',(-54.6506860600281,-83.0131435564107,
171.81109657639));
#38279=CARTESIAN_POINT('Ctrl Pts',(-53.3603546412131,-83.2449827347816,
172.828569176292));
#38280=CARTESIAN_POINT('Ctrl Pts',(-52.0700232223981,-83.4768219131525,
173.846041776195));
#38281=CARTESIAN_POINT('Ctrl Pts',(-51.8759398776621,-83.5917937229092,
175.490142808619));
#38282=CARTESIAN_POINT('Ctrl Pts',(-51.681856532926,-83.7067655326658,177.134243841043));
#38283=CARTESIAN_POINT('Ctrl Pts',(-52.7035342358576,-83.69212909237,178.441881219107));
#38284=CARTESIAN_POINT('Ctrl Pts',(-53.7252119387892,-83.6774926520742,
179.74951859717));
#38285=CARTESIAN_POINT('Ctrl Pts',(-55.3699873298584,-83.5964298353732,
179.954696079469));
#38286=CARTESIAN_POINT('Ctrl Pts',(-57.0147627209276,-83.5153670186722,
180.159873561769));
#38287=CARTESIAN_POINT('Ctrl Pts',(-58.3249702655766,-83.469971369612,179.142400961866));
#38288=CARTESIAN_POINT('Ctrl Pts',(-59.6351778102256,-83.4245757205517,
178.124928361964));
#38289=CARTESIAN_POINT('Ctrl Pts',(-59.8491372807957,-83.4960474401058,
176.48082732954));
#38290=CARTESIAN_POINT('Ctrl Pts',(-60.0630967513658,-83.5675191596599,
174.836726297116));
#38291=CARTESIAN_POINT('Ctrl Pts',(-59.0612951742682,-83.7685991292663,
173.529088919052));
#38292=CARTESIAN_POINT('Ctrl Pts',(-58.0594935971707,-83.9696790988728,
172.221451540989));
#38293=CARTESIAN_POINT('Ctrl Pts',(-56.4345943319355,-84.2371854448845,
172.016274058689));
#38294=CARTESIAN_POINT('Ctrl Pts',(-54.8096950667003,-84.5046917908963,
171.81109657639));
#38295=CARTESIAN_POINT('Ctrl Pts',(-53.5193636478853,-84.7365309692672,
172.828569176292));
#38296=CARTESIAN_POINT('Ctrl Pts',(-52.2290322290704,-84.9683701476381,
173.846041776195));
#38297=CARTESIAN_POINT('Ctrl Pts',(-52.0349488843343,-85.0833419573947,
175.490142808619));
#38298=CARTESIAN_POINT('Ctrl Pts',(-51.8408655395982,-85.1983137671514,
177.134243841043));
#38299=CARTESIAN_POINT('Ctrl Pts',(-52.8625432425298,-85.1836773268556,
178.441881219107));
#38300=CARTESIAN_POINT('Ctrl Pts',(-53.8842209454614,-85.1690408865598,
179.74951859717));
#38301=CARTESIAN_POINT('Ctrl Pts',(-55.5289963365306,-85.0879780698588,
179.954696079469));
#38302=CARTESIAN_POINT('Ctrl Pts',(-57.1737717275998,-85.0069152531578,
180.159873561769));
#38303=CARTESIAN_POINT('Ctrl Pts',(-58.4839792722488,-84.9615196040975,
179.142400961866));
#38304=CARTESIAN_POINT('Ctrl Pts',(-59.7941868168979,-84.9161239550373,
178.124928361964));
#38305=CARTESIAN_POINT('Ctrl Pts',(-60.008146287468,-84.9875956745914,176.48082732954));
#38306=CARTESIAN_POINT('Ctrl Pts',(-60.222105758038,-85.0590673941455,174.836726297116));
#38307=CARTESIAN_POINT('Ctrl Pts',(-59.2203041809405,-85.260147363752,173.529088919052));
#38308=CARTESIAN_POINT('Ctrl Pts',(-58.2185026038429,-85.4612273333584,
172.221451540989));
#38309=CARTESIAN_POINT('Ctrl Pts',(-56.5936033386077,-85.7287336793702,
172.016274058689));
#38310=CARTESIAN_POINT('Ctrl Pts',(-54.9687040733726,-85.9962400253819,
171.81109657639));
#38311=CARTESIAN_POINT('Ctrl Pts',(-53.6783726545576,-86.2280792037528,
172.828569176292));
#38312=CARTESIAN_POINT('Ctrl Pts',(-52.3880412357426,-86.4599183821237,
173.846041776195));
#38313=CARTESIAN_POINT('Ctrl Pts',(-52.1939578910065,-86.5748901918803,
175.490142808619));
#38314=CARTESIAN_POINT('Ctrl Pts',(-51.9998745462705,-86.689862001637,177.134243841043));
#38315=CARTESIAN_POINT('Ctrl Pts',(-53.0215522492021,-86.6752255613412,
178.441881219107));
#38316=CARTESIAN_POINT('Ctrl Pts',(-54.0432299521337,-86.6605891210454,
179.74951859717));
#38317=CARTESIAN_POINT('Ctrl Pts',(-55.6880053432029,-86.5795263043444,
179.954696079469));
#38318=CARTESIAN_POINT('Ctrl Pts',(-57.332780734272,-86.4984634876434,180.159873561769));
#38319=CARTESIAN_POINT('Ctrl Pts',(-58.6429882789211,-86.4530678385832,
179.142400961866));
#38320=CARTESIAN_POINT('Ctrl Pts',(-59.9531958235701,-86.4076721895229,
178.124928361964));
#38321=CARTESIAN_POINT('Ctrl Pts',(-60.1671552941402,-86.479143909077,176.48082732954));
#38322=CARTESIAN_POINT('Ctrl Pts',(-60.3811147647103,-86.5506156286311,
174.836726297116));
#38323=CARTESIAN_POINT('Ctrl Pts',(-59.3793131876127,-86.7516955982376,
173.529088919052));
#38324=CARTESIAN_POINT('Ctrl Pts',(-58.3775116105151,-86.952775567844,172.221451540989));
#38325=CARTESIAN_POINT('Ctrl Pts',(-56.7526123452799,-87.2202819138558,
172.016274058689));
#38326=CARTESIAN_POINT('Ctrl Pts',(-55.1277130800448,-87.4877882598675,
171.81109657639));
#38327=CARTESIAN_POINT('Ctrl Pts',(-53.8373816612298,-87.7196274382384,
172.828569176292));
#38328=CARTESIAN_POINT('Ctrl Pts',(-52.5470502424148,-87.9514666166093,
173.846041776195));
#38329=CARTESIAN_POINT('Ctrl Pts',(-52.3529668976787,-88.0664384263659,
175.490142808619));
#38330=CARTESIAN_POINT('Ctrl Pts',(-52.1588835529427,-88.1814102361226,
177.134243841043));
#38331=CARTESIAN_POINT('Ctrl Pts',(-53.1805612558743,-88.1667737958268,
178.441881219107));
#38332=CARTESIAN_POINT('Ctrl Pts',(-54.2022389588059,-88.152137355531,179.74951859717));
#38333=CARTESIAN_POINT('Ctrl Pts',(-55.8470143498751,-88.07107453883,179.954696079469));
#38334=CARTESIAN_POINT('Ctrl Pts',(-57.4917897409443,-87.990011722129,180.159873561769));
#38335=CARTESIAN_POINT('Ctrl Pts',(-58.8019972855933,-87.9446160730687,
179.142400961866));
#38336=CARTESIAN_POINT('Ctrl Pts',(-60.1122048302423,-87.8992204240085,
178.124928361964));
#38337=CARTESIAN_POINT('Ctrl Pts',(-60.3261643008124,-87.9706921435626,
176.48082732954));
#38338=CARTESIAN_POINT('Ctrl Pts',(-60.5401237713825,-88.0421638631167,
174.836726297116));
#38339=CARTESIAN_POINT('Ctrl Pts',(-59.5383221942849,-88.2432438327232,
173.529088919052));
#38340=CARTESIAN_POINT('Ctrl Pts',(-58.5365206171873,-88.4443238023296,
172.221451540989));
#38341=CARTESIAN_POINT('Ctrl Pts',(-56.9116213519522,-88.7118301483414,
172.016274058689));
#38342=CARTESIAN_POINT('Ctrl Pts',(-55.286722086717,-88.9793364943531,171.81109657639));
#38343=CARTESIAN_POINT('Ctrl Pts',(-53.996390667902,-89.211175672724,172.828569176292));
#38344=CARTESIAN_POINT('Ctrl Pts',(-52.706059249087,-89.4430148510949,173.846041776195));
#38345=CARTESIAN_POINT('Ctrl Pts',(-52.511975904351,-89.5579866608516,175.490142808619));
#38346=CARTESIAN_POINT('Ctrl Pts',(-52.3178925596149,-89.6729584706082,
177.134243841043));
#38347=CARTESIAN_POINT('Ctrl Pts',(-53.3395702625465,-89.6583220303124,
178.441881219107));
#38348=CARTESIAN_POINT('Ctrl Pts',(-54.3612479654781,-89.6436855900166,
179.74951859717));
#38349=CARTESIAN_POINT('Ctrl Pts',(-56.0060233565473,-89.5626227733156,
179.954696079469));
#38350=CARTESIAN_POINT('Ctrl Pts',(-57.6507987476165,-89.4815599566146,
180.159873561769));
#38351=CARTESIAN_POINT('Ctrl Pts',(-58.9610062922655,-89.4361643075543,
179.142400961866));
#38352=CARTESIAN_POINT('Ctrl Pts',(-60.2712138369146,-89.3907686584941,
178.124928361964));
#38353=CARTESIAN_POINT('Ctrl Pts',(-60.4851733074846,-89.4622403780482,
176.48082732954));
#38354=CARTESIAN_POINT('Ctrl Pts',(-60.6991327780547,-89.5337120976023,
174.836726297116));
#38355=CARTESIAN_POINT('Ctrl Pts',(-59.6973312009571,-89.7347920672087,
173.529088919052));
#38356=CARTESIAN_POINT('Ctrl Pts',(-58.6955296238596,-89.9358720368152,
172.221451540989));
#38357=CARTESIAN_POINT('Ctrl Pts',(-57.0706303586244,-90.203378382827,172.016274058689));
#38358=CARTESIAN_POINT('Ctrl Pts',(-55.4457310933893,-90.4708847288387,
171.81109657639));
#38359=CARTESIAN_POINT('Ctrl Pts',(-54.1553996745743,-90.7027239072096,
172.828569176292));
#38360=CARTESIAN_POINT('Ctrl Pts',(-52.8650682557593,-90.9345630855805,
173.846041776195));
#38361=CARTESIAN_POINT('Ctrl Pts',(-52.6709849110232,-91.0495348953371,
175.490142808619));
#38362=CARTESIAN_POINT('Ctrl Pts',(-52.4769015662871,-91.1645067050937,
177.134243841043));
#38363=CARTESIAN_POINT('Ctrl Pts',(-53.4985792692187,-91.149870264798,178.441881219107));
#38364=CARTESIAN_POINT('Ctrl Pts',(-54.5202569721503,-91.1352338245022,
179.74951859717));
#38365=CARTESIAN_POINT('Ctrl Pts',(-56.1650323632195,-91.0541710078012,
179.954696079469));
#38366=CARTESIAN_POINT('Ctrl Pts',(-57.8098077542887,-90.9731081911002,
180.159873561769));
#38367=CARTESIAN_POINT('Ctrl Pts',(-59.1200152989378,-90.92771254204,179.142400961866));
#38368=CARTESIAN_POINT('Ctrl Pts',(-60.4302228435868,-90.8823168929797,
178.124928361964));
#38369=CARTESIAN_POINT('Ctrl Pts',(-60.6441823141569,-90.9537886125338,
176.48082732954));
#38370=CARTESIAN_POINT('Ctrl Pts',(-60.858141784727,-91.0252603320879,174.836726297116));
#38371=CARTESIAN_POINT('Ctrl Pts',(-59.8563402076294,-91.2263403016943,
173.529088919052));
#38372=CARTESIAN_POINT('Ctrl Pts',(-58.8545386305318,-91.4274202713008,
172.221451540989));
#38373=CARTESIAN_POINT('Ctrl Pts',(-57.2296393652966,-91.6949266173126,
172.016274058689));
#38374=CARTESIAN_POINT('Ctrl Pts',(-55.6047401000615,-91.9624329633243,
171.81109657639));
#38375=CARTESIAN_POINT('Ctrl Pts',(-54.3144086812465,-92.1942721416952,
172.828569176292));
#38376=CARTESIAN_POINT('Ctrl Pts',(-53.0240772624315,-92.4261113200661,
173.846041776195));
#38377=CARTESIAN_POINT('Ctrl Pts',(-52.8299939176954,-92.5410831298227,
175.490142808619));
#38378=CARTESIAN_POINT('Ctrl Pts',(-52.6359105729594,-92.6560549395794,
177.134243841043));
#38379=CARTESIAN_POINT('Ctrl Pts',(-53.657588275891,-92.6414184992836,178.441881219107));
#38380=CARTESIAN_POINT('Ctrl Pts',(-54.6792659788226,-92.6267820589878,
179.74951859717));
#38381=CARTESIAN_POINT('Ctrl Pts',(-56.3240413698918,-92.5457192422868,
179.954696079469));
#38382=CARTESIAN_POINT('Ctrl Pts',(-57.968816760961,-92.4646564255858,180.159873561769));
#38383=CARTESIAN_POINT('Ctrl Pts',(-59.27902430561,-92.4192607765256,179.142400961866));
#38384=CARTESIAN_POINT('Ctrl Pts',(-60.589231850259,-92.3738651274653,178.124928361964));
#38385=CARTESIAN_POINT('Ctrl Pts',(-60.8031913208291,-92.4453368470194,
176.48082732954));
#38386=CARTESIAN_POINT('Ctrl Pts',(-61.0171507913992,-92.5168085665735,
174.836726297116));
#38387=CARTESIAN_POINT('Ctrl Pts',(-60.0153492143016,-92.71788853618,173.529088919052));
#38388=CARTESIAN_POINT('Ctrl Pts',(-59.013547637204,-92.9189685057864,172.221451540989));
#38389=CARTESIAN_POINT('Ctrl Pts',(-57.3886483719689,-93.1864748517982,
172.016274058689));
#38390=CARTESIAN_POINT('Ctrl Pts',(-55.7637491067337,-93.4539811978099,
171.81109657639));
#38391=CARTESIAN_POINT('Ctrl Pts',(-54.4734176879187,-93.6858203761808,
172.828569176292));
#38392=CARTESIAN_POINT('Ctrl Pts',(-53.1830862691037,-93.9176595545517,
173.846041776195));
#38393=CARTESIAN_POINT('Ctrl Pts',(-52.9890029243677,-94.0326313643084,
175.490142808619));
#38394=CARTESIAN_POINT('Ctrl Pts',(-52.7949195796316,-94.147603174065,177.134243841043));
#38395=CARTESIAN_POINT('Ctrl Pts',(-53.8165972825632,-94.1329667337692,
178.441881219107));
#38396=CARTESIAN_POINT('Ctrl Pts',(-54.8382749854948,-94.1183302934734,
179.74951859717));
#38397=CARTESIAN_POINT('Ctrl Pts',(-56.483050376564,-94.0372674767724,179.954696079469));
#38398=CARTESIAN_POINT('Ctrl Pts',(-58.1278257676332,-93.9562046600714,
180.159873561769));
#38399=CARTESIAN_POINT('Ctrl Pts',(-59.4380333122822,-93.9108090110112,
179.142400961866));
#38400=CARTESIAN_POINT('Ctrl Pts',(-60.7482408569312,-93.8654133619509,
178.124928361964));
#38401=CARTESIAN_POINT('Ctrl Pts',(-60.9622003275013,-93.936885081505,176.48082732954));
#38402=CARTESIAN_POINT('Ctrl Pts',(-61.1761597980714,-94.0083568010591,
174.836726297116));
#38403=CARTESIAN_POINT('Ctrl Pts',(-60.1743582209738,-94.2094367706656,
173.529088919052));
#38404=CARTESIAN_POINT('Ctrl Pts',(-59.1725566438763,-94.410516740272,172.221451540989));
#38405=CARTESIAN_POINT('Ctrl Pts',(-57.5476573786411,-94.6780230862838,
172.016274058689));
#38406=CARTESIAN_POINT('Ctrl Pts',(-55.9227581134059,-94.9455294322955,
171.81109657639));
#38407=CARTESIAN_POINT('Ctrl Pts',(-54.6324266945909,-95.1773686106664,
172.828569176292));
#38408=CARTESIAN_POINT('Ctrl Pts',(-53.342095275776,-95.4092077890373,173.846041776195));
#38409=CARTESIAN_POINT('Ctrl Pts',(-53.1480119310399,-95.5241795987939,
175.490142808619));
#38410=CARTESIAN_POINT('Ctrl Pts',(-52.9539285863038,-95.6391514085506,
177.134243841043));
#38411=CARTESIAN_POINT('Ctrl Pts',(-53.9756062892354,-95.6245149682548,
178.441881219107));
#38412=CARTESIAN_POINT('Ctrl Pts',(-54.997283992167,-95.609878527959,179.74951859717));
#38413=CARTESIAN_POINT('Ctrl Pts',(-56.6420593832362,-95.528815711258,179.954696079469));
#38414=CARTESIAN_POINT('Ctrl Pts',(-58.2868347743054,-95.447752894557,180.159873561769));
#38415=CARTESIAN_POINT('Ctrl Pts',(-59.5970423189544,-95.4023572454968,
179.142400961866));
#38416=CARTESIAN_POINT('Ctrl Pts',(-60.9072498636035,-95.3569615964365,
178.124928361964));
#38417=CARTESIAN_POINT('Ctrl Pts',(-61.1212093341735,-95.4284333159906,
176.48082732954));
#38418=CARTESIAN_POINT('Ctrl Pts',(-61.3351688047436,-95.4999050355447,
174.836726297116));
#38419=CARTESIAN_POINT('Ctrl Pts',(-60.3333672276461,-95.7009850051512,
173.529088919052));
#38420=CARTESIAN_POINT('Ctrl Pts',(-59.3315656505485,-95.9020649747577,
172.221451540989));
#38421=CARTESIAN_POINT('Ctrl Pts',(-57.7066663853133,-96.1695713207694,
172.016274058689));
#38422=CARTESIAN_POINT('Ctrl Pts',(-56.0817671200782,-96.4370776667811,
171.81109657639));
#38423=CARTESIAN_POINT('Ctrl Pts',(-54.7914357012632,-96.668916845152,172.828569176292));
#38424=CARTESIAN_POINT('Ctrl Pts',(-53.5011042824482,-96.9007560235229,
173.846041776195));
#38425=CARTESIAN_POINT('Ctrl Pts',(-53.3070209377121,-97.0157278332795,
175.490142808619));
#38426=CARTESIAN_POINT('Ctrl Pts',(-53.1129375929761,-97.1306996430362,
177.134243841043));
#38427=CARTESIAN_POINT('Ctrl Pts',(-54.1346152959077,-97.1160632027404,
178.441881219107));
#38428=CARTESIAN_POINT('Ctrl Pts',(-55.1562929988393,-97.1014267624446,
179.74951859717));
#38429=CARTESIAN_POINT('Ctrl Pts',(-56.8010683899085,-97.0203639457436,
179.954696079469));
#38430=CARTESIAN_POINT('Ctrl Pts',(-58.4458437809776,-96.9393011290426,
180.159873561769));
#38431=CARTESIAN_POINT('Ctrl Pts',(-59.7560513256267,-96.8939054799824,
179.142400961866));
#38432=CARTESIAN_POINT('Ctrl Pts',(-61.0662588702757,-96.8485098309221,
178.124928361964));
#38433=CARTESIAN_POINT('Ctrl Pts',(-61.2802183408458,-96.9199815504762,
176.48082732954));
#38434=CARTESIAN_POINT('Ctrl Pts',(-61.4941778114159,-96.9914532700303,
174.836726297116));
#38435=CARTESIAN_POINT('Ctrl Pts',(-60.4923762343183,-97.1925332396368,
173.529088919052));
#38436=CARTESIAN_POINT('Ctrl Pts',(-59.4905746572207,-97.3936132092432,
172.221451540989));
#38437=CARTESIAN_POINT('Ctrl Pts',(-57.8656753919855,-97.661119555255,172.016274058689));
#38438=CARTESIAN_POINT('Ctrl Pts',(-56.2407761267504,-97.9286259012667,
171.81109657639));
#38439=CARTESIAN_POINT('Ctrl Pts',(-54.9504447079354,-98.1604650796376,
172.828569176292));
#38440=CARTESIAN_POINT('Ctrl Pts',(-53.6601132891204,-98.3923042580085,
173.846041776195));
#38441=CARTESIAN_POINT('Ctrl Pts',(-53.4660299443843,-98.5072760677652,
175.490142808619));
#38442=CARTESIAN_POINT('Ctrl Pts',(-53.2719465996483,-98.6222478775218,
177.134243841043));
#38443=CARTESIAN_POINT('Ctrl Pts',(-54.2936243025799,-98.607611437226,178.441881219107));
#38444=CARTESIAN_POINT('Ctrl Pts',(-55.3153020055115,-98.5929749969302,
179.74951859717));
#38445=CARTESIAN_POINT('Ctrl Pts',(-56.9600773965807,-98.5119121802292,
179.954696079469));
#38446=CARTESIAN_POINT('Ctrl Pts',(-58.6048527876499,-98.4308493635282,
180.159873561769));
#38447=CARTESIAN_POINT('Ctrl Pts',(-59.9150603322989,-98.385453714468,179.142400961866));
#38448=CARTESIAN_POINT('Ctrl Pts',(-61.2252678769479,-98.3400580654077,
178.124928361964));
#38449=CARTESIAN_POINT('Ctrl Pts',(-61.439227347518,-98.4115297849618,176.48082732954));
#38450=CARTESIAN_POINT('Ctrl Pts',(-61.6531868180881,-98.4830015045159,
174.836726297116));
#38451=CARTESIAN_POINT('Ctrl Pts',(-60.6513852409905,-98.6840814741224,
173.529088919052));
#38452=CARTESIAN_POINT('Ctrl Pts',(-59.6495836638929,-98.8851614437288,
172.221451540989));
#38453=CARTESIAN_POINT('Ctrl Pts',(-58.0246843986578,-99.1526677897406,
172.016274058689));
#38454=CARTESIAN_POINT('Ctrl Pts',(-56.3997851334226,-99.4201741357523,
171.81109657639));
#38455=CARTESIAN_POINT('Ctrl Pts',(-55.1094537146076,-99.6520133141232,
172.828569176292));
#38456=CARTESIAN_POINT('Ctrl Pts',(-53.8191222957926,-99.8838524924941,
173.846041776195));
#38457=CARTESIAN_POINT('Ctrl Pts',(-53.6250389510566,-99.9988243022507,
175.490142808619));
#38458=CARTESIAN_POINT('Ctrl Pts',(-53.4309556063205,-100.113796112007,
177.134243841043));
#38459=CARTESIAN_POINT('Ctrl Pts',(-54.4526333092521,-100.099159671712,
178.441881219107));
#38460=CARTESIAN_POINT('Ctrl Pts',(-55.4743110121837,-100.084523231416,
179.74951859717));
#38461=CARTESIAN_POINT('Ctrl Pts',(-57.1190864032529,-100.003460414715,
179.954696079469));
#38462=CARTESIAN_POINT('Ctrl Pts',(-58.7638617943221,-99.9223975980138,
180.159873561769));
#38463=CARTESIAN_POINT('Ctrl Pts',(-60.0740693389711,-99.8770019489536,
179.142400961866));
#38464=CARTESIAN_POINT('Ctrl Pts',(-61.3842768836201,-99.8316062998934,
178.124928361964));
#38465=CARTESIAN_POINT('Ctrl Pts',(-61.5982363541902,-99.9030780194474,
176.48082732954));
#38466=CARTESIAN_POINT('Ctrl Pts',(-61.8121958247603,-99.9745497390015,
174.836726297116));
#38467=CARTESIAN_POINT('Ctrl Pts',(-60.8103942476627,-100.175629708608,
173.529088919052));
#38468=CARTESIAN_POINT('Ctrl Pts',(-59.8085926705652,-100.376709678214,
172.221451540989));
#38469=CARTESIAN_POINT('Ctrl Pts',(-58.18369340533,-100.644216024226,172.016274058689));
#38470=CARTESIAN_POINT('Ctrl Pts',(-56.5587941400948,-100.911722370238,
171.81109657639));
#38471=CARTESIAN_POINT('Ctrl Pts',(-55.2684627212798,-101.143561548609,
172.828569176292));
#38472=CARTESIAN_POINT('Ctrl Pts',(-53.9781313024648,-101.37540072698,173.846041776195));
#38473=CARTESIAN_POINT('Ctrl Pts',(-53.7840479577288,-101.490372536736,
175.490142808619));
#38474=CARTESIAN_POINT('Ctrl Pts',(-53.5899646129927,-101.605344346493,
177.134243841043));
#38475=CARTESIAN_POINT('Ctrl Pts',(-54.6116423159243,-101.590707906197,
178.441881219107));
#38476=CARTESIAN_POINT('Ctrl Pts',(-55.6333200188559,-101.576071465901,
179.74951859717));
#38477=CARTESIAN_POINT('Ctrl Pts',(-57.2780954099251,-101.4950086492,179.954696079469));
#38478=CARTESIAN_POINT('Ctrl Pts',(-58.9228708009943,-101.413945832499,
180.159873561769));
#38479=CARTESIAN_POINT('Ctrl Pts',(-60.2330783456433,-101.368550183439,
179.142400961866));
#38480=CARTESIAN_POINT('Ctrl Pts',(-61.5432858902924,-101.323154534379,
178.124928361964));
#38481=CARTESIAN_POINT('Ctrl Pts',(-61.7572453608625,-101.394626253933,
176.48082732954));
#38482=CARTESIAN_POINT('Ctrl Pts',(-61.9712048314326,-101.466097973487,
174.836726297116));
#38483=CARTESIAN_POINT('Ctrl Pts',(-60.969403254335,-101.667177943094,173.529088919052));
#38484=CARTESIAN_POINT('Ctrl Pts',(-59.9676016772374,-101.8682579127,172.221451540989));
#38485=CARTESIAN_POINT('Ctrl Pts',(-58.3427024120022,-102.135764258712,
172.016274058689));
#38486=CARTESIAN_POINT('Ctrl Pts',(-56.7178031467671,-102.403270604724,
171.81109657639));
#38487=CARTESIAN_POINT('Ctrl Pts',(-55.4274717279521,-102.635109783094,
172.828569176292));
#38488=CARTESIAN_POINT('Ctrl Pts',(-54.1371403091371,-102.866948961465,
173.846041776195));
#38489=CARTESIAN_POINT('Ctrl Pts',(-53.943056964401,-102.981920771222,175.490142808619));
#38490=CARTESIAN_POINT('Ctrl Pts',(-53.748973619665,-103.096892580979,177.134243841043));
#38491=CARTESIAN_POINT('Ctrl Pts',(-54.7706513225966,-103.082256140683,
178.441881219107));
#38492=CARTESIAN_POINT('Ctrl Pts',(-55.7923290255282,-103.067619700387,
179.74951859717));
#38493=CARTESIAN_POINT('Ctrl Pts',(-57.4371044165974,-102.986556883686,
179.954696079469));
#38494=CARTESIAN_POINT('Ctrl Pts',(-59.0818798076666,-102.905494066985,
180.159873561769));
#38495=CARTESIAN_POINT('Ctrl Pts',(-60.3920873523156,-102.860098417925,
179.142400961866));
#38496=CARTESIAN_POINT('Ctrl Pts',(-61.7022948969646,-102.814702768865,
178.124928361964));
#38497=CARTESIAN_POINT('Ctrl Pts',(-61.9162543675347,-102.886174488419,
176.48082732954));
#38498=CARTESIAN_POINT('Ctrl Pts',(-62.1302138381048,-102.957646207973,
174.836726297116));
#38499=CARTESIAN_POINT('Ctrl Pts',(-61.1284122610072,-103.158726177579,
173.529088919052));
#38500=CARTESIAN_POINT('Ctrl Pts',(-60.1266106839096,-103.359806147186,
172.221451540989));
#38501=CARTESIAN_POINT('Ctrl Pts',(-58.5017114186745,-103.627312493197,
172.016274058689));
#38502=CARTESIAN_POINT('Ctrl Pts',(-56.8768121534393,-103.894818839209,
171.81109657639));
#38503=CARTESIAN_POINT('Ctrl Pts',(-55.5864807346243,-104.12665801758,172.828569176292));
#38504=CARTESIAN_POINT('Ctrl Pts',(-54.2961493158093,-104.358497195951,
173.846041776195));
#38505=CARTESIAN_POINT('Ctrl Pts',(-54.1020659710732,-104.473469005708,
175.490142808619));
#38506=CARTESIAN_POINT('Ctrl Pts',(-53.9079826263372,-104.588440815464,
177.134243841043));
#38507=CARTESIAN_POINT('Ctrl Pts',(-54.9296603292688,-104.573804375168,
178.441881219107));
#38508=CARTESIAN_POINT('Ctrl Pts',(-55.9513380322004,-104.559167934873,
179.74951859717));
#38509=CARTESIAN_POINT('Ctrl Pts',(-57.5961134232696,-104.478105118172,
179.954696079469));
#38510=CARTESIAN_POINT('Ctrl Pts',(-59.2408888143388,-104.397042301471,
180.159873561769));
#38511=CARTESIAN_POINT('Ctrl Pts',(-60.5510963589878,-104.35164665241,179.142400961866));
#38512=CARTESIAN_POINT('Ctrl Pts',(-61.8613039036368,-104.30625100335,178.124928361964));
#38513=CARTESIAN_POINT('Ctrl Pts',(-62.0752633742069,-104.377722722904,
176.48082732954));
#38514=CARTESIAN_POINT('Ctrl Pts',(-62.289222844777,-104.449194442458,174.836726297116));
#38515=CARTESIAN_POINT('Ctrl Pts',(-61.2874212676794,-104.650274412065,
173.529088919052));
#38516=CARTESIAN_POINT('Ctrl Pts',(-60.2856196905818,-104.851354381671,
172.221451540989));
#38517=CARTESIAN_POINT('Ctrl Pts',(-58.6607204253467,-105.118860727683,
172.016274058689));
#38518=CARTESIAN_POINT('Ctrl Pts',(-57.0358211601115,-105.386367073695,
171.81109657639));
#38519=CARTESIAN_POINT('Ctrl Pts',(-55.7454897412965,-105.618206252066,
172.828569176292));
#38520=CARTESIAN_POINT('Ctrl Pts',(-54.4551583224815,-105.850045430437,
173.846041776195));
#38521=CARTESIAN_POINT('Ctrl Pts',(-54.2610749777455,-105.965017240193,
175.490142808619));
#38522=CARTESIAN_POINT('Ctrl Pts',(-54.0669916330094,-106.07998904995,177.134243841043));
#38523=CARTESIAN_POINT('Ctrl Pts',(-55.088669335941,-106.065352609654,178.441881219107));
#38524=CARTESIAN_POINT('Ctrl Pts',(-56.1103470388726,-106.050716169358,
179.74951859717));
#38525=CARTESIAN_POINT('Ctrl Pts',(-57.7551224299418,-105.969653352657,
179.954696079469));
#38526=CARTESIAN_POINT('Ctrl Pts',(-59.399897821011,-105.888590535956,180.159873561769));
#38527=CARTESIAN_POINT('Ctrl Pts',(-60.71010536566,-105.843194886896,179.142400961866));
#38528=CARTESIAN_POINT('Ctrl Pts',(-62.0203129103091,-105.797799237836,
178.124928361964));
#38529=CARTESIAN_POINT('Ctrl Pts',(-62.2342723808791,-105.86927095739,176.48082732954));
#38530=CARTESIAN_POINT('Ctrl Pts',(-62.4482318514492,-105.940742676944,
174.836726297116));
#38531=CARTESIAN_POINT('Ctrl Pts',(-61.4464302743516,-106.14182264655,173.529088919052));
#38532=CARTESIAN_POINT('Ctrl Pts',(-60.4446286972541,-106.342902616157,
172.221451540989));
#38533=CARTESIAN_POINT('Ctrl Pts',(-58.8197294320189,-106.610408962169,
172.016274058689));
#38534=CARTESIAN_POINT('Ctrl Pts',(-57.1948301667837,-106.87791530818,171.81109657639));
#38535=CARTESIAN_POINT('Ctrl Pts',(-55.9044987479688,-107.109754486551,
172.828569176292));
#38536=CARTESIAN_POINT('Ctrl Pts',(-54.6141673291538,-107.341593664922,
173.846041776195));
#38537=CARTESIAN_POINT('Ctrl Pts',(-54.4200839844177,-107.456565474679,
175.490142808619));
#38538=CARTESIAN_POINT('Ctrl Pts',(-54.2260006396817,-107.571537284435,
177.134243841043));
#38539=CARTESIAN_POINT('Ctrl Pts',(-55.2476783426132,-107.55690084414,178.441881219107));
#38540=CARTESIAN_POINT('Ctrl Pts',(-56.2693560455449,-107.542264403844,
179.74951859717));
#38541=CARTESIAN_POINT('Ctrl Pts',(-57.914131436614,-107.461201587143,179.954696079469));
#38542=CARTESIAN_POINT('Ctrl Pts',(-59.5589068276832,-107.380138770442,
180.159873561769));
#38543=CARTESIAN_POINT('Ctrl Pts',(-60.8691143723323,-107.334743121382,
179.142400961866));
#38544=CARTESIAN_POINT('Ctrl Pts',(-62.1793219169813,-107.289347472321,
178.124928361964));
#38545=CARTESIAN_POINT('Ctrl Pts',(-62.3932813875514,-107.360819191875,
176.48082732954));
#38546=CARTESIAN_POINT('Ctrl Pts',(-62.6072408581214,-107.43229091143,174.836726297116));
#38547=CARTESIAN_POINT('Ctrl Pts',(-61.6054392810239,-107.633370881036,
173.529088919052));
#38548=CARTESIAN_POINT('Ctrl Pts',(-60.6036377039263,-107.834450850642,
172.221451540989));
#38549=CARTESIAN_POINT('Ctrl Pts',(-58.9787384386911,-108.101957196654,
172.016274058689));
#38550=CARTESIAN_POINT('Ctrl Pts',(-57.353839173456,-108.369463542666,171.81109657639));
#38551=CARTESIAN_POINT('Ctrl Pts',(-56.063507754641,-108.601302721037,172.828569176292));
#38552=CARTESIAN_POINT('Ctrl Pts',(-54.773176335826,-108.833141899408,173.846041776195));
#38553=CARTESIAN_POINT('Ctrl Pts',(-54.5790929910899,-108.948113709164,
175.490142808619));
#38554=CARTESIAN_POINT('Ctrl Pts',(-54.3850096463539,-109.063085518921,
177.134243841043));
#38555=CARTESIAN_POINT('Ctrl Pts',(-55.4066873492855,-109.048449078625,
178.441881219107));
#38556=CARTESIAN_POINT('Ctrl Pts',(-56.4283650522171,-109.033812638329,
179.74951859717));
#38557=CARTESIAN_POINT('Ctrl Pts',(-58.0731404432863,-108.952749821628,
179.954696079469));
#38558=CARTESIAN_POINT('Ctrl Pts',(-59.7179158343555,-108.871687004927,
180.159873561769));
#38559=CARTESIAN_POINT('Ctrl Pts',(-61.0281233790045,-108.826291355867,
179.142400961866));
#38560=CARTESIAN_POINT('Ctrl Pts',(-62.3383309236535,-108.780895706807,
178.124928361964));
#38561=CARTESIAN_POINT('Ctrl Pts',(-62.5522903942236,-108.852367426361,
176.48082732954));
#38562=CARTESIAN_POINT('Ctrl Pts',(-62.7662498647937,-108.923839145915,
174.836726297116));
#38563=CARTESIAN_POINT('Ctrl Pts',(-61.7644482876961,-109.124919115522,
173.529088919052));
#38564=CARTESIAN_POINT('Ctrl Pts',(-60.7626467105985,-109.325999085128,
172.221451540989));
#38565=CARTESIAN_POINT('Ctrl Pts',(-59.1377474453634,-109.59350543114,172.016274058689));
#38566=CARTESIAN_POINT('Ctrl Pts',(-57.5128481801282,-109.861011777152,
171.81109657639));
#38567=CARTESIAN_POINT('Ctrl Pts',(-56.2225167613132,-110.092850955522,
172.828569176292));
#38568=CARTESIAN_POINT('Ctrl Pts',(-54.9321853424982,-110.324690133893,
173.846041776195));
#38569=CARTESIAN_POINT('Ctrl Pts',(-54.7381019977622,-110.43966194365,175.490142808619));
#38570=CARTESIAN_POINT('Ctrl Pts',(-54.5440186530261,-110.554633753407,
177.134243841043));
#38571=CARTESIAN_POINT('Ctrl Pts',(-55.5656963559577,-110.539997313111,
178.441881219107));
#38572=CARTESIAN_POINT('Ctrl Pts',(-56.5873740588893,-110.525360872815,
179.74951859717));
#38573=CARTESIAN_POINT('Ctrl Pts',(-58.2321494499585,-110.444298056114,
179.954696079469));
#38574=CARTESIAN_POINT('Ctrl Pts',(-59.8769248410277,-110.363235239413,
180.159873561769));
#38575=CARTESIAN_POINT('Ctrl Pts',(-61.1871323856767,-110.317839590353,
179.142400961866));
#38576=CARTESIAN_POINT('Ctrl Pts',(-62.4973399303257,-110.272443941293,
178.124928361964));
#38577=CARTESIAN_POINT('Ctrl Pts',(-62.7112994008958,-110.343915660847,
176.48082732954));
#38578=CARTESIAN_POINT('Ctrl Pts',(-62.9252588714659,-110.415387380401,
174.836726297116));
#38579=CARTESIAN_POINT('Ctrl Pts',(-61.9234572943683,-110.616467350007,
173.529088919052));
#38580=CARTESIAN_POINT('Ctrl Pts',(-60.9216557172708,-110.817547319614,
172.221451540989));
#38581=CARTESIAN_POINT('Ctrl Pts',(-59.2967564520356,-111.085053665625,
172.016274058689));
#38582=CARTESIAN_POINT('Ctrl Pts',(-57.6718571868004,-111.352560011637,
171.81109657639));
#38583=CARTESIAN_POINT('Ctrl Pts',(-56.3815257679854,-111.584399190008,
172.828569176292));
#38584=CARTESIAN_POINT('Ctrl Pts',(-55.0911943491704,-111.816238368379,
173.846041776195));
#38585=CARTESIAN_POINT('Ctrl Pts',(-54.8971110044344,-111.931210178136,
175.490142808619));
#38586=CARTESIAN_POINT('Ctrl Pts',(-54.7030276596983,-112.046181987892,
177.134243841043));
#38587=CARTESIAN_POINT('Ctrl Pts',(-55.7247053626299,-112.031545547596,
178.441881219107));
#38588=CARTESIAN_POINT('Ctrl Pts',(-56.7463830655615,-112.016909107301,
179.74951859717));
#38589=CARTESIAN_POINT('Ctrl Pts',(-58.3911584566307,-111.9358462906,179.954696079469));
#38590=CARTESIAN_POINT('Ctrl Pts',(-60.0359338476999,-111.854783473899,
180.159873561769));
#38591=CARTESIAN_POINT('Ctrl Pts',(-61.3461413923489,-111.809387824838,
179.142400961866));
#38592=CARTESIAN_POINT('Ctrl Pts',(-62.656348936998,-111.763992175778,178.124928361964));
#38593=CARTESIAN_POINT('Ctrl Pts',(-62.870308407568,-111.835463895332,176.48082732954));
#38594=CARTESIAN_POINT('Ctrl Pts',(-63.0842678781381,-111.906935614886,
174.836726297116));
#38595=CARTESIAN_POINT('Ctrl Pts',(-62.0824663010406,-112.108015584493,
173.529088919052));
#38596=CARTESIAN_POINT('Ctrl Pts',(-61.080664723943,-112.309095554099,172.221451540989));
#38597=CARTESIAN_POINT('Ctrl Pts',(-59.4557654587078,-112.576601900111,
172.016274058689));
#38598=CARTESIAN_POINT('Ctrl Pts',(-57.8308661934727,-112.844108246123,
171.81109657639));
#38599=CARTESIAN_POINT('Ctrl Pts',(-56.5405347746577,-113.075947424494,
172.828569176292));
#38600=CARTESIAN_POINT('Ctrl Pts',(-55.2502033558427,-113.307786602865,
173.846041776195));
#38601=CARTESIAN_POINT('Ctrl Pts',(-55.0561200111066,-113.422758412621,
175.490142808619));
#38602=CARTESIAN_POINT('Ctrl Pts',(-54.8620366663706,-113.537730222378,
177.134243841043));
#38603=CARTESIAN_POINT('Ctrl Pts',(-55.8837143693022,-113.523093782082,
178.441881219107));
#38604=CARTESIAN_POINT('Ctrl Pts',(-56.9053920722338,-113.508457341786,
179.74951859717));
#38605=CARTESIAN_POINT('Ctrl Pts',(-58.550167463303,-113.427394525085,179.954696079469));
#38606=CARTESIAN_POINT('Ctrl Pts',(-60.1949428543721,-113.346331708384,
180.159873561769));
#38607=CARTESIAN_POINT('Ctrl Pts',(-61.5051503990212,-113.300936059324,
179.142400961866));
#38608=CARTESIAN_POINT('Ctrl Pts',(-62.8153579436702,-113.255540410264,
178.124928361964));
#38609=CARTESIAN_POINT('Ctrl Pts',(-63.0293174142403,-113.327012129818,
176.48082732954));
#38610=CARTESIAN_POINT('Ctrl Pts',(-63.2432768848104,-113.398483849372,
174.836726297116));
#38611=CARTESIAN_POINT('Ctrl Pts',(-62.2414753077128,-113.599563818978,
173.529088919052));
#38612=CARTESIAN_POINT('Ctrl Pts',(-61.2396737306152,-113.800643788585,
172.221451540989));
#38613=CARTESIAN_POINT('Ctrl Pts',(-59.6147744653801,-114.068150134597,
172.016274058689));
#38614=CARTESIAN_POINT('Ctrl Pts',(-57.9898752001449,-114.335656480608,
171.81109657639));
#38615=CARTESIAN_POINT('Ctrl Pts',(-56.6995437813299,-114.567495658979,
172.828569176292));
#38616=CARTESIAN_POINT('Ctrl Pts',(-55.4092123625149,-114.79933483735,173.846041776195));
#38617=CARTESIAN_POINT('Ctrl Pts',(-55.2151290177788,-114.914306647107,
175.490142808619));
#38618=CARTESIAN_POINT('Ctrl Pts',(-55.0210456730428,-115.029278456863,
177.134243841043));
#38619=CARTESIAN_POINT('Ctrl Pts',(-56.0427233759744,-115.014642016568,
178.441881219107));
#38620=CARTESIAN_POINT('Ctrl Pts',(-57.064401078906,-115.000005576272,179.74951859717));
#38621=CARTESIAN_POINT('Ctrl Pts',(-58.7091764699752,-114.918942759571,
179.954696079469));
#38622=CARTESIAN_POINT('Ctrl Pts',(-60.3539518610444,-114.83787994287,180.159873561769));
#38623=CARTESIAN_POINT('Ctrl Pts',(-61.6641594056934,-114.79248429381,179.142400961866));
#38624=CARTESIAN_POINT('Ctrl Pts',(-62.9743669503424,-114.747088644749,
178.124928361964));
#38625=CARTESIAN_POINT('Ctrl Pts',(-63.1883264209125,-114.818560364303,
176.48082732954));
#38626=CARTESIAN_POINT('Ctrl Pts',(-63.4022858914826,-114.890032083858,
174.836726297116));
#38627=CARTESIAN_POINT('Ctrl Pts',(-62.400484314385,-115.091112053464,173.529088919052));
#38628=CARTESIAN_POINT('Ctrl Pts',(-61.3986827372874,-115.29219202307,172.221451540989));
#38629=CARTESIAN_POINT('Ctrl Pts',(-59.7737834720523,-115.559698369082,
172.016274058689));
#38630=CARTESIAN_POINT('Ctrl Pts',(-58.1488842068171,-115.827204715094,
171.81109657639));
#38631=CARTESIAN_POINT('Ctrl Pts',(-56.8585527880021,-116.059043893465,
172.828569176292));
#38632=CARTESIAN_POINT('Ctrl Pts',(-55.5682213691871,-116.290883071836,
173.846041776195));
#38633=CARTESIAN_POINT('Ctrl Pts',(-55.3741380244511,-116.405854881592,
175.490142808619));
#38634=CARTESIAN_POINT('Ctrl Pts',(-55.180054679715,-116.520826691349,177.134243841043));
#38635=CARTESIAN_POINT('Ctrl Pts',(-56.2017323826466,-116.506190251053,
178.441881219107));
#38636=CARTESIAN_POINT('Ctrl Pts',(-57.2234100855782,-116.491553810757,
179.74951859717));
#38637=CARTESIAN_POINT('Ctrl Pts',(-58.8681854766474,-116.410490994056,
179.954696079469));
#38638=CARTESIAN_POINT('Ctrl Pts',(-60.5129608677166,-116.329428177355,
180.159873561769));
#38639=CARTESIAN_POINT('Ctrl Pts',(-61.8231684123656,-116.284032528295,
179.142400961866));
#38640=CARTESIAN_POINT('Ctrl Pts',(-63.1333759570146,-116.238636879235,
178.124928361964));
#38641=CARTESIAN_POINT('Ctrl Pts',(-63.3473354275847,-116.310108598789,
176.48082732954));
#38642=CARTESIAN_POINT('Ctrl Pts',(-63.5612948981548,-116.381580318343,
174.836726297116));
#38643=CARTESIAN_POINT('Ctrl Pts',(-62.5594933210572,-116.58266028795,173.529088919052));
#38644=CARTESIAN_POINT('Ctrl Pts',(-61.5576917439597,-116.783740257556,
172.221451540989));
#38645=CARTESIAN_POINT('Ctrl Pts',(-59.9327924787245,-117.051246603568,
172.016274058689));
#38646=CARTESIAN_POINT('Ctrl Pts',(-58.3078932134894,-117.318752949579,
171.81109657639));
#38647=CARTESIAN_POINT('Ctrl Pts',(-57.0175617946743,-117.55059212795,172.828569176292));
#38648=CARTESIAN_POINT('Ctrl Pts',(-55.7272303758593,-117.782431306321,
173.846041776195));
#38649=CARTESIAN_POINT('Ctrl Pts',(-55.5331470311233,-117.897403116078,
175.490142808619));
#38650=CARTESIAN_POINT('Ctrl Pts',(-55.3390636863872,-118.012374925835,
177.134243841043));
#38651=CARTESIAN_POINT('Ctrl Pts',(-56.3607413893188,-117.997738485539,
178.441881219107));
#38652=CARTESIAN_POINT('Ctrl Pts',(-57.3824190922504,-117.983102045243,
179.74951859717));
#38653=CARTESIAN_POINT('Ctrl Pts',(-59.0271944833196,-117.902039228542,
179.954696079469));
#38654=CARTESIAN_POINT('Ctrl Pts',(-60.6719698743888,-117.820976411841,
180.159873561769));
#38655=CARTESIAN_POINT('Ctrl Pts',(-61.9821774190378,-117.775580762781,
179.142400961866));
#38656=CARTESIAN_POINT('Ctrl Pts',(-63.2923849636869,-117.730185113721,
178.124928361964));
#38657=CARTESIAN_POINT('Ctrl Pts',(-63.506344434257,-117.801656833275,176.48082732954));
#38658=CARTESIAN_POINT('Ctrl Pts',(-63.720303904827,-117.873128552829,174.836726297116));
#38659=CARTESIAN_POINT('Ctrl Pts',(-62.7185023277295,-118.074208522435,
173.529088919052));
#38660=CARTESIAN_POINT('Ctrl Pts',(-61.7167007506319,-118.275288492042,
172.221451540989));
#38661=CARTESIAN_POINT('Ctrl Pts',(-60.0918014853967,-118.542794838053,
172.016274058689));
#38662=CARTESIAN_POINT('Ctrl Pts',(-58.4669022201616,-118.810301184065,
171.81109657639));
#38663=CARTESIAN_POINT('Ctrl Pts',(-57.1765708013466,-119.042140362436,
172.828569176292));
#38664=CARTESIAN_POINT('Ctrl Pts',(-55.8862393825316,-119.273979540807,
173.846041776195));
#38665=CARTESIAN_POINT('Ctrl Pts',(-55.6921560377955,-119.388951350564,
175.490142808619));
#38666=CARTESIAN_POINT('Ctrl Pts',(-55.4980726930595,-119.50392316032,177.134243841043));
#38667=CARTESIAN_POINT('Ctrl Pts',(-56.5197503959911,-119.489286720024,
178.441881219107));
#38668=CARTESIAN_POINT('Ctrl Pts',(-57.5414280989227,-119.474650279729,
179.74951859717));
#38669=CARTESIAN_POINT('Ctrl Pts',(-59.1862034899919,-119.393587463028,
179.954696079469));
#38670=CARTESIAN_POINT('Ctrl Pts',(-60.8309788810611,-119.312524646327,
180.159873561769));
#38671=CARTESIAN_POINT('Ctrl Pts',(-62.1411864257101,-119.267128997266,
179.142400961866));
#38672=CARTESIAN_POINT('Ctrl Pts',(-63.4513939703591,-119.221733348206,
178.124928361964));
#38673=CARTESIAN_POINT('Ctrl Pts',(-63.6653534409292,-119.29320506776,176.48082732954));
#38674=CARTESIAN_POINT('Ctrl Pts',(-63.8793129114993,-119.364676787314,
174.836726297116));
#38675=CARTESIAN_POINT('Ctrl Pts',(-62.8775113344017,-119.565756756921,
173.529088919052));
#38676=CARTESIAN_POINT('Ctrl Pts',(-61.8757097573041,-119.766836726527,
172.221451540989));
#38677=CARTESIAN_POINT('Ctrl Pts',(-60.250810492069,-120.034343072539,172.016274058689));
#38678=CARTESIAN_POINT('Ctrl Pts',(-58.6259112268338,-120.301849418551,
171.81109657639));
#38679=CARTESIAN_POINT('Ctrl Pts',(-57.3355798080188,-120.533688596922,
172.828569176292));
#38680=CARTESIAN_POINT('Ctrl Pts',(-56.0452483892038,-120.765527775293,
173.846041776195));
#38681=CARTESIAN_POINT('Ctrl Pts',(-55.8511650444677,-120.880499585049,
175.490142808619));
#38682=CARTESIAN_POINT('Ctrl Pts',(-55.6570816997317,-120.995471394806,
177.134243841043));
#38683=CARTESIAN_POINT('Ctrl Pts',(-56.6787594026633,-120.98083495451,178.441881219107));
#38684=CARTESIAN_POINT('Ctrl Pts',(-57.7004371055949,-120.966198514214,
179.74951859717));
#38685=CARTESIAN_POINT('Ctrl Pts',(-59.3452124966641,-120.885135697513,
179.954696079469));
#38686=CARTESIAN_POINT('Ctrl Pts',(-60.9899878877333,-120.804072880812,
180.159873561769));
#38687=CARTESIAN_POINT('Ctrl Pts',(-62.3001954323823,-120.758677231752,
179.142400961866));
#38688=CARTESIAN_POINT('Ctrl Pts',(-63.6104029770313,-120.713281582692,
178.124928361964));
#38689=CARTESIAN_POINT('Ctrl Pts',(-63.8243624476014,-120.784753302246,
176.48082732954));
#38690=CARTESIAN_POINT('Ctrl Pts',(-64.0383219181715,-120.8562250218,174.836726297116));
#38691=CARTESIAN_POINT('Ctrl Pts',(-63.0365203410739,-121.057304991406,
173.529088919052));
#38692=CARTESIAN_POINT('Ctrl Pts',(-62.0347187639764,-121.258384961013,
172.221451540989));
#38693=CARTESIAN_POINT('Ctrl Pts',(-60.4098194987412,-121.525891307025,
172.016274058689));
#38694=CARTESIAN_POINT('Ctrl Pts',(-58.784920233506,-121.793397653036,171.81109657639));
#38695=CARTESIAN_POINT('Ctrl Pts',(-57.494588814691,-122.025236831407,172.828569176292));
#38696=CARTESIAN_POINT('Ctrl Pts',(-56.204257395876,-122.257076009778,173.846041776195));
#38697=CARTESIAN_POINT('Ctrl Pts',(-56.01017405114,-122.372047819535,175.490142808619));
#38698=CARTESIAN_POINT('Ctrl Pts',(-55.8160907064039,-122.487019629291,
177.134243841043));
#38699=CARTESIAN_POINT('Ctrl Pts',(-56.8377684093355,-122.472383188996,
178.441881219107));
#38700=CARTESIAN_POINT('Ctrl Pts',(-57.8594461122671,-122.4577467487,179.74951859717));
#38701=CARTESIAN_POINT('Ctrl Pts',(-59.5042215033363,-122.376683931999,
179.954696079469));
#38702=CARTESIAN_POINT('Ctrl Pts',(-61.1489968944055,-122.295621115298,
180.159873561769));
#38703=CARTESIAN_POINT('Ctrl Pts',(-62.4592044390545,-122.250225466238,
179.142400961866));
#38704=CARTESIAN_POINT('Ctrl Pts',(-63.7694119837035,-122.204829817177,
178.124928361964));
#38705=CARTESIAN_POINT('Ctrl Pts',(-63.9833714542736,-122.276301536731,
176.48082732954));
#38706=CARTESIAN_POINT('Ctrl Pts',(-64.1973309248437,-122.347773256285,
174.836726297116));
#38707=CARTESIAN_POINT('Ctrl Pts',(-63.1955293477461,-122.548853225892,
173.529088919052));
#38708=CARTESIAN_POINT('Ctrl Pts',(-62.1937277706486,-122.749933195498,
172.221451540989));
#38709=CARTESIAN_POINT('Ctrl Pts',(-60.5688285054134,-123.01743954151,172.016274058689));
#38710=CARTESIAN_POINT('Ctrl Pts',(-58.9439292401782,-123.284945887522,
171.81109657639));
#38711=CARTESIAN_POINT('Ctrl Pts',(-57.6535978213633,-123.516785065893,
172.828569176292));
#38712=CARTESIAN_POINT('Ctrl Pts',(-56.3632664025483,-123.748624244264,
173.846041776195));
#38713=CARTESIAN_POINT('Ctrl Pts',(-56.1691830578122,-123.86359605402,175.490142808619));
#38714=CARTESIAN_POINT('Ctrl Pts',(-55.9750997130761,-123.978567863777,
177.134243841043));
#38715=CARTESIAN_POINT('Ctrl Pts',(-56.9967774160077,-123.963931423481,
178.441881219107));
#38716=CARTESIAN_POINT('Ctrl Pts',(-58.0184551189394,-123.949294983185,
179.74951859717));
#38717=CARTESIAN_POINT('Ctrl Pts',(-59.6632305100085,-123.868232166484,
179.954696079469));
#38718=CARTESIAN_POINT('Ctrl Pts',(-61.3080059010777,-123.787169349783,
180.159873561769));
#38719=CARTESIAN_POINT('Ctrl Pts',(-62.6182134457268,-123.741773700723,
179.142400961866));
#38720=CARTESIAN_POINT('Ctrl Pts',(-63.9284209903758,-123.696378051663,
178.124928361964));
#38721=CARTESIAN_POINT('Ctrl Pts',(-64.1423804609459,-123.767849771217,
176.48082732954));
#38722=CARTESIAN_POINT('Ctrl Pts',(-64.3563399315159,-123.839321490771,
174.836726297116));
#38723=CARTESIAN_POINT('Ctrl Pts',(-63.3545383544184,-124.040401460378,
173.529088919052));
#38724=CARTESIAN_POINT('Ctrl Pts',(-62.3527367773208,-124.241481429984,
172.221451540989));
#38725=CARTESIAN_POINT('Ctrl Pts',(-60.7278375120856,-124.508987775996,
172.016274058689));
#38726=CARTESIAN_POINT('Ctrl Pts',(-59.1029382468505,-124.776494122007,
171.81109657639));
#38727=CARTESIAN_POINT('Ctrl Pts',(-57.8126068280355,-125.008333300378,
172.828569176292));
#38728=CARTESIAN_POINT('Ctrl Pts',(-56.5222754092205,-125.240172478749,
173.846041776195));
#38729=CARTESIAN_POINT('Ctrl Pts',(-56.3281920644844,-125.355144288506,
175.490142808619));
#38730=CARTESIAN_POINT('Ctrl Pts',(-56.1341087197484,-125.470116098263,
177.134243841043));
#38731=CARTESIAN_POINT('Ctrl Pts',(-57.15578642268,-125.455479657967,178.441881219107));
#38732=CARTESIAN_POINT('Ctrl Pts',(-58.1774641256116,-125.440843217671,
179.74951859717));
#38733=CARTESIAN_POINT('Ctrl Pts',(-59.8222395166808,-125.35978040097,179.954696079469));
#38734=CARTESIAN_POINT('Ctrl Pts',(-61.46701490775,-125.278717584269,180.159873561769));
#38735=CARTESIAN_POINT('Ctrl Pts',(-62.777222452399,-125.233321935209,179.142400961866));
#38736=CARTESIAN_POINT('Ctrl Pts',(-64.087429997048,-125.187926286149,178.124928361964));
#38737=CARTESIAN_POINT('Ctrl Pts',(-64.3013894676181,-125.259398005703,
176.48082732954));
#38738=CARTESIAN_POINT('Ctrl Pts',(-64.5153489381882,-125.330869725257,
174.836726297116));
#38739=CARTESIAN_POINT('Ctrl Pts',(-63.5135473610906,-125.531949694863,
173.529088919052));
#38740=CARTESIAN_POINT('Ctrl Pts',(-62.511745783993,-125.73302966447,172.221451540989));
#38741=CARTESIAN_POINT('Ctrl Pts',(-60.8868465187579,-126.000536010481,
172.016274058689));
#38742=CARTESIAN_POINT('Ctrl Pts',(-59.2619472535227,-126.268042356493,
171.81109657639));
#38743=CARTESIAN_POINT('Ctrl Pts',(-57.9716158347077,-126.499881534864,
172.828569176292));
#38744=CARTESIAN_POINT('Ctrl Pts',(-56.6812844158927,-126.731720713235,
173.846041776195));
#38745=CARTESIAN_POINT('Ctrl Pts',(-56.4872010711566,-126.846692522992,
175.490142808619));
#38746=CARTESIAN_POINT('Ctrl Pts',(-56.2931177264206,-126.961664332748,
177.134243841043));
#38747=CARTESIAN_POINT('Ctrl Pts',(-57.3147954293522,-126.947027892452,
178.441881219107));
#38748=CARTESIAN_POINT('Ctrl Pts',(-58.3364731322838,-126.932391452157,
179.74951859717));
#38749=CARTESIAN_POINT('Ctrl Pts',(-59.981248523353,-126.851328635456,179.954696079469));
#38750=CARTESIAN_POINT('Ctrl Pts',(-61.6260239144222,-126.770265818755,
180.159873561769));
#38751=CARTESIAN_POINT('Ctrl Pts',(-62.9362314590712,-126.724870169694,
179.142400961866));
#38752=CARTESIAN_POINT('Ctrl Pts',(-64.2464390037202,-126.679474520634,
178.124928361964));
#38753=CARTESIAN_POINT('Ctrl Pts',(-64.4603984742903,-126.750946240188,
176.48082732954));
#38754=CARTESIAN_POINT('Ctrl Pts',(-64.6743579448604,-126.822417959742,
174.836726297116));
#38755=CARTESIAN_POINT('Ctrl Pts',(-63.6725563677628,-127.023497929349,
173.529088919052));
#38756=CARTESIAN_POINT('Ctrl Pts',(-62.6707547906653,-127.224577898955,
172.221451540989));
#38757=CARTESIAN_POINT('Ctrl Pts',(-61.0458555254301,-127.492084244967,
172.016274058689));
#38758=CARTESIAN_POINT('Ctrl Pts',(-59.4209562601949,-127.759590590979,
171.81109657639));
#38759=CARTESIAN_POINT('Ctrl Pts',(-58.1306248413799,-127.99142976935,172.828569176292));
#38760=CARTESIAN_POINT('Ctrl Pts',(-56.8402934225649,-128.223268947721,
173.846041776195));
#38761=CARTESIAN_POINT('Ctrl Pts',(-56.6462100778289,-128.338240757477,
175.490142808619));
#38762=CARTESIAN_POINT('Ctrl Pts',(-56.4521267330928,-128.453212567234,
177.134243841043));
#38763=CARTESIAN_POINT('Ctrl Pts',(-57.4738044360244,-128.438576126938,
178.441881219107));
#38764=CARTESIAN_POINT('Ctrl Pts',(-58.495482138956,-128.423939686642,179.74951859717));
#38765=CARTESIAN_POINT('Ctrl Pts',(-60.1402575300252,-128.342876869941,
179.954696079469));
#38766=CARTESIAN_POINT('Ctrl Pts',(-61.7850329210944,-128.26181405324,180.159873561769));
#38767=CARTESIAN_POINT('Ctrl Pts',(-63.0952404657434,-128.21641840418,179.142400961866));
#38768=CARTESIAN_POINT('Ctrl Pts',(-64.4054480103925,-128.17102275512,178.124928361964));
#38769=CARTESIAN_POINT('Ctrl Pts',(-64.6194074809625,-128.242494474674,
176.48082732954));
#38770=CARTESIAN_POINT('Ctrl Pts',(-64.8333669515326,-128.313966194228,
174.836726297116));
#38771=CARTESIAN_POINT('Ctrl Pts',(-63.831565374435,-128.515046163834,173.529088919052));
#38772=CARTESIAN_POINT('Ctrl Pts',(-62.8297637973375,-128.716126133441,
172.221451540989));
#38773=CARTESIAN_POINT('Ctrl Pts',(-61.2048645321023,-128.983632479453,
172.016274058689));
#38774=CARTESIAN_POINT('Ctrl Pts',(-59.5799652668672,-129.251138825464,
171.81109657639));
#38775=CARTESIAN_POINT('Ctrl Pts',(-58.2896338480522,-129.482978003835,
172.828569176292));
#38776=CARTESIAN_POINT('Ctrl Pts',(-56.9993024292372,-129.714817182206,
173.846041776195));
#38777=CARTESIAN_POINT('Ctrl Pts',(-56.8052190845011,-129.829788991963,
175.490142808619));
#38778=CARTESIAN_POINT('Ctrl Pts',(-56.611135739765,-129.944760801719,177.134243841043));
#38779=CARTESIAN_POINT('Ctrl Pts',(-57.6328134426967,-129.930124361424,
178.441881219107));
#38780=CARTESIAN_POINT('Ctrl Pts',(-58.6544911456282,-129.915487921128,
179.74951859717));
#38781=CARTESIAN_POINT('Ctrl Pts',(-60.2992665366974,-129.834425104427,
179.954696079469));
#38782=CARTESIAN_POINT('Ctrl Pts',(-61.9440419277666,-129.753362287726,
180.159873561769));
#38783=CARTESIAN_POINT('Ctrl Pts',(-63.2542494724157,-129.707966638666,
179.142400961866));
#38784=CARTESIAN_POINT('Ctrl Pts',(-64.5644570170647,-129.662570989605,
178.124928361964));
#38785=CARTESIAN_POINT('Ctrl Pts',(-64.7784164876348,-129.734042709159,
176.48082732954));
#38786=CARTESIAN_POINT('Ctrl Pts',(-64.9923759582049,-129.805514428714,
174.836726297116));
#38787=CARTESIAN_POINT('Ctrl Pts',(-63.9905743811073,-130.00659439832,173.529088919052));
#38788=CARTESIAN_POINT('Ctrl Pts',(-62.9887728040097,-130.207674367926,
172.221451540989));
#38789=CARTESIAN_POINT('Ctrl Pts',(-61.3638735387745,-130.475180713938,
172.016274058689));
#38790=CARTESIAN_POINT('Ctrl Pts',(-59.7389742735394,-130.74268705995,171.81109657639));
#38791=CARTESIAN_POINT('Ctrl Pts',(-58.4486428547244,-130.974526238321,
172.828569176292));
#38792=CARTESIAN_POINT('Ctrl Pts',(-57.1583114359094,-131.206365416692,
173.846041776195));
#38793=CARTESIAN_POINT('Ctrl Pts',(-56.9642280911733,-131.321337226448,
175.490142808619));
#38794=CARTESIAN_POINT('Ctrl Pts',(-56.7701447464373,-131.436309036205,
177.134243841043));
#38795=CARTESIAN_POINT('Ctrl Pts',(-57.7918224493689,-131.421672595909,
178.441881219107));
#38796=CARTESIAN_POINT('Ctrl Pts',(-58.8135001523005,-131.407036155613,
179.74951859717));
#38797=CARTESIAN_POINT('Ctrl Pts',(-60.4582755433697,-131.325973338912,
179.954696079469));
#38798=CARTESIAN_POINT('Ctrl Pts',(-61.522217219021,-131.273536933612,180.087417468365));
#38799=CARTESIAN_POINT('Ctrl Pts',(-62.5109440081377,-131.233579209696,
179.670624062921));
#38800=CARTESIAN_POINT('Ctrl Pts',(-67.5782957416017,-131.028790744588,
177.534504349347));
#38801=CARTESIAN_POINT('Ctrl Pts',(-72.6456474750658,-130.824002279481,
175.398384635772));
#38802=CARTESIAN_POINT('Ctrl Pts',(-58.0980103408427,-67.1520871615593,
175.424797521432));
#38803=CARTESIAN_POINT('Ctrl Pts',(-57.9563744146254,-67.2322701352371,
174.369925727914));
#38804=CARTESIAN_POINT('Ctrl Pts',(-57.3121961008737,-67.3615685499248,
173.529088919052));
#38805=CARTESIAN_POINT('Ctrl Pts',(-56.3103945237762,-67.5626485195312,
172.221451540989));
#38806=CARTESIAN_POINT('Ctrl Pts',(-54.685495258541,-67.830154865543,172.016274058689));
#38807=CARTESIAN_POINT('Ctrl Pts',(-53.0605959933058,-68.0976612115547,
171.81109657639));
#38808=CARTESIAN_POINT('Ctrl Pts',(-51.7702645744908,-68.3295003899256,
172.828569176292));
#38809=CARTESIAN_POINT('Ctrl Pts',(-50.4799331556759,-68.5613395682965,
173.846041776195));
#38810=CARTESIAN_POINT('Ctrl Pts',(-50.2858498109398,-68.6763113780532,
175.490142808619));
#38811=CARTESIAN_POINT('Ctrl Pts',(-50.0917664662038,-68.7912831878098,
177.134243841043));
#38812=CARTESIAN_POINT('Ctrl Pts',(-51.1134441691353,-68.776646747514,178.441881219107));
#38813=CARTESIAN_POINT('Ctrl Pts',(-52.1351218720669,-68.7620103072182,
179.74951859717));
#38814=CARTESIAN_POINT('Ctrl Pts',(-53.7798972631361,-68.6809474905172,
179.954696079469));
#38815=CARTESIAN_POINT('Ctrl Pts',(-55.4246726542053,-68.5998846738162,
180.159873561769));
#38816=CARTESIAN_POINT('Ctrl Pts',(-56.7348801988543,-68.5544890247559,
179.142400961866));
#38817=CARTESIAN_POINT('Ctrl Pts',(-58.0450877435034,-68.5090933756957,
178.124928361964));
#38818=CARTESIAN_POINT('Ctrl Pts',(-58.2590472140735,-68.5805650952498,
176.48082732954));
#38819=CARTESIAN_POINT('Ctrl Pts',(-58.4730066846436,-68.6520368148039,
174.836726297116));
#38820=CARTESIAN_POINT('Ctrl Pts',(-57.471205107546,-68.8531167844104,173.529088919052));
#38821=CARTESIAN_POINT('Ctrl Pts',(-56.4694035304484,-69.0541967540168,
172.221451540989));
#38822=CARTESIAN_POINT('Ctrl Pts',(-54.8445042652132,-69.3217031000286,
172.016274058689));
#38823=CARTESIAN_POINT('Ctrl Pts',(-53.2196049999781,-69.5892094460403,
171.81109657639));
#38824=CARTESIAN_POINT('Ctrl Pts',(-51.9292735811631,-69.8210486244112,
172.828569176292));
#38825=CARTESIAN_POINT('Ctrl Pts',(-50.6389421623481,-70.0528878027821,
173.846041776195));
#38826=CARTESIAN_POINT('Ctrl Pts',(-50.444858817612,-70.1678596125387,175.490142808619));
#38827=CARTESIAN_POINT('Ctrl Pts',(-50.250775472876,-70.2828314222954,177.134243841043));
#38828=CARTESIAN_POINT('Ctrl Pts',(-51.2724531758076,-70.2681949819996,
178.441881219107));
#38829=CARTESIAN_POINT('Ctrl Pts',(-52.2941308787392,-70.2535585417038,
179.74951859717));
#38830=CARTESIAN_POINT('Ctrl Pts',(-53.9389062698084,-70.1724957250028,
179.954696079469));
#38831=CARTESIAN_POINT('Ctrl Pts',(-55.5836816608776,-70.0914329083018,
180.159873561769));
#38832=CARTESIAN_POINT('Ctrl Pts',(-56.8938892055266,-70.0460372592415,
179.142400961866));
#38833=CARTESIAN_POINT('Ctrl Pts',(-58.2040967501756,-70.0006416101813,
178.124928361964));
#38834=CARTESIAN_POINT('Ctrl Pts',(-58.4180562207457,-70.0721133297354,
176.48082732954));
#38835=CARTESIAN_POINT('Ctrl Pts',(-58.6320156913158,-70.1435850492895,
174.836726297116));
#38836=CARTESIAN_POINT('Ctrl Pts',(-57.6302141142182,-70.344665018896,173.529088919052));
#38837=CARTESIAN_POINT('Ctrl Pts',(-56.6284125371206,-70.5457449885024,
172.221451540989));
#38838=CARTESIAN_POINT('Ctrl Pts',(-55.0035132718855,-70.8132513345142,
172.016274058689));
#38839=CARTESIAN_POINT('Ctrl Pts',(-53.3786140066503,-71.0807576805259,
171.81109657639));
#38840=CARTESIAN_POINT('Ctrl Pts',(-52.0882825878353,-71.3125968588968,
172.828569176292));
#38841=CARTESIAN_POINT('Ctrl Pts',(-50.7979511690203,-71.5444360372677,
173.846041776195));
#38842=CARTESIAN_POINT('Ctrl Pts',(-50.6038678242843,-71.6594078470244,
175.490142808619));
#38843=CARTESIAN_POINT('Ctrl Pts',(-50.4097844795482,-71.774379656781,177.134243841043));
#38844=CARTESIAN_POINT('Ctrl Pts',(-51.4314621824798,-71.7597432164852,
178.441881219107));
#38845=CARTESIAN_POINT('Ctrl Pts',(-52.4531398854114,-71.7451067761894,
179.74951859717));
#38846=CARTESIAN_POINT('Ctrl Pts',(-54.0979152764806,-71.6640439594884,
179.954696079469));
#38847=CARTESIAN_POINT('Ctrl Pts',(-55.7426906675498,-71.5829811427874,
180.159873561769));
#38848=CARTESIAN_POINT('Ctrl Pts',(-57.0528982121988,-71.5375854937271,
179.142400961866));
#38849=CARTESIAN_POINT('Ctrl Pts',(-58.3631057568478,-71.4921898446669,
178.124928361964));
#38850=CARTESIAN_POINT('Ctrl Pts',(-58.5770652274179,-71.563661564221,176.48082732954));
#38851=CARTESIAN_POINT('Ctrl Pts',(-58.791024697988,-71.6351332837751,174.836726297116));
#38852=CARTESIAN_POINT('Ctrl Pts',(-57.7892231208904,-71.8362132533815,
173.529088919052));
#38853=CARTESIAN_POINT('Ctrl Pts',(-56.7874215437929,-72.037293222988,172.221451540989));
#38854=CARTESIAN_POINT('Ctrl Pts',(-55.1625222785577,-72.3047995689997,
172.016274058689));
#38855=CARTESIAN_POINT('Ctrl Pts',(-53.5376230133225,-72.5723059150115,
171.81109657639));
#38856=CARTESIAN_POINT('Ctrl Pts',(-52.2472915945075,-72.8041450933824,
172.828569176292));
#38857=CARTESIAN_POINT('Ctrl Pts',(-50.9569601756925,-73.0359842717533,
173.846041776195));
#38858=CARTESIAN_POINT('Ctrl Pts',(-50.7628768309565,-73.1509560815099,
175.490142808619));
#38859=CARTESIAN_POINT('Ctrl Pts',(-50.5687934862204,-73.2659278912666,
177.134243841043));
#38860=CARTESIAN_POINT('Ctrl Pts',(-51.590471189152,-73.2512914509708,178.441881219107));
#38861=CARTESIAN_POINT('Ctrl Pts',(-52.6121488920836,-73.236655010675,179.74951859717));
#38862=CARTESIAN_POINT('Ctrl Pts',(-54.2569242831528,-73.155592193974,179.954696079469));
#38863=CARTESIAN_POINT('Ctrl Pts',(-55.901699674222,-73.074529377273,180.159873561769));
#38864=CARTESIAN_POINT('Ctrl Pts',(-57.211907218871,-73.0291337282128,179.142400961866));
#38865=CARTESIAN_POINT('Ctrl Pts',(-58.5221147635201,-72.9837380791525,
178.124928361964));
#38866=CARTESIAN_POINT('Ctrl Pts',(-58.7360742340901,-73.0552097987066,
176.48082732954));
#38867=CARTESIAN_POINT('Ctrl Pts',(-58.9500337046602,-73.1266815182607,
174.836726297116));
#38868=CARTESIAN_POINT('Ctrl Pts',(-57.9482321275626,-73.3277614878671,
173.529088919052));
#38869=CARTESIAN_POINT('Ctrl Pts',(-56.9464305504651,-73.5288414574736,
172.221451540989));
#38870=CARTESIAN_POINT('Ctrl Pts',(-55.3215312852299,-73.7963478034854,
172.016274058689));
#38871=CARTESIAN_POINT('Ctrl Pts',(-53.6966320199948,-74.0638541494971,
171.81109657639));
#38872=CARTESIAN_POINT('Ctrl Pts',(-52.4063006011798,-74.295693327868,172.828569176292));
#38873=CARTESIAN_POINT('Ctrl Pts',(-51.1159691823648,-74.5275325062389,
173.846041776195));
#38874=CARTESIAN_POINT('Ctrl Pts',(-50.9218858376287,-74.6425043159955,
175.490142808619));
#38875=CARTESIAN_POINT('Ctrl Pts',(-50.7278024928926,-74.7574761257522,
177.134243841043));
#38876=CARTESIAN_POINT('Ctrl Pts',(-51.7494801958242,-74.7428396854564,
178.441881219107));
#38877=CARTESIAN_POINT('Ctrl Pts',(-52.7711578987559,-74.7282032451606,
179.74951859717));
#38878=CARTESIAN_POINT('Ctrl Pts',(-54.415933289825,-74.6471404284596,179.954696079469));
#38879=CARTESIAN_POINT('Ctrl Pts',(-56.0607086808942,-74.5660776117586,
180.159873561769));
#38880=CARTESIAN_POINT('Ctrl Pts',(-57.3709162255433,-74.5206819626983,
179.142400961866));
#38881=CARTESIAN_POINT('Ctrl Pts',(-58.6811237701923,-74.4752863136381,
178.124928361964));
#38882=CARTESIAN_POINT('Ctrl Pts',(-58.8950832407624,-74.5467580331922,
176.48082732954));
#38883=CARTESIAN_POINT('Ctrl Pts',(-59.1090427113324,-74.6182297527463,
174.836726297116));
#38884=CARTESIAN_POINT('Ctrl Pts',(-58.1072411342349,-74.8193097223528,
173.529088919052));
#38885=CARTESIAN_POINT('Ctrl Pts',(-57.1054395571373,-75.0203896919592,
172.221451540989));
#38886=CARTESIAN_POINT('Ctrl Pts',(-55.4805402919021,-75.287896037971,172.016274058689));
#38887=CARTESIAN_POINT('Ctrl Pts',(-53.855641026667,-75.5554023839827,171.81109657639));
#38888=CARTESIAN_POINT('Ctrl Pts',(-52.565309607852,-75.7872415623536,172.828569176292));
#38889=CARTESIAN_POINT('Ctrl Pts',(-51.274978189037,-76.0190807407245,173.846041776195));
#38890=CARTESIAN_POINT('Ctrl Pts',(-51.0808948443009,-76.1340525504811,
175.490142808619));
#38891=CARTESIAN_POINT('Ctrl Pts',(-50.8868114995649,-76.2490243602378,
177.134243841043));
#38892=CARTESIAN_POINT('Ctrl Pts',(-51.9084892024965,-76.234387919942,178.441881219107));
#38893=CARTESIAN_POINT('Ctrl Pts',(-52.9301669054281,-76.2197514796462,
179.74951859717));
#38894=CARTESIAN_POINT('Ctrl Pts',(-54.5749422964973,-76.1386886629452,
179.954696079469));
#38895=CARTESIAN_POINT('Ctrl Pts',(-56.2197176875665,-76.0576258462442,
180.159873561769));
#38896=CARTESIAN_POINT('Ctrl Pts',(-57.5299252322155,-76.012230197184,179.142400961866));
#38897=CARTESIAN_POINT('Ctrl Pts',(-58.8401327768645,-75.9668345481237,
178.124928361964));
#38898=CARTESIAN_POINT('Ctrl Pts',(-59.0540922474346,-76.0383062676778,
176.48082732954));
#38899=CARTESIAN_POINT('Ctrl Pts',(-59.2680517180047,-76.1097779872319,
174.836726297116));
#38900=CARTESIAN_POINT('Ctrl Pts',(-58.2662501409071,-76.3108579568383,
173.529088919052));
#38901=CARTESIAN_POINT('Ctrl Pts',(-57.2644485638095,-76.5119379264448,
172.221451540989));
#38902=CARTESIAN_POINT('Ctrl Pts',(-55.6395492985744,-76.7794442724566,
172.016274058689));
#38903=CARTESIAN_POINT('Ctrl Pts',(-54.0146500333392,-77.0469506184683,
171.81109657639));
#38904=CARTESIAN_POINT('Ctrl Pts',(-52.7243186145242,-77.2787897968392,
172.828569176292));
#38905=CARTESIAN_POINT('Ctrl Pts',(-51.4339871957092,-77.5106289752101,
173.846041776195));
#38906=CARTESIAN_POINT('Ctrl Pts',(-51.2399038509732,-77.6256007849667,
175.490142808619));
#38907=CARTESIAN_POINT('Ctrl Pts',(-51.0458205062371,-77.7405725947234,
177.134243841043));
#38908=CARTESIAN_POINT('Ctrl Pts',(-52.0674982091687,-77.7259361544276,
178.441881219107));
#38909=CARTESIAN_POINT('Ctrl Pts',(-53.0891759121003,-77.7112997141318,
179.74951859717));
#38910=CARTESIAN_POINT('Ctrl Pts',(-54.7339513031695,-77.6302368974308,
179.954696079469));
#38911=CARTESIAN_POINT('Ctrl Pts',(-56.3787266942387,-77.5491740807298,
180.159873561769));
#38912=CARTESIAN_POINT('Ctrl Pts',(-57.6889342388877,-77.5037784316696,
179.142400961866));
#38913=CARTESIAN_POINT('Ctrl Pts',(-58.9991417835367,-77.4583827826093,
178.124928361964));
#38914=CARTESIAN_POINT('Ctrl Pts',(-59.2131012541068,-77.5298545021634,
176.48082732954));
#38915=CARTESIAN_POINT('Ctrl Pts',(-59.4270607246769,-77.6013262217175,
174.836726297116));
#38916=CARTESIAN_POINT('Ctrl Pts',(-58.4252591475793,-77.802406191324,173.529088919052));
#38917=CARTESIAN_POINT('Ctrl Pts',(-57.4234575704818,-78.0034861609304,
172.221451540989));
#38918=CARTESIAN_POINT('Ctrl Pts',(-55.7985583052466,-78.2709925069422,
172.016274058689));
#38919=CARTESIAN_POINT('Ctrl Pts',(-54.1736590400114,-78.5384988529539,
171.81109657639));
#38920=CARTESIAN_POINT('Ctrl Pts',(-52.8833276211964,-78.7703380313248,
172.828569176292));
#38921=CARTESIAN_POINT('Ctrl Pts',(-51.5929962023814,-79.0021772096957,
173.846041776195));
#38922=CARTESIAN_POINT('Ctrl Pts',(-51.3989128576454,-79.1171490194523,
175.490142808619));
#38923=CARTESIAN_POINT('Ctrl Pts',(-51.2048295129093,-79.232120829209,177.134243841043));
#38924=CARTESIAN_POINT('Ctrl Pts',(-52.2265072158409,-79.2174843889132,
178.441881219107));
#38925=CARTESIAN_POINT('Ctrl Pts',(-53.2481849187725,-79.2028479486174,
179.74951859717));
#38926=CARTESIAN_POINT('Ctrl Pts',(-54.8929603098417,-79.1217851319164,
179.954696079469));
#38927=CARTESIAN_POINT('Ctrl Pts',(-56.5377357009109,-79.0407223152154,
180.159873561769));
#38928=CARTESIAN_POINT('Ctrl Pts',(-57.8479432455599,-78.9953266661552,
179.142400961866));
#38929=CARTESIAN_POINT('Ctrl Pts',(-59.158150790209,-78.9499310170949,178.124928361964));
#38930=CARTESIAN_POINT('Ctrl Pts',(-59.372110260779,-79.021402736649,176.48082732954));
#38931=CARTESIAN_POINT('Ctrl Pts',(-59.5860697313491,-79.0928744562031,
174.836726297116));
#38932=CARTESIAN_POINT('Ctrl Pts',(-58.5842681542516,-79.2939544258096,
173.529088919052));
#38933=CARTESIAN_POINT('Ctrl Pts',(-57.582466577154,-79.495034395416,172.221451540989));
#38934=CARTESIAN_POINT('Ctrl Pts',(-55.9575673119188,-79.7625407414277,
172.016274058689));
#38935=CARTESIAN_POINT('Ctrl Pts',(-54.3326680466837,-80.0300470874395,
171.81109657639));
#38936=CARTESIAN_POINT('Ctrl Pts',(-53.0423366278687,-80.2618862658104,
172.828569176292));
#38937=CARTESIAN_POINT('Ctrl Pts',(-51.7520052090537,-80.4937254441813,
173.846041776195));
#38938=CARTESIAN_POINT('Ctrl Pts',(-51.5579218643176,-80.6086972539379,
175.490142808619));
#38939=CARTESIAN_POINT('Ctrl Pts',(-51.3638385195816,-80.7236690636945,
177.134243841043));
#38940=CARTESIAN_POINT('Ctrl Pts',(-52.3855162225132,-80.7090326233988,
178.441881219107));
#38941=CARTESIAN_POINT('Ctrl Pts',(-53.4071939254448,-80.694396183103,179.74951859717));
#38942=CARTESIAN_POINT('Ctrl Pts',(-55.0519693165139,-80.613333366402,179.954696079469));
#38943=CARTESIAN_POINT('Ctrl Pts',(-56.6967447075831,-80.532270549701,180.159873561769));
#38944=CARTESIAN_POINT('Ctrl Pts',(-58.0069522522322,-80.4868749006407,
179.142400961866));
#38945=CARTESIAN_POINT('Ctrl Pts',(-59.3171597968812,-80.4414792515805,
178.124928361964));
#38946=CARTESIAN_POINT('Ctrl Pts',(-59.5311192674513,-80.5129509711346,
176.48082732954));
#38947=CARTESIAN_POINT('Ctrl Pts',(-59.7450787380214,-80.5844226906887,
174.836726297116));
#38948=CARTESIAN_POINT('Ctrl Pts',(-58.7432771609238,-80.7855026602952,
173.529088919052));
#38949=CARTESIAN_POINT('Ctrl Pts',(-57.7414755838262,-80.9865826299016,
172.221451540989));
#38950=CARTESIAN_POINT('Ctrl Pts',(-56.116576318591,-81.2540889759133,172.016274058689));
#38951=CARTESIAN_POINT('Ctrl Pts',(-54.4916770533559,-81.5215953219251,
171.81109657639));
#38952=CARTESIAN_POINT('Ctrl Pts',(-53.2013456345409,-81.753434500296,172.828569176292));
#38953=CARTESIAN_POINT('Ctrl Pts',(-51.9110142157259,-81.9852736786669,
173.846041776195));
#38954=CARTESIAN_POINT('Ctrl Pts',(-51.7169308709898,-82.1002454884235,
175.490142808619));
#38955=CARTESIAN_POINT('Ctrl Pts',(-51.5228475262538,-82.2152172981801,
177.134243841043));
#38956=CARTESIAN_POINT('Ctrl Pts',(-52.5445252291854,-82.2005808578844,
178.441881219107));
#38957=CARTESIAN_POINT('Ctrl Pts',(-53.566202932117,-82.1859444175886,179.74951859717));
#38958=CARTESIAN_POINT('Ctrl Pts',(-55.2109783231862,-82.1048816008876,
179.954696079469));
#38959=CARTESIAN_POINT('Ctrl Pts',(-56.8557537142554,-82.0238187841866,
180.159873561769));
#38960=CARTESIAN_POINT('Ctrl Pts',(-58.1659612589044,-81.9784231351264,
179.142400961866));
#38961=CARTESIAN_POINT('Ctrl Pts',(-59.4761688035534,-81.9330274860661,
178.124928361964));
#38962=CARTESIAN_POINT('Ctrl Pts',(-59.6901282741235,-82.0044992056202,
176.48082732954));
#38963=CARTESIAN_POINT('Ctrl Pts',(-59.9040877446936,-82.0759709251743,
174.836726297116));
#38964=CARTESIAN_POINT('Ctrl Pts',(-58.902286167596,-82.2770508947808,173.529088919052));
#38965=CARTESIAN_POINT('Ctrl Pts',(-57.9004845904984,-82.4781308643872,
172.221451540989));
#38966=CARTESIAN_POINT('Ctrl Pts',(-56.2755853252633,-82.745637210399,172.016274058689));
#38967=CARTESIAN_POINT('Ctrl Pts',(-54.6506860600281,-83.0131435564107,
171.81109657639));
#38968=CARTESIAN_POINT('Ctrl Pts',(-53.3603546412131,-83.2449827347816,
172.828569176292));
#38969=CARTESIAN_POINT('Ctrl Pts',(-52.0700232223981,-83.4768219131525,
173.846041776195));
#38970=CARTESIAN_POINT('Ctrl Pts',(-51.8759398776621,-83.5917937229092,
175.490142808619));
#38971=CARTESIAN_POINT('Ctrl Pts',(-51.681856532926,-83.7067655326658,177.134243841043));
#38972=CARTESIAN_POINT('Ctrl Pts',(-52.7035342358576,-83.69212909237,178.441881219107));
#38973=CARTESIAN_POINT('Ctrl Pts',(-53.7252119387892,-83.6774926520742,
179.74951859717));
#38974=CARTESIAN_POINT('Ctrl Pts',(-55.3699873298584,-83.5964298353732,
179.954696079469));
#38975=CARTESIAN_POINT('Ctrl Pts',(-57.0147627209276,-83.5153670186722,
180.159873561769));
#38976=CARTESIAN_POINT('Ctrl Pts',(-58.3249702655766,-83.469971369612,179.142400961866));
#38977=CARTESIAN_POINT('Ctrl Pts',(-59.6351778102256,-83.4245757205517,
178.124928361964));
#38978=CARTESIAN_POINT('Ctrl Pts',(-59.8491372807957,-83.4960474401058,
176.48082732954));
#38979=CARTESIAN_POINT('Ctrl Pts',(-60.0630967513658,-83.5675191596599,
174.836726297116));
#38980=CARTESIAN_POINT('Ctrl Pts',(-59.0612951742682,-83.7685991292663,
173.529088919052));
#38981=CARTESIAN_POINT('Ctrl Pts',(-58.0594935971707,-83.9696790988728,
172.221451540989));
#38982=CARTESIAN_POINT('Ctrl Pts',(-56.4345943319355,-84.2371854448845,
172.016274058689));
#38983=CARTESIAN_POINT('Ctrl Pts',(-54.8096950667003,-84.5046917908963,
171.81109657639));
#38984=CARTESIAN_POINT('Ctrl Pts',(-53.5193636478853,-84.7365309692672,
172.828569176292));
#38985=CARTESIAN_POINT('Ctrl Pts',(-52.2290322290704,-84.9683701476381,
173.846041776195));
#38986=CARTESIAN_POINT('Ctrl Pts',(-52.0349488843343,-85.0833419573947,
175.490142808619));
#38987=CARTESIAN_POINT('Ctrl Pts',(-51.8408655395982,-85.1983137671513,
177.134243841043));
#38988=CARTESIAN_POINT('Ctrl Pts',(-52.8625432425298,-85.1836773268556,
178.441881219107));
#38989=CARTESIAN_POINT('Ctrl Pts',(-53.8842209454614,-85.1690408865598,
179.74951859717));
#38990=CARTESIAN_POINT('Ctrl Pts',(-55.5289963365306,-85.0879780698588,
179.954696079469));
#38991=CARTESIAN_POINT('Ctrl Pts',(-57.1737717275998,-85.0069152531578,
180.159873561769));
#38992=CARTESIAN_POINT('Ctrl Pts',(-58.4839792722488,-84.9615196040975,
179.142400961866));
#38993=CARTESIAN_POINT('Ctrl Pts',(-59.7941868168979,-84.9161239550373,
178.124928361964));
#38994=CARTESIAN_POINT('Ctrl Pts',(-60.008146287468,-84.9875956745914,176.48082732954));
#38995=CARTESIAN_POINT('Ctrl Pts',(-60.222105758038,-85.0590673941455,174.836726297116));
#38996=CARTESIAN_POINT('Ctrl Pts',(-59.2203041809405,-85.260147363752,173.529088919052));
#38997=CARTESIAN_POINT('Ctrl Pts',(-58.2185026038429,-85.4612273333584,
172.221451540989));
#38998=CARTESIAN_POINT('Ctrl Pts',(-56.5936033386077,-85.7287336793702,
172.016274058689));
#38999=CARTESIAN_POINT('Ctrl Pts',(-54.9687040733726,-85.9962400253819,
171.81109657639));
#39000=CARTESIAN_POINT('Ctrl Pts',(-53.6783726545576,-86.2280792037528,
172.828569176292));
#39001=CARTESIAN_POINT('Ctrl Pts',(-52.3880412357426,-86.4599183821237,
173.846041776195));
#39002=CARTESIAN_POINT('Ctrl Pts',(-52.1939578910065,-86.5748901918803,
175.490142808619));
#39003=CARTESIAN_POINT('Ctrl Pts',(-51.9998745462705,-86.689862001637,177.134243841043));
#39004=CARTESIAN_POINT('Ctrl Pts',(-53.0215522492021,-86.6752255613412,
178.441881219107));
#39005=CARTESIAN_POINT('Ctrl Pts',(-54.0432299521337,-86.6605891210454,
179.74951859717));
#39006=CARTESIAN_POINT('Ctrl Pts',(-55.6880053432029,-86.5795263043444,
179.954696079469));
#39007=CARTESIAN_POINT('Ctrl Pts',(-57.3327807342721,-86.4984634876434,
180.159873561769));
#39008=CARTESIAN_POINT('Ctrl Pts',(-58.6429882789211,-86.4530678385832,
179.142400961866));
#39009=CARTESIAN_POINT('Ctrl Pts',(-59.9531958235701,-86.4076721895229,
178.124928361964));
#39010=CARTESIAN_POINT('Ctrl Pts',(-60.1671552941402,-86.479143909077,176.48082732954));
#39011=CARTESIAN_POINT('Ctrl Pts',(-60.3811147647103,-86.5506156286311,
174.836726297116));
#39012=CARTESIAN_POINT('Ctrl Pts',(-59.3793131876127,-86.7516955982376,
173.529088919052));
#39013=CARTESIAN_POINT('Ctrl Pts',(-58.3775116105151,-86.952775567844,172.221451540989));
#39014=CARTESIAN_POINT('Ctrl Pts',(-56.7526123452799,-87.2202819138558,
172.016274058689));
#39015=CARTESIAN_POINT('Ctrl Pts',(-55.1277130800448,-87.4877882598675,
171.81109657639));
#39016=CARTESIAN_POINT('Ctrl Pts',(-53.8373816612298,-87.7196274382384,
172.828569176292));
#39017=CARTESIAN_POINT('Ctrl Pts',(-52.5470502424148,-87.9514666166093,
173.846041776195));
#39018=CARTESIAN_POINT('Ctrl Pts',(-52.3529668976787,-88.0664384263659,
175.490142808619));
#39019=CARTESIAN_POINT('Ctrl Pts',(-52.1588835529427,-88.1814102361226,
177.134243841043));
#39020=CARTESIAN_POINT('Ctrl Pts',(-53.1805612558743,-88.1667737958268,
178.441881219107));
#39021=CARTESIAN_POINT('Ctrl Pts',(-54.2022389588059,-88.152137355531,179.74951859717));
#39022=CARTESIAN_POINT('Ctrl Pts',(-55.8470143498751,-88.07107453883,179.954696079469));
#39023=CARTESIAN_POINT('Ctrl Pts',(-57.4917897409443,-87.990011722129,180.159873561769));
#39024=CARTESIAN_POINT('Ctrl Pts',(-58.8019972855933,-87.9446160730687,
179.142400961866));
#39025=CARTESIAN_POINT('Ctrl Pts',(-60.1122048302423,-87.8992204240085,
178.124928361964));
#39026=CARTESIAN_POINT('Ctrl Pts',(-60.3261643008124,-87.9706921435626,
176.48082732954));
#39027=CARTESIAN_POINT('Ctrl Pts',(-60.5401237713825,-88.0421638631167,
174.836726297116));
#39028=CARTESIAN_POINT('Ctrl Pts',(-59.5383221942849,-88.2432438327232,
173.529088919052));
#39029=CARTESIAN_POINT('Ctrl Pts',(-58.5365206171873,-88.4443238023296,
172.221451540989));
#39030=CARTESIAN_POINT('Ctrl Pts',(-56.9116213519522,-88.7118301483414,
172.016274058689));
#39031=CARTESIAN_POINT('Ctrl Pts',(-55.286722086717,-88.9793364943531,171.81109657639));
#39032=CARTESIAN_POINT('Ctrl Pts',(-53.996390667902,-89.211175672724,172.828569176292));
#39033=CARTESIAN_POINT('Ctrl Pts',(-52.706059249087,-89.4430148510949,173.846041776195));
#39034=CARTESIAN_POINT('Ctrl Pts',(-52.511975904351,-89.5579866608516,175.490142808619));
#39035=CARTESIAN_POINT('Ctrl Pts',(-52.3178925596149,-89.6729584706082,
177.134243841043));
#39036=CARTESIAN_POINT('Ctrl Pts',(-53.3395702625465,-89.6583220303124,
178.441881219107));
#39037=CARTESIAN_POINT('Ctrl Pts',(-54.3612479654781,-89.6436855900166,
179.74951859717));
#39038=CARTESIAN_POINT('Ctrl Pts',(-56.0060233565473,-89.5626227733156,
179.954696079469));
#39039=CARTESIAN_POINT('Ctrl Pts',(-57.6507987476165,-89.4815599566146,
180.159873561769));
#39040=CARTESIAN_POINT('Ctrl Pts',(-58.9610062922655,-89.4361643075543,
179.142400961866));
#39041=CARTESIAN_POINT('Ctrl Pts',(-60.2712138369146,-89.3907686584941,
178.124928361964));
#39042=CARTESIAN_POINT('Ctrl Pts',(-60.4851733074846,-89.4622403780482,
176.48082732954));
#39043=CARTESIAN_POINT('Ctrl Pts',(-60.6991327780547,-89.5337120976023,
174.836726297116));
#39044=CARTESIAN_POINT('Ctrl Pts',(-59.6973312009571,-89.7347920672087,
173.529088919052));
#39045=CARTESIAN_POINT('Ctrl Pts',(-58.6955296238596,-89.9358720368152,
172.221451540989));
#39046=CARTESIAN_POINT('Ctrl Pts',(-57.0706303586244,-90.203378382827,172.016274058689));
#39047=CARTESIAN_POINT('Ctrl Pts',(-55.4457310933893,-90.4708847288387,
171.81109657639));
#39048=CARTESIAN_POINT('Ctrl Pts',(-54.1553996745743,-90.7027239072096,
172.828569176292));
#39049=CARTESIAN_POINT('Ctrl Pts',(-52.8650682557593,-90.9345630855805,
173.846041776195));
#39050=CARTESIAN_POINT('Ctrl Pts',(-52.6709849110232,-91.0495348953371,
175.490142808619));
#39051=CARTESIAN_POINT('Ctrl Pts',(-52.4769015662871,-91.1645067050938,
177.134243841043));
#39052=CARTESIAN_POINT('Ctrl Pts',(-53.4985792692187,-91.149870264798,178.441881219107));
#39053=CARTESIAN_POINT('Ctrl Pts',(-54.5202569721503,-91.1352338245022,
179.74951859717));
#39054=CARTESIAN_POINT('Ctrl Pts',(-56.1650323632195,-91.0541710078012,
179.954696079469));
#39055=CARTESIAN_POINT('Ctrl Pts',(-57.8098077542887,-90.9731081911002,
180.159873561769));
#39056=CARTESIAN_POINT('Ctrl Pts',(-59.1200152989378,-90.92771254204,179.142400961866));
#39057=CARTESIAN_POINT('Ctrl Pts',(-60.4302228435868,-90.8823168929797,
178.124928361964));
#39058=CARTESIAN_POINT('Ctrl Pts',(-60.6441823141569,-90.9537886125338,
176.48082732954));
#39059=CARTESIAN_POINT('Ctrl Pts',(-60.858141784727,-91.0252603320879,174.836726297116));
#39060=CARTESIAN_POINT('Ctrl Pts',(-59.8563402076294,-91.2263403016943,
173.529088919052));
#39061=CARTESIAN_POINT('Ctrl Pts',(-58.8545386305318,-91.4274202713008,
172.221451540989));
#39062=CARTESIAN_POINT('Ctrl Pts',(-57.2296393652966,-91.6949266173126,
172.016274058689));
#39063=CARTESIAN_POINT('Ctrl Pts',(-55.6047401000615,-91.9624329633243,
171.81109657639));
#39064=CARTESIAN_POINT('Ctrl Pts',(-54.3144086812465,-92.1942721416952,
172.828569176292));
#39065=CARTESIAN_POINT('Ctrl Pts',(-53.0240772624315,-92.4261113200661,
173.846041776195));
#39066=CARTESIAN_POINT('Ctrl Pts',(-52.8299939176954,-92.5410831298227,
175.490142808619));
#39067=CARTESIAN_POINT('Ctrl Pts',(-52.6359105729594,-92.6560549395793,
177.134243841043));
#39068=CARTESIAN_POINT('Ctrl Pts',(-53.657588275891,-92.6414184992836,178.441881219107));
#39069=CARTESIAN_POINT('Ctrl Pts',(-54.6792659788226,-92.6267820589878,
179.74951859717));
#39070=CARTESIAN_POINT('Ctrl Pts',(-56.3240413698918,-92.5457192422868,
179.954696079469));
#39071=CARTESIAN_POINT('Ctrl Pts',(-57.968816760961,-92.4646564255858,180.159873561769));
#39072=CARTESIAN_POINT('Ctrl Pts',(-59.27902430561,-92.4192607765256,179.142400961866));
#39073=CARTESIAN_POINT('Ctrl Pts',(-60.589231850259,-92.3738651274653,178.124928361964));
#39074=CARTESIAN_POINT('Ctrl Pts',(-60.8031913208291,-92.4453368470194,
176.48082732954));
#39075=CARTESIAN_POINT('Ctrl Pts',(-61.0171507913992,-92.5168085665735,
174.836726297116));
#39076=CARTESIAN_POINT('Ctrl Pts',(-60.0153492143016,-92.71788853618,173.529088919052));
#39077=CARTESIAN_POINT('Ctrl Pts',(-59.013547637204,-92.9189685057864,172.221451540989));
#39078=CARTESIAN_POINT('Ctrl Pts',(-57.3886483719689,-93.1864748517982,
172.016274058689));
#39079=CARTESIAN_POINT('Ctrl Pts',(-55.7637491067337,-93.4539811978099,
171.81109657639));
#39080=CARTESIAN_POINT('Ctrl Pts',(-54.4734176879187,-93.6858203761808,
172.828569176292));
#39081=CARTESIAN_POINT('Ctrl Pts',(-53.1830862691037,-93.9176595545517,
173.846041776195));
#39082=CARTESIAN_POINT('Ctrl Pts',(-52.9890029243677,-94.0326313643084,
175.490142808619));
#39083=CARTESIAN_POINT('Ctrl Pts',(-52.7949195796316,-94.147603174065,177.134243841043));
#39084=CARTESIAN_POINT('Ctrl Pts',(-53.8165972825632,-94.1329667337692,
178.441881219107));
#39085=CARTESIAN_POINT('Ctrl Pts',(-54.8382749854948,-94.1183302934734,
179.74951859717));
#39086=CARTESIAN_POINT('Ctrl Pts',(-56.483050376564,-94.0372674767724,179.954696079469));
#39087=CARTESIAN_POINT('Ctrl Pts',(-58.1278257676332,-93.9562046600714,
180.159873561769));
#39088=CARTESIAN_POINT('Ctrl Pts',(-59.4380333122822,-93.9108090110112,
179.142400961866));
#39089=CARTESIAN_POINT('Ctrl Pts',(-60.7482408569312,-93.8654133619509,
178.124928361964));
#39090=CARTESIAN_POINT('Ctrl Pts',(-60.9622003275013,-93.936885081505,176.48082732954));
#39091=CARTESIAN_POINT('Ctrl Pts',(-61.1761597980714,-94.0083568010591,
174.836726297116));
#39092=CARTESIAN_POINT('Ctrl Pts',(-60.1743582209738,-94.2094367706656,
173.529088919052));
#39093=CARTESIAN_POINT('Ctrl Pts',(-59.1725566438763,-94.4105167402721,
172.221451540989));
#39094=CARTESIAN_POINT('Ctrl Pts',(-57.5476573786411,-94.6780230862838,
172.016274058689));
#39095=CARTESIAN_POINT('Ctrl Pts',(-55.9227581134059,-94.9455294322955,
171.81109657639));
#39096=CARTESIAN_POINT('Ctrl Pts',(-54.6324266945909,-95.1773686106664,
172.828569176292));
#39097=CARTESIAN_POINT('Ctrl Pts',(-53.3420952757759,-95.4092077890373,
173.846041776195));
#39098=CARTESIAN_POINT('Ctrl Pts',(-53.1480119310399,-95.5241795987939,
175.490142808619));
#39099=CARTESIAN_POINT('Ctrl Pts',(-52.9539285863038,-95.6391514085506,
177.134243841043));
#39100=CARTESIAN_POINT('Ctrl Pts',(-53.9756062892354,-95.6245149682548,
178.441881219107));
#39101=CARTESIAN_POINT('Ctrl Pts',(-54.997283992167,-95.609878527959,179.74951859717));
#39102=CARTESIAN_POINT('Ctrl Pts',(-56.6420593832362,-95.528815711258,179.954696079469));
#39103=CARTESIAN_POINT('Ctrl Pts',(-58.2868347743054,-95.447752894557,180.159873561769));
#39104=CARTESIAN_POINT('Ctrl Pts',(-59.5970423189544,-95.4023572454968,
179.142400961866));
#39105=CARTESIAN_POINT('Ctrl Pts',(-60.9072498636035,-95.3569615964365,
178.124928361964));
#39106=CARTESIAN_POINT('Ctrl Pts',(-61.1212093341735,-95.4284333159906,
176.48082732954));
#39107=CARTESIAN_POINT('Ctrl Pts',(-61.3351688047436,-95.4999050355447,
174.836726297116));
#39108=CARTESIAN_POINT('Ctrl Pts',(-60.3333672276461,-95.7009850051512,
173.529088919052));
#39109=CARTESIAN_POINT('Ctrl Pts',(-59.3315656505485,-95.9020649747577,
172.221451540989));
#39110=CARTESIAN_POINT('Ctrl Pts',(-57.7066663853133,-96.1695713207694,
172.016274058689));
#39111=CARTESIAN_POINT('Ctrl Pts',(-56.0817671200782,-96.4370776667811,
171.81109657639));
#39112=CARTESIAN_POINT('Ctrl Pts',(-54.7914357012632,-96.668916845152,172.828569176292));
#39113=CARTESIAN_POINT('Ctrl Pts',(-53.5011042824482,-96.9007560235229,
173.846041776195));
#39114=CARTESIAN_POINT('Ctrl Pts',(-53.3070209377121,-97.0157278332795,
175.490142808619));
#39115=CARTESIAN_POINT('Ctrl Pts',(-53.1129375929761,-97.1306996430362,
177.134243841043));
#39116=CARTESIAN_POINT('Ctrl Pts',(-54.1346152959077,-97.1160632027404,
178.441881219107));
#39117=CARTESIAN_POINT('Ctrl Pts',(-55.1562929988393,-97.1014267624446,
179.74951859717));
#39118=CARTESIAN_POINT('Ctrl Pts',(-56.8010683899085,-97.0203639457436,
179.954696079469));
#39119=CARTESIAN_POINT('Ctrl Pts',(-58.4458437809776,-96.9393011290426,
180.159873561769));
#39120=CARTESIAN_POINT('Ctrl Pts',(-59.7560513256267,-96.8939054799824,
179.142400961866));
#39121=CARTESIAN_POINT('Ctrl Pts',(-61.0662588702757,-96.8485098309222,
178.124928361964));
#39122=CARTESIAN_POINT('Ctrl Pts',(-61.2802183408458,-96.9199815504762,
176.48082732954));
#39123=CARTESIAN_POINT('Ctrl Pts',(-61.4941778114159,-96.9914532700303,
174.836726297116));
#39124=CARTESIAN_POINT('Ctrl Pts',(-60.4923762343183,-97.1925332396368,
173.529088919052));
#39125=CARTESIAN_POINT('Ctrl Pts',(-59.4905746572207,-97.3936132092432,
172.221451540989));
#39126=CARTESIAN_POINT('Ctrl Pts',(-57.8656753919855,-97.661119555255,172.016274058689));
#39127=CARTESIAN_POINT('Ctrl Pts',(-56.2407761267504,-97.9286259012667,
171.81109657639));
#39128=CARTESIAN_POINT('Ctrl Pts',(-54.9504447079354,-98.1604650796376,
172.828569176292));
#39129=CARTESIAN_POINT('Ctrl Pts',(-53.6601132891204,-98.3923042580085,
173.846041776195));
#39130=CARTESIAN_POINT('Ctrl Pts',(-53.4660299443843,-98.5072760677652,
175.490142808619));
#39131=CARTESIAN_POINT('Ctrl Pts',(-53.2719465996483,-98.6222478775218,
177.134243841043));
#39132=CARTESIAN_POINT('Ctrl Pts',(-54.2936243025799,-98.607611437226,178.441881219107));
#39133=CARTESIAN_POINT('Ctrl Pts',(-55.3153020055115,-98.5929749969302,
179.74951859717));
#39134=CARTESIAN_POINT('Ctrl Pts',(-56.9600773965807,-98.5119121802292,
179.954696079469));
#39135=CARTESIAN_POINT('Ctrl Pts',(-58.6048527876499,-98.4308493635282,
180.159873561769));
#39136=CARTESIAN_POINT('Ctrl Pts',(-59.9150603322989,-98.385453714468,179.142400961866));
#39137=CARTESIAN_POINT('Ctrl Pts',(-61.2252678769479,-98.3400580654078,
178.124928361964));
#39138=CARTESIAN_POINT('Ctrl Pts',(-61.439227347518,-98.4115297849618,176.48082732954));
#39139=CARTESIAN_POINT('Ctrl Pts',(-61.6531868180881,-98.4830015045159,
174.836726297116));
#39140=CARTESIAN_POINT('Ctrl Pts',(-60.6513852409905,-98.6840814741224,
173.529088919052));
#39141=CARTESIAN_POINT('Ctrl Pts',(-59.6495836638929,-98.8851614437288,
172.221451540989));
#39142=CARTESIAN_POINT('Ctrl Pts',(-58.0246843986578,-99.1526677897406,
172.016274058689));
#39143=CARTESIAN_POINT('Ctrl Pts',(-56.3997851334226,-99.4201741357523,
171.81109657639));
#39144=CARTESIAN_POINT('Ctrl Pts',(-55.1094537146076,-99.6520133141232,
172.828569176292));
#39145=CARTESIAN_POINT('Ctrl Pts',(-53.8191222957926,-99.8838524924941,
173.846041776195));
#39146=CARTESIAN_POINT('Ctrl Pts',(-53.6250389510566,-99.9988243022507,
175.490142808619));
#39147=CARTESIAN_POINT('Ctrl Pts',(-53.4309556063205,-100.113796112007,
177.134243841043));
#39148=CARTESIAN_POINT('Ctrl Pts',(-54.4526333092521,-100.099159671712,
178.441881219107));
#39149=CARTESIAN_POINT('Ctrl Pts',(-55.4743110121837,-100.084523231416,
179.74951859717));
#39150=CARTESIAN_POINT('Ctrl Pts',(-57.1190864032529,-100.003460414715,
179.954696079469));
#39151=CARTESIAN_POINT('Ctrl Pts',(-58.7638617943221,-99.9223975980138,
180.159873561769));
#39152=CARTESIAN_POINT('Ctrl Pts',(-60.0740693389711,-99.8770019489536,
179.142400961866));
#39153=CARTESIAN_POINT('Ctrl Pts',(-61.3842768836201,-99.8316062998934,
178.124928361964));
#39154=CARTESIAN_POINT('Ctrl Pts',(-61.5982363541902,-99.9030780194474,
176.48082732954));
#39155=CARTESIAN_POINT('Ctrl Pts',(-61.8121958247603,-99.9745497390015,
174.836726297116));
#39156=CARTESIAN_POINT('Ctrl Pts',(-60.8103942476627,-100.175629708608,
173.529088919052));
#39157=CARTESIAN_POINT('Ctrl Pts',(-59.8085926705652,-100.376709678214,
172.221451540989));
#39158=CARTESIAN_POINT('Ctrl Pts',(-58.18369340533,-100.644216024226,172.016274058689));
#39159=CARTESIAN_POINT('Ctrl Pts',(-56.5587941400948,-100.911722370238,
171.81109657639));
#39160=CARTESIAN_POINT('Ctrl Pts',(-55.2684627212798,-101.143561548609,
172.828569176292));
#39161=CARTESIAN_POINT('Ctrl Pts',(-53.9781313024648,-101.37540072698,173.846041776195));
#39162=CARTESIAN_POINT('Ctrl Pts',(-53.7840479577288,-101.490372536736,
175.490142808619));
#39163=CARTESIAN_POINT('Ctrl Pts',(-53.5899646129927,-101.605344346493,
177.134243841043));
#39164=CARTESIAN_POINT('Ctrl Pts',(-54.6116423159243,-101.590707906197,
178.441881219107));
#39165=CARTESIAN_POINT('Ctrl Pts',(-55.6333200188559,-101.576071465901,
179.74951859717));
#39166=CARTESIAN_POINT('Ctrl Pts',(-57.2780954099251,-101.4950086492,179.954696079469));
#39167=CARTESIAN_POINT('Ctrl Pts',(-58.9228708009943,-101.413945832499,
180.159873561769));
#39168=CARTESIAN_POINT('Ctrl Pts',(-60.2330783456433,-101.368550183439,
179.142400961866));
#39169=CARTESIAN_POINT('Ctrl Pts',(-61.5432858902924,-101.323154534379,
178.124928361964));
#39170=CARTESIAN_POINT('Ctrl Pts',(-61.7572453608625,-101.394626253933,
176.48082732954));
#39171=CARTESIAN_POINT('Ctrl Pts',(-61.9712048314325,-101.466097973487,
174.836726297116));
#39172=CARTESIAN_POINT('Ctrl Pts',(-60.969403254335,-101.667177943094,173.529088919052));
#39173=CARTESIAN_POINT('Ctrl Pts',(-59.9676016772374,-101.8682579127,172.221451540989));
#39174=CARTESIAN_POINT('Ctrl Pts',(-58.3427024120022,-102.135764258712,
172.016274058689));
#39175=CARTESIAN_POINT('Ctrl Pts',(-56.7178031467671,-102.403270604724,
171.81109657639));
#39176=CARTESIAN_POINT('Ctrl Pts',(-55.4274717279521,-102.635109783094,
172.828569176292));
#39177=CARTESIAN_POINT('Ctrl Pts',(-54.1371403091371,-102.866948961465,
173.846041776195));
#39178=CARTESIAN_POINT('Ctrl Pts',(-53.943056964401,-102.981920771222,175.490142808619));
#39179=CARTESIAN_POINT('Ctrl Pts',(-53.748973619665,-103.096892580979,177.134243841043));
#39180=CARTESIAN_POINT('Ctrl Pts',(-54.7706513225966,-103.082256140683,
178.441881219107));
#39181=CARTESIAN_POINT('Ctrl Pts',(-55.7923290255282,-103.067619700387,
179.74951859717));
#39182=CARTESIAN_POINT('Ctrl Pts',(-57.4371044165974,-102.986556883686,
179.954696079469));
#39183=CARTESIAN_POINT('Ctrl Pts',(-59.0818798076666,-102.905494066985,
180.159873561769));
#39184=CARTESIAN_POINT('Ctrl Pts',(-60.3920873523156,-102.860098417925,
179.142400961866));
#39185=CARTESIAN_POINT('Ctrl Pts',(-61.7022948969646,-102.814702768865,
178.124928361964));
#39186=CARTESIAN_POINT('Ctrl Pts',(-61.9162543675347,-102.886174488419,
176.48082732954));
#39187=CARTESIAN_POINT('Ctrl Pts',(-62.1302138381048,-102.957646207973,
174.836726297116));
#39188=CARTESIAN_POINT('Ctrl Pts',(-61.1284122610072,-103.158726177579,
173.529088919052));
#39189=CARTESIAN_POINT('Ctrl Pts',(-60.1266106839096,-103.359806147186,
172.221451540989));
#39190=CARTESIAN_POINT('Ctrl Pts',(-58.5017114186745,-103.627312493197,
172.016274058689));
#39191=CARTESIAN_POINT('Ctrl Pts',(-56.8768121534393,-103.894818839209,
171.81109657639));
#39192=CARTESIAN_POINT('Ctrl Pts',(-55.5864807346243,-104.12665801758,172.828569176292));
#39193=CARTESIAN_POINT('Ctrl Pts',(-54.2961493158093,-104.358497195951,
173.846041776195));
#39194=CARTESIAN_POINT('Ctrl Pts',(-54.1020659710732,-104.473469005708,
175.490142808619));
#39195=CARTESIAN_POINT('Ctrl Pts',(-53.9079826263372,-104.588440815464,
177.134243841043));
#39196=CARTESIAN_POINT('Ctrl Pts',(-54.9296603292688,-104.573804375168,
178.441881219107));
#39197=CARTESIAN_POINT('Ctrl Pts',(-55.9513380322004,-104.559167934873,
179.74951859717));
#39198=CARTESIAN_POINT('Ctrl Pts',(-57.5961134232696,-104.478105118172,
179.954696079469));
#39199=CARTESIAN_POINT('Ctrl Pts',(-59.2408888143388,-104.397042301471,
180.159873561769));
#39200=CARTESIAN_POINT('Ctrl Pts',(-60.5510963589878,-104.35164665241,179.142400961866));
#39201=CARTESIAN_POINT('Ctrl Pts',(-61.8613039036368,-104.30625100335,178.124928361964));
#39202=CARTESIAN_POINT('Ctrl Pts',(-62.0752633742069,-104.377722722904,
176.48082732954));
#39203=CARTESIAN_POINT('Ctrl Pts',(-62.289222844777,-104.449194442458,174.836726297116));
#39204=CARTESIAN_POINT('Ctrl Pts',(-61.2874212676794,-104.650274412065,
173.529088919052));
#39205=CARTESIAN_POINT('Ctrl Pts',(-60.2856196905818,-104.851354381671,
172.221451540989));
#39206=CARTESIAN_POINT('Ctrl Pts',(-58.6607204253467,-105.118860727683,
172.016274058689));
#39207=CARTESIAN_POINT('Ctrl Pts',(-57.0358211601115,-105.386367073695,
171.81109657639));
#39208=CARTESIAN_POINT('Ctrl Pts',(-55.7454897412965,-105.618206252066,
172.828569176292));
#39209=CARTESIAN_POINT('Ctrl Pts',(-54.4551583224815,-105.850045430437,
173.846041776195));
#39210=CARTESIAN_POINT('Ctrl Pts',(-54.2610749777455,-105.965017240193,
175.490142808619));
#39211=CARTESIAN_POINT('Ctrl Pts',(-54.0669916330094,-106.07998904995,177.134243841043));
#39212=CARTESIAN_POINT('Ctrl Pts',(-55.088669335941,-106.065352609654,178.441881219107));
#39213=CARTESIAN_POINT('Ctrl Pts',(-56.1103470388726,-106.050716169358,
179.74951859717));
#39214=CARTESIAN_POINT('Ctrl Pts',(-57.7551224299418,-105.969653352657,
179.954696079469));
#39215=CARTESIAN_POINT('Ctrl Pts',(-59.399897821011,-105.888590535956,180.159873561769));
#39216=CARTESIAN_POINT('Ctrl Pts',(-60.71010536566,-105.843194886896,179.142400961866));
#39217=CARTESIAN_POINT('Ctrl Pts',(-62.0203129103091,-105.797799237836,
178.124928361964));
#39218=CARTESIAN_POINT('Ctrl Pts',(-62.2342723808791,-105.86927095739,176.48082732954));
#39219=CARTESIAN_POINT('Ctrl Pts',(-62.4482318514492,-105.940742676944,
174.836726297116));
#39220=CARTESIAN_POINT('Ctrl Pts',(-61.4464302743516,-106.14182264655,173.529088919052));
#39221=CARTESIAN_POINT('Ctrl Pts',(-60.4446286972541,-106.342902616157,
172.221451540989));
#39222=CARTESIAN_POINT('Ctrl Pts',(-58.8197294320189,-106.610408962169,
172.016274058689));
#39223=CARTESIAN_POINT('Ctrl Pts',(-57.1948301667837,-106.87791530818,171.81109657639));
#39224=CARTESIAN_POINT('Ctrl Pts',(-55.9044987479688,-107.109754486551,
172.828569176292));
#39225=CARTESIAN_POINT('Ctrl Pts',(-54.6141673291538,-107.341593664922,
173.846041776195));
#39226=CARTESIAN_POINT('Ctrl Pts',(-54.4200839844177,-107.456565474679,
175.490142808619));
#39227=CARTESIAN_POINT('Ctrl Pts',(-54.2260006396817,-107.571537284435,
177.134243841043));
#39228=CARTESIAN_POINT('Ctrl Pts',(-55.2476783426132,-107.55690084414,178.441881219107));
#39229=CARTESIAN_POINT('Ctrl Pts',(-56.2693560455449,-107.542264403844,
179.74951859717));
#39230=CARTESIAN_POINT('Ctrl Pts',(-57.914131436614,-107.461201587143,179.954696079469));
#39231=CARTESIAN_POINT('Ctrl Pts',(-59.5589068276832,-107.380138770442,
180.159873561769));
#39232=CARTESIAN_POINT('Ctrl Pts',(-60.8691143723323,-107.334743121382,
179.142400961866));
#39233=CARTESIAN_POINT('Ctrl Pts',(-62.1793219169813,-107.289347472321,
178.124928361964));
#39234=CARTESIAN_POINT('Ctrl Pts',(-62.3932813875514,-107.360819191875,
176.48082732954));
#39235=CARTESIAN_POINT('Ctrl Pts',(-62.6072408581214,-107.43229091143,174.836726297116));
#39236=CARTESIAN_POINT('Ctrl Pts',(-61.6054392810239,-107.633370881036,
173.529088919052));
#39237=CARTESIAN_POINT('Ctrl Pts',(-60.6036377039263,-107.834450850642,
172.221451540989));
#39238=CARTESIAN_POINT('Ctrl Pts',(-58.9787384386911,-108.101957196654,
172.016274058689));
#39239=CARTESIAN_POINT('Ctrl Pts',(-57.353839173456,-108.369463542666,171.81109657639));
#39240=CARTESIAN_POINT('Ctrl Pts',(-56.063507754641,-108.601302721037,172.828569176292));
#39241=CARTESIAN_POINT('Ctrl Pts',(-54.773176335826,-108.833141899408,173.846041776195));
#39242=CARTESIAN_POINT('Ctrl Pts',(-54.5790929910899,-108.948113709164,
175.490142808619));
#39243=CARTESIAN_POINT('Ctrl Pts',(-54.3850096463539,-109.063085518921,
177.134243841043));
#39244=CARTESIAN_POINT('Ctrl Pts',(-55.4066873492855,-109.048449078625,
178.441881219107));
#39245=CARTESIAN_POINT('Ctrl Pts',(-56.4283650522171,-109.033812638329,
179.74951859717));
#39246=CARTESIAN_POINT('Ctrl Pts',(-58.0731404432863,-108.952749821628,
179.954696079469));
#39247=CARTESIAN_POINT('Ctrl Pts',(-59.7179158343555,-108.871687004927,
180.159873561769));
#39248=CARTESIAN_POINT('Ctrl Pts',(-61.0281233790045,-108.826291355867,
179.142400961866));
#39249=CARTESIAN_POINT('Ctrl Pts',(-62.3383309236535,-108.780895706807,
178.124928361964));
#39250=CARTESIAN_POINT('Ctrl Pts',(-62.5522903942236,-108.852367426361,
176.48082732954));
#39251=CARTESIAN_POINT('Ctrl Pts',(-62.7662498647937,-108.923839145915,
174.836726297116));
#39252=CARTESIAN_POINT('Ctrl Pts',(-61.7644482876961,-109.124919115522,
173.529088919052));
#39253=CARTESIAN_POINT('Ctrl Pts',(-60.7626467105985,-109.325999085128,
172.221451540989));
#39254=CARTESIAN_POINT('Ctrl Pts',(-59.1377474453634,-109.59350543114,172.016274058689));
#39255=CARTESIAN_POINT('Ctrl Pts',(-57.5128481801282,-109.861011777151,
171.81109657639));
#39256=CARTESIAN_POINT('Ctrl Pts',(-56.2225167613132,-110.092850955522,
172.828569176292));
#39257=CARTESIAN_POINT('Ctrl Pts',(-54.9321853424982,-110.324690133893,
173.846041776195));
#39258=CARTESIAN_POINT('Ctrl Pts',(-54.7381019977622,-110.43966194365,175.490142808619));
#39259=CARTESIAN_POINT('Ctrl Pts',(-54.5440186530261,-110.554633753407,
177.134243841043));
#39260=CARTESIAN_POINT('Ctrl Pts',(-55.5656963559577,-110.539997313111,
178.441881219107));
#39261=CARTESIAN_POINT('Ctrl Pts',(-56.5873740588893,-110.525360872815,
179.74951859717));
#39262=CARTESIAN_POINT('Ctrl Pts',(-58.2321494499585,-110.444298056114,
179.954696079469));
#39263=CARTESIAN_POINT('Ctrl Pts',(-59.8769248410277,-110.363235239413,
180.159873561769));
#39264=CARTESIAN_POINT('Ctrl Pts',(-61.1871323856767,-110.317839590353,
179.142400961866));
#39265=CARTESIAN_POINT('Ctrl Pts',(-62.4973399303257,-110.272443941293,
178.124928361964));
#39266=CARTESIAN_POINT('Ctrl Pts',(-62.7112994008958,-110.343915660847,
176.48082732954));
#39267=CARTESIAN_POINT('Ctrl Pts',(-62.9252588714659,-110.415387380401,
174.836726297116));
#39268=CARTESIAN_POINT('Ctrl Pts',(-61.9234572943683,-110.616467350007,
173.529088919052));
#39269=CARTESIAN_POINT('Ctrl Pts',(-60.9216557172708,-110.817547319614,
172.221451540989));
#39270=CARTESIAN_POINT('Ctrl Pts',(-59.2967564520356,-111.085053665625,
172.016274058689));
#39271=CARTESIAN_POINT('Ctrl Pts',(-57.6718571868004,-111.352560011637,
171.81109657639));
#39272=CARTESIAN_POINT('Ctrl Pts',(-56.3815257679854,-111.584399190008,
172.828569176292));
#39273=CARTESIAN_POINT('Ctrl Pts',(-55.0911943491704,-111.816238368379,
173.846041776195));
#39274=CARTESIAN_POINT('Ctrl Pts',(-54.8971110044344,-111.931210178136,
175.490142808619));
#39275=CARTESIAN_POINT('Ctrl Pts',(-54.7030276596983,-112.046181987892,
177.134243841043));
#39276=CARTESIAN_POINT('Ctrl Pts',(-55.7247053626299,-112.031545547596,
178.441881219107));
#39277=CARTESIAN_POINT('Ctrl Pts',(-56.7463830655615,-112.016909107301,
179.74951859717));
#39278=CARTESIAN_POINT('Ctrl Pts',(-58.3911584566307,-111.9358462906,179.954696079469));
#39279=CARTESIAN_POINT('Ctrl Pts',(-60.0359338476999,-111.854783473899,
180.159873561769));
#39280=CARTESIAN_POINT('Ctrl Pts',(-61.3461413923489,-111.809387824838,
179.142400961866));
#39281=CARTESIAN_POINT('Ctrl Pts',(-62.656348936998,-111.763992175778,178.124928361964));
#39282=CARTESIAN_POINT('Ctrl Pts',(-62.870308407568,-111.835463895332,176.48082732954));
#39283=CARTESIAN_POINT('Ctrl Pts',(-63.0842678781381,-111.906935614886,
174.836726297116));
#39284=CARTESIAN_POINT('Ctrl Pts',(-62.0824663010406,-112.108015584493,
173.529088919052));
#39285=CARTESIAN_POINT('Ctrl Pts',(-61.080664723943,-112.309095554099,172.221451540989));
#39286=CARTESIAN_POINT('Ctrl Pts',(-59.4557654587078,-112.576601900111,
172.016274058689));
#39287=CARTESIAN_POINT('Ctrl Pts',(-57.8308661934727,-112.844108246123,
171.81109657639));
#39288=CARTESIAN_POINT('Ctrl Pts',(-56.5405347746577,-113.075947424494,
172.828569176292));
#39289=CARTESIAN_POINT('Ctrl Pts',(-55.2502033558427,-113.307786602865,
173.846041776195));
#39290=CARTESIAN_POINT('Ctrl Pts',(-55.0561200111066,-113.422758412621,
175.490142808619));
#39291=CARTESIAN_POINT('Ctrl Pts',(-54.8620366663706,-113.537730222378,
177.134243841043));
#39292=CARTESIAN_POINT('Ctrl Pts',(-55.8837143693022,-113.523093782082,
178.441881219107));
#39293=CARTESIAN_POINT('Ctrl Pts',(-56.9053920722338,-113.508457341786,
179.74951859717));
#39294=CARTESIAN_POINT('Ctrl Pts',(-58.550167463303,-113.427394525085,179.954696079469));
#39295=CARTESIAN_POINT('Ctrl Pts',(-60.1949428543721,-113.346331708384,
180.159873561769));
#39296=CARTESIAN_POINT('Ctrl Pts',(-61.5051503990212,-113.300936059324,
179.142400961866));
#39297=CARTESIAN_POINT('Ctrl Pts',(-62.8153579436702,-113.255540410264,
178.124928361964));
#39298=CARTESIAN_POINT('Ctrl Pts',(-63.0293174142403,-113.327012129818,
176.48082732954));
#39299=CARTESIAN_POINT('Ctrl Pts',(-63.2432768848103,-113.398483849372,
174.836726297116));
#39300=CARTESIAN_POINT('Ctrl Pts',(-62.2414753077128,-113.599563818978,
173.529088919052));
#39301=CARTESIAN_POINT('Ctrl Pts',(-61.2396737306152,-113.800643788585,
172.221451540989));
#39302=CARTESIAN_POINT('Ctrl Pts',(-59.6147744653801,-114.068150134597,
172.016274058689));
#39303=CARTESIAN_POINT('Ctrl Pts',(-57.9898752001449,-114.335656480608,
171.81109657639));
#39304=CARTESIAN_POINT('Ctrl Pts',(-56.6995437813299,-114.567495658979,
172.828569176292));
#39305=CARTESIAN_POINT('Ctrl Pts',(-55.4092123625149,-114.79933483735,173.846041776195));
#39306=CARTESIAN_POINT('Ctrl Pts',(-55.2151290177788,-114.914306647107,
175.490142808619));
#39307=CARTESIAN_POINT('Ctrl Pts',(-55.0210456730428,-115.029278456863,
177.134243841043));
#39308=CARTESIAN_POINT('Ctrl Pts',(-56.0427233759744,-115.014642016568,
178.441881219107));
#39309=CARTESIAN_POINT('Ctrl Pts',(-57.064401078906,-115.000005576272,179.74951859717));
#39310=CARTESIAN_POINT('Ctrl Pts',(-58.7091764699752,-114.918942759571,
179.954696079469));
#39311=CARTESIAN_POINT('Ctrl Pts',(-60.3539518610444,-114.83787994287,180.159873561769));
#39312=CARTESIAN_POINT('Ctrl Pts',(-61.6641594056934,-114.79248429381,179.142400961866));
#39313=CARTESIAN_POINT('Ctrl Pts',(-62.9743669503424,-114.747088644749,
178.124928361964));
#39314=CARTESIAN_POINT('Ctrl Pts',(-63.1883264209125,-114.818560364303,
176.48082732954));
#39315=CARTESIAN_POINT('Ctrl Pts',(-63.4022858914826,-114.890032083858,
174.836726297116));
#39316=CARTESIAN_POINT('Ctrl Pts',(-62.400484314385,-115.091112053464,173.529088919052));
#39317=CARTESIAN_POINT('Ctrl Pts',(-61.3986827372874,-115.29219202307,172.221451540989));
#39318=CARTESIAN_POINT('Ctrl Pts',(-59.7737834720523,-115.559698369082,
172.016274058689));
#39319=CARTESIAN_POINT('Ctrl Pts',(-58.1488842068171,-115.827204715094,
171.81109657639));
#39320=CARTESIAN_POINT('Ctrl Pts',(-56.8585527880021,-116.059043893465,
172.828569176292));
#39321=CARTESIAN_POINT('Ctrl Pts',(-55.5682213691871,-116.290883071836,
173.846041776195));
#39322=CARTESIAN_POINT('Ctrl Pts',(-55.3741380244511,-116.405854881592,
175.490142808619));
#39323=CARTESIAN_POINT('Ctrl Pts',(-55.180054679715,-116.520826691349,177.134243841043));
#39324=CARTESIAN_POINT('Ctrl Pts',(-56.2017323826466,-116.506190251053,
178.441881219107));
#39325=CARTESIAN_POINT('Ctrl Pts',(-57.2234100855782,-116.491553810757,
179.74951859717));
#39326=CARTESIAN_POINT('Ctrl Pts',(-58.8681854766474,-116.410490994056,
179.954696079469));
#39327=CARTESIAN_POINT('Ctrl Pts',(-60.5129608677166,-116.329428177355,
180.159873561769));
#39328=CARTESIAN_POINT('Ctrl Pts',(-61.8231684123656,-116.284032528295,
179.142400961866));
#39329=CARTESIAN_POINT('Ctrl Pts',(-63.1333759570147,-116.238636879235,
178.124928361964));
#39330=CARTESIAN_POINT('Ctrl Pts',(-63.3473354275847,-116.310108598789,
176.48082732954));
#39331=CARTESIAN_POINT('Ctrl Pts',(-63.5612948981548,-116.381580318343,
174.836726297116));
#39332=CARTESIAN_POINT('Ctrl Pts',(-62.5594933210572,-116.58266028795,173.529088919052));
#39333=CARTESIAN_POINT('Ctrl Pts',(-61.5576917439597,-116.783740257556,
172.221451540989));
#39334=CARTESIAN_POINT('Ctrl Pts',(-59.9327924787245,-117.051246603568,
172.016274058689));
#39335=CARTESIAN_POINT('Ctrl Pts',(-58.3078932134893,-117.318752949579,
171.81109657639));
#39336=CARTESIAN_POINT('Ctrl Pts',(-57.0175617946743,-117.55059212795,172.828569176292));
#39337=CARTESIAN_POINT('Ctrl Pts',(-55.7272303758593,-117.782431306321,
173.846041776195));
#39338=CARTESIAN_POINT('Ctrl Pts',(-55.5331470311233,-117.897403116078,
175.490142808619));
#39339=CARTESIAN_POINT('Ctrl Pts',(-55.3390636863872,-118.012374925835,
177.134243841043));
#39340=CARTESIAN_POINT('Ctrl Pts',(-56.3607413893188,-117.997738485539,
178.441881219107));
#39341=CARTESIAN_POINT('Ctrl Pts',(-57.3824190922504,-117.983102045243,
179.74951859717));
#39342=CARTESIAN_POINT('Ctrl Pts',(-59.0271944833196,-117.902039228542,
179.954696079469));
#39343=CARTESIAN_POINT('Ctrl Pts',(-60.6719698743888,-117.820976411841,
180.159873561769));
#39344=CARTESIAN_POINT('Ctrl Pts',(-61.9821774190378,-117.775580762781,
179.142400961866));
#39345=CARTESIAN_POINT('Ctrl Pts',(-63.2923849636869,-117.730185113721,
178.124928361964));
#39346=CARTESIAN_POINT('Ctrl Pts',(-63.506344434257,-117.801656833275,176.48082732954));
#39347=CARTESIAN_POINT('Ctrl Pts',(-63.720303904827,-117.873128552829,174.836726297116));
#39348=CARTESIAN_POINT('Ctrl Pts',(-62.7185023277295,-118.074208522435,
173.529088919052));
#39349=CARTESIAN_POINT('Ctrl Pts',(-61.7167007506319,-118.275288492042,
172.221451540989));
#39350=CARTESIAN_POINT('Ctrl Pts',(-60.0918014853967,-118.542794838053,
172.016274058689));
#39351=CARTESIAN_POINT('Ctrl Pts',(-58.4669022201616,-118.810301184065,
171.81109657639));
#39352=CARTESIAN_POINT('Ctrl Pts',(-57.1765708013466,-119.042140362436,
172.828569176292));
#39353=CARTESIAN_POINT('Ctrl Pts',(-55.8862393825316,-119.273979540807,
173.846041776195));
#39354=CARTESIAN_POINT('Ctrl Pts',(-55.6921560377955,-119.388951350564,
175.490142808619));
#39355=CARTESIAN_POINT('Ctrl Pts',(-55.4980726930595,-119.50392316032,177.134243841043));
#39356=CARTESIAN_POINT('Ctrl Pts',(-56.5197503959911,-119.489286720024,
178.441881219107));
#39357=CARTESIAN_POINT('Ctrl Pts',(-57.5414280989227,-119.474650279729,
179.74951859717));
#39358=CARTESIAN_POINT('Ctrl Pts',(-59.1862034899919,-119.393587463028,
179.954696079469));
#39359=CARTESIAN_POINT('Ctrl Pts',(-60.8309788810611,-119.312524646327,
180.159873561769));
#39360=CARTESIAN_POINT('Ctrl Pts',(-62.1411864257101,-119.267128997266,
179.142400961866));
#39361=CARTESIAN_POINT('Ctrl Pts',(-63.4513939703591,-119.221733348206,
178.124928361964));
#39362=CARTESIAN_POINT('Ctrl Pts',(-63.6653534409292,-119.29320506776,176.48082732954));
#39363=CARTESIAN_POINT('Ctrl Pts',(-63.8793129114993,-119.364676787314,
174.836726297116));
#39364=CARTESIAN_POINT('Ctrl Pts',(-62.8775113344017,-119.565756756921,
173.529088919052));
#39365=CARTESIAN_POINT('Ctrl Pts',(-61.8757097573041,-119.766836726527,
172.221451540989));
#39366=CARTESIAN_POINT('Ctrl Pts',(-60.250810492069,-120.034343072539,172.016274058689));
#39367=CARTESIAN_POINT('Ctrl Pts',(-58.6259112268338,-120.301849418551,
171.81109657639));
#39368=CARTESIAN_POINT('Ctrl Pts',(-57.3355798080188,-120.533688596922,
172.828569176292));
#39369=CARTESIAN_POINT('Ctrl Pts',(-56.0452483892038,-120.765527775293,
173.846041776195));
#39370=CARTESIAN_POINT('Ctrl Pts',(-55.8511650444677,-120.880499585049,
175.490142808619));
#39371=CARTESIAN_POINT('Ctrl Pts',(-55.6570816997317,-120.995471394806,
177.134243841043));
#39372=CARTESIAN_POINT('Ctrl Pts',(-56.6787594026633,-120.98083495451,178.441881219107));
#39373=CARTESIAN_POINT('Ctrl Pts',(-57.7004371055949,-120.966198514214,
179.74951859717));
#39374=CARTESIAN_POINT('Ctrl Pts',(-59.3452124966641,-120.885135697513,
179.954696079469));
#39375=CARTESIAN_POINT('Ctrl Pts',(-60.9899878877333,-120.804072880812,
180.159873561769));
#39376=CARTESIAN_POINT('Ctrl Pts',(-62.3001954323823,-120.758677231752,
179.142400961866));
#39377=CARTESIAN_POINT('Ctrl Pts',(-63.6104029770313,-120.713281582692,
178.124928361964));
#39378=CARTESIAN_POINT('Ctrl Pts',(-63.8243624476014,-120.784753302246,
176.48082732954));
#39379=CARTESIAN_POINT('Ctrl Pts',(-64.0383219181715,-120.8562250218,174.836726297116));
#39380=CARTESIAN_POINT('Ctrl Pts',(-63.0365203410739,-121.057304991406,
173.529088919052));
#39381=CARTESIAN_POINT('Ctrl Pts',(-62.0347187639764,-121.258384961013,
172.221451540989));
#39382=CARTESIAN_POINT('Ctrl Pts',(-60.4098194987412,-121.525891307025,
172.016274058689));
#39383=CARTESIAN_POINT('Ctrl Pts',(-58.784920233506,-121.793397653036,171.81109657639));
#39384=CARTESIAN_POINT('Ctrl Pts',(-57.494588814691,-122.025236831407,172.828569176292));
#39385=CARTESIAN_POINT('Ctrl Pts',(-56.204257395876,-122.257076009778,173.846041776195));
#39386=CARTESIAN_POINT('Ctrl Pts',(-56.01017405114,-122.372047819535,175.490142808619));
#39387=CARTESIAN_POINT('Ctrl Pts',(-55.8160907064039,-122.487019629291,
177.134243841043));
#39388=CARTESIAN_POINT('Ctrl Pts',(-56.8377684093355,-122.472383188996,
178.441881219107));
#39389=CARTESIAN_POINT('Ctrl Pts',(-57.8594461122671,-122.4577467487,179.74951859717));
#39390=CARTESIAN_POINT('Ctrl Pts',(-59.5042215033363,-122.376683931999,
179.954696079469));
#39391=CARTESIAN_POINT('Ctrl Pts',(-61.1489968944055,-122.295621115298,
180.159873561769));
#39392=CARTESIAN_POINT('Ctrl Pts',(-62.4592044390545,-122.250225466238,
179.142400961866));
#39393=CARTESIAN_POINT('Ctrl Pts',(-63.7694119837035,-122.204829817177,
178.124928361964));
#39394=CARTESIAN_POINT('Ctrl Pts',(-63.9833714542736,-122.276301536731,
176.48082732954));
#39395=CARTESIAN_POINT('Ctrl Pts',(-64.1973309248437,-122.347773256285,
174.836726297116));
#39396=CARTESIAN_POINT('Ctrl Pts',(-63.1955293477461,-122.548853225892,
173.529088919052));
#39397=CARTESIAN_POINT('Ctrl Pts',(-62.1937277706486,-122.749933195498,
172.221451540989));
#39398=CARTESIAN_POINT('Ctrl Pts',(-60.5688285054134,-123.01743954151,172.016274058689));
#39399=CARTESIAN_POINT('Ctrl Pts',(-58.9439292401782,-123.284945887522,
171.81109657639));
#39400=CARTESIAN_POINT('Ctrl Pts',(-57.6535978213633,-123.516785065893,
172.828569176292));
#39401=CARTESIAN_POINT('Ctrl Pts',(-56.3632664025483,-123.748624244264,
173.846041776195));
#39402=CARTESIAN_POINT('Ctrl Pts',(-56.1691830578122,-123.86359605402,175.490142808619));
#39403=CARTESIAN_POINT('Ctrl Pts',(-55.9750997130761,-123.978567863777,
177.134243841043));
#39404=CARTESIAN_POINT('Ctrl Pts',(-56.9967774160077,-123.963931423481,
178.441881219107));
#39405=CARTESIAN_POINT('Ctrl Pts',(-58.0184551189394,-123.949294983185,
179.74951859717));
#39406=CARTESIAN_POINT('Ctrl Pts',(-59.6632305100085,-123.868232166484,
179.954696079469));
#39407=CARTESIAN_POINT('Ctrl Pts',(-61.3080059010777,-123.787169349783,
180.159873561769));
#39408=CARTESIAN_POINT('Ctrl Pts',(-62.6182134457268,-123.741773700723,
179.142400961866));
#39409=CARTESIAN_POINT('Ctrl Pts',(-63.9284209903758,-123.696378051663,
178.124928361964));
#39410=CARTESIAN_POINT('Ctrl Pts',(-64.1423804609459,-123.767849771217,
176.48082732954));
#39411=CARTESIAN_POINT('Ctrl Pts',(-64.3563399315159,-123.839321490771,
174.836726297116));
#39412=CARTESIAN_POINT('Ctrl Pts',(-63.3545383544184,-124.040401460378,
173.529088919052));
#39413=CARTESIAN_POINT('Ctrl Pts',(-62.3527367773208,-124.241481429984,
172.221451540989));
#39414=CARTESIAN_POINT('Ctrl Pts',(-60.7278375120856,-124.508987775996,
172.016274058689));
#39415=CARTESIAN_POINT('Ctrl Pts',(-59.1029382468505,-124.776494122007,
171.81109657639));
#39416=CARTESIAN_POINT('Ctrl Pts',(-57.8126068280355,-125.008333300378,
172.828569176292));
#39417=CARTESIAN_POINT('Ctrl Pts',(-56.5222754092205,-125.240172478749,
173.846041776195));
#39418=CARTESIAN_POINT('Ctrl Pts',(-56.3281920644844,-125.355144288506,
175.490142808619));
#39419=CARTESIAN_POINT('Ctrl Pts',(-56.1341087197484,-125.470116098263,
177.134243841043));
#39420=CARTESIAN_POINT('Ctrl Pts',(-57.15578642268,-125.455479657967,178.441881219107));
#39421=CARTESIAN_POINT('Ctrl Pts',(-58.1774641256116,-125.440843217671,
179.74951859717));
#39422=CARTESIAN_POINT('Ctrl Pts',(-59.8222395166808,-125.35978040097,179.954696079469));
#39423=CARTESIAN_POINT('Ctrl Pts',(-61.46701490775,-125.278717584269,180.159873561769));
#39424=CARTESIAN_POINT('Ctrl Pts',(-62.777222452399,-125.233321935209,179.142400961866));
#39425=CARTESIAN_POINT('Ctrl Pts',(-64.087429997048,-125.187926286149,178.124928361964));
#39426=CARTESIAN_POINT('Ctrl Pts',(-64.3013894676181,-125.259398005703,
176.48082732954));
#39427=CARTESIAN_POINT('Ctrl Pts',(-64.5153489381882,-125.330869725257,
174.836726297116));
#39428=CARTESIAN_POINT('Ctrl Pts',(-63.5135473610906,-125.531949694863,
173.529088919052));
#39429=CARTESIAN_POINT('Ctrl Pts',(-62.511745783993,-125.73302966447,172.221451540989));
#39430=CARTESIAN_POINT('Ctrl Pts',(-60.8868465187579,-126.000536010481,
172.016274058689));
#39431=CARTESIAN_POINT('Ctrl Pts',(-59.2619472535227,-126.268042356493,
171.81109657639));
#39432=CARTESIAN_POINT('Ctrl Pts',(-57.9716158347077,-126.499881534864,
172.828569176292));
#39433=CARTESIAN_POINT('Ctrl Pts',(-56.6812844158927,-126.731720713235,
173.846041776195));
#39434=CARTESIAN_POINT('Ctrl Pts',(-56.4872010711566,-126.846692522992,
175.490142808619));
#39435=CARTESIAN_POINT('Ctrl Pts',(-56.2931177264206,-126.961664332748,
177.134243841043));
#39436=CARTESIAN_POINT('Ctrl Pts',(-57.3147954293522,-126.947027892452,
178.441881219107));
#39437=CARTESIAN_POINT('Ctrl Pts',(-58.3364731322838,-126.932391452157,
179.74951859717));
#39438=CARTESIAN_POINT('Ctrl Pts',(-59.981248523353,-126.851328635456,179.954696079469));
#39439=CARTESIAN_POINT('Ctrl Pts',(-61.6260239144222,-126.770265818755,
180.159873561769));
#39440=CARTESIAN_POINT('Ctrl Pts',(-62.9362314590712,-126.724870169694,
179.142400961866));
#39441=CARTESIAN_POINT('Ctrl Pts',(-64.2464390037202,-126.679474520634,
178.124928361964));
#39442=CARTESIAN_POINT('Ctrl Pts',(-64.4603984742903,-126.750946240188,
176.48082732954));
#39443=CARTESIAN_POINT('Ctrl Pts',(-64.5291885105023,-126.7739250883,175.952232968864));
#39444=CARTESIAN_POINT('Ctrl Pts',(-64.4583706077394,-126.814016540979,
175.424797521489));
#39445=CARTESIAN_POINT('Ctrl Pts',(-50.179840660106,-67.6819454430842,175.490142424066));
#39446=CARTESIAN_POINT('Ctrl Pts',(-49.9857571569802,-67.7969172697262,
177.134244732869));
#39447=CARTESIAN_POINT('Ctrl Pts',(-51.0074356453643,-67.7822807456959,
178.441883126102));
#39448=CARTESIAN_POINT('Ctrl Pts',(-52.0291141337484,-67.7676442216657,
179.749521519335));
#39449=CARTESIAN_POINT('Ctrl Pts',(-53.6738907940049,-67.6865812696608,
179.954699160921));
#39450=CARTESIAN_POINT('Ctrl Pts',(-55.3186674542614,-67.6055183176559,
180.159876802508));
#39451=CARTESIAN_POINT('Ctrl Pts',(-56.6288760083597,-67.5601225609817,
179.142403412702));
#39452=CARTESIAN_POINT('Ctrl Pts',(-57.9390845624581,-67.5147268043074,
178.124930022896));
#39453=CARTESIAN_POINT('Ctrl Pts',(-58.1530441914179,-67.5861985069761,
176.480827714093));
#39454=CARTESIAN_POINT('Ctrl Pts',(-58.3670038203777,-67.6576702096448,
174.83672540529));
#39455=CARTESIAN_POINT('Ctrl Pts',(-57.3652014578276,-67.8587502629857,
173.529087012057));
#39456=CARTESIAN_POINT('Ctrl Pts',(-56.3633990952775,-68.0598303163267,
172.221448618824));
#39457=CARTESIAN_POINT('Ctrl Pts',(-54.7384985608551,-68.3273367976423,
172.016270977238));
#39458=CARTESIAN_POINT('Ctrl Pts',(-53.1135980264326,-68.5948432789578,
171.811093335651));
#39459=CARTESIAN_POINT('Ctrl Pts',(-51.8232655981683,-68.8266825649428,
172.828566725457));
#39460=CARTESIAN_POINT('Ctrl Pts',(-50.5329331699039,-69.0585218509277,
173.846040115263));
#39461=CARTESIAN_POINT('Ctrl Pts',(-50.3388496667782,-69.1734936775698,
175.490142424066));
#39462=CARTESIAN_POINT('Ctrl Pts',(-50.1447661636524,-69.2884655042118,
177.134244732869));
#39463=CARTESIAN_POINT('Ctrl Pts',(-51.1664446520366,-69.2738289801815,
178.441883126102));
#39464=CARTESIAN_POINT('Ctrl Pts',(-52.1881231404207,-69.2591924561513,
179.749521519335));
#39465=CARTESIAN_POINT('Ctrl Pts',(-53.8328998006771,-69.1781295041464,
179.954699160921));
#39466=CARTESIAN_POINT('Ctrl Pts',(-55.4776764609336,-69.0970665521415,
180.159876802508));
#39467=CARTESIAN_POINT('Ctrl Pts',(-56.787885015032,-69.0516707954673,179.142403412702));
#39468=CARTESIAN_POINT('Ctrl Pts',(-58.0980935691303,-69.006275038793,178.124930022896));
#39469=CARTESIAN_POINT('Ctrl Pts',(-58.3120531980901,-69.0777467414617,
176.480827714093));
#39470=CARTESIAN_POINT('Ctrl Pts',(-58.5260128270499,-69.1492184441304,
174.83672540529));
#39471=CARTESIAN_POINT('Ctrl Pts',(-57.5242104644998,-69.3502984974713,
173.529087012057));
#39472=CARTESIAN_POINT('Ctrl Pts',(-56.5224081019497,-69.5513785508123,
172.221448618824));
#39473=CARTESIAN_POINT('Ctrl Pts',(-54.8975075675273,-69.8188850321279,
172.016270977238));
#39474=CARTESIAN_POINT('Ctrl Pts',(-53.2726070331049,-70.0863915134434,
171.811093335651));
#39475=CARTESIAN_POINT('Ctrl Pts',(-51.9822746048405,-70.3182307994284,
172.828566725457));
#39476=CARTESIAN_POINT('Ctrl Pts',(-50.6919421765762,-70.5500700854134,
173.846040115263));
#39477=CARTESIAN_POINT('Ctrl Pts',(-50.4978586734504,-70.6650419120554,
175.490142424066));
#39478=CARTESIAN_POINT('Ctrl Pts',(-50.3037751703247,-70.7800137386974,
177.134244732869));
#39479=CARTESIAN_POINT('Ctrl Pts',(-51.3254536587088,-70.7653772146671,
178.441883126102));
#39480=CARTESIAN_POINT('Ctrl Pts',(-52.3471321470929,-70.7507406906369,
179.749521519335));
#39481=CARTESIAN_POINT('Ctrl Pts',(-53.9919088073493,-70.669677738632,179.954699160921));
#39482=CARTESIAN_POINT('Ctrl Pts',(-55.6366854676058,-70.5886147866271,
180.159876802508));
#39483=CARTESIAN_POINT('Ctrl Pts',(-56.9468940217042,-70.5432190299529,
179.142403412702));
#39484=CARTESIAN_POINT('Ctrl Pts',(-58.2571025758026,-70.4978232732786,
178.124930022896));
#39485=CARTESIAN_POINT('Ctrl Pts',(-58.4710622047623,-70.5692949759473,
176.480827714093));
#39486=CARTESIAN_POINT('Ctrl Pts',(-58.6850218337221,-70.640766678616,174.83672540529));
#39487=CARTESIAN_POINT('Ctrl Pts',(-57.683219471172,-70.8418467319569,173.529087012057));
#39488=CARTESIAN_POINT('Ctrl Pts',(-56.681417108622,-71.0429267852979,172.221448618824));
#39489=CARTESIAN_POINT('Ctrl Pts',(-55.0565165741995,-71.3104332666134,
172.016270977238));
#39490=CARTESIAN_POINT('Ctrl Pts',(-53.4316160397771,-71.577939747929,171.811093335651));
#39491=CARTESIAN_POINT('Ctrl Pts',(-52.1412836115127,-71.809779033914,172.828566725457));
#39492=CARTESIAN_POINT('Ctrl Pts',(-50.8509511832484,-72.0416183198989,
173.846040115263));
#39493=CARTESIAN_POINT('Ctrl Pts',(-50.6568676801226,-72.156590146541,175.490142424066));
#39494=CARTESIAN_POINT('Ctrl Pts',(-50.4627841769969,-72.271561973183,177.134244732869));
#39495=CARTESIAN_POINT('Ctrl Pts',(-51.484462665381,-72.2569254491527,178.441883126102));
#39496=CARTESIAN_POINT('Ctrl Pts',(-52.5061411537651,-72.2422889251225,
179.749521519335));
#39497=CARTESIAN_POINT('Ctrl Pts',(-54.1509178140216,-72.1612259731176,
179.954699160921));
#39498=CARTESIAN_POINT('Ctrl Pts',(-55.7956944742781,-72.0801630211127,
180.159876802508));
#39499=CARTESIAN_POINT('Ctrl Pts',(-57.1059030283764,-72.0347672644385,
179.142403412702));
#39500=CARTESIAN_POINT('Ctrl Pts',(-58.4161115824748,-71.9893715077642,
178.124930022896));
#39501=CARTESIAN_POINT('Ctrl Pts',(-58.6300712114346,-72.0608432104329,
176.480827714093));
#39502=CARTESIAN_POINT('Ctrl Pts',(-58.8440308403943,-72.1323149131016,
174.83672540529));
#39503=CARTESIAN_POINT('Ctrl Pts',(-57.8422284778443,-72.3333949664425,
173.529087012057));
#39504=CARTESIAN_POINT('Ctrl Pts',(-56.8404261152942,-72.5344750197835,
172.221448618824));
#39505=CARTESIAN_POINT('Ctrl Pts',(-55.2155255808718,-72.801981501099,172.016270977238));
#39506=CARTESIAN_POINT('Ctrl Pts',(-53.5906250464493,-73.0694879824146,
171.811093335651));
#39507=CARTESIAN_POINT('Ctrl Pts',(-52.300292618185,-73.3013272683996,172.828566725457));
#39508=CARTESIAN_POINT('Ctrl Pts',(-51.0099601899206,-73.5331665543845,
173.846040115263));
#39509=CARTESIAN_POINT('Ctrl Pts',(-50.8158766867949,-73.6481383810266,
175.490142424066));
#39510=CARTESIAN_POINT('Ctrl Pts',(-50.6217931836691,-73.7631102076686,
177.134244732869));
#39511=CARTESIAN_POINT('Ctrl Pts',(-51.6434716720532,-73.7484736836383,
178.441883126102));
#39512=CARTESIAN_POINT('Ctrl Pts',(-52.6651501604374,-73.7338371596081,
179.749521519335));
#39513=CARTESIAN_POINT('Ctrl Pts',(-54.3099268206938,-73.6527742076032,
179.954699160921));
#39514=CARTESIAN_POINT('Ctrl Pts',(-55.9547034809503,-73.5717112555984,
180.159876802508));
#39515=CARTESIAN_POINT('Ctrl Pts',(-57.2649120350486,-73.5263154989241,
179.142403412702));
#39516=CARTESIAN_POINT('Ctrl Pts',(-58.575120589147,-73.4809197422498,178.124930022896));
#39517=CARTESIAN_POINT('Ctrl Pts',(-58.7890802181068,-73.5523914449185,
176.480827714093));
#39518=CARTESIAN_POINT('Ctrl Pts',(-59.0030398470666,-73.6238631475872,
174.83672540529));
#39519=CARTESIAN_POINT('Ctrl Pts',(-58.0012374845165,-73.8249432009281,
173.529087012057));
#39520=CARTESIAN_POINT('Ctrl Pts',(-56.9994351219664,-74.0260232542691,
172.221448618824));
#39521=CARTESIAN_POINT('Ctrl Pts',(-55.374534587544,-74.2935297355847,172.016270977238));
#39522=CARTESIAN_POINT('Ctrl Pts',(-53.7496340531215,-74.5610362169002,
171.811093335651));
#39523=CARTESIAN_POINT('Ctrl Pts',(-52.4593016248572,-74.7928755028852,
172.828566725457));
#39524=CARTESIAN_POINT('Ctrl Pts',(-51.1689691965928,-75.0247147888702,
173.846040115263));
#39525=CARTESIAN_POINT('Ctrl Pts',(-50.9748856934671,-75.1396866155122,
175.490142424066));
#39526=CARTESIAN_POINT('Ctrl Pts',(-50.7808021903414,-75.2546584421542,
177.134244732869));
#39527=CARTESIAN_POINT('Ctrl Pts',(-51.8024806787255,-75.2400219181239,
178.441883126102));
#39528=CARTESIAN_POINT('Ctrl Pts',(-52.8241591671096,-75.2253853940937,
179.749521519335));
#39529=CARTESIAN_POINT('Ctrl Pts',(-54.468935827366,-75.1443224420888,179.954699160921));
#39530=CARTESIAN_POINT('Ctrl Pts',(-56.1137124876225,-75.0632594900839,
180.159876802508));
#39531=CARTESIAN_POINT('Ctrl Pts',(-57.4239210417209,-75.0178637334097,
179.142403412702));
#39532=CARTESIAN_POINT('Ctrl Pts',(-58.7341295958193,-74.9724679767354,
178.124930022896));
#39533=CARTESIAN_POINT('Ctrl Pts',(-58.948089224779,-75.0439396794041,176.480827714093));
#39534=CARTESIAN_POINT('Ctrl Pts',(-59.1620488537388,-75.1154113820728,
174.83672540529));
#39535=CARTESIAN_POINT('Ctrl Pts',(-58.1602464911887,-75.3164914354137,
173.529087012057));
#39536=CARTESIAN_POINT('Ctrl Pts',(-57.1584441286386,-75.5175714887547,
172.221448618824));
#39537=CARTESIAN_POINT('Ctrl Pts',(-55.5335435942162,-75.7850779700703,
172.016270977238));
#39538=CARTESIAN_POINT('Ctrl Pts',(-53.9086430597938,-76.0525844513858,
171.811093335651));
#39539=CARTESIAN_POINT('Ctrl Pts',(-52.6183106315294,-76.2844237373708,
172.828566725457));
#39540=CARTESIAN_POINT('Ctrl Pts',(-51.3279782032651,-76.5162630233557,
173.846040115263));
#39541=CARTESIAN_POINT('Ctrl Pts',(-51.1338947001393,-76.6312348499978,
175.490142424066));
#39542=CARTESIAN_POINT('Ctrl Pts',(-50.9398111970136,-76.7462066766398,
177.134244732869));
#39543=CARTESIAN_POINT('Ctrl Pts',(-51.9614896853977,-76.7315701526095,
178.441883126102));
#39544=CARTESIAN_POINT('Ctrl Pts',(-52.9831681737818,-76.7169336285793,
179.749521519335));
#39545=CARTESIAN_POINT('Ctrl Pts',(-54.6279448340383,-76.6358706765744,
179.954699160921));
#39546=CARTESIAN_POINT('Ctrl Pts',(-56.2727214942947,-76.5548077245695,
180.159876802508));
#39547=CARTESIAN_POINT('Ctrl Pts',(-57.5829300483931,-76.5094119678953,
179.142403412702));
#39548=CARTESIAN_POINT('Ctrl Pts',(-58.8931386024915,-76.464016211221,178.124930022896));
#39549=CARTESIAN_POINT('Ctrl Pts',(-59.1070982314513,-76.5354879138897,
176.480827714093));
#39550=CARTESIAN_POINT('Ctrl Pts',(-59.321057860411,-76.6069596165584,174.83672540529));
#39551=CARTESIAN_POINT('Ctrl Pts',(-58.319255497861,-76.8080396698993,173.529087012057));
#39552=CARTESIAN_POINT('Ctrl Pts',(-57.3174531353109,-77.0091197232403,
172.221448618824));
#39553=CARTESIAN_POINT('Ctrl Pts',(-55.6925526008884,-77.2766262045558,
172.016270977238));
#39554=CARTESIAN_POINT('Ctrl Pts',(-54.067652066466,-77.5441326858714,171.811093335651));
#39555=CARTESIAN_POINT('Ctrl Pts',(-52.7773196382016,-77.7759719718564,
172.828566725457));
#39556=CARTESIAN_POINT('Ctrl Pts',(-51.4869872099373,-78.0078112578414,
173.846040115263));
#39557=CARTESIAN_POINT('Ctrl Pts',(-51.2929037068116,-78.1227830844834,
175.490142424066));
#39558=CARTESIAN_POINT('Ctrl Pts',(-51.0988202036858,-78.2377549111254,
177.134244732869));
#39559=CARTESIAN_POINT('Ctrl Pts',(-52.1204986920699,-78.2231183870951,
178.441883126102));
#39560=CARTESIAN_POINT('Ctrl Pts',(-53.142177180454,-78.2084818630649,179.749521519335));
#39561=CARTESIAN_POINT('Ctrl Pts',(-54.7869538407105,-78.12741891106,179.954699160921));
#39562=CARTESIAN_POINT('Ctrl Pts',(-56.431730500967,-78.0463559590551,180.159876802508));
#39563=CARTESIAN_POINT('Ctrl Pts',(-57.7419390550653,-78.0009602023809,
179.142403412702));
#39564=CARTESIAN_POINT('Ctrl Pts',(-59.0521476091637,-77.9555644457066,
178.124930022896));
#39565=CARTESIAN_POINT('Ctrl Pts',(-59.2661072381235,-78.0270361483753,
176.480827714093));
#39566=CARTESIAN_POINT('Ctrl Pts',(-59.4800668670833,-78.098507851044,174.83672540529));
#39567=CARTESIAN_POINT('Ctrl Pts',(-58.4782645045332,-78.2995879043849,
173.529087012057));
#39568=CARTESIAN_POINT('Ctrl Pts',(-57.4764621419831,-78.5006679577259,
172.221448618824));
#39569=CARTESIAN_POINT('Ctrl Pts',(-55.8515616075607,-78.7681744390415,
172.016270977238));
#39570=CARTESIAN_POINT('Ctrl Pts',(-54.2266610731382,-79.035680920357,171.811093335651));
#39571=CARTESIAN_POINT('Ctrl Pts',(-52.9363286448739,-79.267520206342,172.828566725457));
#39572=CARTESIAN_POINT('Ctrl Pts',(-51.6459962166095,-79.4993594923269,
173.846040115263));
#39573=CARTESIAN_POINT('Ctrl Pts',(-51.4519127134838,-79.614331318969,175.490142424066));
#39574=CARTESIAN_POINT('Ctrl Pts',(-51.2578292103581,-79.729303145611,177.134244732869));
#39575=CARTESIAN_POINT('Ctrl Pts',(-52.2795076987422,-79.7146666215807,
178.441883126102));
#39576=CARTESIAN_POINT('Ctrl Pts',(-53.3011861871263,-79.7000300975505,
179.749521519335));
#39577=CARTESIAN_POINT('Ctrl Pts',(-54.9459628473827,-79.6189671455456,
179.954699160921));
#39578=CARTESIAN_POINT('Ctrl Pts',(-56.5907395076392,-79.5379041935407,
180.159876802508));
#39579=CARTESIAN_POINT('Ctrl Pts',(-57.9009480617376,-79.4925084368665,
179.142403412702));
#39580=CARTESIAN_POINT('Ctrl Pts',(-59.2111566158359,-79.4471126801922,
178.124930022896));
#39581=CARTESIAN_POINT('Ctrl Pts',(-59.4251162447957,-79.5185843828609,
176.480827714093));
#39582=CARTESIAN_POINT('Ctrl Pts',(-59.6390758737555,-79.5900560855296,
174.83672540529));
#39583=CARTESIAN_POINT('Ctrl Pts',(-58.6372735112054,-79.7911361388705,
173.529087012057));
#39584=CARTESIAN_POINT('Ctrl Pts',(-57.6354711486553,-79.9922161922115,
172.221448618824));
#39585=CARTESIAN_POINT('Ctrl Pts',(-56.0105706142329,-80.2597226735271,
172.016270977238));
#39586=CARTESIAN_POINT('Ctrl Pts',(-54.3856700798105,-80.5272291548426,
171.811093335651));
#39587=CARTESIAN_POINT('Ctrl Pts',(-53.0953376515461,-80.7590684408276,
172.828566725457));
#39588=CARTESIAN_POINT('Ctrl Pts',(-51.8050052232818,-80.9909077268126,
173.846040115263));
#39589=CARTESIAN_POINT('Ctrl Pts',(-51.610921720156,-81.1058795534546,175.490142424066));
#39590=CARTESIAN_POINT('Ctrl Pts',(-51.4168382170303,-81.2208513800966,
177.134244732869));
#39591=CARTESIAN_POINT('Ctrl Pts',(-52.4385167054144,-81.2062148560663,
178.441883126102));
#39592=CARTESIAN_POINT('Ctrl Pts',(-53.4601951937985,-81.1915783320361,
179.749521519335));
#39593=CARTESIAN_POINT('Ctrl Pts',(-55.104971854055,-81.1105153800312,179.954699160921));
#39594=CARTESIAN_POINT('Ctrl Pts',(-56.7497485143114,-81.0294524280263,
180.159876802508));
#39595=CARTESIAN_POINT('Ctrl Pts',(-58.0599570684098,-80.9840566713521,
179.142403412702));
#39596=CARTESIAN_POINT('Ctrl Pts',(-59.3701656225082,-80.9386609146778,
178.124930022896));
#39597=CARTESIAN_POINT('Ctrl Pts',(-59.5841252514679,-81.0101326173465,
176.480827714093));
#39598=CARTESIAN_POINT('Ctrl Pts',(-59.7980848804277,-81.0816043200152,
174.83672540529));
#39599=CARTESIAN_POINT('Ctrl Pts',(-58.7962825178776,-81.2826843733561,
173.529087012057));
#39600=CARTESIAN_POINT('Ctrl Pts',(-57.7944801553275,-81.4837644266971,
172.221448618824));
#39601=CARTESIAN_POINT('Ctrl Pts',(-56.1695796209051,-81.7512709080127,
172.016270977238));
#39602=CARTESIAN_POINT('Ctrl Pts',(-54.5446790864827,-82.0187773893282,
171.811093335651));
#39603=CARTESIAN_POINT('Ctrl Pts',(-53.2543466582183,-82.2506166753132,
172.828566725457));
#39604=CARTESIAN_POINT('Ctrl Pts',(-51.964014229954,-82.4824559612981,173.846040115263));
#39605=CARTESIAN_POINT('Ctrl Pts',(-51.7699307268282,-82.5974277879402,
175.490142424066));
#39606=CARTESIAN_POINT('Ctrl Pts',(-51.5758472237025,-82.7123996145822,
177.134244732869));
#39607=CARTESIAN_POINT('Ctrl Pts',(-52.5975257120866,-82.6977630905519,
178.441883126102));
#39608=CARTESIAN_POINT('Ctrl Pts',(-53.6192042004707,-82.6831265665217,
179.749521519335));
#39609=CARTESIAN_POINT('Ctrl Pts',(-55.2639808607272,-82.6020636145168,
179.954699160921));
#39610=CARTESIAN_POINT('Ctrl Pts',(-56.9087575209836,-82.521000662512,180.159876802508));
#39611=CARTESIAN_POINT('Ctrl Pts',(-58.218966075082,-82.4756049058377,179.142403412702));
#39612=CARTESIAN_POINT('Ctrl Pts',(-59.5291746291804,-82.4302091491634,
178.124930022896));
#39613=CARTESIAN_POINT('Ctrl Pts',(-59.7431342581402,-82.5016808518321,
176.480827714093));
#39614=CARTESIAN_POINT('Ctrl Pts',(-59.9570938870999,-82.5731525545008,
174.83672540529));
#39615=CARTESIAN_POINT('Ctrl Pts',(-58.9552915245499,-82.7742326078417,
173.529087012057));
#39616=CARTESIAN_POINT('Ctrl Pts',(-57.9534891619998,-82.9753126611827,
172.221448618824));
#39617=CARTESIAN_POINT('Ctrl Pts',(-56.3285886275773,-83.2428191424982,
172.016270977238));
#39618=CARTESIAN_POINT('Ctrl Pts',(-54.7036880931549,-83.5103256238138,
171.811093335651));
#39619=CARTESIAN_POINT('Ctrl Pts',(-53.4133556648906,-83.7421649097988,
172.828566725457));
#39620=CARTESIAN_POINT('Ctrl Pts',(-52.1230232366262,-83.9740041957837,
173.846040115263));
#39621=CARTESIAN_POINT('Ctrl Pts',(-51.9289397335005,-84.0889760224258,
175.490142424066));
#39622=CARTESIAN_POINT('Ctrl Pts',(-51.7348562303747,-84.2039478490678,
177.134244732869));
#39623=CARTESIAN_POINT('Ctrl Pts',(-52.7565347187588,-84.1893113250376,
178.441883126102));
#39624=CARTESIAN_POINT('Ctrl Pts',(-53.7782132071429,-84.1746748010073,
179.749521519335));
#39625=CARTESIAN_POINT('Ctrl Pts',(-55.4229898673994,-84.0936118490024,
179.954699160921));
#39626=CARTESIAN_POINT('Ctrl Pts',(-57.0677665276559,-84.0125488969975,
180.159876802508));
#39627=CARTESIAN_POINT('Ctrl Pts',(-58.3779750817542,-83.9671531403233,
179.142403412702));
#39628=CARTESIAN_POINT('Ctrl Pts',(-59.6881836358526,-83.921757383649,178.124930022896));
#39629=CARTESIAN_POINT('Ctrl Pts',(-59.9021432648124,-83.9932290863177,
176.480827714093));
#39630=CARTESIAN_POINT('Ctrl Pts',(-60.1161028937722,-84.0647007889864,
174.83672540529));
#39631=CARTESIAN_POINT('Ctrl Pts',(-59.1143005312221,-84.2657808423273,
173.529087012057));
#39632=CARTESIAN_POINT('Ctrl Pts',(-58.112498168672,-84.4668608956683,172.221448618824));
#39633=CARTESIAN_POINT('Ctrl Pts',(-56.4875976342496,-84.7343673769838,
172.016270977238));
#39634=CARTESIAN_POINT('Ctrl Pts',(-54.8626970998271,-85.0018738582994,
171.811093335651));
#39635=CARTESIAN_POINT('Ctrl Pts',(-53.5723646715628,-85.2337131442844,
172.828566725457));
#39636=CARTESIAN_POINT('Ctrl Pts',(-52.2820322432984,-85.4655524302694,
173.846040115263));
#39637=CARTESIAN_POINT('Ctrl Pts',(-52.0879487401727,-85.5805242569114,
175.490142424066));
#39638=CARTESIAN_POINT('Ctrl Pts',(-51.8938652370469,-85.6954960835534,
177.134244732869));
#39639=CARTESIAN_POINT('Ctrl Pts',(-52.915543725431,-85.6808595595231,178.441883126102));
#39640=CARTESIAN_POINT('Ctrl Pts',(-53.9372222138152,-85.6662230354929,
179.749521519335));
#39641=CARTESIAN_POINT('Ctrl Pts',(-55.5819988740716,-85.585160083488,179.954699160921));
#39642=CARTESIAN_POINT('Ctrl Pts',(-57.2267755343281,-85.5040971314831,
180.159876802508));
#39643=CARTESIAN_POINT('Ctrl Pts',(-58.5369840884265,-85.4587013748089,
179.142403412702));
#39644=CARTESIAN_POINT('Ctrl Pts',(-59.8471926425249,-85.4133056181346,
178.124930022896));
#39645=CARTESIAN_POINT('Ctrl Pts',(-60.0611522714846,-85.4847773208033,
176.480827714093));
#39646=CARTESIAN_POINT('Ctrl Pts',(-60.2751119004444,-85.556249023472,174.83672540529));
#39647=CARTESIAN_POINT('Ctrl Pts',(-59.2733095378943,-85.7573290768129,
173.529087012057));
#39648=CARTESIAN_POINT('Ctrl Pts',(-58.2715071753442,-85.9584091301539,
172.221448618824));
#39649=CARTESIAN_POINT('Ctrl Pts',(-56.6466066409218,-86.2259156114695,
172.016270977238));
#39650=CARTESIAN_POINT('Ctrl Pts',(-55.0217061064994,-86.493422092785,171.811093335651));
#39651=CARTESIAN_POINT('Ctrl Pts',(-53.731373678235,-86.72526137877,172.828566725457));
#39652=CARTESIAN_POINT('Ctrl Pts',(-52.4410412499707,-86.9571006647549,
173.846040115263));
#39653=CARTESIAN_POINT('Ctrl Pts',(-52.2469577468449,-87.072072491397,175.490142424066));
#39654=CARTESIAN_POINT('Ctrl Pts',(-52.0528742437192,-87.187044318039,177.134244732869));
#39655=CARTESIAN_POINT('Ctrl Pts',(-53.0745527321033,-87.1724077940087,
178.441883126102));
#39656=CARTESIAN_POINT('Ctrl Pts',(-54.0962312204874,-87.1577712699785,
179.749521519335));
#39657=CARTESIAN_POINT('Ctrl Pts',(-55.7410078807439,-87.0767083179736,
179.954699160921));
#39658=CARTESIAN_POINT('Ctrl Pts',(-57.3857845410003,-86.9956453659688,
180.159876802508));
#39659=CARTESIAN_POINT('Ctrl Pts',(-58.6959930950987,-86.9502496092945,
179.142403412702));
#39660=CARTESIAN_POINT('Ctrl Pts',(-60.0062016491971,-86.9048538526202,
178.124930022896));
#39661=CARTESIAN_POINT('Ctrl Pts',(-60.2201612781569,-86.9763255552889,
176.480827714093));
#39662=CARTESIAN_POINT('Ctrl Pts',(-60.4341209071166,-87.0477972579576,
174.83672540529));
#39663=CARTESIAN_POINT('Ctrl Pts',(-59.4323185445665,-87.2488773112985,
173.529087012057));
#39664=CARTESIAN_POINT('Ctrl Pts',(-58.4305161820165,-87.4499573646395,
172.221448618824));
#39665=CARTESIAN_POINT('Ctrl Pts',(-56.805615647594,-87.7174638459551,172.016270977238));
#39666=CARTESIAN_POINT('Ctrl Pts',(-55.1807151131716,-87.9849703272706,
171.811093335651));
#39667=CARTESIAN_POINT('Ctrl Pts',(-53.8903826849072,-88.2168096132556,
172.828566725457));
#39668=CARTESIAN_POINT('Ctrl Pts',(-52.6000502566429,-88.4486488992405,
173.846040115263));
#39669=CARTESIAN_POINT('Ctrl Pts',(-52.4059667535171,-88.5636207258826,
175.490142424066));
#39670=CARTESIAN_POINT('Ctrl Pts',(-52.2118832503914,-88.6785925525246,
177.134244732869));
#39671=CARTESIAN_POINT('Ctrl Pts',(-53.2335617387755,-88.6639560284944,
178.441883126102));
#39672=CARTESIAN_POINT('Ctrl Pts',(-54.2552402271596,-88.6493195044641,
179.749521519335));
#39673=CARTESIAN_POINT('Ctrl Pts',(-55.9000168874161,-88.5682565524592,
179.954699160921));
#39674=CARTESIAN_POINT('Ctrl Pts',(-57.5447935476725,-88.4871936004543,
180.159876802508));
#39675=CARTESIAN_POINT('Ctrl Pts',(-58.8550021017709,-88.4417978437801,
179.142403412702));
#39676=CARTESIAN_POINT('Ctrl Pts',(-60.1652106558693,-88.3964020871058,
178.124930022896));
#39677=CARTESIAN_POINT('Ctrl Pts',(-60.3791702848291,-88.4678737897745,
176.480827714093));
#39678=CARTESIAN_POINT('Ctrl Pts',(-60.5931299137889,-88.5393454924432,
174.83672540529));
#39679=CARTESIAN_POINT('Ctrl Pts',(-59.5913275512388,-88.7404255457841,
173.529087012057));
#39680=CARTESIAN_POINT('Ctrl Pts',(-58.5895251886887,-88.9415055991251,
172.221448618824));
#39681=CARTESIAN_POINT('Ctrl Pts',(-56.9646246542662,-89.2090120804406,
172.016270977238));
#39682=CARTESIAN_POINT('Ctrl Pts',(-55.3397241198438,-89.4765185617563,
171.811093335651));
#39683=CARTESIAN_POINT('Ctrl Pts',(-54.0493916915795,-89.7083578477412,
172.828566725457));
#39684=CARTESIAN_POINT('Ctrl Pts',(-52.7590592633151,-89.9401971337262,
173.846040115263));
#39685=CARTESIAN_POINT('Ctrl Pts',(-52.5649757601894,-90.0551689603682,
175.490142424066));
#39686=CARTESIAN_POINT('Ctrl Pts',(-52.3708922570636,-90.1701407870102,
177.134244732869));
#39687=CARTESIAN_POINT('Ctrl Pts',(-53.3925707454477,-90.1555042629799,
178.441883126102));
#39688=CARTESIAN_POINT('Ctrl Pts',(-54.4142492338319,-90.1408677389497,
179.749521519335));
#39689=CARTESIAN_POINT('Ctrl Pts',(-56.0590258940883,-90.0598047869448,
179.954699160921));
#39690=CARTESIAN_POINT('Ctrl Pts',(-57.7038025543448,-89.9787418349399,
180.159876802508));
#39691=CARTESIAN_POINT('Ctrl Pts',(-59.0140111084431,-89.9333460782657,
179.142403412702));
#39692=CARTESIAN_POINT('Ctrl Pts',(-60.3242196625415,-89.8879503215914,
178.124930022896));
#39693=CARTESIAN_POINT('Ctrl Pts',(-60.5381792915013,-89.9594220242601,
176.480827714093));
#39694=CARTESIAN_POINT('Ctrl Pts',(-60.7521389204611,-90.0308937269288,
174.83672540529));
#39695=CARTESIAN_POINT('Ctrl Pts',(-59.750336557911,-90.2319737802697,173.529087012057));
#39696=CARTESIAN_POINT('Ctrl Pts',(-58.7485341953609,-90.4330538336107,
172.221448618824));
#39697=CARTESIAN_POINT('Ctrl Pts',(-57.1236336609385,-90.7005603149262,
172.016270977238));
#39698=CARTESIAN_POINT('Ctrl Pts',(-55.498733126516,-90.9680667962418,171.811093335651));
#39699=CARTESIAN_POINT('Ctrl Pts',(-54.2084006982517,-91.1999060822268,
172.828566725457));
#39700=CARTESIAN_POINT('Ctrl Pts',(-52.9180682699873,-91.4317453682118,
173.846040115263));
#39701=CARTESIAN_POINT('Ctrl Pts',(-52.7239847668616,-91.5467171948538,
175.490142424066));
#39702=CARTESIAN_POINT('Ctrl Pts',(-52.5299012637359,-91.6616890214958,
177.134244732869));
#39703=CARTESIAN_POINT('Ctrl Pts',(-53.55157975212,-91.6470524974655,178.441883126102));
#39704=CARTESIAN_POINT('Ctrl Pts',(-54.5732582405041,-91.6324159734353,
179.749521519335));
#39705=CARTESIAN_POINT('Ctrl Pts',(-56.2180349007605,-91.5513530214304,
179.954699160921));
#39706=CARTESIAN_POINT('Ctrl Pts',(-57.862811561017,-91.4702900694256,180.159876802508));
#39707=CARTESIAN_POINT('Ctrl Pts',(-59.1730201151154,-91.4248943127513,
179.142403412702));
#39708=CARTESIAN_POINT('Ctrl Pts',(-60.4832286692138,-91.379498556077,178.124930022896));
#39709=CARTESIAN_POINT('Ctrl Pts',(-60.6971882981735,-91.4509702587457,
176.480827714093));
#39710=CARTESIAN_POINT('Ctrl Pts',(-60.9111479271333,-91.5224419614144,
174.83672540529));
#39711=CARTESIAN_POINT('Ctrl Pts',(-59.9093455645832,-91.7235220147553,
173.529087012057));
#39712=CARTESIAN_POINT('Ctrl Pts',(-58.9075432020331,-91.9246020680963,
172.221448618824));
#39713=CARTESIAN_POINT('Ctrl Pts',(-57.2826426676107,-92.1921085494119,
172.016270977238));
#39714=CARTESIAN_POINT('Ctrl Pts',(-55.6577421331883,-92.4596150307274,
171.811093335651));
#39715=CARTESIAN_POINT('Ctrl Pts',(-54.3674097049239,-92.6914543167124,
172.828566725457));
#39716=CARTESIAN_POINT('Ctrl Pts',(-53.0770772766596,-92.9232936026974,
173.846040115263));
#39717=CARTESIAN_POINT('Ctrl Pts',(-52.8829937735338,-93.0382654293394,
175.490142424066));
#39718=CARTESIAN_POINT('Ctrl Pts',(-52.6889102704081,-93.1532372559814,
177.134244732869));
#39719=CARTESIAN_POINT('Ctrl Pts',(-53.7105887587922,-93.1386007319512,
178.441883126102));
#39720=CARTESIAN_POINT('Ctrl Pts',(-54.7322672471763,-93.1239642079209,
179.749521519335));
#39721=CARTESIAN_POINT('Ctrl Pts',(-56.3770439074328,-93.042901255916,179.954699160921));
#39722=CARTESIAN_POINT('Ctrl Pts',(-58.0218205676892,-92.9618383039112,
180.159876802508));
#39723=CARTESIAN_POINT('Ctrl Pts',(-59.3320291217876,-92.9164425472369,
179.142403412702));
#39724=CARTESIAN_POINT('Ctrl Pts',(-60.642237675886,-92.8710467905626,178.124930022896));
#39725=CARTESIAN_POINT('Ctrl Pts',(-60.8561973048458,-92.9425184932313,
176.480827714093));
#39726=CARTESIAN_POINT('Ctrl Pts',(-61.0701569338055,-93.0139901959,174.83672540529));
#39727=CARTESIAN_POINT('Ctrl Pts',(-60.0683545712554,-93.2150702492409,
173.529087012057));
#39728=CARTESIAN_POINT('Ctrl Pts',(-59.0665522087054,-93.4161503025819,
172.221448618824));
#39729=CARTESIAN_POINT('Ctrl Pts',(-57.4416516742829,-93.6836567838974,
172.016270977238));
#39730=CARTESIAN_POINT('Ctrl Pts',(-55.8167511398605,-93.951163265213,171.811093335651));
#39731=CARTESIAN_POINT('Ctrl Pts',(-54.5264187115961,-94.183002551198,172.828566725457));
#39732=CARTESIAN_POINT('Ctrl Pts',(-53.2360862833318,-94.4148418371829,
173.846040115263));
#39733=CARTESIAN_POINT('Ctrl Pts',(-53.042002780206,-94.529813663825,175.490142424066));
#39734=CARTESIAN_POINT('Ctrl Pts',(-52.8479192770803,-94.644785490467,177.134244732869));
#39735=CARTESIAN_POINT('Ctrl Pts',(-53.8695977654644,-94.6301489664367,
178.441883126102));
#39736=CARTESIAN_POINT('Ctrl Pts',(-54.8912762538485,-94.6155124424065,
179.749521519335));
#39737=CARTESIAN_POINT('Ctrl Pts',(-56.536052914105,-94.5344494904016,179.954699160921));
#39738=CARTESIAN_POINT('Ctrl Pts',(-58.1808295743615,-94.4533865383968,
180.159876802508));
#39739=CARTESIAN_POINT('Ctrl Pts',(-59.4910381284598,-94.4079907817225,
179.142403412702));
#39740=CARTESIAN_POINT('Ctrl Pts',(-60.8012466825582,-94.3625950250483,
178.124930022896));
#39741=CARTESIAN_POINT('Ctrl Pts',(-61.015206311518,-94.4340667277169,176.480827714093));
#39742=CARTESIAN_POINT('Ctrl Pts',(-61.2291659404778,-94.5055384303856,
174.83672540529));
#39743=CARTESIAN_POINT('Ctrl Pts',(-60.2273635779277,-94.7066184837265,
173.529087012057));
#39744=CARTESIAN_POINT('Ctrl Pts',(-59.2255612153776,-94.9076985370675,
172.221448618824));
#39745=CARTESIAN_POINT('Ctrl Pts',(-57.6006606809552,-95.1752050183831,
172.016270977238));
#39746=CARTESIAN_POINT('Ctrl Pts',(-55.9757601465327,-95.4427114996986,
171.811093335651));
#39747=CARTESIAN_POINT('Ctrl Pts',(-54.6854277182684,-95.6745507856836,
172.828566725457));
#39748=CARTESIAN_POINT('Ctrl Pts',(-53.395095290004,-95.9063900716686,173.846040115263));
#39749=CARTESIAN_POINT('Ctrl Pts',(-53.2010117868783,-96.0213618983106,
175.490142424066));
#39750=CARTESIAN_POINT('Ctrl Pts',(-53.0069282837525,-96.1363337249526,
177.134244732869));
#39751=CARTESIAN_POINT('Ctrl Pts',(-54.0286067721367,-96.1216972009223,
178.441883126102));
#39752=CARTESIAN_POINT('Ctrl Pts',(-55.0502852605208,-96.1070606768921,
179.749521519335));
#39753=CARTESIAN_POINT('Ctrl Pts',(-56.6950619207772,-96.0259977248872,
179.954699160921));
#39754=CARTESIAN_POINT('Ctrl Pts',(-58.3398385810337,-95.9449347728824,
180.159876802508));
#39755=CARTESIAN_POINT('Ctrl Pts',(-59.6500471351321,-95.8995390162081,
179.142403412702));
#39756=CARTESIAN_POINT('Ctrl Pts',(-60.9602556892304,-95.8541432595338,
178.124930022896));
#39757=CARTESIAN_POINT('Ctrl Pts',(-61.1742153181902,-95.9256149622025,
176.480827714093));
#39758=CARTESIAN_POINT('Ctrl Pts',(-61.38817494715,-95.9970866648712,174.83672540529));
#39759=CARTESIAN_POINT('Ctrl Pts',(-60.3863725845999,-96.1981667182121,
173.529087012057));
#39760=CARTESIAN_POINT('Ctrl Pts',(-59.3845702220498,-96.3992467715531,
172.221448618824));
#39761=CARTESIAN_POINT('Ctrl Pts',(-57.7596696876274,-96.6667532528687,
172.016270977238));
#39762=CARTESIAN_POINT('Ctrl Pts',(-56.134769153205,-96.9342597341842,171.811093335651));
#39763=CARTESIAN_POINT('Ctrl Pts',(-54.8444367249406,-97.1660990201692,
172.828566725457));
#39764=CARTESIAN_POINT('Ctrl Pts',(-53.5541042966763,-97.3979383061541,
173.846040115263));
#39765=CARTESIAN_POINT('Ctrl Pts',(-53.3600207935505,-97.5129101327962,
175.490142424066));
#39766=CARTESIAN_POINT('Ctrl Pts',(-53.1659372904248,-97.6278819594382,
177.134244732869));
#39767=CARTESIAN_POINT('Ctrl Pts',(-54.1876157788089,-97.6132454354079,
178.441883126102));
#39768=CARTESIAN_POINT('Ctrl Pts',(-55.209294267193,-97.5986089113777,179.749521519335));
#39769=CARTESIAN_POINT('Ctrl Pts',(-56.8540709274494,-97.5175459593728,
179.954699160921));
#39770=CARTESIAN_POINT('Ctrl Pts',(-58.4988475877059,-97.436483007368,180.159876802508));
#39771=CARTESIAN_POINT('Ctrl Pts',(-59.8090561418043,-97.3910872506937,
179.142403412702));
#39772=CARTESIAN_POINT('Ctrl Pts',(-61.1192646959027,-97.3456914940194,
178.124930022896));
#39773=CARTESIAN_POINT('Ctrl Pts',(-61.3332243248624,-97.4171631966881,
176.480827714093));
#39774=CARTESIAN_POINT('Ctrl Pts',(-61.5471839538222,-97.4886348993568,
174.83672540529));
#39775=CARTESIAN_POINT('Ctrl Pts',(-60.5453815912721,-97.6897149526977,
173.529087012057));
#39776=CARTESIAN_POINT('Ctrl Pts',(-59.5435792287221,-97.8907950060387,
172.221448618824));
#39777=CARTESIAN_POINT('Ctrl Pts',(-57.9186786942996,-98.1583014873543,
172.016270977238));
#39778=CARTESIAN_POINT('Ctrl Pts',(-56.2937781598772,-98.4258079686698,
171.811093335651));
#39779=CARTESIAN_POINT('Ctrl Pts',(-55.0034457316128,-98.6576472546548,
172.828566725457));
#39780=CARTESIAN_POINT('Ctrl Pts',(-53.7131133033485,-98.8894865406397,
173.846040115263));
#39781=CARTESIAN_POINT('Ctrl Pts',(-53.5190298002227,-99.0044583672818,
175.490142424066));
#39782=CARTESIAN_POINT('Ctrl Pts',(-53.324946297097,-99.1194301939238,177.134244732869));
#39783=CARTESIAN_POINT('Ctrl Pts',(-54.3466247854811,-99.1047936698936,
178.441883126102));
#39784=CARTESIAN_POINT('Ctrl Pts',(-55.3683032738652,-99.0901571458633,
179.749521519335));
#39785=CARTESIAN_POINT('Ctrl Pts',(-57.0130799341217,-99.0090941938584,
179.954699160921));
#39786=CARTESIAN_POINT('Ctrl Pts',(-58.6578565943781,-98.9280312418536,
180.159876802508));
#39787=CARTESIAN_POINT('Ctrl Pts',(-59.9680651484765,-98.8826354851793,
179.142403412702));
#39788=CARTESIAN_POINT('Ctrl Pts',(-61.2782737025749,-98.837239728505,178.124930022896));
#39789=CARTESIAN_POINT('Ctrl Pts',(-61.4922333315347,-98.9087114311737,
176.480827714093));
#39790=CARTESIAN_POINT('Ctrl Pts',(-61.7061929604944,-98.9801831338424,
174.83672540529));
#39791=CARTESIAN_POINT('Ctrl Pts',(-60.7043905979444,-99.1812631871833,
173.529087012057));
#39792=CARTESIAN_POINT('Ctrl Pts',(-59.7025882353943,-99.3823432405243,
172.221448618824));
#39793=CARTESIAN_POINT('Ctrl Pts',(-58.0776877009718,-99.6498497218399,
172.016270977238));
#39794=CARTESIAN_POINT('Ctrl Pts',(-56.4527871665494,-99.9173562031554,
171.811093335651));
#39795=CARTESIAN_POINT('Ctrl Pts',(-55.162454738285,-100.14919548914,172.828566725457));
#39796=CARTESIAN_POINT('Ctrl Pts',(-53.8721223100207,-100.381034775125,
173.846040115263));
#39797=CARTESIAN_POINT('Ctrl Pts',(-53.678038806895,-100.496006601767,175.490142424066));
#39798=CARTESIAN_POINT('Ctrl Pts',(-53.4839553037692,-100.610978428409,
177.134244732869));
#39799=CARTESIAN_POINT('Ctrl Pts',(-54.5056337921533,-100.596341904379,
178.441883126102));
#39800=CARTESIAN_POINT('Ctrl Pts',(-55.5273122805374,-100.581705380349,
179.749521519335));
#39801=CARTESIAN_POINT('Ctrl Pts',(-57.1720889407939,-100.500642428344,
179.954699160921));
#39802=CARTESIAN_POINT('Ctrl Pts',(-58.8168656010504,-100.419579476339,
180.159876802508));
#39803=CARTESIAN_POINT('Ctrl Pts',(-60.1270741551487,-100.374183719665,
179.142403412702));
#39804=CARTESIAN_POINT('Ctrl Pts',(-61.4372827092471,-100.328787962991,
178.124930022896));
#39805=CARTESIAN_POINT('Ctrl Pts',(-61.6512423382069,-100.400259665659,
176.480827714093));
#39806=CARTESIAN_POINT('Ctrl Pts',(-61.8652019671667,-100.471731368328,
174.83672540529));
#39807=CARTESIAN_POINT('Ctrl Pts',(-60.8633996046166,-100.672811421669,
173.529087012057));
#39808=CARTESIAN_POINT('Ctrl Pts',(-59.8615972420665,-100.87389147501,172.221448618824));
#39809=CARTESIAN_POINT('Ctrl Pts',(-58.2366967076441,-101.141397956325,
172.016270977238));
#39810=CARTESIAN_POINT('Ctrl Pts',(-56.6117961732216,-101.408904437641,
171.811093335651));
#39811=CARTESIAN_POINT('Ctrl Pts',(-55.3214637449573,-101.640743723626,
172.828566725457));
#39812=CARTESIAN_POINT('Ctrl Pts',(-54.0311313166929,-101.872583009611,
173.846040115263));
#39813=CARTESIAN_POINT('Ctrl Pts',(-53.8370478135672,-101.987554836253,
175.490142424066));
#39814=CARTESIAN_POINT('Ctrl Pts',(-53.6429643104415,-102.102526662895,
177.134244732869));
#39815=CARTESIAN_POINT('Ctrl Pts',(-54.6646427988256,-102.087890138865,
178.441883126102));
#39816=CARTESIAN_POINT('Ctrl Pts',(-55.6863212872097,-102.073253614834,
179.749521519335));
#39817=CARTESIAN_POINT('Ctrl Pts',(-57.3310979474661,-101.99219066283,179.954699160921));
#39818=CARTESIAN_POINT('Ctrl Pts',(-58.9758746077226,-101.911127710825,
180.159876802508));
#39819=CARTESIAN_POINT('Ctrl Pts',(-60.286083161821,-101.865731954151,179.142403412702));
#39820=CARTESIAN_POINT('Ctrl Pts',(-61.5962917159193,-101.820336197476,
178.124930022896));
#39821=CARTESIAN_POINT('Ctrl Pts',(-61.8102513448791,-101.891807900145,
176.480827714093));
#39822=CARTESIAN_POINT('Ctrl Pts',(-62.0242109738389,-101.963279602814,
174.83672540529));
#39823=CARTESIAN_POINT('Ctrl Pts',(-61.0224086112888,-102.164359656155,
173.529087012057));
#39824=CARTESIAN_POINT('Ctrl Pts',(-60.0206062487387,-102.365439709496,
172.221448618824));
#39825=CARTESIAN_POINT('Ctrl Pts',(-58.3957057143163,-102.632946190811,
172.016270977238));
#39826=CARTESIAN_POINT('Ctrl Pts',(-56.7708051798939,-102.900452672127,
171.811093335651));
#39827=CARTESIAN_POINT('Ctrl Pts',(-55.4804727516295,-103.132291958112,
172.828566725457));
#39828=CARTESIAN_POINT('Ctrl Pts',(-54.1901403233652,-103.364131244097,
173.846040115263));
#39829=CARTESIAN_POINT('Ctrl Pts',(-53.9960568202394,-103.479103070739,
175.490142424066));
#39830=CARTESIAN_POINT('Ctrl Pts',(-53.8019733171137,-103.594074897381,
177.134244732869));
#39831=CARTESIAN_POINT('Ctrl Pts',(-54.8236518054978,-103.57943837335,178.441883126102));
#39832=CARTESIAN_POINT('Ctrl Pts',(-55.8453302938819,-103.56480184932,179.749521519335));
#39833=CARTESIAN_POINT('Ctrl Pts',(-57.4901069541384,-103.483738897315,
179.954699160921));
#39834=CARTESIAN_POINT('Ctrl Pts',(-59.1348836143948,-103.40267594531,180.159876802508));
#39835=CARTESIAN_POINT('Ctrl Pts',(-60.4450921684932,-103.357280188636,
179.142403412702));
#39836=CARTESIAN_POINT('Ctrl Pts',(-61.7553007225916,-103.311884431962,
178.124930022896));
#39837=CARTESIAN_POINT('Ctrl Pts',(-61.9692603515513,-103.383356134631,
176.480827714093));
#39838=CARTESIAN_POINT('Ctrl Pts',(-62.1832199805111,-103.454827837299,
174.83672540529));
#39839=CARTESIAN_POINT('Ctrl Pts',(-61.181417617961,-103.65590789064,173.529087012057));
#39840=CARTESIAN_POINT('Ctrl Pts',(-60.179615255411,-103.856987943981,172.221448618824));
#39841=CARTESIAN_POINT('Ctrl Pts',(-58.5547147209885,-104.124494425297,
172.016270977238));
#39842=CARTESIAN_POINT('Ctrl Pts',(-56.9298141865661,-104.392000906612,
171.811093335651));
#39843=CARTESIAN_POINT('Ctrl Pts',(-55.6394817583017,-104.623840192597,
172.828566725457));
#39844=CARTESIAN_POINT('Ctrl Pts',(-54.3491493300374,-104.855679478582,
173.846040115263));
#39845=CARTESIAN_POINT('Ctrl Pts',(-54.1550658269116,-104.970651305224,
175.490142424066));
#39846=CARTESIAN_POINT('Ctrl Pts',(-53.9609823237859,-105.085623131866,
177.134244732869));
#39847=CARTESIAN_POINT('Ctrl Pts',(-54.98266081217,-105.070986607836,178.441883126102));
#39848=CARTESIAN_POINT('Ctrl Pts',(-56.0043393005541,-105.056350083806,
179.749521519335));
#39849=CARTESIAN_POINT('Ctrl Pts',(-57.6491159608106,-104.975287131801,
179.954699160921));
#39850=CARTESIAN_POINT('Ctrl Pts',(-59.293892621067,-104.894224179796,180.159876802508));
#39851=CARTESIAN_POINT('Ctrl Pts',(-60.6041011751654,-104.848828423122,
179.142403412702));
#39852=CARTESIAN_POINT('Ctrl Pts',(-61.9143097292638,-104.803432666447,
178.124930022896));
#39853=CARTESIAN_POINT('Ctrl Pts',(-62.1282693582236,-104.874904369116,
176.480827714093));
#39854=CARTESIAN_POINT('Ctrl Pts',(-62.3422289871834,-104.946376071785,
174.83672540529));
#39855=CARTESIAN_POINT('Ctrl Pts',(-61.3404266246333,-105.147456125126,
173.529087012057));
#39856=CARTESIAN_POINT('Ctrl Pts',(-60.3386242620832,-105.348536178467,
172.221448618824));
#39857=CARTESIAN_POINT('Ctrl Pts',(-58.7137237276607,-105.616042659782,
172.016270977238));
#39858=CARTESIAN_POINT('Ctrl Pts',(-57.0888231932383,-105.883549141098,
171.811093335651));
#39859=CARTESIAN_POINT('Ctrl Pts',(-55.798490764974,-106.115388427083,172.828566725457));
#39860=CARTESIAN_POINT('Ctrl Pts',(-54.5081583367096,-106.347227713068,
173.846040115263));
#39861=CARTESIAN_POINT('Ctrl Pts',(-54.3140748335839,-106.46219953971,175.490142424066));
#39862=CARTESIAN_POINT('Ctrl Pts',(-54.1199913304581,-106.577171366352,
177.134244732869));
#39863=CARTESIAN_POINT('Ctrl Pts',(-55.1416698188422,-106.562534842322,
178.441883126102));
#39864=CARTESIAN_POINT('Ctrl Pts',(-56.1633483072264,-106.547898318291,
179.749521519335));
#39865=CARTESIAN_POINT('Ctrl Pts',(-57.8081249674828,-106.466835366286,
179.954699160921));
#39866=CARTESIAN_POINT('Ctrl Pts',(-59.4529016277393,-106.385772414282,
180.159876802508));
#39867=CARTESIAN_POINT('Ctrl Pts',(-60.7631101818376,-106.340376657607,
179.142403412702));
#39868=CARTESIAN_POINT('Ctrl Pts',(-62.073318735936,-106.294980900933,178.124930022896));
#39869=CARTESIAN_POINT('Ctrl Pts',(-62.2872783648958,-106.366452603602,
176.480827714093));
#39870=CARTESIAN_POINT('Ctrl Pts',(-62.5012379938556,-106.43792430627,174.83672540529));
#39871=CARTESIAN_POINT('Ctrl Pts',(-61.4994356313055,-106.639004359611,
173.529087012057));
#39872=CARTESIAN_POINT('Ctrl Pts',(-60.4976332687554,-106.840084412952,
172.221448618824));
#39873=CARTESIAN_POINT('Ctrl Pts',(-58.872732734333,-107.107590894268,172.016270977238));
#39874=CARTESIAN_POINT('Ctrl Pts',(-57.2478321999105,-107.375097375583,
171.811093335651));
#39875=CARTESIAN_POINT('Ctrl Pts',(-55.9574997716462,-107.606936661568,
172.828566725457));
#39876=CARTESIAN_POINT('Ctrl Pts',(-54.6671673433818,-107.838775947553,
173.846040115263));
#39877=CARTESIAN_POINT('Ctrl Pts',(-54.4730838402561,-107.953747774195,
175.490142424066));
#39878=CARTESIAN_POINT('Ctrl Pts',(-54.2790003371304,-108.068719600837,
177.134244732869));
#39879=CARTESIAN_POINT('Ctrl Pts',(-55.3006788255145,-108.054083076807,
178.441883126102));
#39880=CARTESIAN_POINT('Ctrl Pts',(-56.3223573138986,-108.039446552777,
179.749521519335));
#39881=CARTESIAN_POINT('Ctrl Pts',(-57.967133974155,-107.958383600772,179.954699160921));
#39882=CARTESIAN_POINT('Ctrl Pts',(-59.6119106344115,-107.877320648767,
180.159876802508));
#39883=CARTESIAN_POINT('Ctrl Pts',(-60.9221191885099,-107.831924892093,
179.142403412702));
#39884=CARTESIAN_POINT('Ctrl Pts',(-62.2323277426083,-107.786529135419,
178.124930022896));
#39885=CARTESIAN_POINT('Ctrl Pts',(-62.446287371568,-107.858000838087,176.480827714093));
#39886=CARTESIAN_POINT('Ctrl Pts',(-62.6602470005278,-107.929472540756,
174.83672540529));
#39887=CARTESIAN_POINT('Ctrl Pts',(-61.6584446379777,-108.130552594097,
173.529087012057));
#39888=CARTESIAN_POINT('Ctrl Pts',(-60.6566422754277,-108.331632647438,
172.221448618824));
#39889=CARTESIAN_POINT('Ctrl Pts',(-59.0317417410052,-108.599139128753,
172.016270977238));
#39890=CARTESIAN_POINT('Ctrl Pts',(-57.4068412065828,-108.866645610069,
171.811093335651));
#39891=CARTESIAN_POINT('Ctrl Pts',(-56.1165087783184,-109.098484896054,
172.828566725457));
#39892=CARTESIAN_POINT('Ctrl Pts',(-54.8261763500541,-109.330324182039,
173.846040115263));
#39893=CARTESIAN_POINT('Ctrl Pts',(-54.6320928469283,-109.445296008681,
175.490142424066));
#39894=CARTESIAN_POINT('Ctrl Pts',(-54.4380093438026,-109.560267835323,
177.134244732869));
#39895=CARTESIAN_POINT('Ctrl Pts',(-55.4596878321867,-109.545631311293,
178.441883126102));
#39896=CARTESIAN_POINT('Ctrl Pts',(-56.4813663205708,-109.530994787262,
179.749521519335));
#39897=CARTESIAN_POINT('Ctrl Pts',(-58.1261429808273,-109.449931835258,
179.954699160921));
#39898=CARTESIAN_POINT('Ctrl Pts',(-59.7709196410837,-109.368868883253,
180.159876802508));
#39899=CARTESIAN_POINT('Ctrl Pts',(-61.0811281951821,-109.323473126579,
179.142403412702));
#39900=CARTESIAN_POINT('Ctrl Pts',(-62.3913367492805,-109.278077369904,
178.124930022896));
#39901=CARTESIAN_POINT('Ctrl Pts',(-62.6052963782402,-109.349549072573,
176.480827714093));
#39902=CARTESIAN_POINT('Ctrl Pts',(-62.8192560072,-109.421020775242,174.83672540529));
#39903=CARTESIAN_POINT('Ctrl Pts',(-61.8174536446499,-109.622100828583,
173.529087012057));
#39904=CARTESIAN_POINT('Ctrl Pts',(-60.8156512820999,-109.823180881923,
172.221448618824));
#39905=CARTESIAN_POINT('Ctrl Pts',(-59.1907507476774,-110.090687363239,
172.016270977238));
#39906=CARTESIAN_POINT('Ctrl Pts',(-57.565850213255,-110.358193844555,171.811093335651));
#39907=CARTESIAN_POINT('Ctrl Pts',(-56.2755177849906,-110.59003313054,172.828566725457));
#39908=CARTESIAN_POINT('Ctrl Pts',(-54.9851853567263,-110.821872416525,
173.846040115263));
#39909=CARTESIAN_POINT('Ctrl Pts',(-54.7911018536006,-110.936844243167,
175.490142424066));
#39910=CARTESIAN_POINT('Ctrl Pts',(-54.5970183504748,-111.051816069809,
177.134244732869));
#39911=CARTESIAN_POINT('Ctrl Pts',(-55.6186968388589,-111.037179545778,
178.441883126102));
#39912=CARTESIAN_POINT('Ctrl Pts',(-56.640375327243,-111.022543021748,179.749521519335));
#39913=CARTESIAN_POINT('Ctrl Pts',(-58.2851519874995,-110.941480069743,
179.954699160921));
#39914=CARTESIAN_POINT('Ctrl Pts',(-59.929928647756,-110.860417117738,180.159876802508));
#39915=CARTESIAN_POINT('Ctrl Pts',(-61.2401372018543,-110.815021361064,
179.142403412702));
#39916=CARTESIAN_POINT('Ctrl Pts',(-62.5503457559527,-110.76962560439,178.124930022896));
#39917=CARTESIAN_POINT('Ctrl Pts',(-62.7643053849125,-110.841097307058,
176.480827714093));
#39918=CARTESIAN_POINT('Ctrl Pts',(-62.9782650138722,-110.912569009727,
174.83672540529));
#39919=CARTESIAN_POINT('Ctrl Pts',(-61.9764626513222,-111.113649063068,
173.529087012057));
#39920=CARTESIAN_POINT('Ctrl Pts',(-60.9746602887721,-111.314729116409,
172.221448618824));
#39921=CARTESIAN_POINT('Ctrl Pts',(-59.3497597543497,-111.582235597725,
172.016270977238));
#39922=CARTESIAN_POINT('Ctrl Pts',(-57.7248592199272,-111.84974207904,171.811093335651));
#39923=CARTESIAN_POINT('Ctrl Pts',(-56.4345267916629,-112.081581365025,
172.828566725457));
#39924=CARTESIAN_POINT('Ctrl Pts',(-55.1441943633985,-112.31342065101,173.846040115263));
#39925=CARTESIAN_POINT('Ctrl Pts',(-54.9501108602728,-112.428392477652,
175.490142424066));
#39926=CARTESIAN_POINT('Ctrl Pts',(-54.756027357147,-112.543364304294,177.134244732869));
#39927=CARTESIAN_POINT('Ctrl Pts',(-55.7777058455311,-112.528727780264,
178.441883126102));
#39928=CARTESIAN_POINT('Ctrl Pts',(-56.7993843339153,-112.514091256234,
179.749521519335));
#39929=CARTESIAN_POINT('Ctrl Pts',(-58.4441609941717,-112.433028304229,
179.954699160921));
#39930=CARTESIAN_POINT('Ctrl Pts',(-60.0889376544282,-112.351965352224,
180.159876802508));
#39931=CARTESIAN_POINT('Ctrl Pts',(-61.3991462085265,-112.30656959555,179.142403412702));
#39932=CARTESIAN_POINT('Ctrl Pts',(-62.7093547626249,-112.261173838875,
178.124930022896));
#39933=CARTESIAN_POINT('Ctrl Pts',(-62.9233143915847,-112.332645541544,
176.480827714093));
#39934=CARTESIAN_POINT('Ctrl Pts',(-63.1372740205445,-112.404117244213,
174.83672540529));
#39935=CARTESIAN_POINT('Ctrl Pts',(-62.1354716579944,-112.605197297554,
173.529087012057));
#39936=CARTESIAN_POINT('Ctrl Pts',(-61.1336692954443,-112.806277350895,
172.221448618824));
#39937=CARTESIAN_POINT('Ctrl Pts',(-59.5087687610219,-113.07378383221,172.016270977238));
#39938=CARTESIAN_POINT('Ctrl Pts',(-57.8838682265995,-113.341290313526,
171.811093335651));
#39939=CARTESIAN_POINT('Ctrl Pts',(-56.5935357983351,-113.573129599511,
172.828566725457));
#39940=CARTESIAN_POINT('Ctrl Pts',(-55.3032033700708,-113.804968885496,
173.846040115263));
#39941=CARTESIAN_POINT('Ctrl Pts',(-55.109119866945,-113.919940712138,175.490142424066));
#39942=CARTESIAN_POINT('Ctrl Pts',(-54.9150363638193,-114.03491253878,177.134244732869));
#39943=CARTESIAN_POINT('Ctrl Pts',(-55.9367148522034,-114.02027601475,178.441883126102));
#39944=CARTESIAN_POINT('Ctrl Pts',(-56.9583933405875,-114.005639490719,
179.749521519335));
#39945=CARTESIAN_POINT('Ctrl Pts',(-58.6031700008439,-113.924576538714,
179.954699160921));
#39946=CARTESIAN_POINT('Ctrl Pts',(-60.2479466611004,-113.84351358671,180.159876802508));
#39947=CARTESIAN_POINT('Ctrl Pts',(-61.5581552151988,-113.798117830035,
179.142403412702));
#39948=CARTESIAN_POINT('Ctrl Pts',(-62.8683637692972,-113.752722073361,
178.124930022896));
#39949=CARTESIAN_POINT('Ctrl Pts',(-63.0823233982569,-113.82419377603,176.480827714093));
#39950=CARTESIAN_POINT('Ctrl Pts',(-63.2962830272167,-113.895665478698,
174.83672540529));
#39951=CARTESIAN_POINT('Ctrl Pts',(-62.2944806646666,-114.096745532039,
173.529087012057));
#39952=CARTESIAN_POINT('Ctrl Pts',(-61.2926783021166,-114.29782558538,172.221448618824));
#39953=CARTESIAN_POINT('Ctrl Pts',(-59.6677777676941,-114.565332066696,
172.016270977238));
#39954=CARTESIAN_POINT('Ctrl Pts',(-58.0428772332717,-114.832838548011,
171.811093335651));
#39955=CARTESIAN_POINT('Ctrl Pts',(-56.7525448050073,-115.064677833996,
172.828566725457));
#39956=CARTESIAN_POINT('Ctrl Pts',(-55.462212376743,-115.296517119981,173.846040115263));
#39957=CARTESIAN_POINT('Ctrl Pts',(-55.2681288736172,-115.411488946623,
175.490142424066));
#39958=CARTESIAN_POINT('Ctrl Pts',(-55.0740453704915,-115.526460773265,
177.134244732869));
#39959=CARTESIAN_POINT('Ctrl Pts',(-56.0957238588756,-115.511824249235,
178.441883126102));
#39960=CARTESIAN_POINT('Ctrl Pts',(-57.1174023472597,-115.497187725205,
179.749521519335));
#39961=CARTESIAN_POINT('Ctrl Pts',(-58.7621790075162,-115.4161247732,179.954699160921));
#39962=CARTESIAN_POINT('Ctrl Pts',(-60.4069556677726,-115.335061821195,
180.159876802508));
#39963=CARTESIAN_POINT('Ctrl Pts',(-61.717164221871,-115.289666064521,179.142403412702));
#39964=CARTESIAN_POINT('Ctrl Pts',(-63.0273727759694,-115.244270307847,
178.124930022896));
#39965=CARTESIAN_POINT('Ctrl Pts',(-63.2413324049292,-115.315742010515,
176.480827714093));
#39966=CARTESIAN_POINT('Ctrl Pts',(-63.4552920338889,-115.387213713184,
174.83672540529));
#39967=CARTESIAN_POINT('Ctrl Pts',(-62.4534896713389,-115.588293766525,
173.529087012057));
#39968=CARTESIAN_POINT('Ctrl Pts',(-61.4516873087888,-115.789373819866,
172.221448618824));
#39969=CARTESIAN_POINT('Ctrl Pts',(-59.8267867743663,-116.056880301181,
172.016270977238));
#39970=CARTESIAN_POINT('Ctrl Pts',(-58.2018862399439,-116.324386782497,
171.811093335651));
#39971=CARTESIAN_POINT('Ctrl Pts',(-56.9115538116796,-116.556226068482,
172.828566725457));
#39972=CARTESIAN_POINT('Ctrl Pts',(-55.6212213834152,-116.788065354467,
173.846040115263));
#39973=CARTESIAN_POINT('Ctrl Pts',(-55.4271378802895,-116.903037181109,
175.490142424066));
#39974=CARTESIAN_POINT('Ctrl Pts',(-55.2330543771637,-117.018009007751,
177.134244732869));
#39975=CARTESIAN_POINT('Ctrl Pts',(-56.2547328655478,-117.003372483721,
178.441883126102));
#39976=CARTESIAN_POINT('Ctrl Pts',(-57.2764113539319,-116.98873595969,179.749521519335));
#39977=CARTESIAN_POINT('Ctrl Pts',(-58.9211880141884,-116.907673007686,
179.954699160921));
#39978=CARTESIAN_POINT('Ctrl Pts',(-60.5659646744449,-116.826610055681,
180.159876802508));
#39979=CARTESIAN_POINT('Ctrl Pts',(-61.8761732285432,-116.781214299006,
179.142403412702));
#39980=CARTESIAN_POINT('Ctrl Pts',(-63.1863817826416,-116.735818542332,
178.124930022896));
#39981=CARTESIAN_POINT('Ctrl Pts',(-63.4003414116014,-116.807290245001,
176.480827714093));
#39982=CARTESIAN_POINT('Ctrl Pts',(-63.6143010405612,-116.87876194767,174.83672540529));
#39983=CARTESIAN_POINT('Ctrl Pts',(-62.6124986780111,-117.079842001011,
173.529087012057));
#39984=CARTESIAN_POINT('Ctrl Pts',(-61.610696315461,-117.280922054351,172.221448618824));
#39985=CARTESIAN_POINT('Ctrl Pts',(-59.9857957810386,-117.548428535667,
172.016270977238));
#39986=CARTESIAN_POINT('Ctrl Pts',(-58.3608952466161,-117.815935016983,
171.811093335651));
#39987=CARTESIAN_POINT('Ctrl Pts',(-57.0705628183518,-118.047774302968,
172.828566725457));
#39988=CARTESIAN_POINT('Ctrl Pts',(-55.7802303900874,-118.279613588953,
173.846040115263));
#39989=CARTESIAN_POINT('Ctrl Pts',(-55.5861468869617,-118.394585415595,
175.490142424066));
#39990=CARTESIAN_POINT('Ctrl Pts',(-55.3920633838359,-118.509557242237,
177.134244732869));
#39991=CARTESIAN_POINT('Ctrl Pts',(-56.4137418722201,-118.494920718206,
178.441883126102));
#39992=CARTESIAN_POINT('Ctrl Pts',(-57.4354203606042,-118.480284194176,
179.749521519335));
#39993=CARTESIAN_POINT('Ctrl Pts',(-59.0801970208606,-118.399221242171,
179.954699160921));
#39994=CARTESIAN_POINT('Ctrl Pts',(-60.7249736811171,-118.318158290166,
180.159876802508));
#39995=CARTESIAN_POINT('Ctrl Pts',(-62.0351822352155,-118.272762533492,
179.142403412702));
#39996=CARTESIAN_POINT('Ctrl Pts',(-63.3453907893139,-118.227366776818,
178.124930022896));
#39997=CARTESIAN_POINT('Ctrl Pts',(-63.5593504182736,-118.298838479487,
176.480827714093));
#39998=CARTESIAN_POINT('Ctrl Pts',(-63.7733100472334,-118.370310182155,
174.83672540529));
#39999=CARTESIAN_POINT('Ctrl Pts',(-62.7715076846833,-118.571390235496,
173.529087012057));
#40000=CARTESIAN_POINT('Ctrl Pts',(-61.7697053221332,-118.772470288837,
172.221448618824));
#40001=CARTESIAN_POINT('Ctrl Pts',(-60.1448047877108,-119.039976770153,
172.016270977238));
#40002=CARTESIAN_POINT('Ctrl Pts',(-58.5199042532884,-119.307483251468,
171.811093335651));
#40003=CARTESIAN_POINT('Ctrl Pts',(-57.229571825024,-119.539322537453,172.828566725457));
#40004=CARTESIAN_POINT('Ctrl Pts',(-55.9392393967597,-119.771161823438,
173.846040115263));
#40005=CARTESIAN_POINT('Ctrl Pts',(-55.7451558936339,-119.88613365008,175.490142424066));
#40006=CARTESIAN_POINT('Ctrl Pts',(-55.5510723905082,-120.001105476722,
177.134244732869));
#40007=CARTESIAN_POINT('Ctrl Pts',(-56.5727508788923,-119.986468952692,
178.441883126102));
#40008=CARTESIAN_POINT('Ctrl Pts',(-57.5944293672764,-119.971832428662,
179.749521519335));
#40009=CARTESIAN_POINT('Ctrl Pts',(-59.2392060275328,-119.890769476657,
179.954699160921));
#40010=CARTESIAN_POINT('Ctrl Pts',(-60.8839826877893,-119.809706524652,
180.159876802508));
#40011=CARTESIAN_POINT('Ctrl Pts',(-62.1941912418877,-119.764310767978,
179.142403412702));
#40012=CARTESIAN_POINT('Ctrl Pts',(-63.5043997959861,-119.718915011303,
178.124930022896));
#40013=CARTESIAN_POINT('Ctrl Pts',(-63.7183594249458,-119.790386713972,
176.480827714093));
#40014=CARTESIAN_POINT('Ctrl Pts',(-63.9323190539056,-119.861858416641,
174.83672540529));
#40015=CARTESIAN_POINT('Ctrl Pts',(-62.9305166913555,-120.062938469982,
173.529087012057));
#40016=CARTESIAN_POINT('Ctrl Pts',(-61.9287143288055,-120.264018523323,
172.221448618824));
#40017=CARTESIAN_POINT('Ctrl Pts',(-60.303813794383,-120.531525004638,172.016270977238));
#40018=CARTESIAN_POINT('Ctrl Pts',(-58.6789132599606,-120.799031485954,
171.811093335651));
#40019=CARTESIAN_POINT('Ctrl Pts',(-57.3885808316962,-121.030870771939,
172.828566725457));
#40020=CARTESIAN_POINT('Ctrl Pts',(-56.0982484034319,-121.262710057924,
173.846040115263));
#40021=CARTESIAN_POINT('Ctrl Pts',(-55.9041649003061,-121.377681884566,
175.490142424066));
#40022=CARTESIAN_POINT('Ctrl Pts',(-55.7100813971804,-121.492653711208,
177.134244732869));
#40023=CARTESIAN_POINT('Ctrl Pts',(-56.7317598855645,-121.478017187178,
178.441883126102));
#40024=CARTESIAN_POINT('Ctrl Pts',(-57.7534383739486,-121.463380663147,
179.749521519335));
#40025=CARTESIAN_POINT('Ctrl Pts',(-59.3982150342051,-121.382317711142,
179.954699160921));
#40026=CARTESIAN_POINT('Ctrl Pts',(-61.0429916944615,-121.301254759138,
180.159876802508));
#40027=CARTESIAN_POINT('Ctrl Pts',(-62.3532002485599,-121.255859002463,
179.142403412702));
#40028=CARTESIAN_POINT('Ctrl Pts',(-63.6634088026583,-121.210463245789,
178.124930022896));
#40029=CARTESIAN_POINT('Ctrl Pts',(-63.8773684316181,-121.281934948458,
176.480827714093));
#40030=CARTESIAN_POINT('Ctrl Pts',(-64.0913280605779,-121.353406651126,
174.83672540529));
#40031=CARTESIAN_POINT('Ctrl Pts',(-63.0895256980278,-121.554486704467,
173.529087012057));
#40032=CARTESIAN_POINT('Ctrl Pts',(-62.0877233354777,-121.755566757808,
172.221448618824));
#40033=CARTESIAN_POINT('Ctrl Pts',(-60.4628228010552,-122.023073239124,
172.016270977238));
#40034=CARTESIAN_POINT('Ctrl Pts',(-58.8379222666328,-122.290579720439,
171.811093335651));
#40035=CARTESIAN_POINT('Ctrl Pts',(-57.5475898383685,-122.522419006424,
172.828566725457));
#40036=CARTESIAN_POINT('Ctrl Pts',(-56.2572574101041,-122.754258292409,
173.846040115263));
#40037=CARTESIAN_POINT('Ctrl Pts',(-56.0631739069784,-122.869230119051,
175.490142424066));
#40038=CARTESIAN_POINT('Ctrl Pts',(-55.8690904038526,-122.984201945693,
177.134244732869));
#40039=CARTESIAN_POINT('Ctrl Pts',(-56.8907688922367,-122.969565421663,
178.441883126102));
#40040=CARTESIAN_POINT('Ctrl Pts',(-57.9124473806208,-122.954928897633,
179.749521519335));
#40041=CARTESIAN_POINT('Ctrl Pts',(-59.5572240408773,-122.873865945628,
179.954699160921));
#40042=CARTESIAN_POINT('Ctrl Pts',(-61.2020007011338,-122.792802993623,
180.159876802508));
#40043=CARTESIAN_POINT('Ctrl Pts',(-62.5122092552321,-122.747407236949,
179.142403412702));
#40044=CARTESIAN_POINT('Ctrl Pts',(-63.8224178093305,-122.702011480275,
178.124930022896));
#40045=CARTESIAN_POINT('Ctrl Pts',(-64.0363774382903,-122.773483182943,
176.480827714093));
#40046=CARTESIAN_POINT('Ctrl Pts',(-64.2503370672501,-122.844954885612,
174.83672540529));
#40047=CARTESIAN_POINT('Ctrl Pts',(-63.2485347047,-123.046034938953,173.529087012057));
#40048=CARTESIAN_POINT('Ctrl Pts',(-62.2467323421499,-123.247114992294,
172.221448618824));
#40049=CARTESIAN_POINT('Ctrl Pts',(-60.6218318077275,-123.514621473609,
172.016270977238));
#40050=CARTESIAN_POINT('Ctrl Pts',(-58.996931273305,-123.782127954925,171.811093335651));
#40051=CARTESIAN_POINT('Ctrl Pts',(-57.7065988450407,-124.01396724091,172.828566725457));
#40052=CARTESIAN_POINT('Ctrl Pts',(-56.4162664167763,-124.245806526895,
173.846040115263));
#40053=CARTESIAN_POINT('Ctrl Pts',(-56.2221829136506,-124.360778353537,
175.490142424066));
#40054=CARTESIAN_POINT('Ctrl Pts',(-56.0280994105248,-124.475750180179,
177.134244732869));
#40055=CARTESIAN_POINT('Ctrl Pts',(-57.049777898909,-124.461113656149,178.441883126102));
#40056=CARTESIAN_POINT('Ctrl Pts',(-58.0714563872931,-124.446477132119,
179.749521519335));
#40057=CARTESIAN_POINT('Ctrl Pts',(-59.7162330475495,-124.365414180114,
179.954699160921));
#40058=CARTESIAN_POINT('Ctrl Pts',(-61.361009707806,-124.284351228109,180.159876802508));
#40059=CARTESIAN_POINT('Ctrl Pts',(-62.6712182619044,-124.238955471435,
179.142403412702));
#40060=CARTESIAN_POINT('Ctrl Pts',(-63.9814268160028,-124.19355971476,178.124930022896));
#40061=CARTESIAN_POINT('Ctrl Pts',(-64.1953864449625,-124.265031417429,
176.480827714093));
#40062=CARTESIAN_POINT('Ctrl Pts',(-64.4093460739223,-124.336503120098,
174.83672540529));
#40063=CARTESIAN_POINT('Ctrl Pts',(-63.4075437113722,-124.537583173439,
173.529087012057));
#40064=CARTESIAN_POINT('Ctrl Pts',(-62.4057413488222,-124.73866322678,172.221448618824));
#40065=CARTESIAN_POINT('Ctrl Pts',(-60.7808408143997,-125.006169708095,
172.016270977238));
#40066=CARTESIAN_POINT('Ctrl Pts',(-59.1559402799773,-125.273676189411,
171.811093335651));
#40067=CARTESIAN_POINT('Ctrl Pts',(-57.8656078517129,-125.505515475396,
172.828566725457));
#40068=CARTESIAN_POINT('Ctrl Pts',(-56.5752754234486,-125.737354761381,
173.846040115263));
#40069=CARTESIAN_POINT('Ctrl Pts',(-56.3811919203228,-125.852326588023,
175.490142424066));
#40070=CARTESIAN_POINT('Ctrl Pts',(-56.1871084171971,-125.967298414665,
177.134244732869));
#40071=CARTESIAN_POINT('Ctrl Pts',(-57.2087869055812,-125.952661890634,
178.441883126102));
#40072=CARTESIAN_POINT('Ctrl Pts',(-58.2304653939653,-125.938025366604,
179.749521519335));
#40073=CARTESIAN_POINT('Ctrl Pts',(-59.8752420542218,-125.856962414599,
179.954699160921));
#40074=CARTESIAN_POINT('Ctrl Pts',(-61.5200187144782,-125.775899462594,
180.159876802508));
#40075=CARTESIAN_POINT('Ctrl Pts',(-62.8302272685766,-125.73050370592,179.142403412702));
#40076=CARTESIAN_POINT('Ctrl Pts',(-64.140435822675,-125.685107949246,178.124930022896));
#40077=CARTESIAN_POINT('Ctrl Pts',(-64.3543954516348,-125.756579651915,
176.480827714093));
#40078=CARTESIAN_POINT('Ctrl Pts',(-64.5683550805945,-125.828051354583,
174.83672540529));
#40079=CARTESIAN_POINT('Ctrl Pts',(-63.5665527180444,-126.029131407924,
173.529087012057));
#40080=CARTESIAN_POINT('Ctrl Pts',(-62.5647503554944,-126.230211461265,
172.221448618824));
#40081=CARTESIAN_POINT('Ctrl Pts',(-60.9398498210719,-126.497717942581,
172.016270977238));
#40082=CARTESIAN_POINT('Ctrl Pts',(-59.3149492866495,-126.765224423896,
171.811093335651));
#40083=CARTESIAN_POINT('Ctrl Pts',(-58.0246168583851,-126.997063709881,
172.828566725457));
#40084=CARTESIAN_POINT('Ctrl Pts',(-56.7342844301208,-127.228902995866,
173.846040115263));
#40085=CARTESIAN_POINT('Ctrl Pts',(-56.5402009269951,-127.343874822508,
175.490142424066));
#40086=CARTESIAN_POINT('Ctrl Pts',(-56.3461174238693,-127.45884664915,177.134244732869));
#40087=CARTESIAN_POINT('Ctrl Pts',(-57.3677959122534,-127.44421012512,178.441883126102));
#40088=CARTESIAN_POINT('Ctrl Pts',(-58.3894744006375,-127.42957360109,179.749521519335));
#40089=CARTESIAN_POINT('Ctrl Pts',(-60.034251060894,-127.348510649085,179.954699160921));
#40090=CARTESIAN_POINT('Ctrl Pts',(-61.6790277211505,-127.26744769708,180.159876802508));
#40091=CARTESIAN_POINT('Ctrl Pts',(-62.9892362752488,-127.222051940406,
179.142403412702));
#40092=CARTESIAN_POINT('Ctrl Pts',(-64.2994448293472,-127.176656183731,
178.124930022896));
#40093=CARTESIAN_POINT('Ctrl Pts',(-64.513404458307,-127.2481278864,176.480827714093));
#40094=CARTESIAN_POINT('Ctrl Pts',(-64.7273640872667,-127.319599589069,
174.83672540529));
#40095=CARTESIAN_POINT('Ctrl Pts',(-63.7255617247167,-127.52067964241,173.529087012057));
#40096=CARTESIAN_POINT('Ctrl Pts',(-62.7237593621666,-127.721759695751,
172.221448618824));
#40097=CARTESIAN_POINT('Ctrl Pts',(-61.0988588277442,-127.989266177066,
172.016270977238));
#40098=CARTESIAN_POINT('Ctrl Pts',(-59.4739582933217,-128.256772658382,
171.811093335651));
#40099=CARTESIAN_POINT('Ctrl Pts',(-58.1836258650574,-128.488611944367,
172.828566725457));
#40100=CARTESIAN_POINT('Ctrl Pts',(-56.893293436793,-128.720451230352,173.846040115263));
#40101=CARTESIAN_POINT('Ctrl Pts',(-56.6992099336673,-128.835423056994,
175.490142424066));
#40102=CARTESIAN_POINT('Ctrl Pts',(-56.5051264305415,-128.950394883636,
177.134244732869));
#40103=CARTESIAN_POINT('Ctrl Pts',(-57.5268049189256,-128.935758359606,
178.441883126102));
#40104=CARTESIAN_POINT('Ctrl Pts',(-58.5484834073098,-128.921121835575,
179.749521519335));
#40105=CARTESIAN_POINT('Ctrl Pts',(-60.1932600675662,-128.84005888357,179.954699160921));
#40106=CARTESIAN_POINT('Ctrl Pts',(-61.8380367278227,-128.758995931566,
180.159876802508));
#40107=CARTESIAN_POINT('Ctrl Pts',(-63.1482452819211,-128.713600174891,
179.142403412702));
#40108=CARTESIAN_POINT('Ctrl Pts',(-64.4584538360194,-128.668204418217,
178.124930022896));
#40109=CARTESIAN_POINT('Ctrl Pts',(-64.6724134649792,-128.739676120886,
176.480827714093));
#40110=CARTESIAN_POINT('Ctrl Pts',(-64.886373093939,-128.811147823554,174.83672540529));
#40111=CARTESIAN_POINT('Ctrl Pts',(-63.8845707313889,-129.012227876895,
173.529087012057));
#40112=CARTESIAN_POINT('Ctrl Pts',(-62.8827683688388,-129.213307930236,
172.221448618824));
#40113=CARTESIAN_POINT('Ctrl Pts',(-61.2578678344164,-129.480814411552,
172.016270977238));
#40114=CARTESIAN_POINT('Ctrl Pts',(-59.632967299994,-129.748320892867,171.811093335651));
#40115=CARTESIAN_POINT('Ctrl Pts',(-58.3426348717296,-129.980160178852,
172.828566725457));
#40116=CARTESIAN_POINT('Ctrl Pts',(-57.0523024434653,-130.211999464837,
173.846040115263));
#40117=CARTESIAN_POINT('Ctrl Pts',(-56.8582189403395,-130.326971291479,
175.490142424066));
#40118=CARTESIAN_POINT('Ctrl Pts',(-56.6641354372138,-130.441943118121,
177.134244732869));
#40119=CARTESIAN_POINT('Ctrl Pts',(-57.6858139255979,-130.427306594091,
178.441883126102));
#40120=CARTESIAN_POINT('Ctrl Pts',(-58.707492413982,-130.412670070061,179.749521519335));
#40121=CARTESIAN_POINT('Ctrl Pts',(-60.3522690742384,-130.331607118056,
179.954699160921));
#40122=CARTESIAN_POINT('Ctrl Pts',(-61.9970457344949,-130.250544166051,
180.159876802508));
#40123=CARTESIAN_POINT('Ctrl Pts',(-63.3072542885933,-130.205148409377,
179.142403412702));
#40124=CARTESIAN_POINT('Ctrl Pts',(-64.6174628426917,-130.159752652703,
178.124930022896));
#40125=CARTESIAN_POINT('Ctrl Pts',(-64.8314224716514,-130.231224355371,
176.480827714093));
#40126=CARTESIAN_POINT('Ctrl Pts',(-65.0453821006112,-130.30269605804,174.83672540529));
#40127=CARTESIAN_POINT('Ctrl Pts',(-64.0435797380611,-130.503776111381,
173.529087012057));
#40128=CARTESIAN_POINT('Ctrl Pts',(-63.041777375511,-130.704856164722,172.221448618824));
#40129=CARTESIAN_POINT('Ctrl Pts',(-61.4168768410886,-130.972362646037,
172.016270977238));
#40130=CARTESIAN_POINT('Ctrl Pts',(-59.7919763066662,-131.239869127353,
171.811093335651));
#40131=CARTESIAN_POINT('Ctrl Pts',(-58.5016438784018,-131.471708413338,
172.828566725457));
#40132=CARTESIAN_POINT('Ctrl Pts',(-57.2113114501375,-131.703547699323,
173.846040115263));
#40133=CARTESIAN_POINT('Ctrl Pts',(-57.0172279470117,-131.818519525965,
175.490142424066));
#40134=CARTESIAN_POINT('Ctrl Pts',(-56.823144443886,-131.933491352607,177.134244732869));
#40135=CARTESIAN_POINT('Ctrl Pts',(-57.8448229322701,-131.918854828577,
178.441883126102));
#40136=CARTESIAN_POINT('Ctrl Pts',(-58.8665014206542,-131.904218304546,
179.749521519335));
#40137=CARTESIAN_POINT('Ctrl Pts',(-60.5112780809107,-131.823155352542,
179.954699160921));
#40138=CARTESIAN_POINT('Ctrl Pts',(-61.5752386421509,-131.770717969403,
180.087422906321));
#40139=CARTESIAN_POINT('Ctrl Pts',(-62.5639794549305,-131.730759788555,
179.67061371833));
#40140=CARTESIAN_POINT('Ctrl Pts',(-51.1930600664641,-67.8253476561165,
175.613978758287));
#40141=CARTESIAN_POINT('Ctrl Pts',(-51.049982232031,-67.9348819377124,176.847053256227));
#40142=CARTESIAN_POINT('Ctrl Pts',(-51.8187242395064,-67.9472101323889,
177.827780274605));
#40143=CARTESIAN_POINT('Ctrl Pts',(-52.5874662469819,-67.9595383270654,
178.808507292983));
#40144=CARTESIAN_POINT('Ctrl Pts',(-53.8235310368257,-67.9220467910073,
178.96239024542));
#40145=CARTESIAN_POINT('Ctrl Pts',(-55.0595958266696,-67.8845552549492,
179.116273197858));
#40146=CARTESIAN_POINT('Ctrl Pts',(-56.0447349914363,-67.8738140669319,
178.353169537834));
#40147=CARTESIAN_POINT('Ctrl Pts',(-57.029874156203,-67.8630728789146,177.590065877811));
#40148=CARTESIAN_POINT('Ctrl Pts',(-57.1928281164701,-67.9399821266294,
176.356991379871));
#40149=CARTESIAN_POINT('Ctrl Pts',(-57.3557820767372,-68.0168913743442,
175.123916881932));
#40150=CARTESIAN_POINT('Ctrl Pts',(-56.6069161950958,-68.1910067089784,
174.143189863554));
#40151=CARTESIAN_POINT('Ctrl Pts',(-55.8580503134544,-68.3651220436126,
173.162462845176));
#40152=CARTESIAN_POINT('Ctrl Pts',(-54.6418616494445,-68.5890571089814,
173.008579892738));
#40153=CARTESIAN_POINT('Ctrl Pts',(-53.4256729854347,-68.8129921743502,
172.854696940301));
#40154=CARTESIAN_POINT('Ctrl Pts',(-52.460409946502,-69.0101768916782,173.617800600325));
#40155=CARTESIAN_POINT('Ctrl Pts',(-51.4951469075694,-69.2073616090062,
174.380904260348));
#40156=CARTESIAN_POINT('Ctrl Pts',(-51.3520690731363,-69.3168958906021,
175.613978758287));
#40157=CARTESIAN_POINT('Ctrl Pts',(-51.2089912387032,-69.426430172198,176.847053256227));
#40158=CARTESIAN_POINT('Ctrl Pts',(-51.9777332461786,-69.4387583668745,
177.827780274605));
#40159=CARTESIAN_POINT('Ctrl Pts',(-52.7464752536541,-69.451086561551,178.808507292983));
#40160=CARTESIAN_POINT('Ctrl Pts',(-53.9825400434979,-69.4135950254929,
178.96239024542));
#40161=CARTESIAN_POINT('Ctrl Pts',(-55.2186048333418,-69.3761034894348,
179.116273197858));
#40162=CARTESIAN_POINT('Ctrl Pts',(-56.2037439981085,-69.3653623014175,
178.353169537834));
#40163=CARTESIAN_POINT('Ctrl Pts',(-57.1888831628752,-69.3546211134002,
177.590065877811));
#40164=CARTESIAN_POINT('Ctrl Pts',(-57.3518371231423,-69.431530361115,176.356991379871));
#40165=CARTESIAN_POINT('Ctrl Pts',(-57.5147910834094,-69.5084396088298,
175.123916881932));
#40166=CARTESIAN_POINT('Ctrl Pts',(-56.765925201768,-69.682554943464,174.143189863554));
#40167=CARTESIAN_POINT('Ctrl Pts',(-56.0170593201266,-69.8566702780982,
173.162462845176));
#40168=CARTESIAN_POINT('Ctrl Pts',(-54.8008706561167,-70.080605343467,173.008579892738));
#40169=CARTESIAN_POINT('Ctrl Pts',(-53.5846819921069,-70.3045404088358,
172.854696940301));
#40170=CARTESIAN_POINT('Ctrl Pts',(-52.6194189531743,-70.5017251261638,
173.617800600325));
#40171=CARTESIAN_POINT('Ctrl Pts',(-51.6541559142416,-70.6989098434918,
174.380904260348));
#40172=CARTESIAN_POINT('Ctrl Pts',(-51.5110780798085,-70.8084441250877,
175.613978758287));
#40173=CARTESIAN_POINT('Ctrl Pts',(-51.3680002453754,-70.9179784066836,
176.847053256227));
#40174=CARTESIAN_POINT('Ctrl Pts',(-52.1367422528509,-70.9303066013601,
177.827780274605));
#40175=CARTESIAN_POINT('Ctrl Pts',(-52.9054842603263,-70.9426347960366,
178.808507292983));
#40176=CARTESIAN_POINT('Ctrl Pts',(-54.1415490501702,-70.9051432599785,
178.96239024542));
#40177=CARTESIAN_POINT('Ctrl Pts',(-55.377613840014,-70.8676517239204,179.116273197858));
#40178=CARTESIAN_POINT('Ctrl Pts',(-56.3627530047807,-70.8569105359031,
178.353169537834));
#40179=CARTESIAN_POINT('Ctrl Pts',(-57.3478921695474,-70.8461693478859,
177.590065877811));
#40180=CARTESIAN_POINT('Ctrl Pts',(-57.5108461298145,-70.9230785956006,
176.356991379871));
#40181=CARTESIAN_POINT('Ctrl Pts',(-57.6738000900816,-70.9999878433154,
175.123916881932));
#40182=CARTESIAN_POINT('Ctrl Pts',(-56.9249342084402,-71.1741031779496,
174.143189863554));
#40183=CARTESIAN_POINT('Ctrl Pts',(-56.1760683267988,-71.3482185125838,
173.162462845176));
#40184=CARTESIAN_POINT('Ctrl Pts',(-54.959879662789,-71.5721535779526,173.008579892738));
#40185=CARTESIAN_POINT('Ctrl Pts',(-53.7436909987791,-71.7960886433214,
172.854696940301));
#40186=CARTESIAN_POINT('Ctrl Pts',(-52.7784279598465,-71.9932733606494,
173.617800600325));
#40187=CARTESIAN_POINT('Ctrl Pts',(-51.8131649209138,-72.1904580779774,
174.380904260348));
#40188=CARTESIAN_POINT('Ctrl Pts',(-51.6700870864807,-72.2999923595733,
175.613978758287));
#40189=CARTESIAN_POINT('Ctrl Pts',(-51.5270092520476,-72.4095266411692,
176.847053256227));
#40190=CARTESIAN_POINT('Ctrl Pts',(-52.2957512595231,-72.4218548358457,
177.827780274605));
#40191=CARTESIAN_POINT('Ctrl Pts',(-53.0644932669986,-72.4341830305222,
178.808507292983));
#40192=CARTESIAN_POINT('Ctrl Pts',(-54.3005580568424,-72.3966914944641,
178.96239024542));
#40193=CARTESIAN_POINT('Ctrl Pts',(-55.5366228466863,-72.359199958406,179.116273197858));
#40194=CARTESIAN_POINT('Ctrl Pts',(-56.5217620114529,-72.3484587703887,
178.353169537834));
#40195=CARTESIAN_POINT('Ctrl Pts',(-57.5069011762196,-72.3377175823714,
177.590065877811));
#40196=CARTESIAN_POINT('Ctrl Pts',(-57.6698551364867,-72.4146268300862,
176.356991379871));
#40197=CARTESIAN_POINT('Ctrl Pts',(-57.8328090967539,-72.491536077801,175.123916881932));
#40198=CARTESIAN_POINT('Ctrl Pts',(-57.0839432151125,-72.6656514124352,
174.143189863554));
#40199=CARTESIAN_POINT('Ctrl Pts',(-56.335077333471,-72.8397667470694,173.162462845176));
#40200=CARTESIAN_POINT('Ctrl Pts',(-55.1188886694612,-73.0637018124382,
173.008579892738));
#40201=CARTESIAN_POINT('Ctrl Pts',(-53.9027000054514,-73.287636877807,172.854696940301));
#40202=CARTESIAN_POINT('Ctrl Pts',(-52.9374369665187,-73.484821595135,173.617800600325));
#40203=CARTESIAN_POINT('Ctrl Pts',(-51.9721739275861,-73.682006312463,174.380904260348));
#40204=CARTESIAN_POINT('Ctrl Pts',(-51.829096093153,-73.7915405940589,175.613978758287));
#40205=CARTESIAN_POINT('Ctrl Pts',(-51.6860182587199,-73.9010748756548,
176.847053256227));
#40206=CARTESIAN_POINT('Ctrl Pts',(-52.4547602661953,-73.9134030703313,
177.827780274605));
#40207=CARTESIAN_POINT('Ctrl Pts',(-53.2235022736708,-73.9257312650078,
178.808507292983));
#40208=CARTESIAN_POINT('Ctrl Pts',(-54.4595670635146,-73.8882397289497,
178.96239024542));
#40209=CARTESIAN_POINT('Ctrl Pts',(-55.6956318533585,-73.8507481928916,
179.116273197858));
#40210=CARTESIAN_POINT('Ctrl Pts',(-56.6807710181252,-73.8400070048743,
178.353169537834));
#40211=CARTESIAN_POINT('Ctrl Pts',(-57.6659101828918,-73.829265816857,177.590065877811));
#40212=CARTESIAN_POINT('Ctrl Pts',(-57.828864143159,-73.9061750645718,176.356991379871));
#40213=CARTESIAN_POINT('Ctrl Pts',(-57.9918181034261,-73.9830843122866,
175.123916881932));
#40214=CARTESIAN_POINT('Ctrl Pts',(-57.2429522217847,-74.1571996469208,
174.143189863554));
#40215=CARTESIAN_POINT('Ctrl Pts',(-56.4940863401433,-74.3313149815551,
173.162462845176));
#40216=CARTESIAN_POINT('Ctrl Pts',(-55.2778976761334,-74.5552500469238,
173.008579892738));
#40217=CARTESIAN_POINT('Ctrl Pts',(-54.0617090121236,-74.7791851122926,
172.854696940301));
#40218=CARTESIAN_POINT('Ctrl Pts',(-53.0964459731909,-74.9763698296206,
173.617800600325));
#40219=CARTESIAN_POINT('Ctrl Pts',(-52.1311829342583,-75.1735545469486,
174.380904260348));
#40220=CARTESIAN_POINT('Ctrl Pts',(-51.9881050998252,-75.2830888285445,
175.613978758287));
#40221=CARTESIAN_POINT('Ctrl Pts',(-51.8450272653921,-75.3926231101404,
176.847053256227));
#40222=CARTESIAN_POINT('Ctrl Pts',(-52.6137692728675,-75.4049513048169,
177.827780274605));
#40223=CARTESIAN_POINT('Ctrl Pts',(-53.382511280343,-75.4172794994934,178.808507292983));
#40224=CARTESIAN_POINT('Ctrl Pts',(-54.6185760701869,-75.3797879634353,
178.96239024542));
#40225=CARTESIAN_POINT('Ctrl Pts',(-55.8546408600307,-75.3422964273772,
179.116273197858));
#40226=CARTESIAN_POINT('Ctrl Pts',(-56.8397800247974,-75.3315552393599,
178.353169537834));
#40227=CARTESIAN_POINT('Ctrl Pts',(-57.8249191895641,-75.3208140513426,
177.590065877811));
#40228=CARTESIAN_POINT('Ctrl Pts',(-57.9878731498312,-75.3977232990574,
176.356991379871));
#40229=CARTESIAN_POINT('Ctrl Pts',(-58.1508271100983,-75.4746325467722,
175.123916881932));
#40230=CARTESIAN_POINT('Ctrl Pts',(-57.4019612284569,-75.6487478814064,
174.143189863554));
#40231=CARTESIAN_POINT('Ctrl Pts',(-56.6530953468155,-75.8228632160406,
173.162462845176));
#40232=CARTESIAN_POINT('Ctrl Pts',(-55.4369066828056,-76.0467982814094,
173.008579892738));
#40233=CARTESIAN_POINT('Ctrl Pts',(-54.2207180187958,-76.2707333467782,
172.854696940301));
#40234=CARTESIAN_POINT('Ctrl Pts',(-53.2554549798632,-76.4679180641062,
173.617800600325));
#40235=CARTESIAN_POINT('Ctrl Pts',(-52.2901919409305,-76.6651027814342,
174.380904260348));
#40236=CARTESIAN_POINT('Ctrl Pts',(-52.1471141064974,-76.7746370630301,
175.613978758287));
#40237=CARTESIAN_POINT('Ctrl Pts',(-52.0040362720643,-76.884171344626,176.847053256227));
#40238=CARTESIAN_POINT('Ctrl Pts',(-52.7727782795398,-76.8964995393025,
177.827780274605));
#40239=CARTESIAN_POINT('Ctrl Pts',(-53.5415202870152,-76.9088277339789,
178.808507292983));
#40240=CARTESIAN_POINT('Ctrl Pts',(-54.7775850768591,-76.8713361979209,
178.96239024542));
#40241=CARTESIAN_POINT('Ctrl Pts',(-56.013649866703,-76.8338446618628,179.116273197858));
#40242=CARTESIAN_POINT('Ctrl Pts',(-56.9987890314696,-76.8231034738455,
178.353169537834));
#40243=CARTESIAN_POINT('Ctrl Pts',(-57.9839281962363,-76.8123622858282,
177.590065877811));
#40244=CARTESIAN_POINT('Ctrl Pts',(-58.1468821565034,-76.8892715335431,
176.356991379871));
#40245=CARTESIAN_POINT('Ctrl Pts',(-58.3098361167706,-76.9661807812578,
175.123916881932));
#40246=CARTESIAN_POINT('Ctrl Pts',(-57.5609702351291,-77.140296115892,174.143189863554));
#40247=CARTESIAN_POINT('Ctrl Pts',(-56.8121043534877,-77.3144114505262,
173.162462845176));
#40248=CARTESIAN_POINT('Ctrl Pts',(-55.5959156894779,-77.538346515895,173.008579892738));
#40249=CARTESIAN_POINT('Ctrl Pts',(-54.379727025468,-77.7622815812638,172.854696940301));
#40250=CARTESIAN_POINT('Ctrl Pts',(-53.4144639865354,-77.9594662985918,
173.617800600325));
#40251=CARTESIAN_POINT('Ctrl Pts',(-52.4492009476028,-78.1566510159198,
174.380904260348));
#40252=CARTESIAN_POINT('Ctrl Pts',(-52.3061231131696,-78.2661852975157,
175.613978758287));
#40253=CARTESIAN_POINT('Ctrl Pts',(-52.1630452787365,-78.3757195791116,
176.847053256227));
#40254=CARTESIAN_POINT('Ctrl Pts',(-52.931787286212,-78.3880477737881,177.827780274605));
#40255=CARTESIAN_POINT('Ctrl Pts',(-53.7005292936875,-78.4003759684646,
178.808507292983));
#40256=CARTESIAN_POINT('Ctrl Pts',(-54.9365940835313,-78.3628844324065,
178.96239024542));
#40257=CARTESIAN_POINT('Ctrl Pts',(-56.1726588733752,-78.3253928963484,
179.116273197858));
#40258=CARTESIAN_POINT('Ctrl Pts',(-57.1577980381419,-78.3146517083311,
178.353169537834));
#40259=CARTESIAN_POINT('Ctrl Pts',(-58.1429372029085,-78.3039105203139,
177.590065877811));
#40260=CARTESIAN_POINT('Ctrl Pts',(-58.3058911631757,-78.3808197680286,
176.356991379871));
#40261=CARTESIAN_POINT('Ctrl Pts',(-58.4688451234428,-78.4577290157434,
175.123916881932));
#40262=CARTESIAN_POINT('Ctrl Pts',(-57.7199792418014,-78.6318443503776,
174.143189863554));
#40263=CARTESIAN_POINT('Ctrl Pts',(-56.9711133601599,-78.8059596850118,
173.162462845176));
#40264=CARTESIAN_POINT('Ctrl Pts',(-55.7549246961501,-79.0298947503806,
173.008579892738));
#40265=CARTESIAN_POINT('Ctrl Pts',(-54.5387360321403,-79.2538298157494,
172.854696940301));
#40266=CARTESIAN_POINT('Ctrl Pts',(-53.5734729932076,-79.4510145330774,
173.617800600325));
#40267=CARTESIAN_POINT('Ctrl Pts',(-52.608209954275,-79.6481992504054,174.380904260348));
#40268=CARTESIAN_POINT('Ctrl Pts',(-52.4651321198419,-79.7577335320013,
175.613978758287));
#40269=CARTESIAN_POINT('Ctrl Pts',(-52.3220542854088,-79.8672678135972,
176.847053256227));
#40270=CARTESIAN_POINT('Ctrl Pts',(-53.0907962928842,-79.8795960082737,
177.827780274605));
#40271=CARTESIAN_POINT('Ctrl Pts',(-53.8595383003597,-79.8919242029502,
178.808507292983));
#40272=CARTESIAN_POINT('Ctrl Pts',(-55.0956030902035,-79.8544326668921,
178.96239024542));
#40273=CARTESIAN_POINT('Ctrl Pts',(-56.3316678800474,-79.816941130834,179.116273197858));
#40274=CARTESIAN_POINT('Ctrl Pts',(-57.3168070448141,-79.8061999428167,
178.353169537834));
#40275=CARTESIAN_POINT('Ctrl Pts',(-58.3019462095808,-79.7954587547994,
177.590065877811));
#40276=CARTESIAN_POINT('Ctrl Pts',(-58.4649001698479,-79.8723680025142,
176.356991379871));
#40277=CARTESIAN_POINT('Ctrl Pts',(-58.627854130115,-79.949277250229,175.123916881932));
#40278=CARTESIAN_POINT('Ctrl Pts',(-57.8789882484736,-80.1233925848632,
174.143189863554));
#40279=CARTESIAN_POINT('Ctrl Pts',(-57.1301223668322,-80.2975079194974,
173.162462845176));
#40280=CARTESIAN_POINT('Ctrl Pts',(-55.9139337028223,-80.5214429848662,
173.008579892738));
#40281=CARTESIAN_POINT('Ctrl Pts',(-54.6977450388125,-80.745378050235,172.854696940301));
#40282=CARTESIAN_POINT('Ctrl Pts',(-53.7324819998798,-80.942562767563,173.617800600325));
#40283=CARTESIAN_POINT('Ctrl Pts',(-52.7672189609472,-81.139747484891,174.380904260348));
#40284=CARTESIAN_POINT('Ctrl Pts',(-52.6241411265141,-81.2492817664869,
175.613978758287));
#40285=CARTESIAN_POINT('Ctrl Pts',(-52.481063292081,-81.3588160480828,176.847053256227));
#40286=CARTESIAN_POINT('Ctrl Pts',(-53.2498052995565,-81.3711442427593,
177.827780274605));
#40287=CARTESIAN_POINT('Ctrl Pts',(-54.0185473070319,-81.3834724374358,
178.808507292983));
#40288=CARTESIAN_POINT('Ctrl Pts',(-55.2546120968758,-81.3459809013777,
178.96239024542));
#40289=CARTESIAN_POINT('Ctrl Pts',(-56.4906768867196,-81.3084893653196,
179.116273197858));
#40290=CARTESIAN_POINT('Ctrl Pts',(-57.4758160514863,-81.2977481773023,
178.353169537834));
#40291=CARTESIAN_POINT('Ctrl Pts',(-58.460955216253,-81.287006989285,177.590065877811));
#40292=CARTESIAN_POINT('Ctrl Pts',(-58.6239091765201,-81.3639162369998,
176.356991379871));
#40293=CARTESIAN_POINT('Ctrl Pts',(-58.7868631367872,-81.4408254847146,
175.123916881932));
#40294=CARTESIAN_POINT('Ctrl Pts',(-58.0379972551458,-81.6149408193488,
174.143189863554));
#40295=CARTESIAN_POINT('Ctrl Pts',(-57.2891313735044,-81.789056153983,173.162462845176));
#40296=CARTESIAN_POINT('Ctrl Pts',(-56.0729427094946,-82.0129912193518,
173.008579892738));
#40297=CARTESIAN_POINT('Ctrl Pts',(-54.8567540454847,-82.2369262847206,
172.854696940301));
#40298=CARTESIAN_POINT('Ctrl Pts',(-53.8914910065521,-82.4341110020486,
173.617800600325));
#40299=CARTESIAN_POINT('Ctrl Pts',(-52.9262279676194,-82.6312957193766,
174.380904260348));
#40300=CARTESIAN_POINT('Ctrl Pts',(-52.7831501331863,-82.7408300009725,
175.613978758287));
#40301=CARTESIAN_POINT('Ctrl Pts',(-52.6400722987532,-82.8503642825684,
176.847053256227));
#40302=CARTESIAN_POINT('Ctrl Pts',(-53.4088143062287,-82.8626924772449,
177.827780274605));
#40303=CARTESIAN_POINT('Ctrl Pts',(-54.1775563137041,-82.8750206719214,
178.808507292983));
#40304=CARTESIAN_POINT('Ctrl Pts',(-55.413621103548,-82.8375291358633,178.96239024542));
#40305=CARTESIAN_POINT('Ctrl Pts',(-56.6496858933919,-82.8000375998052,
179.116273197858));
#40306=CARTESIAN_POINT('Ctrl Pts',(-57.6348250581585,-82.7892964117879,
178.353169537834));
#40307=CARTESIAN_POINT('Ctrl Pts',(-58.6199642229252,-82.7785552237706,
177.590065877811));
#40308=CARTESIAN_POINT('Ctrl Pts',(-58.7829181831923,-82.8554644714854,
176.356991379871));
#40309=CARTESIAN_POINT('Ctrl Pts',(-58.9458721434595,-82.9323737192003,
175.123916881932));
#40310=CARTESIAN_POINT('Ctrl Pts',(-58.197006261818,-83.1064890538344,174.143189863554));
#40311=CARTESIAN_POINT('Ctrl Pts',(-57.4481403801766,-83.2806043884686,
173.162462845176));
#40312=CARTESIAN_POINT('Ctrl Pts',(-56.2319517161668,-83.5045394538374,
173.008579892738));
#40313=CARTESIAN_POINT('Ctrl Pts',(-55.0157630521569,-83.7284745192062,
172.854696940301));
#40314=CARTESIAN_POINT('Ctrl Pts',(-54.0505000132243,-83.9256592365342,
173.617800600325));
#40315=CARTESIAN_POINT('Ctrl Pts',(-53.0852369742917,-84.1228439538622,
174.380904260348));
#40316=CARTESIAN_POINT('Ctrl Pts',(-52.9421591398586,-84.2323782354581,
175.613978758287));
#40317=CARTESIAN_POINT('Ctrl Pts',(-52.7990813054255,-84.341912517054,176.847053256227));
#40318=CARTESIAN_POINT('Ctrl Pts',(-53.5678233129009,-84.3542407117305,
177.827780274605));
#40319=CARTESIAN_POINT('Ctrl Pts',(-54.3365653203764,-84.3665689064069,
178.808507292983));
#40320=CARTESIAN_POINT('Ctrl Pts',(-55.5726301102202,-84.3290773703489,
178.96239024542));
#40321=CARTESIAN_POINT('Ctrl Pts',(-56.8086949000641,-84.2915858342908,
179.116273197858));
#40322=CARTESIAN_POINT('Ctrl Pts',(-57.7938340648308,-84.2808446462735,
178.353169537834));
#40323=CARTESIAN_POINT('Ctrl Pts',(-58.7789732295974,-84.2701034582562,
177.590065877811));
#40324=CARTESIAN_POINT('Ctrl Pts',(-58.9419271898646,-84.347012705971,176.356991379871));
#40325=CARTESIAN_POINT('Ctrl Pts',(-59.1048811501317,-84.4239219536858,
175.123916881932));
#40326=CARTESIAN_POINT('Ctrl Pts',(-58.3560152684903,-84.59803728832,174.143189863554));
#40327=CARTESIAN_POINT('Ctrl Pts',(-57.6071493868488,-84.7721526229542,
173.162462845176));
#40328=CARTESIAN_POINT('Ctrl Pts',(-56.390960722839,-84.996087688323,173.008579892738));
#40329=CARTESIAN_POINT('Ctrl Pts',(-55.1747720588292,-85.2200227536918,
172.854696940301));
#40330=CARTESIAN_POINT('Ctrl Pts',(-54.2095090198965,-85.4172074710198,
173.617800600325));
#40331=CARTESIAN_POINT('Ctrl Pts',(-53.2442459809639,-85.6143921883478,
174.380904260348));
#40332=CARTESIAN_POINT('Ctrl Pts',(-53.1011681465308,-85.7239264699437,
175.613978758287));
#40333=CARTESIAN_POINT('Ctrl Pts',(-52.9580903120977,-85.8334607515396,
176.847053256227));
#40334=CARTESIAN_POINT('Ctrl Pts',(-53.7268323195731,-85.8457889462161,
177.827780274605));
#40335=CARTESIAN_POINT('Ctrl Pts',(-54.4955743270486,-85.8581171408926,
178.808507292983));
#40336=CARTESIAN_POINT('Ctrl Pts',(-55.7316391168925,-85.8206256048345,
178.96239024542));
#40337=CARTESIAN_POINT('Ctrl Pts',(-56.9677039067363,-85.7831340687764,
179.116273197858));
#40338=CARTESIAN_POINT('Ctrl Pts',(-57.952843071503,-85.7723928807591,178.353169537834));
#40339=CARTESIAN_POINT('Ctrl Pts',(-58.9379822362697,-85.7616516927418,
177.590065877811));
#40340=CARTESIAN_POINT('Ctrl Pts',(-59.1009361965368,-85.8385609404566,
176.356991379871));
#40341=CARTESIAN_POINT('Ctrl Pts',(-59.2638901568039,-85.9154701881714,
175.123916881932));
#40342=CARTESIAN_POINT('Ctrl Pts',(-58.5150242751625,-86.0895855228056,
174.143189863554));
#40343=CARTESIAN_POINT('Ctrl Pts',(-57.7661583935211,-86.2637008574398,
173.162462845176));
#40344=CARTESIAN_POINT('Ctrl Pts',(-56.5499697295112,-86.4876359228086,
173.008579892738));
#40345=CARTESIAN_POINT('Ctrl Pts',(-55.3337810655014,-86.7115709881774,
172.854696940301));
#40346=CARTESIAN_POINT('Ctrl Pts',(-54.3685180265688,-86.9087557055054,
173.617800600325));
#40347=CARTESIAN_POINT('Ctrl Pts',(-53.4032549876361,-87.1059404228334,
174.380904260348));
#40348=CARTESIAN_POINT('Ctrl Pts',(-53.260177153203,-87.2154747044293,175.613978758287));
#40349=CARTESIAN_POINT('Ctrl Pts',(-53.1170993187699,-87.3250089860252,
176.847053256227));
#40350=CARTESIAN_POINT('Ctrl Pts',(-53.8858413262454,-87.3373371807017,
177.827780274605));
#40351=CARTESIAN_POINT('Ctrl Pts',(-54.6545833337208,-87.3496653753782,
178.808507292983));
#40352=CARTESIAN_POINT('Ctrl Pts',(-55.8906481235647,-87.3121738393201,
178.96239024542));
#40353=CARTESIAN_POINT('Ctrl Pts',(-57.1267129134086,-87.274682303262,179.116273197858));
#40354=CARTESIAN_POINT('Ctrl Pts',(-58.1118520781752,-87.2639411152447,
178.353169537834));
#40355=CARTESIAN_POINT('Ctrl Pts',(-59.0969912429419,-87.2531999272274,
177.590065877811));
#40356=CARTESIAN_POINT('Ctrl Pts',(-59.259945203209,-87.3301091749422,176.356991379871));
#40357=CARTESIAN_POINT('Ctrl Pts',(-59.4228991634762,-87.407018422657,175.123916881932));
#40358=CARTESIAN_POINT('Ctrl Pts',(-58.6740332818347,-87.5811337572912,
174.143189863554));
#40359=CARTESIAN_POINT('Ctrl Pts',(-57.9251674001933,-87.7552490919254,
173.162462845176));
#40360=CARTESIAN_POINT('Ctrl Pts',(-56.7089787361835,-87.9791841572942,
173.008579892738));
#40361=CARTESIAN_POINT('Ctrl Pts',(-55.4927900721736,-88.203119222663,172.854696940301));
#40362=CARTESIAN_POINT('Ctrl Pts',(-54.527527033241,-88.400303939991,173.617800600325));
#40363=CARTESIAN_POINT('Ctrl Pts',(-53.5622639943083,-88.597488657319,174.380904260348));
#40364=CARTESIAN_POINT('Ctrl Pts',(-53.4191861598752,-88.7070229389149,
175.613978758287));
#40365=CARTESIAN_POINT('Ctrl Pts',(-53.2761083254422,-88.8165572205108,
176.847053256227));
#40366=CARTESIAN_POINT('Ctrl Pts',(-54.0448503329176,-88.8288854151873,
177.827780274605));
#40367=CARTESIAN_POINT('Ctrl Pts',(-54.813592340393,-88.8412136098638,178.808507292983));
#40368=CARTESIAN_POINT('Ctrl Pts',(-56.0496571302369,-88.8037220738057,
178.96239024542));
#40369=CARTESIAN_POINT('Ctrl Pts',(-57.2857219200808,-88.7662305377476,
179.116273197858));
#40370=CARTESIAN_POINT('Ctrl Pts',(-58.2708610848475,-88.7554893497303,
178.353169537834));
#40371=CARTESIAN_POINT('Ctrl Pts',(-59.2560002496141,-88.7447481617131,
177.590065877811));
#40372=CARTESIAN_POINT('Ctrl Pts',(-59.4189542098812,-88.8216574094278,
176.356991379871));
#40373=CARTESIAN_POINT('Ctrl Pts',(-59.5819081701484,-88.8985666571426,
175.123916881932));
#40374=CARTESIAN_POINT('Ctrl Pts',(-58.833042288507,-89.0726819917768,174.143189863554));
#40375=CARTESIAN_POINT('Ctrl Pts',(-58.0841764068655,-89.246797326411,173.162462845176));
#40376=CARTESIAN_POINT('Ctrl Pts',(-56.8679877428557,-89.4707323917798,
173.008579892738));
#40377=CARTESIAN_POINT('Ctrl Pts',(-55.6517990788459,-89.6946674571486,
172.854696940301));
#40378=CARTESIAN_POINT('Ctrl Pts',(-54.6865360399132,-89.8918521744766,
173.617800600325));
#40379=CARTESIAN_POINT('Ctrl Pts',(-53.7212730009806,-90.0890368918046,
174.380904260348));
#40380=CARTESIAN_POINT('Ctrl Pts',(-53.5781951665475,-90.1985711734005,
175.613978758287));
#40381=CARTESIAN_POINT('Ctrl Pts',(-53.4351173321144,-90.3081054549964,
176.847053256227));
#40382=CARTESIAN_POINT('Ctrl Pts',(-54.2038593395898,-90.3204336496729,
177.827780274605));
#40383=CARTESIAN_POINT('Ctrl Pts',(-54.9726013470653,-90.3327618443494,
178.808507292983));
#40384=CARTESIAN_POINT('Ctrl Pts',(-56.2086661369091,-90.2952703082913,
178.96239024542));
#40385=CARTESIAN_POINT('Ctrl Pts',(-57.444730926753,-90.2577787722332,179.116273197858));
#40386=CARTESIAN_POINT('Ctrl Pts',(-58.4298700915197,-90.2470375842159,
178.353169537834));
#40387=CARTESIAN_POINT('Ctrl Pts',(-59.4150092562863,-90.2362963961987,
177.590065877811));
#40388=CARTESIAN_POINT('Ctrl Pts',(-59.5779632165535,-90.3132056439134,
176.356991379871));
#40389=CARTESIAN_POINT('Ctrl Pts',(-59.7409171768206,-90.3901148916282,
175.123916881932));
#40390=CARTESIAN_POINT('Ctrl Pts',(-58.9920512951792,-90.5642302262624,
174.143189863554));
#40391=CARTESIAN_POINT('Ctrl Pts',(-58.2431854135378,-90.7383455608967,
173.162462845176));
#40392=CARTESIAN_POINT('Ctrl Pts',(-57.0269967495279,-90.9622806262654,
173.008579892738));
#40393=CARTESIAN_POINT('Ctrl Pts',(-55.8108080855181,-91.1862156916342,
172.854696940301));
#40394=CARTESIAN_POINT('Ctrl Pts',(-54.8455450465854,-91.3834004089622,
173.617800600325));
#40395=CARTESIAN_POINT('Ctrl Pts',(-53.8802820076528,-91.5805851262902,
174.380904260348));
#40396=CARTESIAN_POINT('Ctrl Pts',(-53.7372041732197,-91.6901194078861,
175.613978758287));
#40397=CARTESIAN_POINT('Ctrl Pts',(-53.5941263387866,-91.799653689482,176.847053256227));
#40398=CARTESIAN_POINT('Ctrl Pts',(-54.362868346262,-91.8119818841585,177.827780274605));
#40399=CARTESIAN_POINT('Ctrl Pts',(-55.1316103537375,-91.824310078835,178.808507292983));
#40400=CARTESIAN_POINT('Ctrl Pts',(-56.3676751435814,-91.7868185427769,
178.96239024542));
#40401=CARTESIAN_POINT('Ctrl Pts',(-57.6037399334252,-91.7493270067188,
179.116273197858));
#40402=CARTESIAN_POINT('Ctrl Pts',(-58.5888790981919,-91.7385858187015,
178.353169537834));
#40403=CARTESIAN_POINT('Ctrl Pts',(-59.5740182629586,-91.7278446306843,
177.590065877811));
#40404=CARTESIAN_POINT('Ctrl Pts',(-59.7369722232257,-91.804753878399,176.356991379871));
#40405=CARTESIAN_POINT('Ctrl Pts',(-59.8999261834928,-91.8816631261138,
175.123916881932));
#40406=CARTESIAN_POINT('Ctrl Pts',(-59.1510603018514,-92.055778460748,174.143189863554));
#40407=CARTESIAN_POINT('Ctrl Pts',(-58.40219442021,-92.2298937953823,173.162462845176));
#40408=CARTESIAN_POINT('Ctrl Pts',(-57.1860057562002,-92.453828860751,173.008579892738));
#40409=CARTESIAN_POINT('Ctrl Pts',(-55.9698170921903,-92.6777639261198,
172.854696940301));
#40410=CARTESIAN_POINT('Ctrl Pts',(-55.0045540532577,-92.8749486434478,
173.617800600325));
#40411=CARTESIAN_POINT('Ctrl Pts',(-54.039291014325,-93.0721333607758,174.380904260348));
#40412=CARTESIAN_POINT('Ctrl Pts',(-53.8962131798919,-93.1816676423717,
175.613978758287));
#40413=CARTESIAN_POINT('Ctrl Pts',(-53.7531353454588,-93.2912019239676,
176.847053256227));
#40414=CARTESIAN_POINT('Ctrl Pts',(-54.5218773529343,-93.3035301186441,
177.827780274605));
#40415=CARTESIAN_POINT('Ctrl Pts',(-55.2906193604097,-93.3158583133206,
178.808507292983));
#40416=CARTESIAN_POINT('Ctrl Pts',(-56.5266841502536,-93.2783667772625,
178.96239024542));
#40417=CARTESIAN_POINT('Ctrl Pts',(-57.7627489400975,-93.2408752412044,
179.116273197858));
#40418=CARTESIAN_POINT('Ctrl Pts',(-58.7478881048641,-93.2301340531871,
178.353169537834));
#40419=CARTESIAN_POINT('Ctrl Pts',(-59.7330272696308,-93.2193928651699,
177.590065877811));
#40420=CARTESIAN_POINT('Ctrl Pts',(-59.8959812298979,-93.2963021128846,
176.356991379871));
#40421=CARTESIAN_POINT('Ctrl Pts',(-60.0589351901651,-93.3732113605994,
175.123916881932));
#40422=CARTESIAN_POINT('Ctrl Pts',(-59.3100693085236,-93.5473266952337,
174.143189863554));
#40423=CARTESIAN_POINT('Ctrl Pts',(-58.5612034268822,-93.7214420298679,
173.162462845176));
#40424=CARTESIAN_POINT('Ctrl Pts',(-57.3450147628724,-93.9453770952366,
173.008579892738));
#40425=CARTESIAN_POINT('Ctrl Pts',(-56.1288260988625,-94.1693121606054,
172.854696940301));
#40426=CARTESIAN_POINT('Ctrl Pts',(-55.1635630599299,-94.3664968779334,
173.617800600325));
#40427=CARTESIAN_POINT('Ctrl Pts',(-54.1983000209973,-94.5636815952613,
174.380904260348));
#40428=CARTESIAN_POINT('Ctrl Pts',(-54.0552221865641,-94.6732158768573,
175.613978758287));
#40429=CARTESIAN_POINT('Ctrl Pts',(-53.9121443521311,-94.7827501584532,
176.847053256227));
#40430=CARTESIAN_POINT('Ctrl Pts',(-54.6808863596065,-94.7950783531297,
177.827780274605));
#40431=CARTESIAN_POINT('Ctrl Pts',(-55.4496283670819,-94.8074065478062,
178.808507292983));
#40432=CARTESIAN_POINT('Ctrl Pts',(-56.6856931569258,-94.7699150117481,
178.96239024542));
#40433=CARTESIAN_POINT('Ctrl Pts',(-57.9217579467697,-94.73242347569,179.116273197858));
#40434=CARTESIAN_POINT('Ctrl Pts',(-58.9068971115363,-94.7216822876727,
178.353169537834));
#40435=CARTESIAN_POINT('Ctrl Pts',(-59.892036276303,-94.7109410996555,177.590065877811));
#40436=CARTESIAN_POINT('Ctrl Pts',(-60.0549902365702,-94.7878503473702,
176.356991379871));
#40437=CARTESIAN_POINT('Ctrl Pts',(-60.2179441968373,-94.864759595085,175.123916881932));
#40438=CARTESIAN_POINT('Ctrl Pts',(-59.4690783151959,-95.0388749297192,
174.143189863554));
#40439=CARTESIAN_POINT('Ctrl Pts',(-58.7202124335545,-95.2129902643534,
173.162462845176));
#40440=CARTESIAN_POINT('Ctrl Pts',(-57.5040237695446,-95.4369253297222,
173.008579892738));
#40441=CARTESIAN_POINT('Ctrl Pts',(-56.2878351055348,-95.660860395091,172.854696940301));
#40442=CARTESIAN_POINT('Ctrl Pts',(-55.3225720666021,-95.858045112419,173.617800600325));
#40443=CARTESIAN_POINT('Ctrl Pts',(-54.3573090276695,-96.055229829747,174.380904260348));
#40444=CARTESIAN_POINT('Ctrl Pts',(-54.2142311932364,-96.1647641113429,
175.613978758287));
#40445=CARTESIAN_POINT('Ctrl Pts',(-54.0711533588033,-96.2742983929388,
176.847053256227));
#40446=CARTESIAN_POINT('Ctrl Pts',(-54.8398953662787,-96.2866265876153,
177.827780274605));
#40447=CARTESIAN_POINT('Ctrl Pts',(-55.6086373737542,-96.2989547822918,
178.808507292983));
#40448=CARTESIAN_POINT('Ctrl Pts',(-56.844702163598,-96.2614632462337,178.96239024542));
#40449=CARTESIAN_POINT('Ctrl Pts',(-58.0807669534419,-96.2239717101756,
179.116273197858));
#40450=CARTESIAN_POINT('Ctrl Pts',(-59.0659061182086,-96.2132305221583,
178.353169537834));
#40451=CARTESIAN_POINT('Ctrl Pts',(-60.0510452829753,-96.202489334141,177.590065877811));
#40452=CARTESIAN_POINT('Ctrl Pts',(-60.2139992432424,-96.2793985818558,
176.356991379871));
#40453=CARTESIAN_POINT('Ctrl Pts',(-60.3769532035095,-96.3563078295706,
175.123916881932));
#40454=CARTESIAN_POINT('Ctrl Pts',(-59.6280873218681,-96.5304231642048,
174.143189863554));
#40455=CARTESIAN_POINT('Ctrl Pts',(-58.8792214402267,-96.7045384988391,
173.162462845176));
#40456=CARTESIAN_POINT('Ctrl Pts',(-57.6630327762168,-96.9284735642078,
173.008579892738));
#40457=CARTESIAN_POINT('Ctrl Pts',(-56.446844112207,-97.1524086295766,172.854696940301));
#40458=CARTESIAN_POINT('Ctrl Pts',(-55.4815810732743,-97.3495933469046,
173.617800600325));
#40459=CARTESIAN_POINT('Ctrl Pts',(-54.5163180343417,-97.5467780642326,
174.380904260348));
#40460=CARTESIAN_POINT('Ctrl Pts',(-54.3732401999086,-97.6563123458285,
175.613978758287));
#40461=CARTESIAN_POINT('Ctrl Pts',(-54.2301623654755,-97.7658466274244,
176.847053256227));
#40462=CARTESIAN_POINT('Ctrl Pts',(-54.9989043729509,-97.7781748221009,
177.827780274605));
#40463=CARTESIAN_POINT('Ctrl Pts',(-55.7676463804264,-97.7905030167774,
178.808507292983));
#40464=CARTESIAN_POINT('Ctrl Pts',(-57.0037111702703,-97.7530114807193,
178.96239024542));
#40465=CARTESIAN_POINT('Ctrl Pts',(-58.2397759601141,-97.7155199446612,
179.116273197858));
#40466=CARTESIAN_POINT('Ctrl Pts',(-59.2249151248808,-97.7047787566439,
178.353169537834));
#40467=CARTESIAN_POINT('Ctrl Pts',(-60.2100542896475,-97.6940375686266,
177.590065877811));
#40468=CARTESIAN_POINT('Ctrl Pts',(-60.3730082499146,-97.7709468163415,
176.356991379871));
#40469=CARTESIAN_POINT('Ctrl Pts',(-60.5359622101818,-97.8478560640562,
175.123916881932));
#40470=CARTESIAN_POINT('Ctrl Pts',(-59.7870963285403,-98.0219713986905,
174.143189863554));
#40471=CARTESIAN_POINT('Ctrl Pts',(-59.0382304468989,-98.1960867333247,
173.162462845176));
#40472=CARTESIAN_POINT('Ctrl Pts',(-57.8220417828891,-98.4200217986935,
173.008579892738));
#40473=CARTESIAN_POINT('Ctrl Pts',(-56.6058531188792,-98.6439568640622,
172.854696940301));
#40474=CARTESIAN_POINT('Ctrl Pts',(-55.6405900799466,-98.8411415813902,
173.617800600325));
#40475=CARTESIAN_POINT('Ctrl Pts',(-54.6753270410139,-99.0383262987182,
174.380904260348));
#40476=CARTESIAN_POINT('Ctrl Pts',(-54.5322492065808,-99.1478605803141,
175.613978758287));
#40477=CARTESIAN_POINT('Ctrl Pts',(-54.3891713721477,-99.25739486191,176.847053256227));
#40478=CARTESIAN_POINT('Ctrl Pts',(-55.1579133796232,-99.2697230565865,
177.827780274605));
#40479=CARTESIAN_POINT('Ctrl Pts',(-55.9266553870986,-99.282051251263,178.808507292983));
#40480=CARTESIAN_POINT('Ctrl Pts',(-57.1627201769425,-99.2445597152049,
178.96239024542));
#40481=CARTESIAN_POINT('Ctrl Pts',(-58.3987849667864,-99.2070681791468,
179.116273197858));
#40482=CARTESIAN_POINT('Ctrl Pts',(-59.383924131553,-99.1963269911295,178.353169537834));
#40483=CARTESIAN_POINT('Ctrl Pts',(-60.3690632963197,-99.1855858031122,
177.590065877811));
#40484=CARTESIAN_POINT('Ctrl Pts',(-60.5320172565868,-99.2624950508271,
176.356991379871));
#40485=CARTESIAN_POINT('Ctrl Pts',(-60.694971216854,-99.3394042985418,175.123916881932));
#40486=CARTESIAN_POINT('Ctrl Pts',(-59.9461053352125,-99.513519633176,174.143189863554));
#40487=CARTESIAN_POINT('Ctrl Pts',(-59.1972394535711,-99.6876349678102,
173.162462845176));
#40488=CARTESIAN_POINT('Ctrl Pts',(-57.9810507895613,-99.9115700331791,
173.008579892738));
#40489=CARTESIAN_POINT('Ctrl Pts',(-56.7648621255514,-100.135505098548,
172.854696940301));
#40490=CARTESIAN_POINT('Ctrl Pts',(-55.7995990866188,-100.332689815876,
173.617800600325));
#40491=CARTESIAN_POINT('Ctrl Pts',(-54.8343360476862,-100.529874533204,
174.380904260348));
#40492=CARTESIAN_POINT('Ctrl Pts',(-54.6912582132531,-100.6394088148,175.613978758287));
#40493=CARTESIAN_POINT('Ctrl Pts',(-54.54818037882,-100.748943096396,176.847053256227));
#40494=CARTESIAN_POINT('Ctrl Pts',(-55.3169223862954,-100.761271291072,
177.827780274605));
#40495=CARTESIAN_POINT('Ctrl Pts',(-56.0856643937708,-100.773599485749,
178.808507292983));
#40496=CARTESIAN_POINT('Ctrl Pts',(-57.3217291836147,-100.73610794969,178.96239024542));
#40497=CARTESIAN_POINT('Ctrl Pts',(-58.5577939734586,-100.698616413632,
179.116273197858));
#40498=CARTESIAN_POINT('Ctrl Pts',(-59.5429331382253,-100.687875225615,
178.353169537834));
#40499=CARTESIAN_POINT('Ctrl Pts',(-60.5280723029919,-100.677134037598,
177.590065877811));
#40500=CARTESIAN_POINT('Ctrl Pts',(-60.6910262632591,-100.754043285313,
176.356991379871));
#40501=CARTESIAN_POINT('Ctrl Pts',(-60.8539802235262,-100.830952533027,
175.123916881932));
#40502=CARTESIAN_POINT('Ctrl Pts',(-60.1051143418848,-101.005067867662,
174.143189863554));
#40503=CARTESIAN_POINT('Ctrl Pts',(-59.3562484602434,-101.179183202296,
173.162462845176));
#40504=CARTESIAN_POINT('Ctrl Pts',(-58.1400597962335,-101.403118267665,
173.008579892738));
#40505=CARTESIAN_POINT('Ctrl Pts',(-56.9238711322237,-101.627053333033,
172.854696940301));
#40506=CARTESIAN_POINT('Ctrl Pts',(-55.958608093291,-101.824238050361,173.617800600325));
#40507=CARTESIAN_POINT('Ctrl Pts',(-54.9933450543584,-102.021422767689,
174.380904260348));
#40508=CARTESIAN_POINT('Ctrl Pts',(-54.8502672199253,-102.130957049285,
175.613978758287));
#40509=CARTESIAN_POINT('Ctrl Pts',(-54.7071893854922,-102.240491330881,
176.847053256227));
#40510=CARTESIAN_POINT('Ctrl Pts',(-55.4759313929676,-102.252819525558,
177.827780274605));
#40511=CARTESIAN_POINT('Ctrl Pts',(-56.2446734004431,-102.265147720234,
178.808507292983));
#40512=CARTESIAN_POINT('Ctrl Pts',(-57.480738190287,-102.227656184176,178.96239024542));
#40513=CARTESIAN_POINT('Ctrl Pts',(-58.7168029801308,-102.190164648118,
179.116273197858));
#40514=CARTESIAN_POINT('Ctrl Pts',(-59.7019421448975,-102.179423460101,
178.353169537834));
#40515=CARTESIAN_POINT('Ctrl Pts',(-60.6870813096642,-102.168682272083,
177.590065877811));
#40516=CARTESIAN_POINT('Ctrl Pts',(-60.8500352699313,-102.245591519798,
176.356991379871));
#40517=CARTESIAN_POINT('Ctrl Pts',(-61.0129892301984,-102.322500767513,
175.123916881932));
#40518=CARTESIAN_POINT('Ctrl Pts',(-60.264123348557,-102.496616102147,174.143189863554));
#40519=CARTESIAN_POINT('Ctrl Pts',(-59.5152574669156,-102.670731436781,
173.162462845176));
#40520=CARTESIAN_POINT('Ctrl Pts',(-58.2990688029057,-102.89466650215,173.008579892738));
#40521=CARTESIAN_POINT('Ctrl Pts',(-57.0828801388959,-103.118601567519,
172.854696940301));
#40522=CARTESIAN_POINT('Ctrl Pts',(-56.1176170999633,-103.315786284847,
173.617800600325));
#40523=CARTESIAN_POINT('Ctrl Pts',(-55.1523540610306,-103.512971002175,
174.380904260348));
#40524=CARTESIAN_POINT('Ctrl Pts',(-55.0092762265975,-103.622505283771,
175.613978758287));
#40525=CARTESIAN_POINT('Ctrl Pts',(-54.8661983921644,-103.732039565367,
176.847053256227));
#40526=CARTESIAN_POINT('Ctrl Pts',(-55.6349403996399,-103.744367760043,
177.827780274605));
#40527=CARTESIAN_POINT('Ctrl Pts',(-56.4036824071153,-103.75669595472,178.808507292983));
#40528=CARTESIAN_POINT('Ctrl Pts',(-57.6397471969592,-103.719204418662,
178.96239024542));
#40529=CARTESIAN_POINT('Ctrl Pts',(-58.8758119868031,-103.681712882604,
179.116273197858));
#40530=CARTESIAN_POINT('Ctrl Pts',(-59.8609511515697,-103.670971694586,
178.353169537834));
#40531=CARTESIAN_POINT('Ctrl Pts',(-60.8460903163364,-103.660230506569,
177.590065877811));
#40532=CARTESIAN_POINT('Ctrl Pts',(-61.0090442766035,-103.737139754284,
176.356991379871));
#40533=CARTESIAN_POINT('Ctrl Pts',(-61.1719982368707,-103.814049001999,
175.123916881932));
#40534=CARTESIAN_POINT('Ctrl Pts',(-60.4231323552292,-103.988164336633,
174.143189863554));
#40535=CARTESIAN_POINT('Ctrl Pts',(-59.6742664735878,-104.162279671267,
173.162462845176));
#40536=CARTESIAN_POINT('Ctrl Pts',(-58.458077809578,-104.386214736636,173.008579892738));
#40537=CARTESIAN_POINT('Ctrl Pts',(-57.2418891455681,-104.610149802005,
172.854696940301));
#40538=CARTESIAN_POINT('Ctrl Pts',(-56.2766261066355,-104.807334519333,
173.617800600325));
#40539=CARTESIAN_POINT('Ctrl Pts',(-55.3113630677028,-105.004519236661,
174.380904260348));
#40540=CARTESIAN_POINT('Ctrl Pts',(-55.1682852332697,-105.114053518257,
175.613978758287));
#40541=CARTESIAN_POINT('Ctrl Pts',(-55.0252073988366,-105.223587799852,
176.847053256227));
#40542=CARTESIAN_POINT('Ctrl Pts',(-55.7939494063121,-105.235915994529,
177.827780274605));
#40543=CARTESIAN_POINT('Ctrl Pts',(-56.5626914137875,-105.248244189205,
178.808507292983));
#40544=CARTESIAN_POINT('Ctrl Pts',(-57.7987562036314,-105.210752653147,
178.96239024542));
#40545=CARTESIAN_POINT('Ctrl Pts',(-59.0348209934753,-105.173261117089,
179.116273197858));
#40546=CARTESIAN_POINT('Ctrl Pts',(-60.0199601582419,-105.162519929072,
178.353169537834));
#40547=CARTESIAN_POINT('Ctrl Pts',(-61.0050993230086,-105.151778741055,
177.590065877811));
#40548=CARTESIAN_POINT('Ctrl Pts',(-61.1680532832757,-105.228687988769,
176.356991379871));
#40549=CARTESIAN_POINT('Ctrl Pts',(-61.3310072435429,-105.305597236484,
175.123916881932));
#40550=CARTESIAN_POINT('Ctrl Pts',(-60.5821413619014,-105.479712571118,
174.143189863554));
#40551=CARTESIAN_POINT('Ctrl Pts',(-59.83327548026,-105.653827905753,173.162462845176));
#40552=CARTESIAN_POINT('Ctrl Pts',(-58.6170868162502,-105.877762971121,
173.008579892738));
#40553=CARTESIAN_POINT('Ctrl Pts',(-57.4008981522404,-106.10169803649,172.854696940301));
#40554=CARTESIAN_POINT('Ctrl Pts',(-56.4356351133077,-106.298882753818,
173.617800600325));
#40555=CARTESIAN_POINT('Ctrl Pts',(-55.4703720743751,-106.496067471146,
174.380904260348));
#40556=CARTESIAN_POINT('Ctrl Pts',(-55.327294239942,-106.605601752742,175.613978758287));
#40557=CARTESIAN_POINT('Ctrl Pts',(-55.1842164055089,-106.715136034338,
176.847053256227));
#40558=CARTESIAN_POINT('Ctrl Pts',(-55.9529584129843,-106.727464229014,
177.827780274605));
#40559=CARTESIAN_POINT('Ctrl Pts',(-56.7217004204598,-106.739792423691,
178.808507292983));
#40560=CARTESIAN_POINT('Ctrl Pts',(-57.9577652103036,-106.702300887633,
178.96239024542));
#40561=CARTESIAN_POINT('Ctrl Pts',(-59.1938300001475,-106.664809351575,
179.116273197858));
#40562=CARTESIAN_POINT('Ctrl Pts',(-60.1789691649142,-106.654068163558,
178.353169537834));
#40563=CARTESIAN_POINT('Ctrl Pts',(-61.1641083296808,-106.64332697554,177.590065877811));
#40564=CARTESIAN_POINT('Ctrl Pts',(-61.327062289948,-106.720236223255,176.356991379871));
#40565=CARTESIAN_POINT('Ctrl Pts',(-61.4900162502151,-106.79714547097,175.123916881932));
#40566=CARTESIAN_POINT('Ctrl Pts',(-60.7411503685737,-106.971260805604,
174.143189863554));
#40567=CARTESIAN_POINT('Ctrl Pts',(-59.9922844869323,-107.145376140238,
173.162462845176));
#40568=CARTESIAN_POINT('Ctrl Pts',(-58.7760958229224,-107.369311205607,
173.008579892738));
#40569=CARTESIAN_POINT('Ctrl Pts',(-57.5599071589126,-107.593246270976,
172.854696940301));
#40570=CARTESIAN_POINT('Ctrl Pts',(-56.5946441199799,-107.790430988304,
173.617800600325));
#40571=CARTESIAN_POINT('Ctrl Pts',(-55.6293810810473,-107.987615705632,
174.380904260348));
#40572=CARTESIAN_POINT('Ctrl Pts',(-55.4863032466142,-108.097149987228,
175.613978758287));
#40573=CARTESIAN_POINT('Ctrl Pts',(-55.3432254121811,-108.206684268824,
176.847053256227));
#40574=CARTESIAN_POINT('Ctrl Pts',(-56.1119674196565,-108.2190124635,177.827780274605));
#40575=CARTESIAN_POINT('Ctrl Pts',(-56.880709427132,-108.231340658177,178.808507292983));
#40576=CARTESIAN_POINT('Ctrl Pts',(-58.1167742169759,-108.193849122118,
178.96239024542));
#40577=CARTESIAN_POINT('Ctrl Pts',(-59.3528390068197,-108.15635758606,179.116273197858));
#40578=CARTESIAN_POINT('Ctrl Pts',(-60.3379781715864,-108.145616398043,
178.353169537834));
#40579=CARTESIAN_POINT('Ctrl Pts',(-61.3231173363531,-108.134875210026,
177.590065877811));
#40580=CARTESIAN_POINT('Ctrl Pts',(-61.4860712966202,-108.211784457741,
176.356991379871));
#40581=CARTESIAN_POINT('Ctrl Pts',(-61.6490252568873,-108.288693705455,
175.123916881932));
#40582=CARTESIAN_POINT('Ctrl Pts',(-60.9001593752459,-108.46280904009,174.143189863554));
#40583=CARTESIAN_POINT('Ctrl Pts',(-60.1512934936045,-108.636924374724,
173.162462845176));
#40584=CARTESIAN_POINT('Ctrl Pts',(-58.9351048295946,-108.860859440093,
173.008579892738));
#40585=CARTESIAN_POINT('Ctrl Pts',(-57.7189161655848,-109.084794505461,
172.854696940301));
#40586=CARTESIAN_POINT('Ctrl Pts',(-56.7536531266522,-109.281979222789,
173.617800600325));
#40587=CARTESIAN_POINT('Ctrl Pts',(-55.7883900877195,-109.479163940117,
174.380904260348));
#40588=CARTESIAN_POINT('Ctrl Pts',(-55.6453122532864,-109.588698221713,
175.613978758287));
#40589=CARTESIAN_POINT('Ctrl Pts',(-55.5022344188533,-109.698232503309,
176.847053256227));
#40590=CARTESIAN_POINT('Ctrl Pts',(-56.2709764263288,-109.710560697986,
177.827780274605));
#40591=CARTESIAN_POINT('Ctrl Pts',(-57.0397184338042,-109.722888892662,
178.808507292983));
#40592=CARTESIAN_POINT('Ctrl Pts',(-58.2757832236481,-109.685397356604,
178.96239024542));
#40593=CARTESIAN_POINT('Ctrl Pts',(-59.511848013492,-109.647905820546,179.116273197858));
#40594=CARTESIAN_POINT('Ctrl Pts',(-60.4969871782586,-109.637164632529,
178.353169537834));
#40595=CARTESIAN_POINT('Ctrl Pts',(-61.4821263430253,-109.626423444511,
177.590065877811));
#40596=CARTESIAN_POINT('Ctrl Pts',(-61.6450803032924,-109.703332692226,
176.356991379871));
#40597=CARTESIAN_POINT('Ctrl Pts',(-61.8080342635596,-109.780241939941,
175.123916881932));
#40598=CARTESIAN_POINT('Ctrl Pts',(-61.0591683819181,-109.954357274575,
174.143189863554));
#40599=CARTESIAN_POINT('Ctrl Pts',(-60.3103025002767,-110.128472609209,
173.162462845176));
#40600=CARTESIAN_POINT('Ctrl Pts',(-59.0941138362669,-110.352407674578,
173.008579892738));
#40601=CARTESIAN_POINT('Ctrl Pts',(-57.877925172257,-110.576342739947,172.854696940301));
#40602=CARTESIAN_POINT('Ctrl Pts',(-56.9126621333244,-110.773527457275,
173.617800600325));
#40603=CARTESIAN_POINT('Ctrl Pts',(-55.9473990943918,-110.970712174603,
174.380904260348));
#40604=CARTESIAN_POINT('Ctrl Pts',(-55.8043212599587,-111.080246456199,
175.613978758287));
#40605=CARTESIAN_POINT('Ctrl Pts',(-55.6612434255256,-111.189780737795,
176.847053256227));
#40606=CARTESIAN_POINT('Ctrl Pts',(-56.429985433001,-111.202108932471,177.827780274605));
#40607=CARTESIAN_POINT('Ctrl Pts',(-57.1987274404764,-111.214437127148,
178.808507292983));
#40608=CARTESIAN_POINT('Ctrl Pts',(-58.4347922303203,-111.17694559109,178.96239024542));
#40609=CARTESIAN_POINT('Ctrl Pts',(-59.6708570201642,-111.139454055032,
179.116273197858));
#40610=CARTESIAN_POINT('Ctrl Pts',(-60.6559961849309,-111.128712867014,
178.353169537834));
#40611=CARTESIAN_POINT('Ctrl Pts',(-61.6411353496975,-111.117971678997,
177.590065877811));
#40612=CARTESIAN_POINT('Ctrl Pts',(-61.8040893099646,-111.194880926712,
176.356991379871));
#40613=CARTESIAN_POINT('Ctrl Pts',(-61.9670432702318,-111.271790174427,
175.123916881932));
#40614=CARTESIAN_POINT('Ctrl Pts',(-61.2181773885904,-111.445905509061,
174.143189863554));
#40615=CARTESIAN_POINT('Ctrl Pts',(-60.4693115069489,-111.620020843695,
173.162462845176));
#40616=CARTESIAN_POINT('Ctrl Pts',(-59.2531228429391,-111.843955909064,
173.008579892738));
#40617=CARTESIAN_POINT('Ctrl Pts',(-58.0369341789293,-112.067890974433,
172.854696940301));
#40618=CARTESIAN_POINT('Ctrl Pts',(-57.0716711399966,-112.265075691761,
173.617800600325));
#40619=CARTESIAN_POINT('Ctrl Pts',(-56.106408101064,-112.462260409089,174.380904260348));
#40620=CARTESIAN_POINT('Ctrl Pts',(-55.9633302666309,-112.571794690684,
175.613978758287));
#40621=CARTESIAN_POINT('Ctrl Pts',(-55.8202524321978,-112.68132897228,176.847053256227));
#40622=CARTESIAN_POINT('Ctrl Pts',(-56.5889944396732,-112.693657166957,
177.827780274605));
#40623=CARTESIAN_POINT('Ctrl Pts',(-57.3577364471487,-112.705985361633,
178.808507292983));
#40624=CARTESIAN_POINT('Ctrl Pts',(-58.5938012369925,-112.668493825575,
178.96239024542));
#40625=CARTESIAN_POINT('Ctrl Pts',(-59.8298660268364,-112.631002289517,
179.116273197858));
#40626=CARTESIAN_POINT('Ctrl Pts',(-60.8150051916031,-112.6202611015,178.353169537834));
#40627=CARTESIAN_POINT('Ctrl Pts',(-61.8001443563698,-112.609519913483,
177.590065877811));
#40628=CARTESIAN_POINT('Ctrl Pts',(-61.9630983166369,-112.686429161197,
176.356991379871));
#40629=CARTESIAN_POINT('Ctrl Pts',(-62.126052276904,-112.763338408912,175.123916881932));
#40630=CARTESIAN_POINT('Ctrl Pts',(-61.3771863952626,-112.937453743546,
174.143189863554));
#40631=CARTESIAN_POINT('Ctrl Pts',(-60.6283205136212,-113.111569078181,
173.162462845176));
#40632=CARTESIAN_POINT('Ctrl Pts',(-59.4121318496113,-113.335504143549,
173.008579892738));
#40633=CARTESIAN_POINT('Ctrl Pts',(-58.1959431856015,-113.559439208918,
172.854696940301));
#40634=CARTESIAN_POINT('Ctrl Pts',(-57.2306801466688,-113.756623926246,
173.617800600325));
#40635=CARTESIAN_POINT('Ctrl Pts',(-56.2654171077362,-113.953808643574,
174.380904260348));
#40636=CARTESIAN_POINT('Ctrl Pts',(-56.1223392733031,-114.06334292517,175.613978758287));
#40637=CARTESIAN_POINT('Ctrl Pts',(-55.97926143887,-114.172877206766,176.847053256227));
#40638=CARTESIAN_POINT('Ctrl Pts',(-56.7480034463455,-114.185205401443,
177.827780274605));
#40639=CARTESIAN_POINT('Ctrl Pts',(-57.5167454538209,-114.197533596119,
178.808507292983));
#40640=CARTESIAN_POINT('Ctrl Pts',(-58.7528102436648,-114.160042060061,
178.96239024542));
#40641=CARTESIAN_POINT('Ctrl Pts',(-59.9888750335086,-114.122550524003,
179.116273197858));
#40642=CARTESIAN_POINT('Ctrl Pts',(-60.9740141982753,-114.111809335986,
178.353169537834));
#40643=CARTESIAN_POINT('Ctrl Pts',(-61.959153363042,-114.101068147968,177.590065877811));
#40644=CARTESIAN_POINT('Ctrl Pts',(-62.1221073233091,-114.177977395683,
176.356991379871));
#40645=CARTESIAN_POINT('Ctrl Pts',(-62.2850612835762,-114.254886643398,
175.123916881932));
#40646=CARTESIAN_POINT('Ctrl Pts',(-61.5361954019348,-114.429001978032,
174.143189863554));
#40647=CARTESIAN_POINT('Ctrl Pts',(-60.7873295202934,-114.603117312666,
173.162462845176));
#40648=CARTESIAN_POINT('Ctrl Pts',(-59.5711408562835,-114.827052378035,
173.008579892738));
#40649=CARTESIAN_POINT('Ctrl Pts',(-58.3549521922737,-115.050987443404,
172.854696940301));
#40650=CARTESIAN_POINT('Ctrl Pts',(-57.3896891533411,-115.248172160732,
173.617800600325));
#40651=CARTESIAN_POINT('Ctrl Pts',(-56.4244261144084,-115.44535687806,174.380904260348));
#40652=CARTESIAN_POINT('Ctrl Pts',(-56.2813482799753,-115.554891159656,
175.613978758287));
#40653=CARTESIAN_POINT('Ctrl Pts',(-56.1382704455422,-115.664425441252,
176.847053256227));
#40654=CARTESIAN_POINT('Ctrl Pts',(-56.9070124530177,-115.676753635928,
177.827780274605));
#40655=CARTESIAN_POINT('Ctrl Pts',(-57.6757544604931,-115.689081830605,
178.808507292983));
#40656=CARTESIAN_POINT('Ctrl Pts',(-58.911819250337,-115.651590294547,178.96239024542));
#40657=CARTESIAN_POINT('Ctrl Pts',(-60.1478840401809,-115.614098758488,
179.116273197858));
#40658=CARTESIAN_POINT('Ctrl Pts',(-61.1330232049475,-115.603357570471,
178.353169537834));
#40659=CARTESIAN_POINT('Ctrl Pts',(-62.1181623697142,-115.592616382454,
177.590065877811));
#40660=CARTESIAN_POINT('Ctrl Pts',(-62.2811163299813,-115.669525630169,
176.356991379871));
#40661=CARTESIAN_POINT('Ctrl Pts',(-62.4440702902485,-115.746434877883,
175.123916881932));
#40662=CARTESIAN_POINT('Ctrl Pts',(-61.695204408607,-115.920550212518,174.143189863554));
#40663=CARTESIAN_POINT('Ctrl Pts',(-60.9463385269656,-116.094665547152,
173.162462845176));
#40664=CARTESIAN_POINT('Ctrl Pts',(-59.7301498629558,-116.318600612521,
173.008579892738));
#40665=CARTESIAN_POINT('Ctrl Pts',(-58.5139611989459,-116.542535677889,
172.854696940301));
#40666=CARTESIAN_POINT('Ctrl Pts',(-57.5486981600133,-116.739720395217,
173.617800600325));
#40667=CARTESIAN_POINT('Ctrl Pts',(-56.5834351210807,-116.936905112545,
174.380904260348));
#40668=CARTESIAN_POINT('Ctrl Pts',(-56.4403572866476,-117.046439394141,
175.613978758287));
#40669=CARTESIAN_POINT('Ctrl Pts',(-56.2972794522145,-117.155973675737,
176.847053256227));
#40670=CARTESIAN_POINT('Ctrl Pts',(-57.0660214596899,-117.168301870414,
177.827780274605));
#40671=CARTESIAN_POINT('Ctrl Pts',(-57.8347634671653,-117.18063006509,178.808507292983));
#40672=CARTESIAN_POINT('Ctrl Pts',(-59.0708282570092,-117.143138529032,
178.96239024542));
#40673=CARTESIAN_POINT('Ctrl Pts',(-60.3068930468531,-117.105646992974,
179.116273197858));
#40674=CARTESIAN_POINT('Ctrl Pts',(-61.2920322116198,-117.094905804957,
178.353169537834));
#40675=CARTESIAN_POINT('Ctrl Pts',(-62.2771713763864,-117.084164616939,
177.590065877811));
#40676=CARTESIAN_POINT('Ctrl Pts',(-62.4401253366536,-117.161073864654,
176.356991379871));
#40677=CARTESIAN_POINT('Ctrl Pts',(-62.6030792969207,-117.237983112369,
175.123916881932));
#40678=CARTESIAN_POINT('Ctrl Pts',(-61.8542134152793,-117.412098447003,
174.143189863554));
#40679=CARTESIAN_POINT('Ctrl Pts',(-61.1053475336379,-117.586213781637,
173.162462845176));
#40680=CARTESIAN_POINT('Ctrl Pts',(-59.889158869628,-117.810148847006,173.008579892738));
#40681=CARTESIAN_POINT('Ctrl Pts',(-58.6729702056182,-118.034083912375,
172.854696940301));
#40682=CARTESIAN_POINT('Ctrl Pts',(-57.7077071666855,-118.231268629703,
173.617800600325));
#40683=CARTESIAN_POINT('Ctrl Pts',(-56.7424441277529,-118.428453347031,
174.380904260348));
#40684=CARTESIAN_POINT('Ctrl Pts',(-56.5993662933198,-118.537987628627,
175.613978758287));
#40685=CARTESIAN_POINT('Ctrl Pts',(-56.4562884588867,-118.647521910223,
176.847053256227));
#40686=CARTESIAN_POINT('Ctrl Pts',(-57.2250304663621,-118.659850104899,
177.827780274605));
#40687=CARTESIAN_POINT('Ctrl Pts',(-57.9937724738376,-118.672178299576,
178.808507292983));
#40688=CARTESIAN_POINT('Ctrl Pts',(-59.2298372636814,-118.634686763518,
178.96239024542));
#40689=CARTESIAN_POINT('Ctrl Pts',(-60.4659020535253,-118.59719522746,179.116273197858));
#40690=CARTESIAN_POINT('Ctrl Pts',(-61.451041218292,-118.586454039442,178.353169537834));
#40691=CARTESIAN_POINT('Ctrl Pts',(-62.4361803830587,-118.575712851425,
177.590065877811));
#40692=CARTESIAN_POINT('Ctrl Pts',(-62.5991343433258,-118.65262209914,176.356991379871));
#40693=CARTESIAN_POINT('Ctrl Pts',(-62.7620883035929,-118.729531346855,
175.123916881932));
#40694=CARTESIAN_POINT('Ctrl Pts',(-62.0132224219515,-118.903646681489,
174.143189863554));
#40695=CARTESIAN_POINT('Ctrl Pts',(-61.2643565403101,-119.077762016123,
173.162462845176));
#40696=CARTESIAN_POINT('Ctrl Pts',(-60.0481678763002,-119.301697081492,
173.008579892738));
#40697=CARTESIAN_POINT('Ctrl Pts',(-58.8319792122904,-119.525632146861,
172.854696940301));
#40698=CARTESIAN_POINT('Ctrl Pts',(-57.8667161733577,-119.722816864189,
173.617800600325));
#40699=CARTESIAN_POINT('Ctrl Pts',(-56.9014531344251,-119.920001581517,
174.380904260348));
#40700=CARTESIAN_POINT('Ctrl Pts',(-56.758375299992,-120.029535863112,175.613978758287));
#40701=CARTESIAN_POINT('Ctrl Pts',(-56.6152974655589,-120.139070144708,
176.847053256227));
#40702=CARTESIAN_POINT('Ctrl Pts',(-57.3840394730344,-120.151398339385,
177.827780274605));
#40703=CARTESIAN_POINT('Ctrl Pts',(-58.1527814805098,-120.163726534061,
178.808507292983));
#40704=CARTESIAN_POINT('Ctrl Pts',(-59.3888462703537,-120.126234998003,
178.96239024542));
#40705=CARTESIAN_POINT('Ctrl Pts',(-60.6249110601976,-120.088743461945,
179.116273197858));
#40706=CARTESIAN_POINT('Ctrl Pts',(-61.6100502249642,-120.078002273928,
178.353169537834));
#40707=CARTESIAN_POINT('Ctrl Pts',(-62.5951893897309,-120.067261085911,
177.590065877811));
#40708=CARTESIAN_POINT('Ctrl Pts',(-62.758143349998,-120.144170333625,176.356991379871));
#40709=CARTESIAN_POINT('Ctrl Pts',(-62.9210973102652,-120.22107958134,175.123916881932));
#40710=CARTESIAN_POINT('Ctrl Pts',(-62.1722314286237,-120.395194915974,
174.143189863554));
#40711=CARTESIAN_POINT('Ctrl Pts',(-61.4233655469823,-120.569310250609,
173.162462845176));
#40712=CARTESIAN_POINT('Ctrl Pts',(-60.2071768829725,-120.793245315977,
173.008579892738));
#40713=CARTESIAN_POINT('Ctrl Pts',(-58.9909882189626,-121.017180381346,
172.854696940301));
#40714=CARTESIAN_POINT('Ctrl Pts',(-58.02572518003,-121.214365098674,173.617800600325));
#40715=CARTESIAN_POINT('Ctrl Pts',(-57.0604621410973,-121.411549816002,
174.380904260348));
#40716=CARTESIAN_POINT('Ctrl Pts',(-56.9173843066642,-121.521084097598,
175.613978758287));
#40717=CARTESIAN_POINT('Ctrl Pts',(-56.7743064722311,-121.630618379194,
176.847053256227));
#40718=CARTESIAN_POINT('Ctrl Pts',(-57.5430484797066,-121.64294657387,177.827780274605));
#40719=CARTESIAN_POINT('Ctrl Pts',(-58.3117904871821,-121.655274768547,
178.808507292983));
#40720=CARTESIAN_POINT('Ctrl Pts',(-59.5478552770259,-121.617783232489,
178.96239024542));
#40721=CARTESIAN_POINT('Ctrl Pts',(-60.7839200668698,-121.580291696431,
179.116273197858));
#40722=CARTESIAN_POINT('Ctrl Pts',(-61.7690592316364,-121.569550508414,
178.353169537834));
#40723=CARTESIAN_POINT('Ctrl Pts',(-62.7541983964031,-121.558809320396,
177.590065877811));
#40724=CARTESIAN_POINT('Ctrl Pts',(-62.9171523566702,-121.635718568111,
176.356991379871));
#40725=CARTESIAN_POINT('Ctrl Pts',(-63.0801063169374,-121.712627815826,
175.123916881932));
#40726=CARTESIAN_POINT('Ctrl Pts',(-62.331240435296,-121.88674315046,174.143189863554));
#40727=CARTESIAN_POINT('Ctrl Pts',(-61.5823745536545,-122.060858485094,
173.162462845176));
#40728=CARTESIAN_POINT('Ctrl Pts',(-60.3661858896447,-122.284793550463,
173.008579892738));
#40729=CARTESIAN_POINT('Ctrl Pts',(-59.1499972256349,-122.508728615832,
172.854696940301));
#40730=CARTESIAN_POINT('Ctrl Pts',(-58.1847341867022,-122.70591333316,173.617800600325));
#40731=CARTESIAN_POINT('Ctrl Pts',(-57.2194711477696,-122.903098050488,
174.380904260348));
#40732=CARTESIAN_POINT('Ctrl Pts',(-57.0763933133365,-123.012632332084,
175.613978758287));
#40733=CARTESIAN_POINT('Ctrl Pts',(-56.9333154789034,-123.12216661368,176.847053256227));
#40734=CARTESIAN_POINT('Ctrl Pts',(-57.7020574863788,-123.134494808356,
177.827780274605));
#40735=CARTESIAN_POINT('Ctrl Pts',(-58.4707994938543,-123.146823003033,
178.808507292983));
#40736=CARTESIAN_POINT('Ctrl Pts',(-59.7068642836981,-123.109331466974,
178.96239024542));
#40737=CARTESIAN_POINT('Ctrl Pts',(-60.942929073542,-123.071839930916,179.116273197858));
#40738=CARTESIAN_POINT('Ctrl Pts',(-61.9280682383087,-123.061098742899,
178.353169537834));
#40739=CARTESIAN_POINT('Ctrl Pts',(-62.9132074030754,-123.050357554882,
177.590065877811));
#40740=CARTESIAN_POINT('Ctrl Pts',(-63.0761613633425,-123.127266802597,
176.356991379871));
#40741=CARTESIAN_POINT('Ctrl Pts',(-63.2391153236096,-123.204176050311,
175.123916881932));
#40742=CARTESIAN_POINT('Ctrl Pts',(-62.4902494419682,-123.378291384946,
174.143189863554));
#40743=CARTESIAN_POINT('Ctrl Pts',(-61.7413835603268,-123.55240671958,173.162462845176));
#40744=CARTESIAN_POINT('Ctrl Pts',(-60.5251948963169,-123.776341784949,
173.008579892738));
#40745=CARTESIAN_POINT('Ctrl Pts',(-59.3090062323071,-124.000276850317,
172.854696940301));
#40746=CARTESIAN_POINT('Ctrl Pts',(-58.3437431933744,-124.197461567645,
173.617800600325));
#40747=CARTESIAN_POINT('Ctrl Pts',(-57.3784801544418,-124.394646284973,
174.380904260348));
#40748=CARTESIAN_POINT('Ctrl Pts',(-57.2354023200087,-124.504180566569,
175.613978758287));
#40749=CARTESIAN_POINT('Ctrl Pts',(-57.0923244855756,-124.613714848165,
176.847053256227));
#40750=CARTESIAN_POINT('Ctrl Pts',(-57.861066493051,-124.626043042842,177.827780274605));
#40751=CARTESIAN_POINT('Ctrl Pts',(-58.6298085005265,-124.638371237518,
178.808507292983));
#40752=CARTESIAN_POINT('Ctrl Pts',(-59.8658732903704,-124.60087970146,178.96239024542));
#40753=CARTESIAN_POINT('Ctrl Pts',(-61.1019380802142,-124.563388165402,
179.116273197858));
#40754=CARTESIAN_POINT('Ctrl Pts',(-62.0870772449809,-124.552646977385,
178.353169537834));
#40755=CARTESIAN_POINT('Ctrl Pts',(-63.0722164097476,-124.541905789367,
177.590065877811));
#40756=CARTESIAN_POINT('Ctrl Pts',(-63.2351703700147,-124.618815037082,
176.356991379871));
#40757=CARTESIAN_POINT('Ctrl Pts',(-63.3981243302818,-124.695724284797,
175.123916881932));
#40758=CARTESIAN_POINT('Ctrl Pts',(-62.6492584486404,-124.869839619431,
174.143189863554));
#40759=CARTESIAN_POINT('Ctrl Pts',(-61.900392566999,-125.043954954065,173.162462845176));
#40760=CARTESIAN_POINT('Ctrl Pts',(-60.6842039029891,-125.267890019434,
173.008579892738));
#40761=CARTESIAN_POINT('Ctrl Pts',(-59.4680152389793,-125.491825084803,
172.854696940301));
#40762=CARTESIAN_POINT('Ctrl Pts',(-58.5027522000467,-125.689009802131,
173.617800600325));
#40763=CARTESIAN_POINT('Ctrl Pts',(-57.537489161114,-125.886194519459,174.380904260348));
#40764=CARTESIAN_POINT('Ctrl Pts',(-57.3944113266809,-125.995728801055,
175.613978758287));
#40765=CARTESIAN_POINT('Ctrl Pts',(-57.2513334922478,-126.105263082651,
176.847053256227));
#40766=CARTESIAN_POINT('Ctrl Pts',(-58.0200754997233,-126.117591277327,
177.827780274605));
#40767=CARTESIAN_POINT('Ctrl Pts',(-58.7888175071987,-126.129919472004,
178.808507292983));
#40768=CARTESIAN_POINT('Ctrl Pts',(-60.0248822970426,-126.092427935946,
178.96239024542));
#40769=CARTESIAN_POINT('Ctrl Pts',(-61.2609470868864,-126.054936399888,
179.116273197858));
#40770=CARTESIAN_POINT('Ctrl Pts',(-62.2460862516531,-126.04419521187,178.353169537834));
#40771=CARTESIAN_POINT('Ctrl Pts',(-63.2312254164198,-126.033454023853,
177.590065877811));
#40772=CARTESIAN_POINT('Ctrl Pts',(-63.3941793766869,-126.110363271568,
176.356991379871));
#40773=CARTESIAN_POINT('Ctrl Pts',(-63.5571333369541,-126.187272519283,
175.123916881932));
#40774=CARTESIAN_POINT('Ctrl Pts',(-62.8082674553126,-126.361387853917,
174.143189863554));
#40775=CARTESIAN_POINT('Ctrl Pts',(-62.0594015736712,-126.535503188551,
173.162462845176));
#40776=CARTESIAN_POINT('Ctrl Pts',(-60.8432129096614,-126.75943825392,173.008579892738));
#40777=CARTESIAN_POINT('Ctrl Pts',(-59.6270242456515,-126.983373319289,
172.854696940301));
#40778=CARTESIAN_POINT('Ctrl Pts',(-58.6617612067189,-127.180558036617,
173.617800600325));
#40779=CARTESIAN_POINT('Ctrl Pts',(-57.6964981677863,-127.377742753945,
174.380904260348));
#40780=CARTESIAN_POINT('Ctrl Pts',(-57.5534203333531,-127.487277035541,
175.613978758287));
#40781=CARTESIAN_POINT('Ctrl Pts',(-57.41034249892,-127.596811317136,176.847053256227));
#40782=CARTESIAN_POINT('Ctrl Pts',(-58.1790845063955,-127.609139511813,
177.827780274605));
#40783=CARTESIAN_POINT('Ctrl Pts',(-58.947826513871,-127.621467706489,178.808507292983));
#40784=CARTESIAN_POINT('Ctrl Pts',(-60.1838913037148,-127.583976170431,
178.96239024542));
#40785=CARTESIAN_POINT('Ctrl Pts',(-61.4199560935587,-127.546484634373,
179.116273197858));
#40786=CARTESIAN_POINT('Ctrl Pts',(-62.4050952583254,-127.535743446356,
178.353169537834));
#40787=CARTESIAN_POINT('Ctrl Pts',(-63.390234423092,-127.525002258339,177.590065877811));
#40788=CARTESIAN_POINT('Ctrl Pts',(-63.5531883833591,-127.601911506053,
176.356991379871));
#40789=CARTESIAN_POINT('Ctrl Pts',(-63.7161423436263,-127.678820753768,
175.123916881932));
#40790=CARTESIAN_POINT('Ctrl Pts',(-62.9672764619849,-127.852936088402,
174.143189863554));
#40791=CARTESIAN_POINT('Ctrl Pts',(-62.2184105803435,-128.027051423037,
173.162462845176));
#40792=CARTESIAN_POINT('Ctrl Pts',(-61.0022219163336,-128.250986488405,
173.008579892738));
#40793=CARTESIAN_POINT('Ctrl Pts',(-59.7860332523238,-128.474921553774,
172.854696940301));
#40794=CARTESIAN_POINT('Ctrl Pts',(-58.8207702133911,-128.672106271102,
173.617800600325));
#40795=CARTESIAN_POINT('Ctrl Pts',(-57.8555071744585,-128.86929098843,174.380904260348));
#40796=CARTESIAN_POINT('Ctrl Pts',(-57.7124293400254,-128.978825270026,
175.613978758287));
#40797=CARTESIAN_POINT('Ctrl Pts',(-57.5693515055923,-129.088359551622,
176.847053256227));
#40798=CARTESIAN_POINT('Ctrl Pts',(-58.3380935130677,-129.100687746298,
177.827780274605));
#40799=CARTESIAN_POINT('Ctrl Pts',(-59.1068355205432,-129.113015940975,
178.808507292983));
#40800=CARTESIAN_POINT('Ctrl Pts',(-60.342900310387,-129.075524404917,178.96239024542));
#40801=CARTESIAN_POINT('Ctrl Pts',(-61.5789651002309,-129.038032868859,
179.116273197858));
#40802=CARTESIAN_POINT('Ctrl Pts',(-62.5641042649976,-129.027291680842,
178.353169537834));
#40803=CARTESIAN_POINT('Ctrl Pts',(-63.5492434297643,-129.016550492824,
177.590065877811));
#40804=CARTESIAN_POINT('Ctrl Pts',(-63.7121973900314,-129.093459740539,
176.356991379871));
#40805=CARTESIAN_POINT('Ctrl Pts',(-63.8751513502985,-129.170368988254,
175.123916881932));
#40806=CARTESIAN_POINT('Ctrl Pts',(-63.1262854686571,-129.344484322888,
174.143189863554));
#40807=CARTESIAN_POINT('Ctrl Pts',(-62.3774195870157,-129.518599657522,
173.162462845176));
#40808=CARTESIAN_POINT('Ctrl Pts',(-61.1612309230058,-129.742534722891,
173.008579892738));
#40809=CARTESIAN_POINT('Ctrl Pts',(-59.945042258996,-129.96646978826,172.854696940301));
#40810=CARTESIAN_POINT('Ctrl Pts',(-58.9797792200633,-130.163654505588,
173.617800600325));
#40811=CARTESIAN_POINT('Ctrl Pts',(-58.0145161811307,-130.360839222916,
174.380904260348));
#40812=CARTESIAN_POINT('Ctrl Pts',(-57.8714383466976,-130.470373504512,
175.613978758287));
#40813=CARTESIAN_POINT('Ctrl Pts',(-57.7283605122645,-130.579907786108,
176.847053256227));
#40814=CARTESIAN_POINT('Ctrl Pts',(-58.4971025197399,-130.592235980784,
177.827780274605));
#40815=CARTESIAN_POINT('Ctrl Pts',(-59.2658445272154,-130.604564175461,
178.808507292983));
#40816=CARTESIAN_POINT('Ctrl Pts',(-60.5019093170593,-130.567072639403,
178.96239024542));
#40817=CARTESIAN_POINT('Ctrl Pts',(-61.7379741069031,-130.529581103344,
179.116273197858));
#40818=CARTESIAN_POINT('Ctrl Pts',(-62.7231132716698,-130.518839915327,
178.353169537834));
#40819=CARTESIAN_POINT('Ctrl Pts',(-63.7082524364365,-130.50809872731,177.590065877811));
#40820=CARTESIAN_POINT('Ctrl Pts',(-63.8712063967036,-130.585007975025,
176.356991379871));
#40821=CARTESIAN_POINT('Ctrl Pts',(-64.0341603569708,-130.661917222739,
175.123916881932));
#40822=CARTESIAN_POINT('Ctrl Pts',(-63.2852944753293,-130.836032557374,
174.143189863554));
#40823=CARTESIAN_POINT('Ctrl Pts',(-62.5364285936879,-131.010147892008,
173.162462845176));
#40824=CARTESIAN_POINT('Ctrl Pts',(-61.3202399296781,-131.234082957377,
173.008579892738));
#40825=CARTESIAN_POINT('Ctrl Pts',(-60.1040512656682,-131.458018022745,
172.854696940301));
#40826=CARTESIAN_POINT('Ctrl Pts',(-59.1387882267356,-131.655202740073,
173.617800600325));
#40827=CARTESIAN_POINT('Ctrl Pts',(-58.1735251878029,-131.852387457401,
174.380904260348));
#40828=CARTESIAN_POINT('Ctrl Pts',(-58.0304473533698,-131.961921738997,
175.613978758287));
#40829=CARTESIAN_POINT('Ctrl Pts',(-57.8873695189367,-132.071456020593,
176.847053256227));
#40830=CARTESIAN_POINT('Ctrl Pts',(-58.6561115264122,-132.08378421527,177.827780274605));
#40831=CARTESIAN_POINT('Ctrl Pts',(-59.4248535338876,-132.096112409946,
178.808507292983));
#40832=CARTESIAN_POINT('Ctrl Pts',(-60.6609183237315,-132.058620873888,
178.96239024542));
#40833=CARTESIAN_POINT('Ctrl Pts',(-61.4604944724631,-132.034368635448,
179.061932874153));
#40834=CARTESIAN_POINT('Ctrl Pts',(-62.203773450631,-132.020578326074,178.749326549433));
#40835=CARTESIAN_POINT('Ctrl Pts',(-52.6515183282542,-67.7327195975386,
179.686725372378));
#40836=CARTESIAN_POINT('Ctrl Pts',(-53.1450794947509,-67.7126445084354,
179.888729463648));
#40837=CARTESIAN_POINT('Ctrl Pts',(-53.673891258688,-67.6865820008601,179.954696079469));
#40838=CARTESIAN_POINT('Ctrl Pts',(-55.3186666497572,-67.6055191841591,
180.159873561769));
#40839=CARTESIAN_POINT('Ctrl Pts',(-56.6288741944062,-67.5601235350989,
179.142400961866));
#40840=CARTESIAN_POINT('Ctrl Pts',(-57.9390817390552,-67.5147278860387,
178.124928361964));
#40841=CARTESIAN_POINT('Ctrl Pts',(-58.1530412096253,-67.5861996055927,
176.48082732954));
#40842=CARTESIAN_POINT('Ctrl Pts',(-58.3670006801954,-67.6576713251468,
174.836726297116));
#40843=CARTESIAN_POINT('Ctrl Pts',(-57.3651991030978,-67.8587512947533,
173.529088919052));
#40844=CARTESIAN_POINT('Ctrl Pts',(-56.3633975260002,-68.0598312643598,
172.221451540989));
#40845=CARTESIAN_POINT('Ctrl Pts',(-54.7384982607651,-68.3273376103715,
172.016274058689));
#40846=CARTESIAN_POINT('Ctrl Pts',(-53.1135989955299,-68.5948439563832,
171.81109657639));
#40847=CARTESIAN_POINT('Ctrl Pts',(-51.8232675767149,-68.8266831347541,
172.828569176292));
#40848=CARTESIAN_POINT('Ctrl Pts',(-50.5329361578999,-69.0585223131251,
173.846041776195));
#40849=CARTESIAN_POINT('Ctrl Pts',(-50.3388528131639,-69.1734941228817,
175.490142808619));
#40850=CARTESIAN_POINT('Ctrl Pts',(-50.1447694684278,-69.2884659326383,
177.134243841043));
#40851=CARTESIAN_POINT('Ctrl Pts',(-51.1664471713594,-69.2738294923425,
178.441881219107));
#40852=CARTESIAN_POINT('Ctrl Pts',(-52.188124874291,-69.2591930520467,179.74951859717));
#40853=CARTESIAN_POINT('Ctrl Pts',(-53.8329002653602,-69.1781302353457,
179.954696079469));
#40854=CARTESIAN_POINT('Ctrl Pts',(-55.4776756564294,-69.0970674186447,
180.159873561769));
#40855=CARTESIAN_POINT('Ctrl Pts',(-56.7878832010784,-69.0516717695845,
179.142400961866));
#40856=CARTESIAN_POINT('Ctrl Pts',(-58.0980907457274,-69.0062761205243,
178.124928361964));
#40857=CARTESIAN_POINT('Ctrl Pts',(-58.3120502162975,-69.0777478400783,
176.48082732954));
#40858=CARTESIAN_POINT('Ctrl Pts',(-58.5260096868676,-69.1492195596324,
174.836726297116));
#40859=CARTESIAN_POINT('Ctrl Pts',(-57.52420810977,-69.3502995292389,173.529088919052));
#40860=CARTESIAN_POINT('Ctrl Pts',(-56.5224065326725,-69.5513794988454,
172.221451540989));
#40861=CARTESIAN_POINT('Ctrl Pts',(-54.8975072674373,-69.8188858448571,
172.016274058689));
#40862=CARTESIAN_POINT('Ctrl Pts',(-53.2726080022022,-70.0863921908688,
171.81109657639));
#40863=CARTESIAN_POINT('Ctrl Pts',(-51.9822765833872,-70.3182313692397,
172.828569176292));
#40864=CARTESIAN_POINT('Ctrl Pts',(-50.6919451645722,-70.5500705476106,
173.846041776195));
#40865=CARTESIAN_POINT('Ctrl Pts',(-50.4978618198361,-70.6650423573673,
175.490142808619));
#40866=CARTESIAN_POINT('Ctrl Pts',(-50.3037784751,-70.7800141671239,177.134243841043));
#40867=CARTESIAN_POINT('Ctrl Pts',(-51.3254561780316,-70.7653777268281,
178.441881219107));
#40868=CARTESIAN_POINT('Ctrl Pts',(-52.3471338809632,-70.7507412865323,
179.74951859717));
#40869=CARTESIAN_POINT('Ctrl Pts',(-53.9919092720324,-70.6696784698313,
179.954696079469));
#40870=CARTESIAN_POINT('Ctrl Pts',(-55.6366846631016,-70.5886156531303,
180.159873561769));
#40871=CARTESIAN_POINT('Ctrl Pts',(-56.9468922077507,-70.5432200040701,
179.142400961866));
#40872=CARTESIAN_POINT('Ctrl Pts',(-58.2570997523997,-70.4978243550099,
178.124928361964));
#40873=CARTESIAN_POINT('Ctrl Pts',(-58.4710592229698,-70.5692960745639,
176.48082732954));
#40874=CARTESIAN_POINT('Ctrl Pts',(-58.6850186935399,-70.640767794118,174.836726297116));
#40875=CARTESIAN_POINT('Ctrl Pts',(-57.6832171164423,-70.8418477637245,
173.529088919052));
#40876=CARTESIAN_POINT('Ctrl Pts',(-56.6814155393447,-71.042927733331,172.221451540989));
#40877=CARTESIAN_POINT('Ctrl Pts',(-55.0565162741095,-71.3104340793427,
172.016274058689));
#40878=CARTESIAN_POINT('Ctrl Pts',(-53.4316170088744,-71.5779404253544,
171.81109657639));
#40879=CARTESIAN_POINT('Ctrl Pts',(-52.1412855900594,-71.8097796037253,
172.828569176292));
#40880=CARTESIAN_POINT('Ctrl Pts',(-50.8509541712444,-72.0416187820962,
173.846041776195));
#40881=CARTESIAN_POINT('Ctrl Pts',(-50.6568708265083,-72.1565905918529,
175.490142808619));
#40882=CARTESIAN_POINT('Ctrl Pts',(-50.4627874817723,-72.2715624016095,
177.134243841043));
#40883=CARTESIAN_POINT('Ctrl Pts',(-51.4844651847039,-72.2569259613137,
178.441881219107));
#40884=CARTESIAN_POINT('Ctrl Pts',(-52.5061428876355,-72.242289521018,179.74951859717));
#40885=CARTESIAN_POINT('Ctrl Pts',(-54.1509182787047,-72.1612267043169,
179.954696079469));
#40886=CARTESIAN_POINT('Ctrl Pts',(-55.7956936697739,-72.0801638876159,
180.159873561769));
#40887=CARTESIAN_POINT('Ctrl Pts',(-57.1059012144229,-72.0347682385557,
179.142400961866));
#40888=CARTESIAN_POINT('Ctrl Pts',(-58.4161087590719,-71.9893725894955,
178.124928361964));
#40889=CARTESIAN_POINT('Ctrl Pts',(-58.630068229642,-72.0608443090495,176.48082732954));
#40890=CARTESIAN_POINT('Ctrl Pts',(-58.8440277002121,-72.1323160286036,
174.836726297116));
#40891=CARTESIAN_POINT('Ctrl Pts',(-57.8422261231145,-72.3333959982101,
173.529088919052));
#40892=CARTESIAN_POINT('Ctrl Pts',(-56.8404245460169,-72.5344759678166,
172.221451540989));
#40893=CARTESIAN_POINT('Ctrl Pts',(-55.2155252807818,-72.8019823138283,
172.016274058689));
#40894=CARTESIAN_POINT('Ctrl Pts',(-53.5906260155466,-73.06948865984,171.81109657639));
#40895=CARTESIAN_POINT('Ctrl Pts',(-52.3002945967316,-73.3013278382109,
172.828569176292));
#40896=CARTESIAN_POINT('Ctrl Pts',(-51.0099631779166,-73.5331670165818,
173.846041776195));
#40897=CARTESIAN_POINT('Ctrl Pts',(-50.8158798331806,-73.6481388263385,
175.490142808619));
#40898=CARTESIAN_POINT('Ctrl Pts',(-50.6217964884445,-73.7631106360951,
177.134243841043));
#40899=CARTESIAN_POINT('Ctrl Pts',(-51.6434741913761,-73.7484741957993,
178.441881219107));
#40900=CARTESIAN_POINT('Ctrl Pts',(-52.6651518943077,-73.7338377555035,
179.74951859717));
#40901=CARTESIAN_POINT('Ctrl Pts',(-54.3099272853769,-73.6527749388025,
179.954696079469));
#40902=CARTESIAN_POINT('Ctrl Pts',(-55.9547026764461,-73.5717121221015,
180.159873561769));
#40903=CARTESIAN_POINT('Ctrl Pts',(-57.2649102210951,-73.5263164730413,
179.142400961866));
#40904=CARTESIAN_POINT('Ctrl Pts',(-58.5751177657441,-73.4809208239811,
178.124928361964));
#40905=CARTESIAN_POINT('Ctrl Pts',(-58.7890772363142,-73.5523925435351,
176.48082732954));
#40906=CARTESIAN_POINT('Ctrl Pts',(-59.0030367068843,-73.6238642630892,
174.836726297116));
#40907=CARTESIAN_POINT('Ctrl Pts',(-58.0012351297867,-73.8249442326957,
173.529088919052));
#40908=CARTESIAN_POINT('Ctrl Pts',(-56.9994335526892,-74.0260242023022,
172.221451540989));
#40909=CARTESIAN_POINT('Ctrl Pts',(-55.374534287454,-74.2935305483139,172.016274058689));
#40910=CARTESIAN_POINT('Ctrl Pts',(-53.7496350222188,-74.5610368943256,
171.81109657639));
#40911=CARTESIAN_POINT('Ctrl Pts',(-52.4593036034038,-74.7928760726965,
172.828569176292));
#40912=CARTESIAN_POINT('Ctrl Pts',(-51.1689721845888,-75.0247152510674,
173.846041776195));
#40913=CARTESIAN_POINT('Ctrl Pts',(-50.9748888398528,-75.1396870608241,
175.490142808619));
#40914=CARTESIAN_POINT('Ctrl Pts',(-50.7808054951167,-75.2546588705807,
177.134243841043));
#40915=CARTESIAN_POINT('Ctrl Pts',(-51.8024831980483,-75.2400224302849,
178.441881219107));
#40916=CARTESIAN_POINT('Ctrl Pts',(-52.8241609009799,-75.2253859899891,
179.74951859717));
#40917=CARTESIAN_POINT('Ctrl Pts',(-54.4689362920491,-75.1443231732881,
179.954696079469));
#40918=CARTESIAN_POINT('Ctrl Pts',(-56.1137116831183,-75.0632603565871,
180.159873561769));
#40919=CARTESIAN_POINT('Ctrl Pts',(-57.4239192277673,-75.0178647075269,
179.142400961866));
#40920=CARTESIAN_POINT('Ctrl Pts',(-58.7341267724164,-74.9724690584667,
178.124928361964));
#40921=CARTESIAN_POINT('Ctrl Pts',(-58.9480862429864,-75.0439407780207,
176.48082732954));
#40922=CARTESIAN_POINT('Ctrl Pts',(-59.1620457135565,-75.1154124975748,
174.836726297116));
#40923=CARTESIAN_POINT('Ctrl Pts',(-58.1602441364589,-75.3164924671813,
173.529088919052));
#40924=CARTESIAN_POINT('Ctrl Pts',(-57.1584425593614,-75.5175724367878,
172.221451540989));
#40925=CARTESIAN_POINT('Ctrl Pts',(-55.5335432941262,-75.7850787827995,
172.016274058689));
#40926=CARTESIAN_POINT('Ctrl Pts',(-53.9086440288911,-76.0525851288112,
171.81109657639));
#40927=CARTESIAN_POINT('Ctrl Pts',(-52.6183126100761,-76.2844243071821,
172.828569176292));
#40928=CARTESIAN_POINT('Ctrl Pts',(-51.3279811912611,-76.5162634855531,
173.846041776195));
#40929=CARTESIAN_POINT('Ctrl Pts',(-51.133897846525,-76.6312352953097,175.490142808619));
#40930=CARTESIAN_POINT('Ctrl Pts',(-50.939814501789,-76.7462071050663,177.134243841043));
#40931=CARTESIAN_POINT('Ctrl Pts',(-51.9614922047205,-76.7315706647705,
178.441881219107));
#40932=CARTESIAN_POINT('Ctrl Pts',(-52.9831699076522,-76.7169342244747,
179.74951859717));
#40933=CARTESIAN_POINT('Ctrl Pts',(-54.6279452987213,-76.6358714077737,
179.954696079469));
#40934=CARTESIAN_POINT('Ctrl Pts',(-56.2727206897905,-76.5548085910727,
180.159873561769));
#40935=CARTESIAN_POINT('Ctrl Pts',(-57.5829282344396,-76.5094129420125,
179.142400961866));
#40936=CARTESIAN_POINT('Ctrl Pts',(-58.8931357790886,-76.4640172929522,
178.124928361964));
#40937=CARTESIAN_POINT('Ctrl Pts',(-59.1070952496587,-76.5354890125063,
176.48082732954));
#40938=CARTESIAN_POINT('Ctrl Pts',(-59.3210547202288,-76.6069607320604,
174.836726297116));
#40939=CARTESIAN_POINT('Ctrl Pts',(-58.3192531431312,-76.8080407016669,
173.529088919052));
#40940=CARTESIAN_POINT('Ctrl Pts',(-57.3174515660336,-77.0091206712734,
172.221451540989));
#40941=CARTESIAN_POINT('Ctrl Pts',(-55.6925523007984,-77.2766270172851,
172.016274058689));
#40942=CARTESIAN_POINT('Ctrl Pts',(-54.0676530355633,-77.5441333632968,
171.81109657639));
#40943=CARTESIAN_POINT('Ctrl Pts',(-52.7773216167483,-77.7759725416677,
172.828569176292));
#40944=CARTESIAN_POINT('Ctrl Pts',(-51.4869901979333,-78.0078117200386,
173.846041776195));
#40945=CARTESIAN_POINT('Ctrl Pts',(-51.2929068531972,-78.1227835297953,
175.490142808619));
#40946=CARTESIAN_POINT('Ctrl Pts',(-51.0988235084612,-78.2377553395519,
177.134243841043));
#40947=CARTESIAN_POINT('Ctrl Pts',(-52.1205012113928,-78.2231188992561,
178.441881219107));
#40948=CARTESIAN_POINT('Ctrl Pts',(-53.1421789143244,-78.2084824589603,
179.74951859717));
#40949=CARTESIAN_POINT('Ctrl Pts',(-54.7869543053936,-78.1274196422593,
179.954696079469));
#40950=CARTESIAN_POINT('Ctrl Pts',(-56.4317296964628,-78.0463568255583,
180.159873561769));
#40951=CARTESIAN_POINT('Ctrl Pts',(-57.7419372411118,-78.0009611764981,
179.142400961866));
#40952=CARTESIAN_POINT('Ctrl Pts',(-59.0521447857608,-77.9555655274379,
178.124928361964));
#40953=CARTESIAN_POINT('Ctrl Pts',(-59.2661042563309,-78.0270372469919,
176.48082732954));
#40954=CARTESIAN_POINT('Ctrl Pts',(-59.480063726901,-78.098508966546,174.836726297116));
#40955=CARTESIAN_POINT('Ctrl Pts',(-58.4782621498034,-78.2995889361525,
173.529088919052));
#40956=CARTESIAN_POINT('Ctrl Pts',(-57.4764605727058,-78.500668905759,172.221451540989));
#40957=CARTESIAN_POINT('Ctrl Pts',(-55.8515613074707,-78.7681752517707,
172.016274058689));
#40958=CARTESIAN_POINT('Ctrl Pts',(-54.2266620422355,-79.0356815977824,
171.81109657639));
#40959=CARTESIAN_POINT('Ctrl Pts',(-52.9363306234205,-79.2675207761533,
172.828569176292));
#40960=CARTESIAN_POINT('Ctrl Pts',(-51.6459992046055,-79.4993599545243,
173.846041776195));
#40961=CARTESIAN_POINT('Ctrl Pts',(-51.4519158598695,-79.6143317642809,
175.490142808619));
#40962=CARTESIAN_POINT('Ctrl Pts',(-51.2578325151334,-79.7293035740375,
177.134243841043));
#40963=CARTESIAN_POINT('Ctrl Pts',(-52.279510218065,-79.7146671337417,178.441881219107));
#40964=CARTESIAN_POINT('Ctrl Pts',(-53.3011879209966,-79.7000306934459,
179.74951859717));
#40965=CARTESIAN_POINT('Ctrl Pts',(-54.9459633120658,-79.6189678767449,
179.954696079469));
#40966=CARTESIAN_POINT('Ctrl Pts',(-56.590738703135,-79.5379050600439,180.159873561769));
#40967=CARTESIAN_POINT('Ctrl Pts',(-57.900946247784,-79.4925094109837,179.142400961866));
#40968=CARTESIAN_POINT('Ctrl Pts',(-59.211153792433,-79.4471137619235,178.124928361964));
#40969=CARTESIAN_POINT('Ctrl Pts',(-59.4251132630031,-79.5185854814775,
176.48082732954));
#40970=CARTESIAN_POINT('Ctrl Pts',(-59.6390727335732,-79.5900572010316,
174.836726297116));
#40971=CARTESIAN_POINT('Ctrl Pts',(-58.6372711564756,-79.7911371706381,
173.529088919052));
#40972=CARTESIAN_POINT('Ctrl Pts',(-57.6354695793781,-79.9922171402446,
172.221451540989));
#40973=CARTESIAN_POINT('Ctrl Pts',(-56.0105703141429,-80.2597234862563,
172.016274058689));
#40974=CARTESIAN_POINT('Ctrl Pts',(-54.3856710489078,-80.527229832268,171.81109657639));
#40975=CARTESIAN_POINT('Ctrl Pts',(-53.0953396300927,-80.7590690106389,
172.828569176292));
#40976=CARTESIAN_POINT('Ctrl Pts',(-51.8050082112778,-80.9909081890099,
173.846041776195));
#40977=CARTESIAN_POINT('Ctrl Pts',(-51.6109248665417,-81.1058799987665,
175.490142808619));
#40978=CARTESIAN_POINT('Ctrl Pts',(-51.4168415218056,-81.2208518085231,
177.134243841043));
#40979=CARTESIAN_POINT('Ctrl Pts',(-52.4385192247372,-81.2062153682273,
178.441881219107));
#40980=CARTESIAN_POINT('Ctrl Pts',(-53.4601969276688,-81.1915789279315,
179.74951859717));
#40981=CARTESIAN_POINT('Ctrl Pts',(-55.104972318738,-81.1105161112305,179.954696079469));
#40982=CARTESIAN_POINT('Ctrl Pts',(-56.7497477098072,-81.0294532945295,
180.159873561769));
#40983=CARTESIAN_POINT('Ctrl Pts',(-58.0599552544562,-80.9840576454693,
179.142400961866));
#40984=CARTESIAN_POINT('Ctrl Pts',(-59.3701627991053,-80.9386619964091,
178.124928361964));
#40985=CARTESIAN_POINT('Ctrl Pts',(-59.5841222696753,-81.0101337159631,
176.48082732954));
#40986=CARTESIAN_POINT('Ctrl Pts',(-59.7980817402454,-81.0816054355172,
174.836726297116));
#40987=CARTESIAN_POINT('Ctrl Pts',(-58.7962801631479,-81.2826854051237,
173.529088919052));
#40988=CARTESIAN_POINT('Ctrl Pts',(-57.7944785860503,-81.4837653747302,
172.221451540989));
#40989=CARTESIAN_POINT('Ctrl Pts',(-56.1695793208151,-81.7512717207419,
172.016274058689));
#40990=CARTESIAN_POINT('Ctrl Pts',(-54.54468005558,-82.0187780667536,171.81109657639));
#40991=CARTESIAN_POINT('Ctrl Pts',(-53.254348636765,-82.2506172451245,172.828569176292));
#40992=CARTESIAN_POINT('Ctrl Pts',(-51.96401721795,-82.4824564234954,173.846041776195));
#40993=CARTESIAN_POINT('Ctrl Pts',(-51.7699338732139,-82.5974282332521,
175.490142808619));
#40994=CARTESIAN_POINT('Ctrl Pts',(-51.5758505284779,-82.7124000430087,
177.134243841043));
#40995=CARTESIAN_POINT('Ctrl Pts',(-52.5975282314095,-82.6977636027129,
178.441881219107));
#40996=CARTESIAN_POINT('Ctrl Pts',(-53.6192059343411,-82.6831271624172,
179.74951859717));
#40997=CARTESIAN_POINT('Ctrl Pts',(-55.2639813254103,-82.6020643457161,
179.954696079469));
#40998=CARTESIAN_POINT('Ctrl Pts',(-56.9087567164794,-82.5210015290151,
180.159873561769));
#40999=CARTESIAN_POINT('Ctrl Pts',(-58.2189642611285,-82.4756058799549,
179.142400961866));
#41000=CARTESIAN_POINT('Ctrl Pts',(-59.5291718057775,-82.4302102308947,
178.124928361964));
#41001=CARTESIAN_POINT('Ctrl Pts',(-59.7431312763476,-82.5016819504488,
176.48082732954));
#41002=CARTESIAN_POINT('Ctrl Pts',(-59.9570907469177,-82.5731536700028,
174.836726297116));
#41003=CARTESIAN_POINT('Ctrl Pts',(-58.9552891698201,-82.7742336396093,
173.529088919052));
#41004=CARTESIAN_POINT('Ctrl Pts',(-57.9534875927225,-82.9753136092158,
172.221451540989));
#41005=CARTESIAN_POINT('Ctrl Pts',(-56.3285883274873,-83.2428199552275,
172.016274058689));
#41006=CARTESIAN_POINT('Ctrl Pts',(-54.7036890622522,-83.5103263012392,
171.81109657639));
#41007=CARTESIAN_POINT('Ctrl Pts',(-53.4133576434372,-83.7421654796101,
172.828569176292));
#41008=CARTESIAN_POINT('Ctrl Pts',(-52.1230262246222,-83.9740046579811,
173.846041776195));
#41009=CARTESIAN_POINT('Ctrl Pts',(-51.9289428798862,-84.0889764677377,
175.490142808619));
#41010=CARTESIAN_POINT('Ctrl Pts',(-51.7348595351501,-84.2039482774943,
177.134243841043));
#41011=CARTESIAN_POINT('Ctrl Pts',(-52.7565372380817,-84.1893118371985,
178.441881219107));
#41012=CARTESIAN_POINT('Ctrl Pts',(-53.7782149410133,-84.1746753969028,
179.74951859717));
#41013=CARTESIAN_POINT('Ctrl Pts',(-55.4229903320825,-84.0936125802018,
179.954696079469));
#41014=CARTESIAN_POINT('Ctrl Pts',(-57.0677657231517,-84.0125497635007,
180.159873561769));
#41015=CARTESIAN_POINT('Ctrl Pts',(-58.3779732678007,-83.9671541144405,
179.142400961866));
#41016=CARTESIAN_POINT('Ctrl Pts',(-59.6881808124497,-83.9217584653803,
178.124928361964));
#41017=CARTESIAN_POINT('Ctrl Pts',(-59.9021402830198,-83.9932301849343,
176.48082732954));
#41018=CARTESIAN_POINT('Ctrl Pts',(-60.1160997535899,-84.0647019044884,
174.836726297116));
#41019=CARTESIAN_POINT('Ctrl Pts',(-59.1142981764923,-84.2657818740949,
173.529088919052));
#41020=CARTESIAN_POINT('Ctrl Pts',(-58.1124965993947,-84.4668618437014,
172.221451540989));
#41021=CARTESIAN_POINT('Ctrl Pts',(-56.4875973341596,-84.7343681897131,
172.016274058689));
#41022=CARTESIAN_POINT('Ctrl Pts',(-54.8626980689244,-85.0018745357248,
171.81109657639));
#41023=CARTESIAN_POINT('Ctrl Pts',(-53.5723666501094,-85.2337137140957,
172.828569176292));
#41024=CARTESIAN_POINT('Ctrl Pts',(-52.2820352312944,-85.4655528924667,
173.846041776195));
#41025=CARTESIAN_POINT('Ctrl Pts',(-52.0879518865584,-85.5805247022233,
175.490142808619));
#41026=CARTESIAN_POINT('Ctrl Pts',(-51.8938685418223,-85.6954965119799,
177.134243841043));
#41027=CARTESIAN_POINT('Ctrl Pts',(-52.9155462447539,-85.6808600716841,
178.441881219107));
#41028=CARTESIAN_POINT('Ctrl Pts',(-53.9372239476855,-85.6662236313884,
179.74951859717));
#41029=CARTESIAN_POINT('Ctrl Pts',(-55.5819993387547,-85.5851608146873,
179.954696079469));
#41030=CARTESIAN_POINT('Ctrl Pts',(-57.2267747298239,-85.5040979979863,
180.159873561769));
#41031=CARTESIAN_POINT('Ctrl Pts',(-58.5369822744729,-85.4587023489261,
179.142400961866));
#41032=CARTESIAN_POINT('Ctrl Pts',(-59.847189819122,-85.4133066998659,178.124928361964));
#41033=CARTESIAN_POINT('Ctrl Pts',(-60.061149289692,-85.4847784194199,176.48082732954));
#41034=CARTESIAN_POINT('Ctrl Pts',(-60.2751087602621,-85.556250138974,174.836726297116));
#41035=CARTESIAN_POINT('Ctrl Pts',(-59.2733071831645,-85.7573301085805,
173.529088919052));
#41036=CARTESIAN_POINT('Ctrl Pts',(-58.271505606067,-85.958410078187,172.221451540989));
#41037=CARTESIAN_POINT('Ctrl Pts',(-56.6466063408318,-86.2259164241987,
172.016274058689));
#41038=CARTESIAN_POINT('Ctrl Pts',(-55.0217070755966,-86.4934227702104,
171.81109657639));
#41039=CARTESIAN_POINT('Ctrl Pts',(-53.7313756567816,-86.7252619485813,
172.828569176292));
#41040=CARTESIAN_POINT('Ctrl Pts',(-52.4410442379667,-86.9571011269523,
173.846041776195));
#41041=CARTESIAN_POINT('Ctrl Pts',(-52.2469608932306,-87.0720729367089,
175.490142808619));
#41042=CARTESIAN_POINT('Ctrl Pts',(-52.0528775484945,-87.1870447464655,
177.134243841043));
#41043=CARTESIAN_POINT('Ctrl Pts',(-53.0745552514261,-87.1724083061697,
178.441881219107));
#41044=CARTESIAN_POINT('Ctrl Pts',(-54.0962329543578,-87.157771865874,179.74951859717));
#41045=CARTESIAN_POINT('Ctrl Pts',(-55.7410083454269,-87.0767090491729,
179.954696079469));
#41046=CARTESIAN_POINT('Ctrl Pts',(-57.3857837364961,-86.9956462324719,
180.159873561769));
#41047=CARTESIAN_POINT('Ctrl Pts',(-58.6959912811452,-86.9502505834117,
179.142400961866));
#41048=CARTESIAN_POINT('Ctrl Pts',(-60.0061988257942,-86.9048549343515,
178.124928361964));
#41049=CARTESIAN_POINT('Ctrl Pts',(-60.2201582963643,-86.9763266539055,
176.48082732954));
#41050=CARTESIAN_POINT('Ctrl Pts',(-60.4341177669343,-87.0477983734596,
174.836726297116));
#41051=CARTESIAN_POINT('Ctrl Pts',(-59.4323161898368,-87.2488783430661,
173.529088919052));
#41052=CARTESIAN_POINT('Ctrl Pts',(-58.4305146127392,-87.4499583126726,
172.221451540989));
#41053=CARTESIAN_POINT('Ctrl Pts',(-56.805615347504,-87.7174646586843,172.016274058689));
#41054=CARTESIAN_POINT('Ctrl Pts',(-55.1807160822689,-87.984971004696,171.81109657639));
#41055=CARTESIAN_POINT('Ctrl Pts',(-53.8903846634539,-88.2168101830669,
172.828569176292));
#41056=CARTESIAN_POINT('Ctrl Pts',(-52.6000532446389,-88.4486493614378,
173.846041776195));
#41057=CARTESIAN_POINT('Ctrl Pts',(-52.4059698999028,-88.5636211711945,
175.490142808619));
#41058=CARTESIAN_POINT('Ctrl Pts',(-52.2118865551668,-88.6785929809511,
177.134243841043));
#41059=CARTESIAN_POINT('Ctrl Pts',(-53.2335642580984,-88.6639565406553,
178.441881219107));
#41060=CARTESIAN_POINT('Ctrl Pts',(-54.25524196103,-88.6493201003596,179.74951859717));
#41061=CARTESIAN_POINT('Ctrl Pts',(-55.9000173520992,-88.5682572836585,
179.954696079469));
#41062=CARTESIAN_POINT('Ctrl Pts',(-57.5447927431684,-88.4871944669575,
180.159873561769));
#41063=CARTESIAN_POINT('Ctrl Pts',(-58.8550002878174,-88.4417988178973,
179.142400961866));
#41064=CARTESIAN_POINT('Ctrl Pts',(-60.1652078324664,-88.3964031688371,
178.124928361964));
#41065=CARTESIAN_POINT('Ctrl Pts',(-60.3791673030365,-88.4678748883911,
176.48082732954));
#41066=CARTESIAN_POINT('Ctrl Pts',(-60.5931267736066,-88.5393466079452,
174.836726297116));
#41067=CARTESIAN_POINT('Ctrl Pts',(-59.591325196509,-88.7404265775517,173.529088919052));
#41068=CARTESIAN_POINT('Ctrl Pts',(-58.5895236194114,-88.9415065471582,
172.221451540989));
#41069=CARTESIAN_POINT('Ctrl Pts',(-56.9646243541763,-89.2090128931699,
172.016274058689));
#41070=CARTESIAN_POINT('Ctrl Pts',(-55.3397250889411,-89.4765192391816,
171.81109657639));
#41071=CARTESIAN_POINT('Ctrl Pts',(-54.0493936701261,-89.7083584175525,
172.828569176292));
#41072=CARTESIAN_POINT('Ctrl Pts',(-52.7590622513111,-89.9401975959235,
173.846041776195));
#41073=CARTESIAN_POINT('Ctrl Pts',(-52.5649789065751,-90.0551694056801,
175.490142808619));
#41074=CARTESIAN_POINT('Ctrl Pts',(-52.370895561839,-90.1701412154367,177.134243841043));
#41075=CARTESIAN_POINT('Ctrl Pts',(-53.3925732647706,-90.1555047751409,
178.441881219107));
#41076=CARTESIAN_POINT('Ctrl Pts',(-54.4142509677022,-90.1408683348452,
179.74951859717));
#41077=CARTESIAN_POINT('Ctrl Pts',(-56.0590263587714,-90.0598055181441,
179.954696079469));
#41078=CARTESIAN_POINT('Ctrl Pts',(-57.7038017498406,-89.9787427014431,
180.159873561769));
#41079=CARTESIAN_POINT('Ctrl Pts',(-59.0140092944896,-89.9333470523829,
179.142400961866));
#41080=CARTESIAN_POINT('Ctrl Pts',(-60.3242168391386,-89.8879514033227,
178.124928361964));
#41081=CARTESIAN_POINT('Ctrl Pts',(-60.5381763097087,-89.9594231228767,
176.48082732954));
#41082=CARTESIAN_POINT('Ctrl Pts',(-60.7521357802788,-90.0308948424308,
174.836726297116));
#41083=CARTESIAN_POINT('Ctrl Pts',(-59.7503342031812,-90.2319748120373,
173.529088919052));
#41084=CARTESIAN_POINT('Ctrl Pts',(-58.7485326260837,-90.4330547816438,
172.221451540989));
#41085=CARTESIAN_POINT('Ctrl Pts',(-57.1236333608485,-90.7005611276555,
172.016274058689));
#41086=CARTESIAN_POINT('Ctrl Pts',(-55.4987340956133,-90.9680674736672,
171.81109657639));
#41087=CARTESIAN_POINT('Ctrl Pts',(-54.2084026767983,-91.1999066520381,
172.828569176292));
#41088=CARTESIAN_POINT('Ctrl Pts',(-52.9180712579833,-91.4317458304091,
173.846041776195));
#41089=CARTESIAN_POINT('Ctrl Pts',(-52.7239879132473,-91.5467176401657,
175.490142808619));
#41090=CARTESIAN_POINT('Ctrl Pts',(-52.5299045685112,-91.6616894499223,
177.134243841043));
#41091=CARTESIAN_POINT('Ctrl Pts',(-53.5515822714428,-91.6470530096265,
178.441881219107));
#41092=CARTESIAN_POINT('Ctrl Pts',(-54.5732599743744,-91.6324165693307,
179.74951859717));
#41093=CARTESIAN_POINT('Ctrl Pts',(-56.2180353654436,-91.5513537526297,
179.954696079469));
#41094=CARTESIAN_POINT('Ctrl Pts',(-57.8628107565128,-91.4702909359287,
180.159873561769));
#41095=CARTESIAN_POINT('Ctrl Pts',(-59.1730183011618,-91.4248952868685,
179.142400961866));
#41096=CARTESIAN_POINT('Ctrl Pts',(-60.4832258458109,-91.3794996378083,
178.124928361964));
#41097=CARTESIAN_POINT('Ctrl Pts',(-60.6971853163809,-91.4509713573623,
176.48082732954));
#41098=CARTESIAN_POINT('Ctrl Pts',(-60.911144786951,-91.5224430769164,174.836726297116));
#41099=CARTESIAN_POINT('Ctrl Pts',(-59.9093432098535,-91.7235230465229,
173.529088919052));
#41100=CARTESIAN_POINT('Ctrl Pts',(-58.9075416327559,-91.9246030161294,
172.221451540989));
#41101=CARTESIAN_POINT('Ctrl Pts',(-57.2826423675207,-92.1921093621411,
172.016274058689));
#41102=CARTESIAN_POINT('Ctrl Pts',(-55.6577431022856,-92.4596157081528,
171.81109657639));
#41103=CARTESIAN_POINT('Ctrl Pts',(-54.3674116834706,-92.6914548865237,
172.828569176292));
#41104=CARTESIAN_POINT('Ctrl Pts',(-53.0770802646556,-92.9232940648947,
173.846041776195));
#41105=CARTESIAN_POINT('Ctrl Pts',(-52.8829969199195,-93.0382658746513,
175.490142808619));
#41106=CARTESIAN_POINT('Ctrl Pts',(-52.6889135751835,-93.1532376844079,
177.134243841043));
#41107=CARTESIAN_POINT('Ctrl Pts',(-53.7105912781151,-93.1386012441121,
178.441881219107));
#41108=CARTESIAN_POINT('Ctrl Pts',(-54.7322689810467,-93.1239648038163,
179.74951859717));
#41109=CARTESIAN_POINT('Ctrl Pts',(-56.3770443721158,-93.0429019871153,
179.954696079469));
#41110=CARTESIAN_POINT('Ctrl Pts',(-58.021819763185,-92.9618391704143,180.159873561769));
#41111=CARTESIAN_POINT('Ctrl Pts',(-59.3320273078341,-92.9164435213541,
179.142400961866));
#41112=CARTESIAN_POINT('Ctrl Pts',(-60.6422348524831,-92.8710478722939,
178.124928361964));
#41113=CARTESIAN_POINT('Ctrl Pts',(-60.8561943230532,-92.9425195918479,
176.48082732954));
#41114=CARTESIAN_POINT('Ctrl Pts',(-61.0701537936233,-93.013991311402,174.836726297116));
#41115=CARTESIAN_POINT('Ctrl Pts',(-60.0683522165257,-93.2150712810085,
173.529088919052));
#41116=CARTESIAN_POINT('Ctrl Pts',(-59.0665506394281,-93.416151250615,172.221451540989));
#41117=CARTESIAN_POINT('Ctrl Pts',(-57.4416513741929,-93.6836575966267,
172.016274058689));
#41118=CARTESIAN_POINT('Ctrl Pts',(-55.8167521089578,-93.9511639426384,
171.81109657639));
#41119=CARTESIAN_POINT('Ctrl Pts',(-54.5264206901428,-94.1830031210093,
172.828569176292));
#41120=CARTESIAN_POINT('Ctrl Pts',(-53.2360892713278,-94.4148422993803,
173.846041776195));
#41121=CARTESIAN_POINT('Ctrl Pts',(-53.0420059265917,-94.5298141091369,
175.490142808619));
#41122=CARTESIAN_POINT('Ctrl Pts',(-52.8479225818557,-94.6447859188935,
177.134243841043));
#41123=CARTESIAN_POINT('Ctrl Pts',(-53.8696002847873,-94.6301494785977,
178.441881219107));
#41124=CARTESIAN_POINT('Ctrl Pts',(-54.8912779877189,-94.615513038302,179.74951859717));
#41125=CARTESIAN_POINT('Ctrl Pts',(-56.5360533787881,-94.5344502216009,
179.954696079469));
#41126=CARTESIAN_POINT('Ctrl Pts',(-58.1808287698573,-94.4533874048999,
180.159873561769));
#41127=CARTESIAN_POINT('Ctrl Pts',(-59.4910363145063,-94.4079917558397,
179.142400961866));
#41128=CARTESIAN_POINT('Ctrl Pts',(-60.8012438591553,-94.3625961067795,
178.124928361964));
#41129=CARTESIAN_POINT('Ctrl Pts',(-61.0152033297254,-94.4340678263335,
176.48082732954));
#41130=CARTESIAN_POINT('Ctrl Pts',(-61.2291628002955,-94.5055395458876,
174.836726297116));
#41131=CARTESIAN_POINT('Ctrl Pts',(-60.2273612231979,-94.7066195154941,
173.529088919052));
#41132=CARTESIAN_POINT('Ctrl Pts',(-59.2255596461003,-94.9076994851006,
172.221451540989));
#41133=CARTESIAN_POINT('Ctrl Pts',(-57.6006603808652,-95.1752058311123,
172.016274058689));
#41134=CARTESIAN_POINT('Ctrl Pts',(-55.97576111563,-95.442712177124,171.81109657639));
#41135=CARTESIAN_POINT('Ctrl Pts',(-54.685429696815,-95.6745513554949,172.828569176292));
#41136=CARTESIAN_POINT('Ctrl Pts',(-53.395098278,-95.9063905338659,173.846041776195));
#41137=CARTESIAN_POINT('Ctrl Pts',(-53.201014933264,-96.0213623436225,175.490142808619));
#41138=CARTESIAN_POINT('Ctrl Pts',(-53.0069315885279,-96.1363341533791,
177.134243841043));
#41139=CARTESIAN_POINT('Ctrl Pts',(-54.0286092914595,-96.1216977130833,
178.441881219107));
#41140=CARTESIAN_POINT('Ctrl Pts',(-55.0502869943911,-96.1070612727875,
179.74951859717));
#41141=CARTESIAN_POINT('Ctrl Pts',(-56.6950623854603,-96.0259984560865,
179.954696079469));
#41142=CARTESIAN_POINT('Ctrl Pts',(-58.3398377765295,-95.9449356393855,
180.159873561769));
#41143=CARTESIAN_POINT('Ctrl Pts',(-59.6500453211785,-95.8995399903253,
179.142400961866));
#41144=CARTESIAN_POINT('Ctrl Pts',(-60.9602528658275,-95.8541443412651,
178.124928361964));
#41145=CARTESIAN_POINT('Ctrl Pts',(-61.1742123363976,-95.9256160608192,
176.48082732954));
#41146=CARTESIAN_POINT('Ctrl Pts',(-61.3881718069677,-95.9970877803732,
174.836726297116));
#41147=CARTESIAN_POINT('Ctrl Pts',(-60.3863702298701,-96.1981677499797,
173.529088919052));
#41148=CARTESIAN_POINT('Ctrl Pts',(-59.3845686527726,-96.3992477195862,
172.221451540989));
#41149=CARTESIAN_POINT('Ctrl Pts',(-57.7596693875374,-96.6667540655979,
172.016274058689));
#41150=CARTESIAN_POINT('Ctrl Pts',(-56.1347701223022,-96.9342604116096,
171.81109657639));
#41151=CARTESIAN_POINT('Ctrl Pts',(-54.8444387034872,-97.1660995899806,
172.828569176292));
#41152=CARTESIAN_POINT('Ctrl Pts',(-53.5541072846722,-97.3979387683514,
173.846041776195));
#41153=CARTESIAN_POINT('Ctrl Pts',(-53.3600239399362,-97.5129105781081,
175.490142808619));
#41154=CARTESIAN_POINT('Ctrl Pts',(-53.1659405952001,-97.6278823878647,
177.134243841043));
#41155=CARTESIAN_POINT('Ctrl Pts',(-54.1876182981317,-97.6132459475689,
178.441881219107));
#41156=CARTESIAN_POINT('Ctrl Pts',(-55.2092960010633,-97.5986095072732,
179.74951859717));
#41157=CARTESIAN_POINT('Ctrl Pts',(-56.8540713921325,-97.5175466905721,
179.954696079469));
#41158=CARTESIAN_POINT('Ctrl Pts',(-58.4988467832017,-97.4364838738711,
180.159873561769));
#41159=CARTESIAN_POINT('Ctrl Pts',(-59.8090543278507,-97.3910882248109,
179.142400961866));
#41160=CARTESIAN_POINT('Ctrl Pts',(-61.1192618724998,-97.3456925757507,
178.124928361964));
#41161=CARTESIAN_POINT('Ctrl Pts',(-61.3332213430699,-97.4171642953048,
176.48082732954));
#41162=CARTESIAN_POINT('Ctrl Pts',(-61.5471808136399,-97.4886360148588,
174.836726297116));
#41163=CARTESIAN_POINT('Ctrl Pts',(-60.5453792365424,-97.6897159844653,
173.529088919052));
#41164=CARTESIAN_POINT('Ctrl Pts',(-59.5435776594448,-97.8907959540718,
172.221451540989));
#41165=CARTESIAN_POINT('Ctrl Pts',(-57.9186783942096,-98.1583023000835,
172.016274058689));
#41166=CARTESIAN_POINT('Ctrl Pts',(-56.2937791289745,-98.4258086460952,
171.81109657639));
#41167=CARTESIAN_POINT('Ctrl Pts',(-55.0034477101595,-98.6576478244661,
172.828569176292));
#41168=CARTESIAN_POINT('Ctrl Pts',(-53.7131162913445,-98.8894870028371,
173.846041776195));
#41169=CARTESIAN_POINT('Ctrl Pts',(-53.5190329466084,-99.0044588125937,
175.490142808619));
#41170=CARTESIAN_POINT('Ctrl Pts',(-53.3249496018724,-99.1194306223503,
177.134243841043));
#41171=CARTESIAN_POINT('Ctrl Pts',(-54.346627304804,-99.1047941820545,178.441881219107));
#41172=CARTESIAN_POINT('Ctrl Pts',(-55.3683050077356,-99.0901577417588,
179.74951859717));
#41173=CARTESIAN_POINT('Ctrl Pts',(-57.0130803988047,-99.0090949250577,
179.954696079469));
#41174=CARTESIAN_POINT('Ctrl Pts',(-58.6578557898739,-98.9280321083567,
180.159873561769));
#41175=CARTESIAN_POINT('Ctrl Pts',(-59.968063334523,-98.8826364592965,179.142400961866));
#41176=CARTESIAN_POINT('Ctrl Pts',(-61.278270879172,-98.8372408102363,178.124928361964));
#41177=CARTESIAN_POINT('Ctrl Pts',(-61.4922303497421,-98.9087125297904,
176.48082732954));
#41178=CARTESIAN_POINT('Ctrl Pts',(-61.7061898203122,-98.9801842493444,
174.836726297116));
#41179=CARTESIAN_POINT('Ctrl Pts',(-60.7043882432146,-99.1812642189509,
173.529088919052));
#41180=CARTESIAN_POINT('Ctrl Pts',(-59.702586666117,-99.3823441885574,172.221451540989));
#41181=CARTESIAN_POINT('Ctrl Pts',(-58.0776874008818,-99.6498505345691,
172.016274058689));
#41182=CARTESIAN_POINT('Ctrl Pts',(-56.4527881356467,-99.9173568805808,
171.81109657639));
#41183=CARTESIAN_POINT('Ctrl Pts',(-55.1624567168317,-100.149196058952,
172.828569176292));
#41184=CARTESIAN_POINT('Ctrl Pts',(-53.8721252980167,-100.381035237323,
173.846041776195));
#41185=CARTESIAN_POINT('Ctrl Pts',(-53.6780419532806,-100.496007047079,
175.490142808619));
#41186=CARTESIAN_POINT('Ctrl Pts',(-53.4839586085446,-100.610978856836,
177.134243841043));
#41187=CARTESIAN_POINT('Ctrl Pts',(-54.5056363114762,-100.59634241654,178.441881219107));
#41188=CARTESIAN_POINT('Ctrl Pts',(-55.5273140144078,-100.581705976244,
179.74951859717));
#41189=CARTESIAN_POINT('Ctrl Pts',(-57.172089405477,-100.500643159543,179.954696079469));
#41190=CARTESIAN_POINT('Ctrl Pts',(-58.8168647965462,-100.419580342842,
180.159873561769));
#41191=CARTESIAN_POINT('Ctrl Pts',(-60.1270723411952,-100.374184693782,
179.142400961866));
#41192=CARTESIAN_POINT('Ctrl Pts',(-61.4372798858442,-100.328789044722,
178.124928361964));
#41193=CARTESIAN_POINT('Ctrl Pts',(-61.6512393564143,-100.400260764276,
176.48082732954));
#41194=CARTESIAN_POINT('Ctrl Pts',(-61.8651988269844,-100.47173248383,174.836726297116));
#41195=CARTESIAN_POINT('Ctrl Pts',(-60.8633972498868,-100.672812453437,
173.529088919052));
#41196=CARTESIAN_POINT('Ctrl Pts',(-59.8615956727892,-100.873892423043,
172.221451540989));
#41197=CARTESIAN_POINT('Ctrl Pts',(-58.2366964075541,-101.141398769055,
172.016274058689));
#41198=CARTESIAN_POINT('Ctrl Pts',(-56.6117971423189,-101.408905115066,
171.81109657639));
#41199=CARTESIAN_POINT('Ctrl Pts',(-55.3214657235039,-101.640744293437,
172.828569176292));
#41200=CARTESIAN_POINT('Ctrl Pts',(-54.0311343046889,-101.872583471808,
173.846041776195));
#41201=CARTESIAN_POINT('Ctrl Pts',(-53.8370509599529,-101.987555281565,
175.490142808619));
#41202=CARTESIAN_POINT('Ctrl Pts',(-53.6429676152168,-102.102527091322,
177.134243841043));
#41203=CARTESIAN_POINT('Ctrl Pts',(-54.6646453181484,-102.087890651026,
178.441881219107));
#41204=CARTESIAN_POINT('Ctrl Pts',(-55.68632302108,-102.07325421073,179.74951859717));
#41205=CARTESIAN_POINT('Ctrl Pts',(-57.3310984121492,-101.992191394029,
179.954696079469));
#41206=CARTESIAN_POINT('Ctrl Pts',(-58.9758738032184,-101.911128577328,
180.159873561769));
#41207=CARTESIAN_POINT('Ctrl Pts',(-60.2860813478674,-101.865732928268,
179.142400961866));
#41208=CARTESIAN_POINT('Ctrl Pts',(-61.5962888925164,-101.820337279207,
178.124928361964));
#41209=CARTESIAN_POINT('Ctrl Pts',(-61.8102483630865,-101.891808998762,
176.48082732954));
#41210=CARTESIAN_POINT('Ctrl Pts',(-62.0242078336566,-101.963280718316,
174.836726297116));
#41211=CARTESIAN_POINT('Ctrl Pts',(-61.022406256559,-102.164360687922,173.529088919052));
#41212=CARTESIAN_POINT('Ctrl Pts',(-60.0206046794615,-102.365440657529,
172.221451540989));
#41213=CARTESIAN_POINT('Ctrl Pts',(-58.3957054142263,-102.63294700354,172.016274058689));
#41214=CARTESIAN_POINT('Ctrl Pts',(-56.7708061489911,-102.900453349552,
171.81109657639));
#41215=CARTESIAN_POINT('Ctrl Pts',(-55.4804747301761,-103.132292527923,
172.828569176292));
#41216=CARTESIAN_POINT('Ctrl Pts',(-54.1901433113612,-103.364131706294,
173.846041776195));
#41217=CARTESIAN_POINT('Ctrl Pts',(-53.9960599666251,-103.479103516051,
175.490142808619));
#41218=CARTESIAN_POINT('Ctrl Pts',(-53.801976621889,-103.594075325807,177.134243841043));
#41219=CARTESIAN_POINT('Ctrl Pts',(-54.8236543248206,-103.579438885511,
178.441881219107));
#41220=CARTESIAN_POINT('Ctrl Pts',(-55.8453320277522,-103.564802445216,
179.74951859717));
#41221=CARTESIAN_POINT('Ctrl Pts',(-57.4901074188214,-103.483739628515,
179.954696079469));
#41222=CARTESIAN_POINT('Ctrl Pts',(-59.1348828098906,-103.402676811814,
180.159873561769));
#41223=CARTESIAN_POINT('Ctrl Pts',(-60.4450903545396,-103.357281162753,
179.142400961866));
#41224=CARTESIAN_POINT('Ctrl Pts',(-61.7552978991887,-103.311885513693,
178.124928361964));
#41225=CARTESIAN_POINT('Ctrl Pts',(-61.9692573697588,-103.383357233247,
176.48082732954));
#41226=CARTESIAN_POINT('Ctrl Pts',(-62.1832168403288,-103.454828952801,
174.836726297116));
#41227=CARTESIAN_POINT('Ctrl Pts',(-61.1814152632313,-103.655908922408,
173.529088919052));
#41228=CARTESIAN_POINT('Ctrl Pts',(-60.1796136861337,-103.856988892014,
172.221451540989));
#41229=CARTESIAN_POINT('Ctrl Pts',(-58.5547144208985,-104.124495238026,
172.016274058689));
#41230=CARTESIAN_POINT('Ctrl Pts',(-56.9298151556634,-104.392001584038,
171.81109657639));
#41231=CARTESIAN_POINT('Ctrl Pts',(-55.6394837368484,-104.623840762409,
172.828569176292));
#41232=CARTESIAN_POINT('Ctrl Pts',(-54.3491523180334,-104.855679940779,
173.846041776195));
#41233=CARTESIAN_POINT('Ctrl Pts',(-54.1550689732973,-104.970651750536,
175.490142808619));
#41234=CARTESIAN_POINT('Ctrl Pts',(-53.9609856285613,-105.085623560293,
177.134243841043));
#41235=CARTESIAN_POINT('Ctrl Pts',(-54.9826633314929,-105.070987119997,
178.441881219107));
#41236=CARTESIAN_POINT('Ctrl Pts',(-56.0043410344245,-105.056350679701,
179.74951859717));
#41237=CARTESIAN_POINT('Ctrl Pts',(-57.6491164254937,-104.975287863,179.954696079469));
#41238=CARTESIAN_POINT('Ctrl Pts',(-59.2938918165629,-104.894225046299,
180.159873561769));
#41239=CARTESIAN_POINT('Ctrl Pts',(-60.6040993612119,-104.848829397239,
179.142400961866));
#41240=CARTESIAN_POINT('Ctrl Pts',(-61.9143069058609,-104.803433748179,
178.124928361964));
#41241=CARTESIAN_POINT('Ctrl Pts',(-62.128266376431,-104.874905467733,176.48082732954));
#41242=CARTESIAN_POINT('Ctrl Pts',(-62.3422258470011,-104.946377187287,
174.836726297116));
#41243=CARTESIAN_POINT('Ctrl Pts',(-61.3404242699035,-105.147457156893,
173.529088919052));
#41244=CARTESIAN_POINT('Ctrl Pts',(-60.3386226928059,-105.3485371265,172.221451540989));
#41245=CARTESIAN_POINT('Ctrl Pts',(-58.7137234275708,-105.616043472511,
172.016274058689));
#41246=CARTESIAN_POINT('Ctrl Pts',(-57.0888241623356,-105.883549818523,
171.81109657639));
#41247=CARTESIAN_POINT('Ctrl Pts',(-55.7984927435206,-106.115388996894,
172.828569176292));
#41248=CARTESIAN_POINT('Ctrl Pts',(-54.5081613247056,-106.347228175265,
173.846041776195));
#41249=CARTESIAN_POINT('Ctrl Pts',(-54.3140779799695,-106.462199985022,
175.490142808619));
#41250=CARTESIAN_POINT('Ctrl Pts',(-54.1199946352335,-106.577171794778,
177.134243841043));
#41251=CARTESIAN_POINT('Ctrl Pts',(-55.1416723381651,-106.562535354483,
178.441881219107));
#41252=CARTESIAN_POINT('Ctrl Pts',(-56.1633500410967,-106.547898914187,
179.74951859717));
#41253=CARTESIAN_POINT('Ctrl Pts',(-57.8081254321659,-106.466836097486,
179.954696079469));
#41254=CARTESIAN_POINT('Ctrl Pts',(-59.4529008232351,-106.385773280785,
180.159873561769));
#41255=CARTESIAN_POINT('Ctrl Pts',(-60.7631083678841,-106.340377631725,
179.142400961866));
#41256=CARTESIAN_POINT('Ctrl Pts',(-62.0733159125331,-106.294981982664,
178.124928361964));
#41257=CARTESIAN_POINT('Ctrl Pts',(-62.2872753831032,-106.366453702218,
176.48082732954));
#41258=CARTESIAN_POINT('Ctrl Pts',(-62.5012348536733,-106.437925421772,
174.836726297116));
#41259=CARTESIAN_POINT('Ctrl Pts',(-61.4994332765757,-106.639005391379,
173.529088919052));
#41260=CARTESIAN_POINT('Ctrl Pts',(-60.4976316994782,-106.840085360985,
172.221451540989));
#41261=CARTESIAN_POINT('Ctrl Pts',(-58.872732434243,-107.107591706997,172.016274058689));
#41262=CARTESIAN_POINT('Ctrl Pts',(-57.2478331690078,-107.375098053009,
171.81109657639));
#41263=CARTESIAN_POINT('Ctrl Pts',(-55.9575017501928,-107.60693723138,172.828569176292));
#41264=CARTESIAN_POINT('Ctrl Pts',(-54.6671703313778,-107.838776409751,
173.846041776195));
#41265=CARTESIAN_POINT('Ctrl Pts',(-54.4730869866418,-107.953748219507,
175.490142808619));
#41266=CARTESIAN_POINT('Ctrl Pts',(-54.2790036419057,-108.068720029264,
177.134243841043));
#41267=CARTESIAN_POINT('Ctrl Pts',(-55.3006813448373,-108.054083588968,
178.441881219107));
#41268=CARTESIAN_POINT('Ctrl Pts',(-56.3223590477689,-108.039447148672,
179.74951859717));
#41269=CARTESIAN_POINT('Ctrl Pts',(-57.9671344388381,-107.958384331971,
179.954696079469));
#41270=CARTESIAN_POINT('Ctrl Pts',(-59.6119098299073,-107.87732151527,180.159873561769));
#41271=CARTESIAN_POINT('Ctrl Pts',(-60.9221173745563,-107.83192586621,179.142400961866));
#41272=CARTESIAN_POINT('Ctrl Pts',(-62.2323249192054,-107.78653021715,178.124928361964));
#41273=CARTESIAN_POINT('Ctrl Pts',(-62.4462843897754,-107.858001936704,
176.48082732954));
#41274=CARTESIAN_POINT('Ctrl Pts',(-62.6602438603455,-107.929473656258,
174.836726297116));
#41275=CARTESIAN_POINT('Ctrl Pts',(-61.6584422832479,-108.130553625865,
173.529088919052));
#41276=CARTESIAN_POINT('Ctrl Pts',(-60.6566407061504,-108.331633595471,
172.221451540989));
#41277=CARTESIAN_POINT('Ctrl Pts',(-59.0317414409152,-108.599139941483,
172.016274058689));
#41278=CARTESIAN_POINT('Ctrl Pts',(-57.4068421756801,-108.866646287494,
171.81109657639));
#41279=CARTESIAN_POINT('Ctrl Pts',(-56.1165107568651,-109.098485465865,
172.828569176292));
#41280=CARTESIAN_POINT('Ctrl Pts',(-54.8261793380501,-109.330324644236,
173.846041776195));
#41281=CARTESIAN_POINT('Ctrl Pts',(-54.632095993314,-109.445296453993,175.490142808619));
#41282=CARTESIAN_POINT('Ctrl Pts',(-54.438012648578,-109.56026826375,177.134243841043));
#41283=CARTESIAN_POINT('Ctrl Pts',(-55.4596903515096,-109.545631823454,
178.441881219107));
#41284=CARTESIAN_POINT('Ctrl Pts',(-56.4813680544411,-109.530995383158,
179.74951859717));
#41285=CARTESIAN_POINT('Ctrl Pts',(-58.1261434455103,-109.449932566457,
179.954696079469));
#41286=CARTESIAN_POINT('Ctrl Pts',(-59.7709188365795,-109.368869749756,
180.159873561769));
#41287=CARTESIAN_POINT('Ctrl Pts',(-61.0811263812286,-109.323474100696,
179.142400961866));
#41288=CARTESIAN_POINT('Ctrl Pts',(-62.3913339258776,-109.278078451635,
178.124928361964));
#41289=CARTESIAN_POINT('Ctrl Pts',(-62.6052933964477,-109.34955017119,176.48082732954));
#41290=CARTESIAN_POINT('Ctrl Pts',(-62.8192528670178,-109.421021890744,
174.836726297116));
#41291=CARTESIAN_POINT('Ctrl Pts',(-61.8174512899202,-109.62210186035,173.529088919052));
#41292=CARTESIAN_POINT('Ctrl Pts',(-60.8156497128226,-109.823181829957,
172.221451540989));
#41293=CARTESIAN_POINT('Ctrl Pts',(-59.1907504475874,-110.090688175968,
172.016274058689));
#41294=CARTESIAN_POINT('Ctrl Pts',(-57.5658511823523,-110.35819452198,171.81109657639));
#41295=CARTESIAN_POINT('Ctrl Pts',(-56.2755197635373,-110.590033700351,
172.828569176292));
#41296=CARTESIAN_POINT('Ctrl Pts',(-54.9851883447223,-110.821872878722,
173.846041776195));
#41297=CARTESIAN_POINT('Ctrl Pts',(-54.7911049999862,-110.936844688478,
175.490142808619));
#41298=CARTESIAN_POINT('Ctrl Pts',(-54.5970216552502,-111.051816498235,
177.134243841043));
#41299=CARTESIAN_POINT('Ctrl Pts',(-55.6186993581818,-111.037180057939,
178.441881219107));
#41300=CARTESIAN_POINT('Ctrl Pts',(-56.6403770611134,-111.022543617644,
179.74951859717));
#41301=CARTESIAN_POINT('Ctrl Pts',(-58.2851524521826,-110.941480800943,
179.954696079469));
#41302=CARTESIAN_POINT('Ctrl Pts',(-59.9299278432518,-110.860417984242,
180.159873561769));
#41303=CARTESIAN_POINT('Ctrl Pts',(-61.2401353879008,-110.815022335181,
179.142400961866));
#41304=CARTESIAN_POINT('Ctrl Pts',(-62.5503429325498,-110.769626686121,
178.124928361964));
#41305=CARTESIAN_POINT('Ctrl Pts',(-62.7643024031199,-110.841098405675,
176.48082732954));
#41306=CARTESIAN_POINT('Ctrl Pts',(-62.97826187369,-110.912570125229,174.836726297116));
#41307=CARTESIAN_POINT('Ctrl Pts',(-61.9764602965924,-111.113650094836,
173.529088919052));
#41308=CARTESIAN_POINT('Ctrl Pts',(-60.9746587194948,-111.314730064442,
172.221451540989));
#41309=CARTESIAN_POINT('Ctrl Pts',(-59.3497594542597,-111.582236410454,
172.016274058689));
#41310=CARTESIAN_POINT('Ctrl Pts',(-57.7248601890245,-111.849742756466,
171.81109657639));
#41311=CARTESIAN_POINT('Ctrl Pts',(-56.4345287702095,-112.081581934837,
172.828569176292));
#41312=CARTESIAN_POINT('Ctrl Pts',(-55.1441973513945,-112.313421113207,
173.846041776195));
#41313=CARTESIAN_POINT('Ctrl Pts',(-54.9501140066585,-112.428392922964,
175.490142808619));
#41314=CARTESIAN_POINT('Ctrl Pts',(-54.7560306619224,-112.543364732721,
177.134243841043));
#41315=CARTESIAN_POINT('Ctrl Pts',(-55.777708364854,-112.528728292425,178.441881219107));
#41316=CARTESIAN_POINT('Ctrl Pts',(-56.7993860677856,-112.514091852129,
179.74951859717));
#41317=CARTESIAN_POINT('Ctrl Pts',(-58.4441614588548,-112.433029035428,
179.954696079469));
#41318=CARTESIAN_POINT('Ctrl Pts',(-60.088936849924,-112.351966218727,180.159873561769));
#41319=CARTESIAN_POINT('Ctrl Pts',(-61.399144394573,-112.306570569667,179.142400961866));
#41320=CARTESIAN_POINT('Ctrl Pts',(-62.709351939222,-112.261174920607,178.124928361964));
#41321=CARTESIAN_POINT('Ctrl Pts',(-62.9233114097921,-112.332646640161,
176.48082732954));
#41322=CARTESIAN_POINT('Ctrl Pts',(-63.1372708803622,-112.404118359715,
174.836726297116));
#41323=CARTESIAN_POINT('Ctrl Pts',(-62.1354693032646,-112.605198329321,
173.529088919052));
#41324=CARTESIAN_POINT('Ctrl Pts',(-61.1336677261671,-112.806278298928,
172.221451540989));
#41325=CARTESIAN_POINT('Ctrl Pts',(-59.5087684609319,-113.07378464494,172.016274058689));
#41326=CARTESIAN_POINT('Ctrl Pts',(-57.8838691956967,-113.341290990951,
171.81109657639));
#41327=CARTESIAN_POINT('Ctrl Pts',(-56.5935377768817,-113.573130169322,
172.828569176292));
#41328=CARTESIAN_POINT('Ctrl Pts',(-55.3032063580667,-113.804969347693,
173.846041776195));
#41329=CARTESIAN_POINT('Ctrl Pts',(-55.1091230133307,-113.91994115745,175.490142808619));
#41330=CARTESIAN_POINT('Ctrl Pts',(-54.9150396685946,-114.034912967206,
177.134243841043));
#41331=CARTESIAN_POINT('Ctrl Pts',(-55.9367173715262,-114.020276526911,
178.441881219107));
#41332=CARTESIAN_POINT('Ctrl Pts',(-56.9583950744578,-114.005640086615,
179.74951859717));
#41333=CARTESIAN_POINT('Ctrl Pts',(-58.603170465527,-113.924577269914,179.954696079469));
#41334=CARTESIAN_POINT('Ctrl Pts',(-60.2479458565962,-113.843514453213,
180.159873561769));
#41335=CARTESIAN_POINT('Ctrl Pts',(-61.5581534012452,-113.798118804152,
179.142400961866));
#41336=CARTESIAN_POINT('Ctrl Pts',(-62.8683609458943,-113.752723155092,
178.124928361964));
#41337=CARTESIAN_POINT('Ctrl Pts',(-63.0823204164643,-113.824194874646,
176.48082732954));
#41338=CARTESIAN_POINT('Ctrl Pts',(-63.2962798870344,-113.8956665942,174.836726297116));
#41339=CARTESIAN_POINT('Ctrl Pts',(-62.2944783099369,-114.096746563807,
173.529088919052));
#41340=CARTESIAN_POINT('Ctrl Pts',(-61.2926767328393,-114.297826533413,
172.221451540989));
#41341=CARTESIAN_POINT('Ctrl Pts',(-59.6677774676041,-114.565332879425,
172.016274058689));
#41342=CARTESIAN_POINT('Ctrl Pts',(-58.042878202369,-114.832839225437,171.81109657639));
#41343=CARTESIAN_POINT('Ctrl Pts',(-56.752546783554,-115.064678403808,172.828569176292));
#41344=CARTESIAN_POINT('Ctrl Pts',(-55.462215364739,-115.296517582179,173.846041776195));
#41345=CARTESIAN_POINT('Ctrl Pts',(-55.2681320200029,-115.411489391935,
175.490142808619));
#41346=CARTESIAN_POINT('Ctrl Pts',(-55.0740486752669,-115.526461201692,
177.134243841043));
#41347=CARTESIAN_POINT('Ctrl Pts',(-56.0957263781985,-115.511824761396,
178.441881219107));
#41348=CARTESIAN_POINT('Ctrl Pts',(-57.1174040811301,-115.4971883211,179.74951859717));
#41349=CARTESIAN_POINT('Ctrl Pts',(-58.7621794721992,-115.416125504399,
179.954696079469));
#41350=CARTESIAN_POINT('Ctrl Pts',(-60.4069548632684,-115.335062687698,
180.159873561769));
#41351=CARTESIAN_POINT('Ctrl Pts',(-61.7171624079175,-115.289667038638,
179.142400961866));
#41352=CARTESIAN_POINT('Ctrl Pts',(-63.0273699525665,-115.244271389578,
178.124928361964));
#41353=CARTESIAN_POINT('Ctrl Pts',(-63.2413294231366,-115.315743109132,
176.48082732954));
#41354=CARTESIAN_POINT('Ctrl Pts',(-63.4552888937067,-115.387214828686,
174.836726297116));
#41355=CARTESIAN_POINT('Ctrl Pts',(-62.4534873166091,-115.588294798292,
173.529088919052));
#41356=CARTESIAN_POINT('Ctrl Pts',(-61.4516857395115,-115.789374767899,
172.221451540989));
#41357=CARTESIAN_POINT('Ctrl Pts',(-59.8267864742763,-116.056881113911,
172.016274058689));
#41358=CARTESIAN_POINT('Ctrl Pts',(-58.2018872090412,-116.324387459922,
171.81109657639));
#41359=CARTESIAN_POINT('Ctrl Pts',(-56.9115557902262,-116.556226638293,
172.828569176292));
#41360=CARTESIAN_POINT('Ctrl Pts',(-55.6212243714112,-116.788065816664,
173.846041776195));
#41361=CARTESIAN_POINT('Ctrl Pts',(-55.4271410266751,-116.903037626421,
175.490142808619));
#41362=CARTESIAN_POINT('Ctrl Pts',(-55.2330576819391,-117.018009436178,
177.134243841043));
#41363=CARTESIAN_POINT('Ctrl Pts',(-56.2547353848707,-117.003372995882,
178.441881219107));
#41364=CARTESIAN_POINT('Ctrl Pts',(-57.2764130878023,-116.988736555586,
179.74951859717));
#41365=CARTESIAN_POINT('Ctrl Pts',(-58.9211884788715,-116.907673738885,
179.954696079469));
#41366=CARTESIAN_POINT('Ctrl Pts',(-60.5659638699407,-116.826610922184,
180.159873561769));
#41367=CARTESIAN_POINT('Ctrl Pts',(-61.8761714145897,-116.781215273124,
179.142400961866));
#41368=CARTESIAN_POINT('Ctrl Pts',(-63.1863789592387,-116.735819624063,
178.124928361964));
#41369=CARTESIAN_POINT('Ctrl Pts',(-63.4003384298088,-116.807291343618,
176.48082732954));
#41370=CARTESIAN_POINT('Ctrl Pts',(-63.6142979003789,-116.878763063172,
174.836726297116));
#41371=CARTESIAN_POINT('Ctrl Pts',(-62.6124963232813,-117.079843032778,
173.529088919052));
#41372=CARTESIAN_POINT('Ctrl Pts',(-61.6106947461837,-117.280923002385,
172.221451540989));
#41373=CARTESIAN_POINT('Ctrl Pts',(-59.9857954809486,-117.548429348396,
172.016274058689));
#41374=CARTESIAN_POINT('Ctrl Pts',(-58.3608962157134,-117.815935694408,
171.81109657639));
#41375=CARTESIAN_POINT('Ctrl Pts',(-57.0705647968984,-118.047774872779,
172.828569176292));
#41376=CARTESIAN_POINT('Ctrl Pts',(-55.7802333780834,-118.27961405115,173.846041776195));
#41377=CARTESIAN_POINT('Ctrl Pts',(-55.5861500333474,-118.394585860907,
175.490142808619));
#41378=CARTESIAN_POINT('Ctrl Pts',(-55.3920666886113,-118.509557670663,
177.134243841043));
#41379=CARTESIAN_POINT('Ctrl Pts',(-56.4137443915429,-118.494921230367,
178.441881219107));
#41380=CARTESIAN_POINT('Ctrl Pts',(-57.4354220944745,-118.480284790072,
179.74951859717));
#41381=CARTESIAN_POINT('Ctrl Pts',(-59.0801974855437,-118.399221973371,
179.954696079469));
#41382=CARTESIAN_POINT('Ctrl Pts',(-60.7249728766129,-118.31815915667,180.159873561769));
#41383=CARTESIAN_POINT('Ctrl Pts',(-62.0351804212619,-118.272763507609,
179.142400961866));
#41384=CARTESIAN_POINT('Ctrl Pts',(-63.345387965911,-118.227367858549,178.124928361964));
#41385=CARTESIAN_POINT('Ctrl Pts',(-63.559347436481,-118.298839578103,176.48082732954));
#41386=CARTESIAN_POINT('Ctrl Pts',(-63.7733069070511,-118.370311297657,
174.836726297116));
#41387=CARTESIAN_POINT('Ctrl Pts',(-62.7715053299535,-118.571391267264,
173.529088919052));
#41388=CARTESIAN_POINT('Ctrl Pts',(-61.769703752856,-118.77247123687,172.221451540989));
#41389=CARTESIAN_POINT('Ctrl Pts',(-60.1448044876208,-119.039977582882,
172.016274058689));
#41390=CARTESIAN_POINT('Ctrl Pts',(-58.5199052223856,-119.307483928894,
171.81109657639));
#41391=CARTESIAN_POINT('Ctrl Pts',(-57.2295738035707,-119.539323107265,
172.828569176292));
#41392=CARTESIAN_POINT('Ctrl Pts',(-55.9392423847557,-119.771162285635,
173.846041776195));
#41393=CARTESIAN_POINT('Ctrl Pts',(-55.7451590400196,-119.886134095392,
175.490142808619));
#41394=CARTESIAN_POINT('Ctrl Pts',(-55.5510756952835,-120.001105905149,
177.134243841043));
#41395=CARTESIAN_POINT('Ctrl Pts',(-56.5727533982151,-119.986469464853,
178.441881219107));
#41396=CARTESIAN_POINT('Ctrl Pts',(-57.5944311011467,-119.971833024557,
179.74951859717));
#41397=CARTESIAN_POINT('Ctrl Pts',(-59.2392064922159,-119.890770207856,
179.954696079469));
#41398=CARTESIAN_POINT('Ctrl Pts',(-60.8839818832851,-119.809707391155,
180.159873561769));
#41399=CARTESIAN_POINT('Ctrl Pts',(-62.1941894279341,-119.764311742095,
179.142400961866));
#41400=CARTESIAN_POINT('Ctrl Pts',(-63.5043969725832,-119.718916093035,
178.124928361964));
#41401=CARTESIAN_POINT('Ctrl Pts',(-63.7183564431533,-119.790387812589,
176.48082732954));
#41402=CARTESIAN_POINT('Ctrl Pts',(-63.9323159137233,-119.861859532143,
174.836726297116));
#41403=CARTESIAN_POINT('Ctrl Pts',(-62.9305143366258,-120.062939501749,
173.529088919052));
#41404=CARTESIAN_POINT('Ctrl Pts',(-61.9287127595282,-120.264019471356,
172.221451540989));
#41405=CARTESIAN_POINT('Ctrl Pts',(-60.303813494293,-120.531525817368,172.016274058689));
#41406=CARTESIAN_POINT('Ctrl Pts',(-58.6789142290579,-120.799032163379,
171.81109657639));
#41407=CARTESIAN_POINT('Ctrl Pts',(-57.3885828102429,-121.03087134175,172.828569176292));
#41408=CARTESIAN_POINT('Ctrl Pts',(-56.0982513914279,-121.262710520121,
173.846041776195));
#41409=CARTESIAN_POINT('Ctrl Pts',(-55.9041680466918,-121.377682329878,
175.490142808619));
#41410=CARTESIAN_POINT('Ctrl Pts',(-55.7100847019558,-121.492654139634,
177.134243841043));
#41411=CARTESIAN_POINT('Ctrl Pts',(-56.7317624048874,-121.478017699339,
178.441881219107));
#41412=CARTESIAN_POINT('Ctrl Pts',(-57.753440107819,-121.463381259043,179.74951859717));
#41413=CARTESIAN_POINT('Ctrl Pts',(-59.3982154988882,-121.382318442342,
179.954696079469));
#41414=CARTESIAN_POINT('Ctrl Pts',(-61.0429908899573,-121.301255625641,
180.159873561769));
#41415=CARTESIAN_POINT('Ctrl Pts',(-62.3531984346064,-121.25585997658,179.142400961866));
#41416=CARTESIAN_POINT('Ctrl Pts',(-63.6634059792554,-121.21046432752,178.124928361964));
#41417=CARTESIAN_POINT('Ctrl Pts',(-63.8773654498255,-121.281936047074,
176.48082732954));
#41418=CARTESIAN_POINT('Ctrl Pts',(-64.0913249203956,-121.353407766628,
174.836726297116));
#41419=CARTESIAN_POINT('Ctrl Pts',(-63.089523343298,-121.554487736235,173.529088919052));
#41420=CARTESIAN_POINT('Ctrl Pts',(-62.0877217662004,-121.755567705841,
172.221451540989));
#41421=CARTESIAN_POINT('Ctrl Pts',(-60.4628225009653,-122.023074051853,
172.016274058689));
#41422=CARTESIAN_POINT('Ctrl Pts',(-58.8379232357301,-122.290580397865,
171.81109657639));
#41423=CARTESIAN_POINT('Ctrl Pts',(-57.5475918169151,-122.522419576236,
172.828569176292));
#41424=CARTESIAN_POINT('Ctrl Pts',(-56.2572603981001,-122.754258754607,
173.846041776195));
#41425=CARTESIAN_POINT('Ctrl Pts',(-56.0631770533641,-122.869230564363,
175.490142808619));
#41426=CARTESIAN_POINT('Ctrl Pts',(-55.869093708628,-122.98420237412,177.134243841043));
#41427=CARTESIAN_POINT('Ctrl Pts',(-56.8907714115596,-122.969565933824,
178.441881219107));
#41428=CARTESIAN_POINT('Ctrl Pts',(-57.9124491144912,-122.954929493528,
179.74951859717));
#41429=CARTESIAN_POINT('Ctrl Pts',(-59.5572245055604,-122.873866676827,
179.954696079469));
#41430=CARTESIAN_POINT('Ctrl Pts',(-61.2019998966296,-122.792803860126,
180.159873561769));
#41431=CARTESIAN_POINT('Ctrl Pts',(-62.5122074412786,-122.747408211066,
179.142400961866));
#41432=CARTESIAN_POINT('Ctrl Pts',(-63.8224149859276,-122.702012562006,
178.124928361964));
#41433=CARTESIAN_POINT('Ctrl Pts',(-64.0363744564977,-122.77348428156,176.48082732954));
#41434=CARTESIAN_POINT('Ctrl Pts',(-64.2503339270678,-122.844956001114,
174.836726297116));
#41435=CARTESIAN_POINT('Ctrl Pts',(-63.2485323499702,-123.046035970721,
173.529088919052));
#41436=CARTESIAN_POINT('Ctrl Pts',(-62.2467307728726,-123.247115940327,
172.221451540989));
#41437=CARTESIAN_POINT('Ctrl Pts',(-60.6218315076375,-123.514622286339,
172.016274058689));
#41438=CARTESIAN_POINT('Ctrl Pts',(-58.9969322424023,-123.78212863235,171.81109657639));
#41439=CARTESIAN_POINT('Ctrl Pts',(-57.7066008235873,-124.013967810721,
172.828569176292));
#41440=CARTESIAN_POINT('Ctrl Pts',(-56.4162694047723,-124.245806989092,
173.846041776195));
#41441=CARTESIAN_POINT('Ctrl Pts',(-56.2221860600363,-124.360778798849,
175.490142808619));
#41442=CARTESIAN_POINT('Ctrl Pts',(-56.0281027153002,-124.475750608606,
177.134243841043));
#41443=CARTESIAN_POINT('Ctrl Pts',(-57.0497804182318,-124.46111416831,178.441881219107));
#41444=CARTESIAN_POINT('Ctrl Pts',(-58.0714581211634,-124.446477728014,
179.74951859717));
#41445=CARTESIAN_POINT('Ctrl Pts',(-59.7162335122326,-124.365414911313,
179.954696079469));
#41446=CARTESIAN_POINT('Ctrl Pts',(-61.3610089033018,-124.284352094612,
180.159873561769));
#41447=CARTESIAN_POINT('Ctrl Pts',(-62.6712164479508,-124.238956445552,
179.142400961866));
#41448=CARTESIAN_POINT('Ctrl Pts',(-63.9814239925999,-124.193560796491,
178.124928361964));
#41449=CARTESIAN_POINT('Ctrl Pts',(-64.1953834631699,-124.265032516046,
176.48082732954));
#41450=CARTESIAN_POINT('Ctrl Pts',(-64.40934293374,-124.3365042356,174.836726297116));
#41451=CARTESIAN_POINT('Ctrl Pts',(-63.4075413566424,-124.537584205206,
173.529088919052));
#41452=CARTESIAN_POINT('Ctrl Pts',(-62.4057397795449,-124.738664174813,
172.221451540989));
#41453=CARTESIAN_POINT('Ctrl Pts',(-60.7808405143097,-125.006170520824,
172.016274058689));
#41454=CARTESIAN_POINT('Ctrl Pts',(-59.1559412490746,-125.273676866836,
171.81109657639));
#41455=CARTESIAN_POINT('Ctrl Pts',(-57.8656098302596,-125.505516045207,
172.828569176292));
#41456=CARTESIAN_POINT('Ctrl Pts',(-56.5752784114446,-125.737355223578,
173.846041776195));
#41457=CARTESIAN_POINT('Ctrl Pts',(-56.3811950667085,-125.852327033334,
175.490142808619));
#41458=CARTESIAN_POINT('Ctrl Pts',(-56.1871117219724,-125.967298843091,
177.134243841043));
#41459=CARTESIAN_POINT('Ctrl Pts',(-57.208789424904,-125.952662402795,178.441881219107));
#41460=CARTESIAN_POINT('Ctrl Pts',(-58.2304671278357,-125.9380259625,179.74951859717));
#41461=CARTESIAN_POINT('Ctrl Pts',(-59.8752425189048,-125.856963145799,
179.954696079469));
#41462=CARTESIAN_POINT('Ctrl Pts',(-61.520017909974,-125.775900329098,180.159873561769));
#41463=CARTESIAN_POINT('Ctrl Pts',(-62.8302254546231,-125.730504680037,
179.142400961866));
#41464=CARTESIAN_POINT('Ctrl Pts',(-64.1404329992721,-125.685109030977,
178.124928361964));
#41465=CARTESIAN_POINT('Ctrl Pts',(-64.3543924698422,-125.756580750531,
176.48082732954));
#41466=CARTESIAN_POINT('Ctrl Pts',(-64.5683519404122,-125.828052470085,
174.836726297116));
#41467=CARTESIAN_POINT('Ctrl Pts',(-63.5665503633147,-126.029132439692,
173.529088919052));
#41468=CARTESIAN_POINT('Ctrl Pts',(-62.5647487862171,-126.230212409298,
172.221451540989));
#41469=CARTESIAN_POINT('Ctrl Pts',(-60.9398495209819,-126.49771875531,172.016274058689));
#41470=CARTESIAN_POINT('Ctrl Pts',(-59.3149502557468,-126.765225101322,
171.81109657639));
#41471=CARTESIAN_POINT('Ctrl Pts',(-58.0246188369318,-126.997064279693,
172.828569176292));
#41472=CARTESIAN_POINT('Ctrl Pts',(-56.7342874181168,-127.228903458063,
173.846041776195));
#41473=CARTESIAN_POINT('Ctrl Pts',(-56.5402040733807,-127.34387526782,175.490142808619));
#41474=CARTESIAN_POINT('Ctrl Pts',(-56.3461207286447,-127.458847077577,
177.134243841043));
#41475=CARTESIAN_POINT('Ctrl Pts',(-57.3677984315763,-127.444210637281,
178.441881219107));
#41476=CARTESIAN_POINT('Ctrl Pts',(-58.0247571031797,-127.434799120962,
179.282717534088));
#41477=CARTESIAN_POINT('Ctrl Pts',(-59.0118785952597,-127.394648976958,
179.686725372425));
#41478=CARTESIAN_POINT('Ctrl Pts',(-50.1268408042676,-67.1847631435675,
175.490142808619));
#41479=CARTESIAN_POINT('Ctrl Pts',(-49.9327574595315,-67.2997349533242,
177.134243841043));
#41480=CARTESIAN_POINT('Ctrl Pts',(-50.9544351624631,-67.2850985130284,
178.441881219107));
#41481=CARTESIAN_POINT('Ctrl Pts',(-51.9761128653947,-67.2704620727326,
179.74951859717));
#41482=CARTESIAN_POINT('Ctrl Pts',(-53.6208882564639,-67.1893992560316,
179.954696079469));
#41483=CARTESIAN_POINT('Ctrl Pts',(-55.2656636475331,-67.1083364393306,
180.159873561769));
#41484=CARTESIAN_POINT('Ctrl Pts',(-56.5758711921821,-67.0629407902703,
179.142400961866));
#41485=CARTESIAN_POINT('Ctrl Pts',(-57.8860787368312,-67.0175451412101,
178.124928361964));
#41486=CARTESIAN_POINT('Ctrl Pts',(-58.1000382074012,-67.0890168607642,
176.48082732954));
#41487=CARTESIAN_POINT('Ctrl Pts',(-58.3139976779713,-67.1604885803183,
174.836726297116));
#41488=CARTESIAN_POINT('Ctrl Pts',(-57.3121961008737,-67.3615685499248,
173.529088919052));
#41489=CARTESIAN_POINT('Ctrl Pts',(-56.3103945237762,-67.5626485195312,
172.221451540989));
#41490=CARTESIAN_POINT('Ctrl Pts',(-54.685495258541,-67.830154865543,172.016274058689));
#41491=CARTESIAN_POINT('Ctrl Pts',(-53.0605959933058,-68.0976612115547,
171.81109657639));
#41492=CARTESIAN_POINT('Ctrl Pts',(-51.7702645744908,-68.3295003899256,
172.828569176292));
#41493=CARTESIAN_POINT('Ctrl Pts',(-50.4799331556759,-68.5613395682965,
173.846041776195));
#41494=CARTESIAN_POINT('Ctrl Pts',(-50.2858498109398,-68.6763113780532,
175.490142808619));
#41495=CARTESIAN_POINT('Ctrl Pts',(-50.0917664662038,-68.7912831878098,
177.134243841043));
#41496=CARTESIAN_POINT('Ctrl Pts',(-51.1134441691353,-68.776646747514,178.441881219107));
#41497=CARTESIAN_POINT('Ctrl Pts',(-52.1351218720669,-68.7620103072182,
179.74951859717));
#41498=CARTESIAN_POINT('Ctrl Pts',(-53.7798972631361,-68.6809474905172,
179.954696079469));
#41499=CARTESIAN_POINT('Ctrl Pts',(-55.4246726542053,-68.5998846738162,
180.159873561769));
#41500=CARTESIAN_POINT('Ctrl Pts',(-56.7348801988543,-68.5544890247559,
179.142400961866));
#41501=CARTESIAN_POINT('Ctrl Pts',(-58.0450877435034,-68.5090933756957,
178.124928361964));
#41502=CARTESIAN_POINT('Ctrl Pts',(-58.2590472140735,-68.5805650952498,
176.48082732954));
#41503=CARTESIAN_POINT('Ctrl Pts',(-58.4730066846436,-68.6520368148039,
174.836726297116));
#41504=CARTESIAN_POINT('Ctrl Pts',(-57.471205107546,-68.8531167844104,173.529088919052));
#41505=CARTESIAN_POINT('Ctrl Pts',(-56.4694035304484,-69.0541967540168,
172.221451540989));
#41506=CARTESIAN_POINT('Ctrl Pts',(-54.8445042652132,-69.3217031000286,
172.016274058689));
#41507=CARTESIAN_POINT('Ctrl Pts',(-53.2196049999781,-69.5892094460403,
171.81109657639));
#41508=CARTESIAN_POINT('Ctrl Pts',(-51.9292735811631,-69.8210486244112,
172.828569176292));
#41509=CARTESIAN_POINT('Ctrl Pts',(-50.6389421623481,-70.0528878027821,
173.846041776195));
#41510=CARTESIAN_POINT('Ctrl Pts',(-50.444858817612,-70.1678596125387,175.490142808619));
#41511=CARTESIAN_POINT('Ctrl Pts',(-50.250775472876,-70.2828314222954,177.134243841043));
#41512=CARTESIAN_POINT('Ctrl Pts',(-51.2724531758076,-70.2681949819996,
178.441881219107));
#41513=CARTESIAN_POINT('Ctrl Pts',(-52.2941308787392,-70.2535585417038,
179.74951859717));
#41514=CARTESIAN_POINT('Ctrl Pts',(-53.9389062698084,-70.1724957250028,
179.954696079469));
#41515=CARTESIAN_POINT('Ctrl Pts',(-55.5836816608776,-70.0914329083018,
180.159873561769));
#41516=CARTESIAN_POINT('Ctrl Pts',(-56.8938892055266,-70.0460372592415,
179.142400961866));
#41517=CARTESIAN_POINT('Ctrl Pts',(-58.2040967501756,-70.0006416101813,
178.124928361964));
#41518=CARTESIAN_POINT('Ctrl Pts',(-58.4180562207457,-70.0721133297354,
176.48082732954));
#41519=CARTESIAN_POINT('Ctrl Pts',(-58.6320156913158,-70.1435850492895,
174.836726297116));
#41520=CARTESIAN_POINT('Ctrl Pts',(-57.6302141142182,-70.344665018896,173.529088919052));
#41521=CARTESIAN_POINT('Ctrl Pts',(-56.6284125371206,-70.5457449885024,
172.221451540989));
#41522=CARTESIAN_POINT('Ctrl Pts',(-55.0035132718855,-70.8132513345142,
172.016274058689));
#41523=CARTESIAN_POINT('Ctrl Pts',(-53.3786140066503,-71.0807576805259,
171.81109657639));
#41524=CARTESIAN_POINT('Ctrl Pts',(-52.0882825878353,-71.3125968588968,
172.828569176292));
#41525=CARTESIAN_POINT('Ctrl Pts',(-50.7979511690203,-71.5444360372677,
173.846041776195));
#41526=CARTESIAN_POINT('Ctrl Pts',(-50.6038678242843,-71.6594078470244,
175.490142808619));
#41527=CARTESIAN_POINT('Ctrl Pts',(-50.4097844795482,-71.774379656781,177.134243841043));
#41528=CARTESIAN_POINT('Ctrl Pts',(-51.4314621824798,-71.7597432164852,
178.441881219107));
#41529=CARTESIAN_POINT('Ctrl Pts',(-52.4531398854114,-71.7451067761894,
179.74951859717));
#41530=CARTESIAN_POINT('Ctrl Pts',(-54.0979152764806,-71.6640439594884,
179.954696079469));
#41531=CARTESIAN_POINT('Ctrl Pts',(-55.7426906675498,-71.5829811427874,
180.159873561769));
#41532=CARTESIAN_POINT('Ctrl Pts',(-57.0528982121988,-71.5375854937271,
179.142400961866));
#41533=CARTESIAN_POINT('Ctrl Pts',(-58.3631057568478,-71.4921898446669,
178.124928361964));
#41534=CARTESIAN_POINT('Ctrl Pts',(-58.5770652274179,-71.563661564221,176.48082732954));
#41535=CARTESIAN_POINT('Ctrl Pts',(-58.791024697988,-71.6351332837751,174.836726297116));
#41536=CARTESIAN_POINT('Ctrl Pts',(-57.7892231208904,-71.8362132533815,
173.529088919052));
#41537=CARTESIAN_POINT('Ctrl Pts',(-56.7874215437929,-72.037293222988,172.221451540989));
#41538=CARTESIAN_POINT('Ctrl Pts',(-55.1625222785577,-72.3047995689997,
172.016274058689));
#41539=CARTESIAN_POINT('Ctrl Pts',(-53.5376230133225,-72.5723059150115,
171.81109657639));
#41540=CARTESIAN_POINT('Ctrl Pts',(-52.2472915945075,-72.8041450933824,
172.828569176292));
#41541=CARTESIAN_POINT('Ctrl Pts',(-50.9569601756925,-73.0359842717533,
173.846041776195));
#41542=CARTESIAN_POINT('Ctrl Pts',(-50.7628768309565,-73.1509560815099,
175.490142808619));
#41543=CARTESIAN_POINT('Ctrl Pts',(-50.5687934862204,-73.2659278912666,
177.134243841043));
#41544=CARTESIAN_POINT('Ctrl Pts',(-51.590471189152,-73.2512914509708,178.441881219107));
#41545=CARTESIAN_POINT('Ctrl Pts',(-52.6121488920836,-73.236655010675,179.74951859717));
#41546=CARTESIAN_POINT('Ctrl Pts',(-54.2569242831528,-73.155592193974,179.954696079469));
#41547=CARTESIAN_POINT('Ctrl Pts',(-55.901699674222,-73.074529377273,180.159873561769));
#41548=CARTESIAN_POINT('Ctrl Pts',(-57.211907218871,-73.0291337282128,179.142400961866));
#41549=CARTESIAN_POINT('Ctrl Pts',(-58.5221147635201,-72.9837380791525,
178.124928361964));
#41550=CARTESIAN_POINT('Ctrl Pts',(-58.7360742340901,-73.0552097987066,
176.48082732954));
#41551=CARTESIAN_POINT('Ctrl Pts',(-58.9500337046602,-73.1266815182607,
174.836726297116));
#41552=CARTESIAN_POINT('Ctrl Pts',(-57.9482321275626,-73.3277614878671,
173.529088919052));
#41553=CARTESIAN_POINT('Ctrl Pts',(-56.9464305504651,-73.5288414574736,
172.221451540989));
#41554=CARTESIAN_POINT('Ctrl Pts',(-55.3215312852299,-73.7963478034854,
172.016274058689));
#41555=CARTESIAN_POINT('Ctrl Pts',(-53.6966320199948,-74.0638541494971,
171.81109657639));
#41556=CARTESIAN_POINT('Ctrl Pts',(-52.4063006011798,-74.295693327868,172.828569176292));
#41557=CARTESIAN_POINT('Ctrl Pts',(-51.1159691823648,-74.5275325062389,
173.846041776195));
#41558=CARTESIAN_POINT('Ctrl Pts',(-50.9218858376287,-74.6425043159955,
175.490142808619));
#41559=CARTESIAN_POINT('Ctrl Pts',(-50.7278024928926,-74.7574761257522,
177.134243841043));
#41560=CARTESIAN_POINT('Ctrl Pts',(-51.7494801958242,-74.7428396854564,
178.441881219107));
#41561=CARTESIAN_POINT('Ctrl Pts',(-52.7711578987558,-74.7282032451606,
179.74951859717));
#41562=CARTESIAN_POINT('Ctrl Pts',(-54.415933289825,-74.6471404284596,179.954696079469));
#41563=CARTESIAN_POINT('Ctrl Pts',(-56.0607086808942,-74.5660776117586,
180.159873561769));
#41564=CARTESIAN_POINT('Ctrl Pts',(-57.3709162255433,-74.5206819626983,
179.142400961866));
#41565=CARTESIAN_POINT('Ctrl Pts',(-58.6811237701923,-74.4752863136381,
178.124928361964));
#41566=CARTESIAN_POINT('Ctrl Pts',(-58.8950832407624,-74.5467580331922,
176.48082732954));
#41567=CARTESIAN_POINT('Ctrl Pts',(-59.1090427113324,-74.6182297527463,
174.836726297116));
#41568=CARTESIAN_POINT('Ctrl Pts',(-58.1072411342349,-74.8193097223528,
173.529088919052));
#41569=CARTESIAN_POINT('Ctrl Pts',(-57.1054395571373,-75.0203896919592,
172.221451540989));
#41570=CARTESIAN_POINT('Ctrl Pts',(-55.4805402919021,-75.287896037971,172.016274058689));
#41571=CARTESIAN_POINT('Ctrl Pts',(-53.855641026667,-75.5554023839827,171.81109657639));
#41572=CARTESIAN_POINT('Ctrl Pts',(-52.565309607852,-75.7872415623536,172.828569176292));
#41573=CARTESIAN_POINT('Ctrl Pts',(-51.274978189037,-76.0190807407245,173.846041776195));
#41574=CARTESIAN_POINT('Ctrl Pts',(-51.0808948443009,-76.1340525504811,
175.490142808619));
#41575=CARTESIAN_POINT('Ctrl Pts',(-50.8868114995649,-76.2490243602377,
177.134243841043));
#41576=CARTESIAN_POINT('Ctrl Pts',(-51.9084892024965,-76.234387919942,178.441881219107));
#41577=CARTESIAN_POINT('Ctrl Pts',(-52.9301669054281,-76.2197514796462,
179.74951859717));
#41578=CARTESIAN_POINT('Ctrl Pts',(-54.5749422964973,-76.1386886629452,
179.954696079469));
#41579=CARTESIAN_POINT('Ctrl Pts',(-56.2197176875665,-76.0576258462442,
180.159873561769));
#41580=CARTESIAN_POINT('Ctrl Pts',(-57.5299252322155,-76.012230197184,179.142400961866));
#41581=CARTESIAN_POINT('Ctrl Pts',(-58.8401327768645,-75.9668345481237,
178.124928361964));
#41582=CARTESIAN_POINT('Ctrl Pts',(-59.0540922474346,-76.0383062676778,
176.48082732954));
#41583=CARTESIAN_POINT('Ctrl Pts',(-59.2680517180047,-76.1097779872319,
174.836726297116));
#41584=CARTESIAN_POINT('Ctrl Pts',(-58.2662501409071,-76.3108579568383,
173.529088919052));
#41585=CARTESIAN_POINT('Ctrl Pts',(-57.2644485638095,-76.5119379264448,
172.221451540989));
#41586=CARTESIAN_POINT('Ctrl Pts',(-55.6395492985744,-76.7794442724566,
172.016274058689));
#41587=CARTESIAN_POINT('Ctrl Pts',(-54.0146500333392,-77.0469506184683,
171.81109657639));
#41588=CARTESIAN_POINT('Ctrl Pts',(-52.7243186145242,-77.2787897968392,
172.828569176292));
#41589=CARTESIAN_POINT('Ctrl Pts',(-51.4339871957092,-77.5106289752101,
173.846041776195));
#41590=CARTESIAN_POINT('Ctrl Pts',(-51.2399038509732,-77.6256007849667,
175.490142808619));
#41591=CARTESIAN_POINT('Ctrl Pts',(-51.0458205062371,-77.7405725947234,
177.134243841043));
#41592=CARTESIAN_POINT('Ctrl Pts',(-52.0674982091687,-77.7259361544276,
178.441881219107));
#41593=CARTESIAN_POINT('Ctrl Pts',(-53.0891759121003,-77.7112997141318,
179.74951859717));
#41594=CARTESIAN_POINT('Ctrl Pts',(-54.7339513031695,-77.6302368974308,
179.954696079469));
#41595=CARTESIAN_POINT('Ctrl Pts',(-56.3787266942387,-77.5491740807298,
180.159873561769));
#41596=CARTESIAN_POINT('Ctrl Pts',(-57.6889342388877,-77.5037784316696,
179.142400961866));
#41597=CARTESIAN_POINT('Ctrl Pts',(-58.9991417835367,-77.4583827826093,
178.124928361964));
#41598=CARTESIAN_POINT('Ctrl Pts',(-59.2131012541068,-77.5298545021634,
176.48082732954));
#41599=CARTESIAN_POINT('Ctrl Pts',(-59.4270607246769,-77.6013262217175,
174.836726297116));
#41600=CARTESIAN_POINT('Ctrl Pts',(-58.4252591475793,-77.802406191324,173.529088919052));
#41601=CARTESIAN_POINT('Ctrl Pts',(-57.4234575704818,-78.0034861609304,
172.221451540989));
#41602=CARTESIAN_POINT('Ctrl Pts',(-55.7985583052466,-78.2709925069422,
172.016274058689));
#41603=CARTESIAN_POINT('Ctrl Pts',(-54.1736590400114,-78.5384988529539,
171.81109657639));
#41604=CARTESIAN_POINT('Ctrl Pts',(-52.8833276211964,-78.7703380313248,
172.828569176292));
#41605=CARTESIAN_POINT('Ctrl Pts',(-51.5929962023814,-79.0021772096957,
173.846041776195));
#41606=CARTESIAN_POINT('Ctrl Pts',(-51.3989128576454,-79.1171490194523,
175.490142808619));
#41607=CARTESIAN_POINT('Ctrl Pts',(-51.2048295129093,-79.232120829209,177.134243841043));
#41608=CARTESIAN_POINT('Ctrl Pts',(-52.2265072158409,-79.2174843889132,
178.441881219107));
#41609=CARTESIAN_POINT('Ctrl Pts',(-53.2481849187725,-79.2028479486174,
179.74951859717));
#41610=CARTESIAN_POINT('Ctrl Pts',(-54.8929603098417,-79.1217851319164,
179.954696079469));
#41611=CARTESIAN_POINT('Ctrl Pts',(-56.5377357009109,-79.0407223152154,
180.159873561769));
#41612=CARTESIAN_POINT('Ctrl Pts',(-57.8479432455599,-78.9953266661552,
179.142400961866));
#41613=CARTESIAN_POINT('Ctrl Pts',(-59.158150790209,-78.9499310170949,178.124928361964));
#41614=CARTESIAN_POINT('Ctrl Pts',(-59.372110260779,-79.021402736649,176.48082732954));
#41615=CARTESIAN_POINT('Ctrl Pts',(-59.5860697313491,-79.0928744562031,
174.836726297116));
#41616=CARTESIAN_POINT('Ctrl Pts',(-58.5842681542516,-79.2939544258096,
173.529088919052));
#41617=CARTESIAN_POINT('Ctrl Pts',(-57.582466577154,-79.495034395416,172.221451540989));
#41618=CARTESIAN_POINT('Ctrl Pts',(-55.9575673119188,-79.7625407414277,
172.016274058689));
#41619=CARTESIAN_POINT('Ctrl Pts',(-54.3326680466837,-80.0300470874395,
171.81109657639));
#41620=CARTESIAN_POINT('Ctrl Pts',(-53.0423366278687,-80.2618862658104,
172.828569176292));
#41621=CARTESIAN_POINT('Ctrl Pts',(-51.7520052090537,-80.4937254441813,
173.846041776195));
#41622=CARTESIAN_POINT('Ctrl Pts',(-51.5579218643176,-80.6086972539379,
175.490142808619));
#41623=CARTESIAN_POINT('Ctrl Pts',(-51.3638385195816,-80.7236690636945,
177.134243841043));
#41624=CARTESIAN_POINT('Ctrl Pts',(-52.3855162225132,-80.7090326233988,
178.441881219107));
#41625=CARTESIAN_POINT('Ctrl Pts',(-53.4071939254448,-80.694396183103,179.74951859717));
#41626=CARTESIAN_POINT('Ctrl Pts',(-55.0519693165139,-80.613333366402,179.954696079469));
#41627=CARTESIAN_POINT('Ctrl Pts',(-56.6967447075831,-80.532270549701,180.159873561769));
#41628=CARTESIAN_POINT('Ctrl Pts',(-58.0069522522322,-80.4868749006407,
179.142400961866));
#41629=CARTESIAN_POINT('Ctrl Pts',(-59.3171597968812,-80.4414792515805,
178.124928361964));
#41630=CARTESIAN_POINT('Ctrl Pts',(-59.5311192674513,-80.5129509711346,
176.48082732954));
#41631=CARTESIAN_POINT('Ctrl Pts',(-59.7450787380214,-80.5844226906887,
174.836726297116));
#41632=CARTESIAN_POINT('Ctrl Pts',(-58.7432771609238,-80.7855026602952,
173.529088919052));
#41633=CARTESIAN_POINT('Ctrl Pts',(-57.7414755838262,-80.9865826299016,
172.221451540989));
#41634=CARTESIAN_POINT('Ctrl Pts',(-56.116576318591,-81.2540889759133,172.016274058689));
#41635=CARTESIAN_POINT('Ctrl Pts',(-54.4916770533559,-81.5215953219251,
171.81109657639));
#41636=CARTESIAN_POINT('Ctrl Pts',(-53.2013456345409,-81.753434500296,172.828569176292));
#41637=CARTESIAN_POINT('Ctrl Pts',(-51.9110142157259,-81.9852736786669,
173.846041776195));
#41638=CARTESIAN_POINT('Ctrl Pts',(-51.7169308709898,-82.1002454884235,
175.490142808619));
#41639=CARTESIAN_POINT('Ctrl Pts',(-51.5228475262538,-82.2152172981802,
177.134243841043));
#41640=CARTESIAN_POINT('Ctrl Pts',(-52.5445252291854,-82.2005808578844,
178.441881219107));
#41641=CARTESIAN_POINT('Ctrl Pts',(-53.566202932117,-82.1859444175886,179.74951859717));
#41642=CARTESIAN_POINT('Ctrl Pts',(-55.2109783231862,-82.1048816008876,
179.954696079469));
#41643=CARTESIAN_POINT('Ctrl Pts',(-56.8557537142554,-82.0238187841866,
180.159873561769));
#41644=CARTESIAN_POINT('Ctrl Pts',(-58.1659612589044,-81.9784231351264,
179.142400961866));
#41645=CARTESIAN_POINT('Ctrl Pts',(-59.4761688035534,-81.9330274860661,
178.124928361964));
#41646=CARTESIAN_POINT('Ctrl Pts',(-59.6901282741235,-82.0044992056202,
176.48082732954));
#41647=CARTESIAN_POINT('Ctrl Pts',(-59.9040877446936,-82.0759709251743,
174.836726297116));
#41648=CARTESIAN_POINT('Ctrl Pts',(-58.902286167596,-82.2770508947808,173.529088919052));
#41649=CARTESIAN_POINT('Ctrl Pts',(-57.9004845904984,-82.4781308643872,
172.221451540989));
#41650=CARTESIAN_POINT('Ctrl Pts',(-56.2755853252633,-82.745637210399,172.016274058689));
#41651=CARTESIAN_POINT('Ctrl Pts',(-54.6506860600281,-83.0131435564107,
171.81109657639));
#41652=CARTESIAN_POINT('Ctrl Pts',(-53.3603546412131,-83.2449827347816,
172.828569176292));
#41653=CARTESIAN_POINT('Ctrl Pts',(-52.0700232223981,-83.4768219131525,
173.846041776195));
#41654=CARTESIAN_POINT('Ctrl Pts',(-51.8759398776621,-83.5917937229092,
175.490142808619));
#41655=CARTESIAN_POINT('Ctrl Pts',(-51.681856532926,-83.7067655326658,177.134243841043));
#41656=CARTESIAN_POINT('Ctrl Pts',(-52.7035342358576,-83.69212909237,178.441881219107));
#41657=CARTESIAN_POINT('Ctrl Pts',(-53.7252119387892,-83.6774926520742,
179.74951859717));
#41658=CARTESIAN_POINT('Ctrl Pts',(-55.3699873298584,-83.5964298353732,
179.954696079469));
#41659=CARTESIAN_POINT('Ctrl Pts',(-57.0147627209276,-83.5153670186722,
180.159873561769));
#41660=CARTESIAN_POINT('Ctrl Pts',(-58.3249702655766,-83.469971369612,179.142400961866));
#41661=CARTESIAN_POINT('Ctrl Pts',(-59.6351778102256,-83.4245757205517,
178.124928361964));
#41662=CARTESIAN_POINT('Ctrl Pts',(-59.8491372807957,-83.4960474401058,
176.48082732954));
#41663=CARTESIAN_POINT('Ctrl Pts',(-60.0630967513658,-83.5675191596599,
174.836726297116));
#41664=CARTESIAN_POINT('Ctrl Pts',(-59.0612951742682,-83.7685991292663,
173.529088919052));
#41665=CARTESIAN_POINT('Ctrl Pts',(-58.0594935971707,-83.9696790988728,
172.221451540989));
#41666=CARTESIAN_POINT('Ctrl Pts',(-56.4345943319355,-84.2371854448845,
172.016274058689));
#41667=CARTESIAN_POINT('Ctrl Pts',(-54.8096950667003,-84.5046917908963,
171.81109657639));
#41668=CARTESIAN_POINT('Ctrl Pts',(-53.5193636478853,-84.7365309692672,
172.828569176292));
#41669=CARTESIAN_POINT('Ctrl Pts',(-52.2290322290704,-84.9683701476381,
173.846041776195));
#41670=CARTESIAN_POINT('Ctrl Pts',(-52.0349488843343,-85.0833419573947,
175.490142808619));
#41671=CARTESIAN_POINT('Ctrl Pts',(-51.8408655395982,-85.1983137671514,
177.134243841043));
#41672=CARTESIAN_POINT('Ctrl Pts',(-52.8625432425298,-85.1836773268556,
178.441881219107));
#41673=CARTESIAN_POINT('Ctrl Pts',(-53.8842209454614,-85.1690408865598,
179.74951859717));
#41674=CARTESIAN_POINT('Ctrl Pts',(-55.5289963365306,-85.0879780698588,
179.954696079469));
#41675=CARTESIAN_POINT('Ctrl Pts',(-57.1737717275998,-85.0069152531578,
180.159873561769));
#41676=CARTESIAN_POINT('Ctrl Pts',(-58.4839792722488,-84.9615196040975,
179.142400961866));
#41677=CARTESIAN_POINT('Ctrl Pts',(-59.7941868168979,-84.9161239550373,
178.124928361964));
#41678=CARTESIAN_POINT('Ctrl Pts',(-60.008146287468,-84.9875956745914,176.48082732954));
#41679=CARTESIAN_POINT('Ctrl Pts',(-60.222105758038,-85.0590673941455,174.836726297116));
#41680=CARTESIAN_POINT('Ctrl Pts',(-59.2203041809405,-85.260147363752,173.529088919052));
#41681=CARTESIAN_POINT('Ctrl Pts',(-58.2185026038429,-85.4612273333584,
172.221451540989));
#41682=CARTESIAN_POINT('Ctrl Pts',(-56.5936033386077,-85.7287336793702,
172.016274058689));
#41683=CARTESIAN_POINT('Ctrl Pts',(-54.9687040733726,-85.9962400253819,
171.81109657639));
#41684=CARTESIAN_POINT('Ctrl Pts',(-53.6783726545576,-86.2280792037528,
172.828569176292));
#41685=CARTESIAN_POINT('Ctrl Pts',(-52.3880412357426,-86.4599183821237,
173.846041776195));
#41686=CARTESIAN_POINT('Ctrl Pts',(-52.1939578910065,-86.5748901918803,
175.490142808619));
#41687=CARTESIAN_POINT('Ctrl Pts',(-51.9998745462705,-86.689862001637,177.134243841043));
#41688=CARTESIAN_POINT('Ctrl Pts',(-53.0215522492021,-86.6752255613412,
178.441881219107));
#41689=CARTESIAN_POINT('Ctrl Pts',(-54.0432299521337,-86.6605891210454,
179.74951859717));
#41690=CARTESIAN_POINT('Ctrl Pts',(-55.6880053432029,-86.5795263043444,
179.954696079469));
#41691=CARTESIAN_POINT('Ctrl Pts',(-57.332780734272,-86.4984634876434,180.159873561769));
#41692=CARTESIAN_POINT('Ctrl Pts',(-58.6429882789211,-86.4530678385832,
179.142400961866));
#41693=CARTESIAN_POINT('Ctrl Pts',(-59.9531958235701,-86.4076721895229,
178.124928361964));
#41694=CARTESIAN_POINT('Ctrl Pts',(-60.1671552941402,-86.479143909077,176.48082732954));
#41695=CARTESIAN_POINT('Ctrl Pts',(-60.3811147647103,-86.5506156286311,
174.836726297116));
#41696=CARTESIAN_POINT('Ctrl Pts',(-59.3793131876127,-86.7516955982376,
173.529088919052));
#41697=CARTESIAN_POINT('Ctrl Pts',(-58.3775116105151,-86.952775567844,172.221451540989));
#41698=CARTESIAN_POINT('Ctrl Pts',(-56.7526123452799,-87.2202819138558,
172.016274058689));
#41699=CARTESIAN_POINT('Ctrl Pts',(-55.1277130800448,-87.4877882598675,
171.81109657639));
#41700=CARTESIAN_POINT('Ctrl Pts',(-53.8373816612298,-87.7196274382384,
172.828569176292));
#41701=CARTESIAN_POINT('Ctrl Pts',(-52.5470502424148,-87.9514666166093,
173.846041776195));
#41702=CARTESIAN_POINT('Ctrl Pts',(-52.3529668976787,-88.0664384263659,
175.490142808619));
#41703=CARTESIAN_POINT('Ctrl Pts',(-52.1588835529427,-88.1814102361226,
177.134243841043));
#41704=CARTESIAN_POINT('Ctrl Pts',(-53.1805612558743,-88.1667737958268,
178.441881219107));
#41705=CARTESIAN_POINT('Ctrl Pts',(-54.2022389588059,-88.152137355531,179.74951859717));
#41706=CARTESIAN_POINT('Ctrl Pts',(-55.8470143498751,-88.07107453883,179.954696079469));
#41707=CARTESIAN_POINT('Ctrl Pts',(-57.4917897409443,-87.990011722129,180.159873561769));
#41708=CARTESIAN_POINT('Ctrl Pts',(-58.8019972855933,-87.9446160730687,
179.142400961866));
#41709=CARTESIAN_POINT('Ctrl Pts',(-60.1122048302423,-87.8992204240085,
178.124928361964));
#41710=CARTESIAN_POINT('Ctrl Pts',(-60.3261643008124,-87.9706921435626,
176.48082732954));
#41711=CARTESIAN_POINT('Ctrl Pts',(-60.5401237713825,-88.0421638631167,
174.836726297116));
#41712=CARTESIAN_POINT('Ctrl Pts',(-59.5383221942849,-88.2432438327232,
173.529088919052));
#41713=CARTESIAN_POINT('Ctrl Pts',(-58.5365206171873,-88.4443238023296,
172.221451540989));
#41714=CARTESIAN_POINT('Ctrl Pts',(-56.9116213519522,-88.7118301483414,
172.016274058689));
#41715=CARTESIAN_POINT('Ctrl Pts',(-55.286722086717,-88.9793364943531,171.81109657639));
#41716=CARTESIAN_POINT('Ctrl Pts',(-53.996390667902,-89.211175672724,172.828569176292));
#41717=CARTESIAN_POINT('Ctrl Pts',(-52.706059249087,-89.4430148510949,173.846041776195));
#41718=CARTESIAN_POINT('Ctrl Pts',(-52.511975904351,-89.5579866608516,175.490142808619));
#41719=CARTESIAN_POINT('Ctrl Pts',(-52.3178925596149,-89.6729584706082,
177.134243841043));
#41720=CARTESIAN_POINT('Ctrl Pts',(-53.3395702625465,-89.6583220303124,
178.441881219107));
#41721=CARTESIAN_POINT('Ctrl Pts',(-54.3612479654781,-89.6436855900166,
179.74951859717));
#41722=CARTESIAN_POINT('Ctrl Pts',(-56.0060233565473,-89.5626227733156,
179.954696079469));
#41723=CARTESIAN_POINT('Ctrl Pts',(-57.6507987476165,-89.4815599566146,
180.159873561769));
#41724=CARTESIAN_POINT('Ctrl Pts',(-58.9610062922655,-89.4361643075543,
179.142400961866));
#41725=CARTESIAN_POINT('Ctrl Pts',(-60.2712138369146,-89.3907686584941,
178.124928361964));
#41726=CARTESIAN_POINT('Ctrl Pts',(-60.4851733074846,-89.4622403780482,
176.48082732954));
#41727=CARTESIAN_POINT('Ctrl Pts',(-60.6991327780547,-89.5337120976023,
174.836726297116));
#41728=CARTESIAN_POINT('Ctrl Pts',(-59.6973312009571,-89.7347920672087,
173.529088919052));
#41729=CARTESIAN_POINT('Ctrl Pts',(-58.6955296238596,-89.9358720368152,
172.221451540989));
#41730=CARTESIAN_POINT('Ctrl Pts',(-57.0706303586244,-90.203378382827,172.016274058689));
#41731=CARTESIAN_POINT('Ctrl Pts',(-55.4457310933893,-90.4708847288387,
171.81109657639));
#41732=CARTESIAN_POINT('Ctrl Pts',(-54.1553996745743,-90.7027239072096,
172.828569176292));
#41733=CARTESIAN_POINT('Ctrl Pts',(-52.8650682557593,-90.9345630855805,
173.846041776195));
#41734=CARTESIAN_POINT('Ctrl Pts',(-52.6709849110232,-91.0495348953371,
175.490142808619));
#41735=CARTESIAN_POINT('Ctrl Pts',(-52.4769015662871,-91.1645067050937,
177.134243841043));
#41736=CARTESIAN_POINT('Ctrl Pts',(-53.4985792692187,-91.149870264798,178.441881219107));
#41737=CARTESIAN_POINT('Ctrl Pts',(-54.5202569721503,-91.1352338245022,
179.74951859717));
#41738=CARTESIAN_POINT('Ctrl Pts',(-56.1650323632195,-91.0541710078012,
179.954696079469));
#41739=CARTESIAN_POINT('Ctrl Pts',(-57.8098077542887,-90.9731081911002,
180.159873561769));
#41740=CARTESIAN_POINT('Ctrl Pts',(-59.1200152989378,-90.92771254204,179.142400961866));
#41741=CARTESIAN_POINT('Ctrl Pts',(-60.4302228435868,-90.8823168929797,
178.124928361964));
#41742=CARTESIAN_POINT('Ctrl Pts',(-60.6441823141569,-90.9537886125338,
176.48082732954));
#41743=CARTESIAN_POINT('Ctrl Pts',(-60.858141784727,-91.0252603320879,174.836726297116));
#41744=CARTESIAN_POINT('Ctrl Pts',(-59.8563402076294,-91.2263403016943,
173.529088919052));
#41745=CARTESIAN_POINT('Ctrl Pts',(-58.8545386305318,-91.4274202713008,
172.221451540989));
#41746=CARTESIAN_POINT('Ctrl Pts',(-57.2296393652966,-91.6949266173126,
172.016274058689));
#41747=CARTESIAN_POINT('Ctrl Pts',(-55.6047401000615,-91.9624329633243,
171.81109657639));
#41748=CARTESIAN_POINT('Ctrl Pts',(-54.3144086812465,-92.1942721416952,
172.828569176292));
#41749=CARTESIAN_POINT('Ctrl Pts',(-53.0240772624315,-92.4261113200661,
173.846041776195));
#41750=CARTESIAN_POINT('Ctrl Pts',(-52.8299939176954,-92.5410831298227,
175.490142808619));
#41751=CARTESIAN_POINT('Ctrl Pts',(-52.6359105729594,-92.6560549395794,
177.134243841043));
#41752=CARTESIAN_POINT('Ctrl Pts',(-53.657588275891,-92.6414184992836,178.441881219107));
#41753=CARTESIAN_POINT('Ctrl Pts',(-54.6792659788226,-92.6267820589878,
179.74951859717));
#41754=CARTESIAN_POINT('Ctrl Pts',(-56.3240413698918,-92.5457192422868,
179.954696079469));
#41755=CARTESIAN_POINT('Ctrl Pts',(-57.968816760961,-92.4646564255858,180.159873561769));
#41756=CARTESIAN_POINT('Ctrl Pts',(-59.27902430561,-92.4192607765256,179.142400961866));
#41757=CARTESIAN_POINT('Ctrl Pts',(-60.589231850259,-92.3738651274653,178.124928361964));
#41758=CARTESIAN_POINT('Ctrl Pts',(-60.8031913208291,-92.4453368470194,
176.48082732954));
#41759=CARTESIAN_POINT('Ctrl Pts',(-61.0171507913992,-92.5168085665735,
174.836726297116));
#41760=CARTESIAN_POINT('Ctrl Pts',(-60.0153492143016,-92.71788853618,173.529088919052));
#41761=CARTESIAN_POINT('Ctrl Pts',(-59.013547637204,-92.9189685057864,172.221451540989));
#41762=CARTESIAN_POINT('Ctrl Pts',(-57.3886483719689,-93.1864748517982,
172.016274058689));
#41763=CARTESIAN_POINT('Ctrl Pts',(-55.7637491067337,-93.4539811978099,
171.81109657639));
#41764=CARTESIAN_POINT('Ctrl Pts',(-54.4734176879187,-93.6858203761808,
172.828569176292));
#41765=CARTESIAN_POINT('Ctrl Pts',(-53.1830862691037,-93.9176595545517,
173.846041776195));
#41766=CARTESIAN_POINT('Ctrl Pts',(-52.9890029243677,-94.0326313643084,
175.490142808619));
#41767=CARTESIAN_POINT('Ctrl Pts',(-52.7949195796316,-94.147603174065,177.134243841043));
#41768=CARTESIAN_POINT('Ctrl Pts',(-53.8165972825632,-94.1329667337692,
178.441881219107));
#41769=CARTESIAN_POINT('Ctrl Pts',(-54.8382749854948,-94.1183302934734,
179.74951859717));
#41770=CARTESIAN_POINT('Ctrl Pts',(-56.483050376564,-94.0372674767724,179.954696079469));
#41771=CARTESIAN_POINT('Ctrl Pts',(-58.1278257676332,-93.9562046600714,
180.159873561769));
#41772=CARTESIAN_POINT('Ctrl Pts',(-59.4380333122822,-93.9108090110112,
179.142400961866));
#41773=CARTESIAN_POINT('Ctrl Pts',(-60.7482408569312,-93.8654133619509,
178.124928361964));
#41774=CARTESIAN_POINT('Ctrl Pts',(-60.9622003275013,-93.936885081505,176.48082732954));
#41775=CARTESIAN_POINT('Ctrl Pts',(-61.1761597980714,-94.0083568010591,
174.836726297116));
#41776=CARTESIAN_POINT('Ctrl Pts',(-60.1743582209738,-94.2094367706656,
173.529088919052));
#41777=CARTESIAN_POINT('Ctrl Pts',(-59.1725566438763,-94.410516740272,172.221451540989));
#41778=CARTESIAN_POINT('Ctrl Pts',(-57.5476573786411,-94.6780230862838,
172.016274058689));
#41779=CARTESIAN_POINT('Ctrl Pts',(-55.9227581134059,-94.9455294322955,
171.81109657639));
#41780=CARTESIAN_POINT('Ctrl Pts',(-54.6324266945909,-95.1773686106664,
172.828569176292));
#41781=CARTESIAN_POINT('Ctrl Pts',(-53.342095275776,-95.4092077890373,173.846041776195));
#41782=CARTESIAN_POINT('Ctrl Pts',(-53.1480119310399,-95.5241795987939,
175.490142808619));
#41783=CARTESIAN_POINT('Ctrl Pts',(-52.9539285863038,-95.6391514085506,
177.134243841043));
#41784=CARTESIAN_POINT('Ctrl Pts',(-53.9756062892354,-95.6245149682548,
178.441881219107));
#41785=CARTESIAN_POINT('Ctrl Pts',(-54.997283992167,-95.609878527959,179.74951859717));
#41786=CARTESIAN_POINT('Ctrl Pts',(-56.6420593832362,-95.528815711258,179.954696079469));
#41787=CARTESIAN_POINT('Ctrl Pts',(-58.2868347743054,-95.447752894557,180.159873561769));
#41788=CARTESIAN_POINT('Ctrl Pts',(-59.5970423189544,-95.4023572454968,
179.142400961866));
#41789=CARTESIAN_POINT('Ctrl Pts',(-60.9072498636035,-95.3569615964365,
178.124928361964));
#41790=CARTESIAN_POINT('Ctrl Pts',(-61.1212093341735,-95.4284333159906,
176.48082732954));
#41791=CARTESIAN_POINT('Ctrl Pts',(-61.3351688047436,-95.4999050355447,
174.836726297116));
#41792=CARTESIAN_POINT('Ctrl Pts',(-60.3333672276461,-95.7009850051512,
173.529088919052));
#41793=CARTESIAN_POINT('Ctrl Pts',(-59.3315656505485,-95.9020649747577,
172.221451540989));
#41794=CARTESIAN_POINT('Ctrl Pts',(-57.7066663853133,-96.1695713207694,
172.016274058689));
#41795=CARTESIAN_POINT('Ctrl Pts',(-56.0817671200782,-96.4370776667811,
171.81109657639));
#41796=CARTESIAN_POINT('Ctrl Pts',(-54.7914357012632,-96.668916845152,172.828569176292));
#41797=CARTESIAN_POINT('Ctrl Pts',(-53.5011042824482,-96.9007560235229,
173.846041776195));
#41798=CARTESIAN_POINT('Ctrl Pts',(-53.3070209377121,-97.0157278332795,
175.490142808619));
#41799=CARTESIAN_POINT('Ctrl Pts',(-53.1129375929761,-97.1306996430362,
177.134243841043));
#41800=CARTESIAN_POINT('Ctrl Pts',(-54.1346152959077,-97.1160632027404,
178.441881219107));
#41801=CARTESIAN_POINT('Ctrl Pts',(-55.1562929988393,-97.1014267624446,
179.74951859717));
#41802=CARTESIAN_POINT('Ctrl Pts',(-56.8010683899085,-97.0203639457436,
179.954696079469));
#41803=CARTESIAN_POINT('Ctrl Pts',(-58.4458437809776,-96.9393011290426,
180.159873561769));
#41804=CARTESIAN_POINT('Ctrl Pts',(-59.7560513256267,-96.8939054799824,
179.142400961866));
#41805=CARTESIAN_POINT('Ctrl Pts',(-61.0662588702757,-96.8485098309221,
178.124928361964));
#41806=CARTESIAN_POINT('Ctrl Pts',(-61.2802183408458,-96.9199815504762,
176.48082732954));
#41807=CARTESIAN_POINT('Ctrl Pts',(-61.4941778114159,-96.9914532700303,
174.836726297116));
#41808=CARTESIAN_POINT('Ctrl Pts',(-60.4923762343183,-97.1925332396368,
173.529088919052));
#41809=CARTESIAN_POINT('Ctrl Pts',(-59.4905746572207,-97.3936132092432,
172.221451540989));
#41810=CARTESIAN_POINT('Ctrl Pts',(-57.8656753919855,-97.661119555255,172.016274058689));
#41811=CARTESIAN_POINT('Ctrl Pts',(-56.2407761267504,-97.9286259012667,
171.81109657639));
#41812=CARTESIAN_POINT('Ctrl Pts',(-54.9504447079354,-98.1604650796376,
172.828569176292));
#41813=CARTESIAN_POINT('Ctrl Pts',(-53.6601132891204,-98.3923042580085,
173.846041776195));
#41814=CARTESIAN_POINT('Ctrl Pts',(-53.4660299443843,-98.5072760677652,
175.490142808619));
#41815=CARTESIAN_POINT('Ctrl Pts',(-53.2719465996483,-98.6222478775218,
177.134243841043));
#41816=CARTESIAN_POINT('Ctrl Pts',(-54.2936243025799,-98.607611437226,178.441881219107));
#41817=CARTESIAN_POINT('Ctrl Pts',(-55.3153020055115,-98.5929749969302,
179.74951859717));
#41818=CARTESIAN_POINT('Ctrl Pts',(-56.9600773965807,-98.5119121802292,
179.954696079469));
#41819=CARTESIAN_POINT('Ctrl Pts',(-58.6048527876499,-98.4308493635282,
180.159873561769));
#41820=CARTESIAN_POINT('Ctrl Pts',(-59.9150603322989,-98.385453714468,179.142400961866));
#41821=CARTESIAN_POINT('Ctrl Pts',(-61.2252678769479,-98.3400580654077,
178.124928361964));
#41822=CARTESIAN_POINT('Ctrl Pts',(-61.439227347518,-98.4115297849618,176.48082732954));
#41823=CARTESIAN_POINT('Ctrl Pts',(-61.6531868180881,-98.4830015045159,
174.836726297116));
#41824=CARTESIAN_POINT('Ctrl Pts',(-60.6513852409905,-98.6840814741224,
173.529088919052));
#41825=CARTESIAN_POINT('Ctrl Pts',(-59.6495836638929,-98.8851614437288,
172.221451540989));
#41826=CARTESIAN_POINT('Ctrl Pts',(-58.0246843986578,-99.1526677897406,
172.016274058689));
#41827=CARTESIAN_POINT('Ctrl Pts',(-56.3997851334226,-99.4201741357523,
171.81109657639));
#41828=CARTESIAN_POINT('Ctrl Pts',(-55.1094537146076,-99.6520133141232,
172.828569176292));
#41829=CARTESIAN_POINT('Ctrl Pts',(-53.8191222957926,-99.8838524924941,
173.846041776195));
#41830=CARTESIAN_POINT('Ctrl Pts',(-53.6250389510566,-99.9988243022507,
175.490142808619));
#41831=CARTESIAN_POINT('Ctrl Pts',(-53.4309556063205,-100.113796112007,
177.134243841043));
#41832=CARTESIAN_POINT('Ctrl Pts',(-54.4526333092521,-100.099159671712,
178.441881219107));
#41833=CARTESIAN_POINT('Ctrl Pts',(-55.4743110121837,-100.084523231416,
179.74951859717));
#41834=CARTESIAN_POINT('Ctrl Pts',(-57.1190864032529,-100.003460414715,
179.954696079469));
#41835=CARTESIAN_POINT('Ctrl Pts',(-58.7638617943221,-99.9223975980138,
180.159873561769));
#41836=CARTESIAN_POINT('Ctrl Pts',(-60.0740693389711,-99.8770019489536,
179.142400961866));
#41837=CARTESIAN_POINT('Ctrl Pts',(-61.3842768836201,-99.8316062998934,
178.124928361964));
#41838=CARTESIAN_POINT('Ctrl Pts',(-61.5982363541902,-99.9030780194474,
176.48082732954));
#41839=CARTESIAN_POINT('Ctrl Pts',(-61.8121958247603,-99.9745497390015,
174.836726297116));
#41840=CARTESIAN_POINT('Ctrl Pts',(-60.8103942476627,-100.175629708608,
173.529088919052));
#41841=CARTESIAN_POINT('Ctrl Pts',(-59.8085926705652,-100.376709678214,
172.221451540989));
#41842=CARTESIAN_POINT('Ctrl Pts',(-58.18369340533,-100.644216024226,172.016274058689));
#41843=CARTESIAN_POINT('Ctrl Pts',(-56.5587941400948,-100.911722370238,
171.81109657639));
#41844=CARTESIAN_POINT('Ctrl Pts',(-55.2684627212798,-101.143561548609,
172.828569176292));
#41845=CARTESIAN_POINT('Ctrl Pts',(-53.9781313024648,-101.37540072698,173.846041776195));
#41846=CARTESIAN_POINT('Ctrl Pts',(-53.7840479577288,-101.490372536736,
175.490142808619));
#41847=CARTESIAN_POINT('Ctrl Pts',(-53.5899646129927,-101.605344346493,
177.134243841043));
#41848=CARTESIAN_POINT('Ctrl Pts',(-54.6116423159243,-101.590707906197,
178.441881219107));
#41849=CARTESIAN_POINT('Ctrl Pts',(-55.6333200188559,-101.576071465901,
179.74951859717));
#41850=CARTESIAN_POINT('Ctrl Pts',(-57.2780954099251,-101.4950086492,179.954696079469));
#41851=CARTESIAN_POINT('Ctrl Pts',(-58.9228708009943,-101.413945832499,
180.159873561769));
#41852=CARTESIAN_POINT('Ctrl Pts',(-60.2330783456433,-101.368550183439,
179.142400961866));
#41853=CARTESIAN_POINT('Ctrl Pts',(-61.5432858902924,-101.323154534379,
178.124928361964));
#41854=CARTESIAN_POINT('Ctrl Pts',(-61.7572453608625,-101.394626253933,
176.48082732954));
#41855=CARTESIAN_POINT('Ctrl Pts',(-61.9712048314326,-101.466097973487,
174.836726297116));
#41856=CARTESIAN_POINT('Ctrl Pts',(-60.969403254335,-101.667177943094,173.529088919052));
#41857=CARTESIAN_POINT('Ctrl Pts',(-59.9676016772374,-101.8682579127,172.221451540989));
#41858=CARTESIAN_POINT('Ctrl Pts',(-58.3427024120022,-102.135764258712,
172.016274058689));
#41859=CARTESIAN_POINT('Ctrl Pts',(-56.7178031467671,-102.403270604724,
171.81109657639));
#41860=CARTESIAN_POINT('Ctrl Pts',(-55.4274717279521,-102.635109783094,
172.828569176292));
#41861=CARTESIAN_POINT('Ctrl Pts',(-54.1371403091371,-102.866948961465,
173.846041776195));
#41862=CARTESIAN_POINT('Ctrl Pts',(-53.943056964401,-102.981920771222,175.490142808619));
#41863=CARTESIAN_POINT('Ctrl Pts',(-53.748973619665,-103.096892580979,177.134243841043));
#41864=CARTESIAN_POINT('Ctrl Pts',(-54.7706513225966,-103.082256140683,
178.441881219107));
#41865=CARTESIAN_POINT('Ctrl Pts',(-55.7923290255282,-103.067619700387,
179.74951859717));
#41866=CARTESIAN_POINT('Ctrl Pts',(-57.4371044165974,-102.986556883686,
179.954696079469));
#41867=CARTESIAN_POINT('Ctrl Pts',(-59.0818798076666,-102.905494066985,
180.159873561769));
#41868=CARTESIAN_POINT('Ctrl Pts',(-60.3920873523156,-102.860098417925,
179.142400961866));
#41869=CARTESIAN_POINT('Ctrl Pts',(-61.7022948969646,-102.814702768865,
178.124928361964));
#41870=CARTESIAN_POINT('Ctrl Pts',(-61.9162543675347,-102.886174488419,
176.48082732954));
#41871=CARTESIAN_POINT('Ctrl Pts',(-62.1302138381048,-102.957646207973,
174.836726297116));
#41872=CARTESIAN_POINT('Ctrl Pts',(-61.1284122610072,-103.158726177579,
173.529088919052));
#41873=CARTESIAN_POINT('Ctrl Pts',(-60.1266106839096,-103.359806147186,
172.221451540989));
#41874=CARTESIAN_POINT('Ctrl Pts',(-58.5017114186745,-103.627312493197,
172.016274058689));
#41875=CARTESIAN_POINT('Ctrl Pts',(-56.8768121534393,-103.894818839209,
171.81109657639));
#41876=CARTESIAN_POINT('Ctrl Pts',(-55.5864807346243,-104.12665801758,172.828569176292));
#41877=CARTESIAN_POINT('Ctrl Pts',(-54.2961493158093,-104.358497195951,
173.846041776195));
#41878=CARTESIAN_POINT('Ctrl Pts',(-54.1020659710732,-104.473469005708,
175.490142808619));
#41879=CARTESIAN_POINT('Ctrl Pts',(-53.9079826263372,-104.588440815464,
177.134243841043));
#41880=CARTESIAN_POINT('Ctrl Pts',(-54.9296603292688,-104.573804375168,
178.441881219107));
#41881=CARTESIAN_POINT('Ctrl Pts',(-55.9513380322004,-104.559167934873,
179.74951859717));
#41882=CARTESIAN_POINT('Ctrl Pts',(-57.5961134232696,-104.478105118172,
179.954696079469));
#41883=CARTESIAN_POINT('Ctrl Pts',(-59.2408888143388,-104.397042301471,
180.159873561769));
#41884=CARTESIAN_POINT('Ctrl Pts',(-60.5510963589878,-104.35164665241,179.142400961866));
#41885=CARTESIAN_POINT('Ctrl Pts',(-61.8613039036368,-104.30625100335,178.124928361964));
#41886=CARTESIAN_POINT('Ctrl Pts',(-62.0752633742069,-104.377722722904,
176.48082732954));
#41887=CARTESIAN_POINT('Ctrl Pts',(-62.289222844777,-104.449194442458,174.836726297116));
#41888=CARTESIAN_POINT('Ctrl Pts',(-61.2874212676794,-104.650274412065,
173.529088919052));
#41889=CARTESIAN_POINT('Ctrl Pts',(-60.2856196905818,-104.851354381671,
172.221451540989));
#41890=CARTESIAN_POINT('Ctrl Pts',(-58.6607204253467,-105.118860727683,
172.016274058689));
#41891=CARTESIAN_POINT('Ctrl Pts',(-57.0358211601115,-105.386367073695,
171.81109657639));
#41892=CARTESIAN_POINT('Ctrl Pts',(-55.7454897412965,-105.618206252066,
172.828569176292));
#41893=CARTESIAN_POINT('Ctrl Pts',(-54.4551583224815,-105.850045430437,
173.846041776195));
#41894=CARTESIAN_POINT('Ctrl Pts',(-54.2610749777455,-105.965017240193,
175.490142808619));
#41895=CARTESIAN_POINT('Ctrl Pts',(-54.0669916330094,-106.07998904995,177.134243841043));
#41896=CARTESIAN_POINT('Ctrl Pts',(-55.088669335941,-106.065352609654,178.441881219107));
#41897=CARTESIAN_POINT('Ctrl Pts',(-56.1103470388726,-106.050716169358,
179.74951859717));
#41898=CARTESIAN_POINT('Ctrl Pts',(-57.7551224299418,-105.969653352657,
179.954696079469));
#41899=CARTESIAN_POINT('Ctrl Pts',(-59.399897821011,-105.888590535956,180.159873561769));
#41900=CARTESIAN_POINT('Ctrl Pts',(-60.71010536566,-105.843194886896,179.142400961866));
#41901=CARTESIAN_POINT('Ctrl Pts',(-62.0203129103091,-105.797799237836,
178.124928361964));
#41902=CARTESIAN_POINT('Ctrl Pts',(-62.2342723808791,-105.86927095739,176.48082732954));
#41903=CARTESIAN_POINT('Ctrl Pts',(-62.4482318514492,-105.940742676944,
174.836726297116));
#41904=CARTESIAN_POINT('Ctrl Pts',(-61.4464302743516,-106.14182264655,173.529088919052));
#41905=CARTESIAN_POINT('Ctrl Pts',(-60.4446286972541,-106.342902616157,
172.221451540989));
#41906=CARTESIAN_POINT('Ctrl Pts',(-58.8197294320189,-106.610408962169,
172.016274058689));
#41907=CARTESIAN_POINT('Ctrl Pts',(-57.1948301667837,-106.87791530818,171.81109657639));
#41908=CARTESIAN_POINT('Ctrl Pts',(-55.9044987479688,-107.109754486551,
172.828569176292));
#41909=CARTESIAN_POINT('Ctrl Pts',(-54.6141673291538,-107.341593664922,
173.846041776195));
#41910=CARTESIAN_POINT('Ctrl Pts',(-54.4200839844177,-107.456565474679,
175.490142808619));
#41911=CARTESIAN_POINT('Ctrl Pts',(-54.2260006396817,-107.571537284435,
177.134243841043));
#41912=CARTESIAN_POINT('Ctrl Pts',(-55.2476783426132,-107.55690084414,178.441881219107));
#41913=CARTESIAN_POINT('Ctrl Pts',(-56.2693560455449,-107.542264403844,
179.74951859717));
#41914=CARTESIAN_POINT('Ctrl Pts',(-57.914131436614,-107.461201587143,179.954696079469));
#41915=CARTESIAN_POINT('Ctrl Pts',(-59.5589068276832,-107.380138770442,
180.159873561769));
#41916=CARTESIAN_POINT('Ctrl Pts',(-60.8691143723323,-107.334743121382,
179.142400961866));
#41917=CARTESIAN_POINT('Ctrl Pts',(-62.1793219169813,-107.289347472321,
178.124928361964));
#41918=CARTESIAN_POINT('Ctrl Pts',(-62.3932813875514,-107.360819191875,
176.48082732954));
#41919=CARTESIAN_POINT('Ctrl Pts',(-62.6072408581214,-107.43229091143,174.836726297116));
#41920=CARTESIAN_POINT('Ctrl Pts',(-61.6054392810239,-107.633370881036,
173.529088919052));
#41921=CARTESIAN_POINT('Ctrl Pts',(-60.6036377039263,-107.834450850642,
172.221451540989));
#41922=CARTESIAN_POINT('Ctrl Pts',(-58.9787384386911,-108.101957196654,
172.016274058689));
#41923=CARTESIAN_POINT('Ctrl Pts',(-57.353839173456,-108.369463542666,171.81109657639));
#41924=CARTESIAN_POINT('Ctrl Pts',(-56.063507754641,-108.601302721037,172.828569176292));
#41925=CARTESIAN_POINT('Ctrl Pts',(-54.773176335826,-108.833141899408,173.846041776195));
#41926=CARTESIAN_POINT('Ctrl Pts',(-54.5790929910899,-108.948113709164,
175.490142808619));
#41927=CARTESIAN_POINT('Ctrl Pts',(-54.3850096463539,-109.063085518921,
177.134243841043));
#41928=CARTESIAN_POINT('Ctrl Pts',(-55.4066873492855,-109.048449078625,
178.441881219107));
#41929=CARTESIAN_POINT('Ctrl Pts',(-56.4283650522171,-109.033812638329,
179.74951859717));
#41930=CARTESIAN_POINT('Ctrl Pts',(-58.0731404432863,-108.952749821628,
179.954696079469));
#41931=CARTESIAN_POINT('Ctrl Pts',(-59.7179158343555,-108.871687004927,
180.159873561769));
#41932=CARTESIAN_POINT('Ctrl Pts',(-61.0281233790045,-108.826291355867,
179.142400961866));
#41933=CARTESIAN_POINT('Ctrl Pts',(-62.3383309236535,-108.780895706807,
178.124928361964));
#41934=CARTESIAN_POINT('Ctrl Pts',(-62.5522903942236,-108.852367426361,
176.48082732954));
#41935=CARTESIAN_POINT('Ctrl Pts',(-62.7662498647937,-108.923839145915,
174.836726297116));
#41936=CARTESIAN_POINT('Ctrl Pts',(-61.7644482876961,-109.124919115522,
173.529088919052));
#41937=CARTESIAN_POINT('Ctrl Pts',(-60.7626467105985,-109.325999085128,
172.221451540989));
#41938=CARTESIAN_POINT('Ctrl Pts',(-59.1377474453634,-109.59350543114,172.016274058689));
#41939=CARTESIAN_POINT('Ctrl Pts',(-57.5128481801282,-109.861011777152,
171.81109657639));
#41940=CARTESIAN_POINT('Ctrl Pts',(-56.2225167613132,-110.092850955522,
172.828569176292));
#41941=CARTESIAN_POINT('Ctrl Pts',(-54.9321853424982,-110.324690133893,
173.846041776195));
#41942=CARTESIAN_POINT('Ctrl Pts',(-54.7381019977622,-110.43966194365,175.490142808619));
#41943=CARTESIAN_POINT('Ctrl Pts',(-54.5440186530261,-110.554633753407,
177.134243841043));
#41944=CARTESIAN_POINT('Ctrl Pts',(-55.5656963559577,-110.539997313111,
178.441881219107));
#41945=CARTESIAN_POINT('Ctrl Pts',(-56.5873740588893,-110.525360872815,
179.74951859717));
#41946=CARTESIAN_POINT('Ctrl Pts',(-58.2321494499585,-110.444298056114,
179.954696079469));
#41947=CARTESIAN_POINT('Ctrl Pts',(-59.8769248410277,-110.363235239413,
180.159873561769));
#41948=CARTESIAN_POINT('Ctrl Pts',(-61.1871323856767,-110.317839590353,
179.142400961866));
#41949=CARTESIAN_POINT('Ctrl Pts',(-62.4973399303257,-110.272443941293,
178.124928361964));
#41950=CARTESIAN_POINT('Ctrl Pts',(-62.7112994008958,-110.343915660847,
176.48082732954));
#41951=CARTESIAN_POINT('Ctrl Pts',(-62.9252588714659,-110.415387380401,
174.836726297116));
#41952=CARTESIAN_POINT('Ctrl Pts',(-61.9234572943683,-110.616467350007,
173.529088919052));
#41953=CARTESIAN_POINT('Ctrl Pts',(-60.9216557172708,-110.817547319614,
172.221451540989));
#41954=CARTESIAN_POINT('Ctrl Pts',(-59.2967564520356,-111.085053665625,
172.016274058689));
#41955=CARTESIAN_POINT('Ctrl Pts',(-57.6718571868004,-111.352560011637,
171.81109657639));
#41956=CARTESIAN_POINT('Ctrl Pts',(-56.3815257679854,-111.584399190008,
172.828569176292));
#41957=CARTESIAN_POINT('Ctrl Pts',(-55.0911943491704,-111.816238368379,
173.846041776195));
#41958=CARTESIAN_POINT('Ctrl Pts',(-54.8971110044344,-111.931210178136,
175.490142808619));
#41959=CARTESIAN_POINT('Ctrl Pts',(-54.7030276596983,-112.046181987892,
177.134243841043));
#41960=CARTESIAN_POINT('Ctrl Pts',(-55.7247053626299,-112.031545547596,
178.441881219107));
#41961=CARTESIAN_POINT('Ctrl Pts',(-56.7463830655615,-112.016909107301,
179.74951859717));
#41962=CARTESIAN_POINT('Ctrl Pts',(-58.3911584566307,-111.9358462906,179.954696079469));
#41963=CARTESIAN_POINT('Ctrl Pts',(-60.0359338476999,-111.854783473899,
180.159873561769));
#41964=CARTESIAN_POINT('Ctrl Pts',(-61.3461413923489,-111.809387824838,
179.142400961866));
#41965=CARTESIAN_POINT('Ctrl Pts',(-62.656348936998,-111.763992175778,178.124928361964));
#41966=CARTESIAN_POINT('Ctrl Pts',(-62.870308407568,-111.835463895332,176.48082732954));
#41967=CARTESIAN_POINT('Ctrl Pts',(-63.0842678781381,-111.906935614886,
174.836726297116));
#41968=CARTESIAN_POINT('Ctrl Pts',(-62.0824663010406,-112.108015584493,
173.529088919052));
#41969=CARTESIAN_POINT('Ctrl Pts',(-61.080664723943,-112.309095554099,172.221451540989));
#41970=CARTESIAN_POINT('Ctrl Pts',(-59.4557654587078,-112.576601900111,
172.016274058689));
#41971=CARTESIAN_POINT('Ctrl Pts',(-57.8308661934727,-112.844108246123,
171.81109657639));
#41972=CARTESIAN_POINT('Ctrl Pts',(-56.5405347746577,-113.075947424494,
172.828569176292));
#41973=CARTESIAN_POINT('Ctrl Pts',(-55.2502033558427,-113.307786602865,
173.846041776195));
#41974=CARTESIAN_POINT('Ctrl Pts',(-55.0561200111066,-113.422758412621,
175.490142808619));
#41975=CARTESIAN_POINT('Ctrl Pts',(-54.8620366663706,-113.537730222378,
177.134243841043));
#41976=CARTESIAN_POINT('Ctrl Pts',(-55.8837143693022,-113.523093782082,
178.441881219107));
#41977=CARTESIAN_POINT('Ctrl Pts',(-56.9053920722338,-113.508457341786,
179.74951859717));
#41978=CARTESIAN_POINT('Ctrl Pts',(-58.550167463303,-113.427394525085,179.954696079469));
#41979=CARTESIAN_POINT('Ctrl Pts',(-60.1949428543721,-113.346331708384,
180.159873561769));
#41980=CARTESIAN_POINT('Ctrl Pts',(-61.5051503990212,-113.300936059324,
179.142400961866));
#41981=CARTESIAN_POINT('Ctrl Pts',(-62.8153579436702,-113.255540410264,
178.124928361964));
#41982=CARTESIAN_POINT('Ctrl Pts',(-63.0293174142403,-113.327012129818,
176.48082732954));
#41983=CARTESIAN_POINT('Ctrl Pts',(-63.2432768848104,-113.398483849372,
174.836726297116));
#41984=CARTESIAN_POINT('Ctrl Pts',(-62.2414753077128,-113.599563818978,
173.529088919052));
#41985=CARTESIAN_POINT('Ctrl Pts',(-61.2396737306152,-113.800643788585,
172.221451540989));
#41986=CARTESIAN_POINT('Ctrl Pts',(-59.6147744653801,-114.068150134597,
172.016274058689));
#41987=CARTESIAN_POINT('Ctrl Pts',(-57.9898752001449,-114.335656480608,
171.81109657639));
#41988=CARTESIAN_POINT('Ctrl Pts',(-56.6995437813299,-114.567495658979,
172.828569176292));
#41989=CARTESIAN_POINT('Ctrl Pts',(-55.4092123625149,-114.79933483735,173.846041776195));
#41990=CARTESIAN_POINT('Ctrl Pts',(-55.2151290177788,-114.914306647107,
175.490142808619));
#41991=CARTESIAN_POINT('Ctrl Pts',(-55.0210456730428,-115.029278456863,
177.134243841043));
#41992=CARTESIAN_POINT('Ctrl Pts',(-56.0427233759744,-115.014642016568,
178.441881219107));
#41993=CARTESIAN_POINT('Ctrl Pts',(-57.064401078906,-115.000005576272,179.74951859717));
#41994=CARTESIAN_POINT('Ctrl Pts',(-58.7091764699752,-114.918942759571,
179.954696079469));
#41995=CARTESIAN_POINT('Ctrl Pts',(-60.3539518610444,-114.83787994287,180.159873561769));
#41996=CARTESIAN_POINT('Ctrl Pts',(-61.6641594056934,-114.79248429381,179.142400961866));
#41997=CARTESIAN_POINT('Ctrl Pts',(-62.9743669503424,-114.747088644749,
178.124928361964));
#41998=CARTESIAN_POINT('Ctrl Pts',(-63.1883264209125,-114.818560364303,
176.48082732954));
#41999=CARTESIAN_POINT('Ctrl Pts',(-63.4022858914826,-114.890032083858,
174.836726297116));
#42000=CARTESIAN_POINT('Ctrl Pts',(-62.400484314385,-115.091112053464,173.529088919052));
#42001=CARTESIAN_POINT('Ctrl Pts',(-61.3986827372874,-115.29219202307,172.221451540989));
#42002=CARTESIAN_POINT('Ctrl Pts',(-59.7737834720523,-115.559698369082,
172.016274058689));
#42003=CARTESIAN_POINT('Ctrl Pts',(-58.1488842068171,-115.827204715094,
171.81109657639));
#42004=CARTESIAN_POINT('Ctrl Pts',(-56.8585527880021,-116.059043893465,
172.828569176292));
#42005=CARTESIAN_POINT('Ctrl Pts',(-55.5682213691871,-116.290883071836,
173.846041776195));
#42006=CARTESIAN_POINT('Ctrl Pts',(-55.3741380244511,-116.405854881592,
175.490142808619));
#42007=CARTESIAN_POINT('Ctrl Pts',(-55.180054679715,-116.520826691349,177.134243841043));
#42008=CARTESIAN_POINT('Ctrl Pts',(-56.2017323826466,-116.506190251053,
178.441881219107));
#42009=CARTESIAN_POINT('Ctrl Pts',(-57.2234100855782,-116.491553810757,
179.74951859717));
#42010=CARTESIAN_POINT('Ctrl Pts',(-58.8681854766474,-116.410490994056,
179.954696079469));
#42011=CARTESIAN_POINT('Ctrl Pts',(-60.5129608677166,-116.329428177355,
180.159873561769));
#42012=CARTESIAN_POINT('Ctrl Pts',(-61.8231684123656,-116.284032528295,
179.142400961866));
#42013=CARTESIAN_POINT('Ctrl Pts',(-63.1333759570146,-116.238636879235,
178.124928361964));
#42014=CARTESIAN_POINT('Ctrl Pts',(-63.3473354275847,-116.310108598789,
176.48082732954));
#42015=CARTESIAN_POINT('Ctrl Pts',(-63.5612948981548,-116.381580318343,
174.836726297116));
#42016=CARTESIAN_POINT('Ctrl Pts',(-62.5594933210572,-116.58266028795,173.529088919052));
#42017=CARTESIAN_POINT('Ctrl Pts',(-61.5576917439597,-116.783740257556,
172.221451540989));
#42018=CARTESIAN_POINT('Ctrl Pts',(-59.9327924787245,-117.051246603568,
172.016274058689));
#42019=CARTESIAN_POINT('Ctrl Pts',(-58.3078932134894,-117.318752949579,
171.81109657639));
#42020=CARTESIAN_POINT('Ctrl Pts',(-57.0175617946743,-117.55059212795,172.828569176292));
#42021=CARTESIAN_POINT('Ctrl Pts',(-55.7272303758593,-117.782431306321,
173.846041776195));
#42022=CARTESIAN_POINT('Ctrl Pts',(-55.5331470311233,-117.897403116078,
175.490142808619));
#42023=CARTESIAN_POINT('Ctrl Pts',(-55.3390636863872,-118.012374925835,
177.134243841043));
#42024=CARTESIAN_POINT('Ctrl Pts',(-56.3607413893188,-117.997738485539,
178.441881219107));
#42025=CARTESIAN_POINT('Ctrl Pts',(-57.3824190922504,-117.983102045243,
179.74951859717));
#42026=CARTESIAN_POINT('Ctrl Pts',(-59.0271944833196,-117.902039228542,
179.954696079469));
#42027=CARTESIAN_POINT('Ctrl Pts',(-60.6719698743888,-117.820976411841,
180.159873561769));
#42028=CARTESIAN_POINT('Ctrl Pts',(-61.9821774190378,-117.775580762781,
179.142400961866));
#42029=CARTESIAN_POINT('Ctrl Pts',(-63.2923849636869,-117.730185113721,
178.124928361964));
#42030=CARTESIAN_POINT('Ctrl Pts',(-63.506344434257,-117.801656833275,176.48082732954));
#42031=CARTESIAN_POINT('Ctrl Pts',(-63.720303904827,-117.873128552829,174.836726297116));
#42032=CARTESIAN_POINT('Ctrl Pts',(-62.7185023277295,-118.074208522435,
173.529088919052));
#42033=CARTESIAN_POINT('Ctrl Pts',(-61.7167007506319,-118.275288492042,
172.221451540989));
#42034=CARTESIAN_POINT('Ctrl Pts',(-60.0918014853967,-118.542794838053,
172.016274058689));
#42035=CARTESIAN_POINT('Ctrl Pts',(-58.4669022201616,-118.810301184065,
171.81109657639));
#42036=CARTESIAN_POINT('Ctrl Pts',(-57.1765708013466,-119.042140362436,
172.828569176292));
#42037=CARTESIAN_POINT('Ctrl Pts',(-55.8862393825316,-119.273979540807,
173.846041776195));
#42038=CARTESIAN_POINT('Ctrl Pts',(-55.6921560377955,-119.388951350564,
175.490142808619));
#42039=CARTESIAN_POINT('Ctrl Pts',(-55.4980726930595,-119.50392316032,177.134243841043));
#42040=CARTESIAN_POINT('Ctrl Pts',(-56.5197503959911,-119.489286720024,
178.441881219107));
#42041=CARTESIAN_POINT('Ctrl Pts',(-57.5414280989227,-119.474650279729,
179.74951859717));
#42042=CARTESIAN_POINT('Ctrl Pts',(-59.1862034899919,-119.393587463028,
179.954696079469));
#42043=CARTESIAN_POINT('Ctrl Pts',(-60.8309788810611,-119.312524646327,
180.159873561769));
#42044=CARTESIAN_POINT('Ctrl Pts',(-62.1411864257101,-119.267128997266,
179.142400961866));
#42045=CARTESIAN_POINT('Ctrl Pts',(-63.4513939703591,-119.221733348206,
178.124928361964));
#42046=CARTESIAN_POINT('Ctrl Pts',(-63.6653534409292,-119.29320506776,176.48082732954));
#42047=CARTESIAN_POINT('Ctrl Pts',(-63.8793129114993,-119.364676787314,
174.836726297116));
#42048=CARTESIAN_POINT('Ctrl Pts',(-62.8775113344017,-119.565756756921,
173.529088919052));
#42049=CARTESIAN_POINT('Ctrl Pts',(-61.8757097573041,-119.766836726527,
172.221451540989));
#42050=CARTESIAN_POINT('Ctrl Pts',(-60.250810492069,-120.034343072539,172.016274058689));
#42051=CARTESIAN_POINT('Ctrl Pts',(-58.6259112268338,-120.301849418551,
171.81109657639));
#42052=CARTESIAN_POINT('Ctrl Pts',(-57.3355798080188,-120.533688596922,
172.828569176292));
#42053=CARTESIAN_POINT('Ctrl Pts',(-56.0452483892038,-120.765527775293,
173.846041776195));
#42054=CARTESIAN_POINT('Ctrl Pts',(-55.8511650444677,-120.880499585049,
175.490142808619));
#42055=CARTESIAN_POINT('Ctrl Pts',(-55.6570816997317,-120.995471394806,
177.134243841043));
#42056=CARTESIAN_POINT('Ctrl Pts',(-56.6787594026633,-120.98083495451,178.441881219107));
#42057=CARTESIAN_POINT('Ctrl Pts',(-57.7004371055949,-120.966198514214,
179.74951859717));
#42058=CARTESIAN_POINT('Ctrl Pts',(-59.3452124966641,-120.885135697513,
179.954696079469));
#42059=CARTESIAN_POINT('Ctrl Pts',(-60.9899878877333,-120.804072880812,
180.159873561769));
#42060=CARTESIAN_POINT('Ctrl Pts',(-62.3001954323823,-120.758677231752,
179.142400961866));
#42061=CARTESIAN_POINT('Ctrl Pts',(-63.6104029770313,-120.713281582692,
178.124928361964));
#42062=CARTESIAN_POINT('Ctrl Pts',(-63.8243624476014,-120.784753302246,
176.48082732954));
#42063=CARTESIAN_POINT('Ctrl Pts',(-64.0383219181715,-120.8562250218,174.836726297116));
#42064=CARTESIAN_POINT('Ctrl Pts',(-63.0365203410739,-121.057304991406,
173.529088919052));
#42065=CARTESIAN_POINT('Ctrl Pts',(-62.0347187639764,-121.258384961013,
172.221451540989));
#42066=CARTESIAN_POINT('Ctrl Pts',(-60.4098194987412,-121.525891307025,
172.016274058689));
#42067=CARTESIAN_POINT('Ctrl Pts',(-58.784920233506,-121.793397653036,171.81109657639));
#42068=CARTESIAN_POINT('Ctrl Pts',(-57.494588814691,-122.025236831407,172.828569176292));
#42069=CARTESIAN_POINT('Ctrl Pts',(-56.204257395876,-122.257076009778,173.846041776195));
#42070=CARTESIAN_POINT('Ctrl Pts',(-56.01017405114,-122.372047819535,175.490142808619));
#42071=CARTESIAN_POINT('Ctrl Pts',(-55.8160907064039,-122.487019629291,
177.134243841043));
#42072=CARTESIAN_POINT('Ctrl Pts',(-56.8377684093355,-122.472383188996,
178.441881219107));
#42073=CARTESIAN_POINT('Ctrl Pts',(-57.8594461122671,-122.4577467487,179.74951859717));
#42074=CARTESIAN_POINT('Ctrl Pts',(-59.5042215033363,-122.376683931999,
179.954696079469));
#42075=CARTESIAN_POINT('Ctrl Pts',(-61.1489968944055,-122.295621115298,
180.159873561769));
#42076=CARTESIAN_POINT('Ctrl Pts',(-62.4592044390545,-122.250225466238,
179.142400961866));
#42077=CARTESIAN_POINT('Ctrl Pts',(-63.7694119837035,-122.204829817177,
178.124928361964));
#42078=CARTESIAN_POINT('Ctrl Pts',(-63.9833714542736,-122.276301536731,
176.48082732954));
#42079=CARTESIAN_POINT('Ctrl Pts',(-64.1973309248437,-122.347773256285,
174.836726297116));
#42080=CARTESIAN_POINT('Ctrl Pts',(-63.1955293477461,-122.548853225892,
173.529088919052));
#42081=CARTESIAN_POINT('Ctrl Pts',(-62.1937277706486,-122.749933195498,
172.221451540989));
#42082=CARTESIAN_POINT('Ctrl Pts',(-60.5688285054134,-123.01743954151,172.016274058689));
#42083=CARTESIAN_POINT('Ctrl Pts',(-58.9439292401782,-123.284945887522,
171.81109657639));
#42084=CARTESIAN_POINT('Ctrl Pts',(-57.6535978213633,-123.516785065893,
172.828569176292));
#42085=CARTESIAN_POINT('Ctrl Pts',(-56.3632664025483,-123.748624244264,
173.846041776195));
#42086=CARTESIAN_POINT('Ctrl Pts',(-56.1691830578122,-123.86359605402,175.490142808619));
#42087=CARTESIAN_POINT('Ctrl Pts',(-55.9750997130761,-123.978567863777,
177.134243841043));
#42088=CARTESIAN_POINT('Ctrl Pts',(-56.9967774160077,-123.963931423481,
178.441881219107));
#42089=CARTESIAN_POINT('Ctrl Pts',(-58.0184551189394,-123.949294983185,
179.74951859717));
#42090=CARTESIAN_POINT('Ctrl Pts',(-59.6632305100085,-123.868232166484,
179.954696079469));
#42091=CARTESIAN_POINT('Ctrl Pts',(-61.3080059010777,-123.787169349783,
180.159873561769));
#42092=CARTESIAN_POINT('Ctrl Pts',(-62.6182134457268,-123.741773700723,
179.142400961866));
#42093=CARTESIAN_POINT('Ctrl Pts',(-63.9284209903758,-123.696378051663,
178.124928361964));
#42094=CARTESIAN_POINT('Ctrl Pts',(-64.1423804609459,-123.767849771217,
176.48082732954));
#42095=CARTESIAN_POINT('Ctrl Pts',(-64.3563399315159,-123.839321490771,
174.836726297116));
#42096=CARTESIAN_POINT('Ctrl Pts',(-63.3545383544184,-124.040401460378,
173.529088919052));
#42097=CARTESIAN_POINT('Ctrl Pts',(-62.3527367773208,-124.241481429984,
172.221451540989));
#42098=CARTESIAN_POINT('Ctrl Pts',(-60.7278375120856,-124.508987775996,
172.016274058689));
#42099=CARTESIAN_POINT('Ctrl Pts',(-59.1029382468505,-124.776494122007,
171.81109657639));
#42100=CARTESIAN_POINT('Ctrl Pts',(-57.8126068280355,-125.008333300378,
172.828569176292));
#42101=CARTESIAN_POINT('Ctrl Pts',(-56.5222754092205,-125.240172478749,
173.846041776195));
#42102=CARTESIAN_POINT('Ctrl Pts',(-56.3281920644844,-125.355144288506,
175.490142808619));
#42103=CARTESIAN_POINT('Ctrl Pts',(-56.1341087197484,-125.470116098263,
177.134243841043));
#42104=CARTESIAN_POINT('Ctrl Pts',(-57.15578642268,-125.455479657967,178.441881219107));
#42105=CARTESIAN_POINT('Ctrl Pts',(-58.1774641256116,-125.440843217671,
179.74951859717));
#42106=CARTESIAN_POINT('Ctrl Pts',(-59.8222395166808,-125.35978040097,179.954696079469));
#42107=CARTESIAN_POINT('Ctrl Pts',(-61.46701490775,-125.278717584269,180.159873561769));
#42108=CARTESIAN_POINT('Ctrl Pts',(-62.777222452399,-125.233321935209,179.142400961866));
#42109=CARTESIAN_POINT('Ctrl Pts',(-64.087429997048,-125.187926286149,178.124928361964));
#42110=CARTESIAN_POINT('Ctrl Pts',(-64.3013894676181,-125.259398005703,
176.48082732954));
#42111=CARTESIAN_POINT('Ctrl Pts',(-64.5153489381882,-125.330869725257,
174.836726297116));
#42112=CARTESIAN_POINT('Ctrl Pts',(-63.5135473610906,-125.531949694863,
173.529088919052));
#42113=CARTESIAN_POINT('Ctrl Pts',(-62.511745783993,-125.73302966447,172.221451540989));
#42114=CARTESIAN_POINT('Ctrl Pts',(-60.8868465187579,-126.000536010481,
172.016274058689));
#42115=CARTESIAN_POINT('Ctrl Pts',(-59.2619472535227,-126.268042356493,
171.81109657639));
#42116=CARTESIAN_POINT('Ctrl Pts',(-57.9716158347077,-126.499881534864,
172.828569176292));
#42117=CARTESIAN_POINT('Ctrl Pts',(-56.6812844158927,-126.731720713235,
173.846041776195));
#42118=CARTESIAN_POINT('Ctrl Pts',(-56.4872010711566,-126.846692522992,
175.490142808619));
#42119=CARTESIAN_POINT('Ctrl Pts',(-56.2931177264206,-126.961664332748,
177.134243841043));
#42120=CARTESIAN_POINT('Ctrl Pts',(-57.3147954293522,-126.947027892452,
178.441881219107));
#42121=CARTESIAN_POINT('Ctrl Pts',(-58.3364731322838,-126.932391452157,
179.74951859717));
#42122=CARTESIAN_POINT('Ctrl Pts',(-59.981248523353,-126.851328635456,179.954696079469));
#42123=CARTESIAN_POINT('Ctrl Pts',(-61.6260239144222,-126.770265818755,
180.159873561769));
#42124=CARTESIAN_POINT('Ctrl Pts',(-62.9362314590712,-126.724870169694,
179.142400961866));
#42125=CARTESIAN_POINT('Ctrl Pts',(-64.2464390037202,-126.679474520634,
178.124928361964));
#42126=CARTESIAN_POINT('Ctrl Pts',(-64.4603984742903,-126.750946240188,
176.48082732954));
#42127=CARTESIAN_POINT('Ctrl Pts',(-64.6743579448604,-126.822417959742,
174.836726297116));
#42128=CARTESIAN_POINT('Ctrl Pts',(-63.6725563677628,-127.023497929349,
173.529088919052));
#42129=CARTESIAN_POINT('Ctrl Pts',(-62.6707547906653,-127.224577898955,
172.221451540989));
#42130=CARTESIAN_POINT('Ctrl Pts',(-61.0458555254301,-127.492084244967,
172.016274058689));
#42131=CARTESIAN_POINT('Ctrl Pts',(-59.4209562601949,-127.759590590979,
171.81109657639));
#42132=CARTESIAN_POINT('Ctrl Pts',(-58.1306248413799,-127.99142976935,172.828569176292));
#42133=CARTESIAN_POINT('Ctrl Pts',(-56.8402934225649,-128.223268947721,
173.846041776195));
#42134=CARTESIAN_POINT('Ctrl Pts',(-56.6462100778289,-128.338240757477,
175.490142808619));
#42135=CARTESIAN_POINT('Ctrl Pts',(-56.4521267330928,-128.453212567234,
177.134243841043));
#42136=CARTESIAN_POINT('Ctrl Pts',(-57.4738044360244,-128.438576126938,
178.441881219107));
#42137=CARTESIAN_POINT('Ctrl Pts',(-58.495482138956,-128.423939686642,179.74951859717));
#42138=CARTESIAN_POINT('Ctrl Pts',(-60.1402575300252,-128.342876869941,
179.954696079469));
#42139=CARTESIAN_POINT('Ctrl Pts',(-61.7850329210944,-128.26181405324,180.159873561769));
#42140=CARTESIAN_POINT('Ctrl Pts',(-63.0952404657434,-128.21641840418,179.142400961866));
#42141=CARTESIAN_POINT('Ctrl Pts',(-64.4054480103925,-128.17102275512,178.124928361964));
#42142=CARTESIAN_POINT('Ctrl Pts',(-64.6194074809625,-128.242494474674,
176.48082732954));
#42143=CARTESIAN_POINT('Ctrl Pts',(-64.8333669515326,-128.313966194228,
174.836726297116));
#42144=CARTESIAN_POINT('Ctrl Pts',(-63.831565374435,-128.515046163834,173.529088919052));
#42145=CARTESIAN_POINT('Ctrl Pts',(-62.8297637973375,-128.716126133441,
172.221451540989));
#42146=CARTESIAN_POINT('Ctrl Pts',(-61.2048645321023,-128.983632479453,
172.016274058689));
#42147=CARTESIAN_POINT('Ctrl Pts',(-59.5799652668672,-129.251138825464,
171.81109657639));
#42148=CARTESIAN_POINT('Ctrl Pts',(-58.2896338480522,-129.482978003835,
172.828569176292));
#42149=CARTESIAN_POINT('Ctrl Pts',(-56.9993024292372,-129.714817182206,
173.846041776195));
#42150=CARTESIAN_POINT('Ctrl Pts',(-56.8052190845011,-129.829788991963,
175.490142808619));
#42151=CARTESIAN_POINT('Ctrl Pts',(-56.611135739765,-129.944760801719,177.134243841043));
#42152=CARTESIAN_POINT('Ctrl Pts',(-57.6328134426967,-129.930124361424,
178.441881219107));
#42153=CARTESIAN_POINT('Ctrl Pts',(-58.6544911456282,-129.915487921128,
179.74951859717));
#42154=CARTESIAN_POINT('Ctrl Pts',(-60.2992665366974,-129.834425104427,
179.954696079469));
#42155=CARTESIAN_POINT('Ctrl Pts',(-61.9440419277666,-129.753362287726,
180.159873561769));
#42156=CARTESIAN_POINT('Ctrl Pts',(-63.2542494724157,-129.707966638666,
179.142400961866));
#42157=CARTESIAN_POINT('Ctrl Pts',(-64.5644570170647,-129.662570989605,
178.124928361964));
#42158=CARTESIAN_POINT('Ctrl Pts',(-64.7784164876348,-129.734042709159,
176.48082732954));
#42159=CARTESIAN_POINT('Ctrl Pts',(-64.9923759582049,-129.805514428714,
174.836726297116));
#42160=CARTESIAN_POINT('Ctrl Pts',(-63.9905743811073,-130.00659439832,173.529088919052));
#42161=CARTESIAN_POINT('Ctrl Pts',(-62.9887728040097,-130.207674367926,
172.221451540989));
#42162=CARTESIAN_POINT('Ctrl Pts',(-61.3638735387746,-130.475180713938,
172.016274058689));
#42163=CARTESIAN_POINT('Ctrl Pts',(-59.7389742735394,-130.74268705995,171.81109657639));
#42164=CARTESIAN_POINT('Ctrl Pts',(-58.4486428547244,-130.974526238321,
172.828569176292));
#42165=CARTESIAN_POINT('Ctrl Pts',(-57.1583114359094,-131.206365416692,
173.846041776195));
#42166=CARTESIAN_POINT('Ctrl Pts',(-56.9642280911733,-131.321337226448,
175.490142808619));
#42167=CARTESIAN_POINT('Ctrl Pts',(-56.7701447464373,-131.436309036205,
177.134243841043));
#42168=CARTESIAN_POINT('Ctrl Pts',(-57.7918224493689,-131.421672595909,
178.441881219107));
#42169=CARTESIAN_POINT('Ctrl Pts',(-58.8135001523005,-131.407036155613,
179.74951859717));
#42170=CARTESIAN_POINT('Ctrl Pts',(-60.4582755433697,-131.325973338912,
179.954696079469));
#42171=CARTESIAN_POINT('Ctrl Pts',(-61.5222352836034,-131.273536043299,
180.087419721831));
#42172=CARTESIAN_POINT('Ctrl Pts',(-62.5109753341386,-131.233577943711,
179.670610857428));
#42173=CARTESIAN_POINT('Ctrl Pts',(-50.1237974946936,-67.3522581446913,
175.487549340184));
#42174=CARTESIAN_POINT('Ctrl Pts',(-49.9286459530297,-67.4673438313769,
177.140258408853));
#42175=CARTESIAN_POINT('Ctrl Pts',(-50.9556208313297,-67.452142676797,178.454742197037));
#42176=CARTESIAN_POINT('Ctrl Pts',(-51.9825957096297,-67.4369415222171,
179.76922598522));
#42177=CARTESIAN_POINT('Ctrl Pts',(-53.6359306348749,-67.3549662019876,
179.975477717318));
#42178=CARTESIAN_POINT('Ctrl Pts',(-55.2892655601202,-67.272990881758,180.181729449417));
#42179=CARTESIAN_POINT('Ctrl Pts',(-56.6062809387202,-67.2268694721162,
179.158929658031));
#42180=CARTESIAN_POINT('Ctrl Pts',(-57.9232963173202,-67.1807480624744,
178.136129866644));
#42181=CARTESIAN_POINT('Ctrl Pts',(-58.1383239848182,-67.2521059050995,
176.483420797975));
#42182=CARTESIAN_POINT('Ctrl Pts',(-58.3533516523161,-67.3234637477245,
174.830711729305));
#42183=CARTESIAN_POINT('Ctrl Pts',(-57.3462528998501,-67.5251084316151,
173.516227941122));
#42184=CARTESIAN_POINT('Ctrl Pts',(-56.3391541473842,-67.7267531155057,
172.201744152939));
#42185=CARTESIAN_POINT('Ctrl Pts',(-54.705695347973,-67.995171965046,171.99549242084));
#42186=CARTESIAN_POINT('Ctrl Pts',(-53.0722365485618,-68.2635908145862,
171.789240688742));
#42187=CARTESIAN_POINT('Ctrl Pts',(-51.7750972957957,-68.4961557535387,
172.812040480128));
#42188=CARTESIAN_POINT('Ctrl Pts',(-50.4779580430297,-68.7287206924912,
173.834840271514));
#42189=CARTESIAN_POINT('Ctrl Pts',(-50.2828065013658,-68.8438063791769,
175.487549340184));
#42190=CARTESIAN_POINT('Ctrl Pts',(-50.0876549597019,-68.9588920658625,
177.140258408853));
#42191=CARTESIAN_POINT('Ctrl Pts',(-51.1146298380019,-68.9436909112826,
178.454742197037));
#42192=CARTESIAN_POINT('Ctrl Pts',(-52.1416047163019,-68.9284897567027,
179.76922598522));
#42193=CARTESIAN_POINT('Ctrl Pts',(-53.7949396415471,-68.8465144364732,
179.975477717318));
#42194=CARTESIAN_POINT('Ctrl Pts',(-55.4482745667924,-68.7645391162437,
180.181729449417));
#42195=CARTESIAN_POINT('Ctrl Pts',(-56.7652899453924,-68.7184177066018,
179.158929658031));
#42196=CARTESIAN_POINT('Ctrl Pts',(-58.0823053239925,-68.67229629696,178.136129866644));
#42197=CARTESIAN_POINT('Ctrl Pts',(-58.2973329914904,-68.7436541395851,
176.483420797975));
#42198=CARTESIAN_POINT('Ctrl Pts',(-58.5123606589883,-68.8150119822101,
174.830711729305));
#42199=CARTESIAN_POINT('Ctrl Pts',(-57.5052619065224,-69.0166566661007,
173.516227941122));
#42200=CARTESIAN_POINT('Ctrl Pts',(-56.4981631540564,-69.2183013499913,
172.201744152939));
#42201=CARTESIAN_POINT('Ctrl Pts',(-54.8647043546452,-69.4867201995316,
171.99549242084));
#42202=CARTESIAN_POINT('Ctrl Pts',(-53.231245555234,-69.7551390490718,171.789240688742));
#42203=CARTESIAN_POINT('Ctrl Pts',(-51.934106302468,-69.9877039880243,172.812040480128));
#42204=CARTESIAN_POINT('Ctrl Pts',(-50.636967049702,-70.2202689269768,173.834840271514));
#42205=CARTESIAN_POINT('Ctrl Pts',(-50.4418155080381,-70.3353546136625,
175.487549340184));
#42206=CARTESIAN_POINT('Ctrl Pts',(-50.2466639663742,-70.4504403003481,
177.140258408853));
#42207=CARTESIAN_POINT('Ctrl Pts',(-51.2736388446741,-70.4352391457682,
178.454742197037));
#42208=CARTESIAN_POINT('Ctrl Pts',(-52.3006137229741,-70.4200379911883,
179.76922598522));
#42209=CARTESIAN_POINT('Ctrl Pts',(-53.9539486482194,-70.3380626709587,
179.975477717318));
#42210=CARTESIAN_POINT('Ctrl Pts',(-55.6072835734646,-70.2560873507292,
180.181729449417));
#42211=CARTESIAN_POINT('Ctrl Pts',(-56.9242989520647,-70.2099659410874,
179.158929658031));
#42212=CARTESIAN_POINT('Ctrl Pts',(-58.2413143306647,-70.1638445314456,
178.136129866644));
#42213=CARTESIAN_POINT('Ctrl Pts',(-58.4563419981626,-70.2352023740707,
176.483420797975));
#42214=CARTESIAN_POINT('Ctrl Pts',(-58.6713696656605,-70.3065602166957,
174.830711729305));
#42215=CARTESIAN_POINT('Ctrl Pts',(-57.6642709131946,-70.5082049005863,
173.516227941122));
#42216=CARTESIAN_POINT('Ctrl Pts',(-56.6571721607287,-70.7098495844769,
172.201744152939));
#42217=CARTESIAN_POINT('Ctrl Pts',(-55.0237133613174,-70.9782684340172,
171.99549242084));
#42218=CARTESIAN_POINT('Ctrl Pts',(-53.3902545619062,-71.2466872835574,
171.789240688742));
#42219=CARTESIAN_POINT('Ctrl Pts',(-52.0931153091402,-71.4792522225099,
172.812040480128));
#42220=CARTESIAN_POINT('Ctrl Pts',(-50.7959760563742,-71.7118171614624,
173.834840271514));
#42221=CARTESIAN_POINT('Ctrl Pts',(-50.6008245147103,-71.8269028481481,
175.487549340184));
#42222=CARTESIAN_POINT('Ctrl Pts',(-50.4056729730464,-71.9419885348337,
177.140258408853));
#42223=CARTESIAN_POINT('Ctrl Pts',(-51.4326478513464,-71.9267873802538,
178.454742197037));
#42224=CARTESIAN_POINT('Ctrl Pts',(-52.4596227296463,-71.9115862256739,
179.76922598522));
#42225=CARTESIAN_POINT('Ctrl Pts',(-54.1129576548916,-71.8296109054444,
179.975477717318));
#42226=CARTESIAN_POINT('Ctrl Pts',(-55.7662925801368,-71.7476355852148,
180.181729449417));
#42227=CARTESIAN_POINT('Ctrl Pts',(-57.0833079587369,-71.701514175573,179.158929658031));
#42228=CARTESIAN_POINT('Ctrl Pts',(-58.4003233373369,-71.6553927659312,
178.136129866644));
#42229=CARTESIAN_POINT('Ctrl Pts',(-58.6153510048348,-71.7267506085562,
176.483420797975));
#42230=CARTESIAN_POINT('Ctrl Pts',(-58.8303786723328,-71.7981084511813,
174.830711729305));
#42231=CARTESIAN_POINT('Ctrl Pts',(-57.8232799198668,-71.9997531350719,
173.516227941122));
#42232=CARTESIAN_POINT('Ctrl Pts',(-56.8161811674009,-72.2013978189625,
172.201744152939));
#42233=CARTESIAN_POINT('Ctrl Pts',(-55.1827223679897,-72.4698166685028,
171.99549242084));
#42234=CARTESIAN_POINT('Ctrl Pts',(-53.5492635685784,-72.738235518043,171.789240688742));
#42235=CARTESIAN_POINT('Ctrl Pts',(-52.2521243158124,-72.9708004569955,
172.812040480128));
#42236=CARTESIAN_POINT('Ctrl Pts',(-50.9549850630464,-73.203365395948,173.834840271514));
#42237=CARTESIAN_POINT('Ctrl Pts',(-50.7598335213825,-73.3184510826337,
175.487549340184));
#42238=CARTESIAN_POINT('Ctrl Pts',(-50.5646819797186,-73.4335367693193,
177.140258408853));
#42239=CARTESIAN_POINT('Ctrl Pts',(-51.5916568580186,-73.4183356147394,
178.454742197037));
#42240=CARTESIAN_POINT('Ctrl Pts',(-52.6186317363186,-73.4031344601595,
179.76922598522));
#42241=CARTESIAN_POINT('Ctrl Pts',(-54.2719666615638,-73.32115913993,179.975477717318));
#42242=CARTESIAN_POINT('Ctrl Pts',(-55.9253015868091,-73.2391838197004,
180.181729449417));
#42243=CARTESIAN_POINT('Ctrl Pts',(-57.2423169654091,-73.1930624100586,
179.158929658031));
#42244=CARTESIAN_POINT('Ctrl Pts',(-58.5593323440091,-73.1469410004168,
178.136129866644));
#42245=CARTESIAN_POINT('Ctrl Pts',(-58.7743600115071,-73.2182988430419,
176.483420797975));
#42246=CARTESIAN_POINT('Ctrl Pts',(-58.989387679005,-73.2896566856669,174.830711729305));
#42247=CARTESIAN_POINT('Ctrl Pts',(-57.9822889265391,-73.4913013695575,
173.516227941122));
#42248=CARTESIAN_POINT('Ctrl Pts',(-56.9751901740731,-73.6929460534481,
172.201744152939));
#42249=CARTESIAN_POINT('Ctrl Pts',(-55.3417313746619,-73.9613649029884,
171.99549242084));
#42250=CARTESIAN_POINT('Ctrl Pts',(-53.7082725752507,-74.2297837525286,
171.789240688742));
#42251=CARTESIAN_POINT('Ctrl Pts',(-52.4111333224846,-74.4623486914811,
172.812040480128));
#42252=CARTESIAN_POINT('Ctrl Pts',(-51.1139940697186,-74.6949136304336,
173.834840271514));
#42253=CARTESIAN_POINT('Ctrl Pts',(-50.9188425280547,-74.8099993171193,
175.487549340184));
#42254=CARTESIAN_POINT('Ctrl Pts',(-50.7236909863908,-74.9250850038049,
177.140258408853));
#42255=CARTESIAN_POINT('Ctrl Pts',(-51.7506658646908,-74.909883849225,178.454742197037));
#42256=CARTESIAN_POINT('Ctrl Pts',(-52.7776407429908,-74.8946826946451,
179.76922598522));
#42257=CARTESIAN_POINT('Ctrl Pts',(-54.430975668236,-74.8127073744155,179.975477717318));
#42258=CARTESIAN_POINT('Ctrl Pts',(-56.0843105934813,-74.730732054186,180.181729449417));
#42259=CARTESIAN_POINT('Ctrl Pts',(-57.4013259720813,-74.6846106445442,
179.158929658031));
#42260=CARTESIAN_POINT('Ctrl Pts',(-58.7183413506814,-74.6384892349024,
178.136129866644));
#42261=CARTESIAN_POINT('Ctrl Pts',(-58.9333690181793,-74.7098470775275,
176.483420797975));
#42262=CARTESIAN_POINT('Ctrl Pts',(-59.1483966856772,-74.7812049201525,
174.830711729305));
#42263=CARTESIAN_POINT('Ctrl Pts',(-58.1412979332113,-74.9828496040431,
173.516227941122));
#42264=CARTESIAN_POINT('Ctrl Pts',(-57.1341991807453,-75.1844942879338,
172.201744152939));
#42265=CARTESIAN_POINT('Ctrl Pts',(-55.5007403813341,-75.452913137474,171.99549242084));
#42266=CARTESIAN_POINT('Ctrl Pts',(-53.8672815819229,-75.7213319870142,
171.789240688742));
#42267=CARTESIAN_POINT('Ctrl Pts',(-52.5701423291569,-75.9538969259667,
172.812040480128));
#42268=CARTESIAN_POINT('Ctrl Pts',(-51.2730030763909,-76.1864618649192,
173.834840271514));
#42269=CARTESIAN_POINT('Ctrl Pts',(-51.077851534727,-76.3015475516049,175.487549340184));
#42270=CARTESIAN_POINT('Ctrl Pts',(-50.8826999930631,-76.4166332382905,
177.140258408853));
#42271=CARTESIAN_POINT('Ctrl Pts',(-51.9096748713631,-76.4014320837106,
178.454742197037));
#42272=CARTESIAN_POINT('Ctrl Pts',(-52.936649749663,-76.3862309291307,179.76922598522));
#42273=CARTESIAN_POINT('Ctrl Pts',(-54.5899846749083,-76.3042556089012,
179.975477717318));
#42274=CARTESIAN_POINT('Ctrl Pts',(-56.2433196001535,-76.2222802886716,
180.181729449417));
#42275=CARTESIAN_POINT('Ctrl Pts',(-57.5603349787536,-76.1761588790298,
179.158929658031));
#42276=CARTESIAN_POINT('Ctrl Pts',(-58.8773503573536,-76.130037469388,178.136129866644));
#42277=CARTESIAN_POINT('Ctrl Pts',(-59.0923780248515,-76.2013953120131,
176.483420797975));
#42278=CARTESIAN_POINT('Ctrl Pts',(-59.3074056923495,-76.2727531546381,
174.830711729305));
#42279=CARTESIAN_POINT('Ctrl Pts',(-58.3003069398835,-76.4743978385287,
173.516227941122));
#42280=CARTESIAN_POINT('Ctrl Pts',(-57.2932081874176,-76.6760425224193,
172.201744152939));
#42281=CARTESIAN_POINT('Ctrl Pts',(-55.6597493880063,-76.9444613719596,
171.99549242084));
#42282=CARTESIAN_POINT('Ctrl Pts',(-54.0262905885951,-77.2128802214998,
171.789240688742));
#42283=CARTESIAN_POINT('Ctrl Pts',(-52.7291513358291,-77.4454451604523,
172.812040480128));
#42284=CARTESIAN_POINT('Ctrl Pts',(-51.4320120830631,-77.6780100994048,
173.834840271514));
#42285=CARTESIAN_POINT('Ctrl Pts',(-51.2368605413992,-77.7930957860905,
175.487549340184));
#42286=CARTESIAN_POINT('Ctrl Pts',(-51.0417089997353,-77.9081814727761,
177.140258408853));
#42287=CARTESIAN_POINT('Ctrl Pts',(-52.0686838780353,-77.8929803181962,
178.454742197037));
#42288=CARTESIAN_POINT('Ctrl Pts',(-53.0956587563352,-77.8777791636163,
179.76922598522));
#42289=CARTESIAN_POINT('Ctrl Pts',(-54.7489936815805,-77.7958038433868,
179.975477717318));
#42290=CARTESIAN_POINT('Ctrl Pts',(-56.4023286068258,-77.7138285231572,
180.181729449417));
#42291=CARTESIAN_POINT('Ctrl Pts',(-57.7193439854258,-77.6677071135154,
179.158929658031));
#42292=CARTESIAN_POINT('Ctrl Pts',(-59.0363593640258,-77.6215857038736,
178.136129866644));
#42293=CARTESIAN_POINT('Ctrl Pts',(-59.2513870315238,-77.6929435464986,
176.483420797975));
#42294=CARTESIAN_POINT('Ctrl Pts',(-59.4664146990217,-77.7643013891237,
174.830711729305));
#42295=CARTESIAN_POINT('Ctrl Pts',(-58.4593159465557,-77.9659460730143,
173.516227941122));
#42296=CARTESIAN_POINT('Ctrl Pts',(-57.4522171940898,-78.167590756905,172.201744152939));
#42297=CARTESIAN_POINT('Ctrl Pts',(-55.8187583946786,-78.4360096064452,
171.99549242084));
#42298=CARTESIAN_POINT('Ctrl Pts',(-54.1852995952674,-78.7044284559854,
171.789240688742));
#42299=CARTESIAN_POINT('Ctrl Pts',(-52.8881603425013,-78.9369933949379,
172.812040480128));
#42300=CARTESIAN_POINT('Ctrl Pts',(-51.5910210897353,-79.1695583338904,
173.834840271514));
#42301=CARTESIAN_POINT('Ctrl Pts',(-51.3958695480714,-79.2846440205761,
175.487549340184));
#42302=CARTESIAN_POINT('Ctrl Pts',(-51.2007180064075,-79.3997297072617,
177.140258408853));
#42303=CARTESIAN_POINT('Ctrl Pts',(-52.2276928847075,-79.3845285526818,
178.454742197037));
#42304=CARTESIAN_POINT('Ctrl Pts',(-53.2546677630075,-79.3693273981019,
179.76922598522));
#42305=CARTESIAN_POINT('Ctrl Pts',(-54.9080026882527,-79.2873520778724,
179.975477717318));
#42306=CARTESIAN_POINT('Ctrl Pts',(-56.561337613498,-79.2053767576428,180.181729449417));
#42307=CARTESIAN_POINT('Ctrl Pts',(-57.878352992098,-79.159255348001,179.158929658031));
#42308=CARTESIAN_POINT('Ctrl Pts',(-59.1953683706981,-79.1131339383592,
178.136129866644));
#42309=CARTESIAN_POINT('Ctrl Pts',(-59.410396038196,-79.1844917809843,176.483420797975));
#42310=CARTESIAN_POINT('Ctrl Pts',(-59.6254237056939,-79.2558496236093,
174.830711729305));
#42311=CARTESIAN_POINT('Ctrl Pts',(-58.618324953228,-79.4574943074999,173.516227941122));
#42312=CARTESIAN_POINT('Ctrl Pts',(-57.611226200762,-79.6591389913905,172.201744152939));
#42313=CARTESIAN_POINT('Ctrl Pts',(-55.9777674013508,-79.9275578409308,
171.99549242084));
#42314=CARTESIAN_POINT('Ctrl Pts',(-54.3443086019396,-80.195976690471,171.789240688742));
#42315=CARTESIAN_POINT('Ctrl Pts',(-53.0471693491736,-80.4285416294235,
172.812040480128));
#42316=CARTESIAN_POINT('Ctrl Pts',(-51.7500300964075,-80.6611065683761,
173.834840271514));
#42317=CARTESIAN_POINT('Ctrl Pts',(-51.5548785547437,-80.7761922550617,
175.487549340184));
#42318=CARTESIAN_POINT('Ctrl Pts',(-51.3597270130797,-80.8912779417473,
177.140258408853));
#42319=CARTESIAN_POINT('Ctrl Pts',(-52.3867018913797,-80.8760767871674,
178.454742197037));
#42320=CARTESIAN_POINT('Ctrl Pts',(-53.4136767696797,-80.8608756325875,
179.76922598522));
#42321=CARTESIAN_POINT('Ctrl Pts',(-55.067011694925,-80.778900312358,179.975477717318));
#42322=CARTESIAN_POINT('Ctrl Pts',(-56.7203466201702,-80.6969249921285,
180.181729449417));
#42323=CARTESIAN_POINT('Ctrl Pts',(-58.0373619987702,-80.6508035824866,
179.158929658031));
#42324=CARTESIAN_POINT('Ctrl Pts',(-59.3543773773703,-80.6046821728448,
178.136129866644));
#42325=CARTESIAN_POINT('Ctrl Pts',(-59.5694050448682,-80.6760400154699,
176.483420797975));
#42326=CARTESIAN_POINT('Ctrl Pts',(-59.7844327123661,-80.7473978580949,
174.830711729305));
#42327=CARTESIAN_POINT('Ctrl Pts',(-58.7773339599002,-80.9490425419855,
173.516227941122));
#42328=CARTESIAN_POINT('Ctrl Pts',(-57.7702352074343,-81.1506872258762,
172.201744152939));
#42329=CARTESIAN_POINT('Ctrl Pts',(-56.136776408023,-81.4191060754164,171.99549242084));
#42330=CARTESIAN_POINT('Ctrl Pts',(-54.5033176086118,-81.6875249249566,
171.789240688742));
#42331=CARTESIAN_POINT('Ctrl Pts',(-53.2061783558458,-81.9200898639091,
172.812040480128));
#42332=CARTESIAN_POINT('Ctrl Pts',(-51.9090391030798,-82.1526548028617,
173.834840271514));
#42333=CARTESIAN_POINT('Ctrl Pts',(-51.7138875614159,-82.2677404895473,
175.487549340184));
#42334=CARTESIAN_POINT('Ctrl Pts',(-51.518736019752,-82.382826176233,177.140258408853));
#42335=CARTESIAN_POINT('Ctrl Pts',(-52.545710898052,-82.367625021653,178.454742197037));
#42336=CARTESIAN_POINT('Ctrl Pts',(-53.5726857763519,-82.3524238670731,
179.76922598522));
#42337=CARTESIAN_POINT('Ctrl Pts',(-55.2260207015972,-82.2704485468436,
179.975477717318));
#42338=CARTESIAN_POINT('Ctrl Pts',(-56.8793556268424,-82.188473226614,180.181729449417));
#42339=CARTESIAN_POINT('Ctrl Pts',(-58.1963710054425,-82.1423518169722,
179.158929658031));
#42340=CARTESIAN_POINT('Ctrl Pts',(-59.5133863840425,-82.0962304073304,
178.136129866644));
#42341=CARTESIAN_POINT('Ctrl Pts',(-59.7284140515404,-82.1675882499554,
176.483420797975));
#42342=CARTESIAN_POINT('Ctrl Pts',(-59.9434417190384,-82.2389460925805,
174.830711729305));
#42343=CARTESIAN_POINT('Ctrl Pts',(-58.9363429665724,-82.4405907764711,
173.516227941122));
#42344=CARTESIAN_POINT('Ctrl Pts',(-57.9292442141065,-82.6422354603618,
172.201744152939));
#42345=CARTESIAN_POINT('Ctrl Pts',(-56.2957854146952,-82.910654309902,171.99549242084));
#42346=CARTESIAN_POINT('Ctrl Pts',(-54.662326615284,-83.1790731594422,171.789240688742));
#42347=CARTESIAN_POINT('Ctrl Pts',(-53.365187362518,-83.4116380983947,172.812040480128));
#42348=CARTESIAN_POINT('Ctrl Pts',(-52.068048109752,-83.6442030373472,173.834840271514));
#42349=CARTESIAN_POINT('Ctrl Pts',(-51.8728965680881,-83.7592887240329,
175.487549340184));
#42350=CARTESIAN_POINT('Ctrl Pts',(-51.6777450264242,-83.8743744107186,
177.140258408853));
#42351=CARTESIAN_POINT('Ctrl Pts',(-52.7047199047242,-83.8591732561386,
178.454742197037));
#42352=CARTESIAN_POINT('Ctrl Pts',(-53.7316947830242,-83.8439721015587,
179.76922598522));
#42353=CARTESIAN_POINT('Ctrl Pts',(-55.3850297082694,-83.7619967813292,
179.975477717318));
#42354=CARTESIAN_POINT('Ctrl Pts',(-57.0383646335147,-83.6800214610996,
180.181729449417));
#42355=CARTESIAN_POINT('Ctrl Pts',(-58.3553800121147,-83.6339000514578,
179.158929658031));
#42356=CARTESIAN_POINT('Ctrl Pts',(-59.6723953907147,-83.587778641816,178.136129866644));
#42357=CARTESIAN_POINT('Ctrl Pts',(-59.8874230582127,-83.6591364844411,
176.483420797975));
#42358=CARTESIAN_POINT('Ctrl Pts',(-60.1024507257106,-83.7304943270661,
174.830711729305));
#42359=CARTESIAN_POINT('Ctrl Pts',(-59.0953519732446,-83.9321390109568,
173.516227941122));
#42360=CARTESIAN_POINT('Ctrl Pts',(-58.0882532207787,-84.1337836948473,
172.201744152939));
#42361=CARTESIAN_POINT('Ctrl Pts',(-56.4547944213675,-84.4022025443876,
171.99549242084));
#42362=CARTESIAN_POINT('Ctrl Pts',(-54.8213356219563,-84.6706213939278,
171.789240688742));
#42363=CARTESIAN_POINT('Ctrl Pts',(-53.5241963691902,-84.9031863328803,
172.812040480128));
#42364=CARTESIAN_POINT('Ctrl Pts',(-52.2270571164242,-85.1357512718329,
173.834840271514));
#42365=CARTESIAN_POINT('Ctrl Pts',(-52.0319055747603,-85.2508369585185,
175.487549340184));
#42366=CARTESIAN_POINT('Ctrl Pts',(-51.8367540330964,-85.3659226452041,
177.140258408853));
#42367=CARTESIAN_POINT('Ctrl Pts',(-52.8637289113964,-85.3507214906242,
178.454742197037));
#42368=CARTESIAN_POINT('Ctrl Pts',(-53.8907037896964,-85.3355203360443,
179.76922598522));
#42369=CARTESIAN_POINT('Ctrl Pts',(-55.5440387149416,-85.2535450158148,
179.975477717318));
#42370=CARTESIAN_POINT('Ctrl Pts',(-57.1973736401869,-85.1715696955852,
180.181729449417));
#42371=CARTESIAN_POINT('Ctrl Pts',(-58.5143890187869,-85.1254482859434,
179.158929658031));
#42372=CARTESIAN_POINT('Ctrl Pts',(-59.831404397387,-85.0793268763016,178.136129866644));
#42373=CARTESIAN_POINT('Ctrl Pts',(-60.0464320648849,-85.1506847189267,
176.483420797975));
#42374=CARTESIAN_POINT('Ctrl Pts',(-60.2614597323828,-85.2220425615517,
174.830711729305));
#42375=CARTESIAN_POINT('Ctrl Pts',(-59.2543609799169,-85.4236872454423,
173.516227941122));
#42376=CARTESIAN_POINT('Ctrl Pts',(-58.2472622274509,-85.6253319293329,
172.201744152939));
#42377=CARTESIAN_POINT('Ctrl Pts',(-56.6138034280397,-85.8937507788732,
171.99549242084));
#42378=CARTESIAN_POINT('Ctrl Pts',(-54.9803446286285,-86.1621696284134,
171.789240688742));
#42379=CARTESIAN_POINT('Ctrl Pts',(-53.6832053758625,-86.3947345673659,
172.812040480128));
#42380=CARTESIAN_POINT('Ctrl Pts',(-52.3860661230965,-86.6272995063184,
173.834840271514));
#42381=CARTESIAN_POINT('Ctrl Pts',(-52.1909145814326,-86.7423851930041,
175.487549340184));
#42382=CARTESIAN_POINT('Ctrl Pts',(-51.9957630397687,-86.8574708796897,
177.140258408853));
#42383=CARTESIAN_POINT('Ctrl Pts',(-53.0227379180686,-86.8422697251098,
178.454742197037));
#42384=CARTESIAN_POINT('Ctrl Pts',(-54.0497127963686,-86.8270685705299,
179.76922598522));
#42385=CARTESIAN_POINT('Ctrl Pts',(-55.7030477216139,-86.7450932503004,
179.975477717318));
#42386=CARTESIAN_POINT('Ctrl Pts',(-57.3563826468591,-86.6631179300708,
180.181729449417));
#42387=CARTESIAN_POINT('Ctrl Pts',(-58.6733980254591,-86.616996520429,179.158929658031));
#42388=CARTESIAN_POINT('Ctrl Pts',(-59.9904134040592,-86.5708751107872,
178.136129866644));
#42389=CARTESIAN_POINT('Ctrl Pts',(-60.2054410715571,-86.6422329534122,
176.483420797975));
#42390=CARTESIAN_POINT('Ctrl Pts',(-60.4204687390551,-86.7135907960373,
174.830711729305));
#42391=CARTESIAN_POINT('Ctrl Pts',(-59.4133699865891,-86.9152354799279,
173.516227941122));
#42392=CARTESIAN_POINT('Ctrl Pts',(-58.4062712341232,-87.1168801638185,
172.201744152939));
#42393=CARTESIAN_POINT('Ctrl Pts',(-56.7728124347119,-87.3852990133588,
171.99549242084));
#42394=CARTESIAN_POINT('Ctrl Pts',(-55.1393536353007,-87.653717862899,171.789240688742));
#42395=CARTESIAN_POINT('Ctrl Pts',(-53.8422143825347,-87.8862828018515,
172.812040480128));
#42396=CARTESIAN_POINT('Ctrl Pts',(-52.5450751297687,-88.118847740804,173.834840271514));
#42397=CARTESIAN_POINT('Ctrl Pts',(-52.3499235881048,-88.2339334274897,
175.487549340184));
#42398=CARTESIAN_POINT('Ctrl Pts',(-52.1547720464409,-88.3490191141753,
177.140258408853));
#42399=CARTESIAN_POINT('Ctrl Pts',(-53.1817469247409,-88.3338179595954,
178.454742197037));
#42400=CARTESIAN_POINT('Ctrl Pts',(-54.2087218030408,-88.3186168050155,
179.76922598522));
#42401=CARTESIAN_POINT('Ctrl Pts',(-55.8620567282861,-88.236641484786,179.975477717318));
#42402=CARTESIAN_POINT('Ctrl Pts',(-57.5153916535314,-88.1546661645564,
180.181729449417));
#42403=CARTESIAN_POINT('Ctrl Pts',(-58.8324070321314,-88.1085447549146,
179.158929658031));
#42404=CARTESIAN_POINT('Ctrl Pts',(-60.1494224107314,-88.0624233452728,
178.136129866644));
#42405=CARTESIAN_POINT('Ctrl Pts',(-60.3644500782293,-88.1337811878979,
176.483420797975));
#42406=CARTESIAN_POINT('Ctrl Pts',(-60.5794777457273,-88.2051390305229,
174.830711729305));
#42407=CARTESIAN_POINT('Ctrl Pts',(-59.5723789932613,-88.4067837144135,
173.516227941122));
#42408=CARTESIAN_POINT('Ctrl Pts',(-58.5652802407954,-88.6084283983041,
172.201744152939));
#42409=CARTESIAN_POINT('Ctrl Pts',(-56.9318214413842,-88.8768472478444,
171.99549242084));
#42410=CARTESIAN_POINT('Ctrl Pts',(-55.2983626419729,-89.1452660973846,
171.789240688742));
#42411=CARTESIAN_POINT('Ctrl Pts',(-54.0012233892069,-89.3778310363371,
172.812040480128));
#42412=CARTESIAN_POINT('Ctrl Pts',(-52.7040841364409,-89.6103959752896,
173.834840271514));
#42413=CARTESIAN_POINT('Ctrl Pts',(-52.508932594777,-89.7254816619753,175.487549340184));
#42414=CARTESIAN_POINT('Ctrl Pts',(-52.3137810531131,-89.840567348661,177.140258408853));
#42415=CARTESIAN_POINT('Ctrl Pts',(-53.3407559314131,-89.825366194081,178.454742197037));
#42416=CARTESIAN_POINT('Ctrl Pts',(-54.3677308097131,-89.8101650395011,
179.76922598522));
#42417=CARTESIAN_POINT('Ctrl Pts',(-56.0210657349583,-89.7281897192716,
179.975477717318));
#42418=CARTESIAN_POINT('Ctrl Pts',(-57.6744006602036,-89.6462143990421,
180.181729449417));
#42419=CARTESIAN_POINT('Ctrl Pts',(-58.9914160388036,-89.6000929894002,
179.158929658031));
#42420=CARTESIAN_POINT('Ctrl Pts',(-60.3084314174037,-89.5539715797584,
178.136129866644));
#42421=CARTESIAN_POINT('Ctrl Pts',(-60.5234590849016,-89.6253294223835,
176.483420797975));
#42422=CARTESIAN_POINT('Ctrl Pts',(-60.7384867523995,-89.6966872650085,
174.830711729305));
#42423=CARTESIAN_POINT('Ctrl Pts',(-59.7313879999336,-89.8983319488991,
173.516227941122));
#42424=CARTESIAN_POINT('Ctrl Pts',(-58.7242892474676,-90.0999766327898,
172.201744152939));
#42425=CARTESIAN_POINT('Ctrl Pts',(-57.0908304480564,-90.36839548233,171.99549242084));
#42426=CARTESIAN_POINT('Ctrl Pts',(-55.4573716486452,-90.6368143318702,
171.789240688742));
#42427=CARTESIAN_POINT('Ctrl Pts',(-54.1602323958791,-90.8693792708227,
172.812040480128));
#42428=CARTESIAN_POINT('Ctrl Pts',(-52.8630931431131,-91.1019442097752,
173.834840271514));
#42429=CARTESIAN_POINT('Ctrl Pts',(-52.6679416014493,-91.2170298964609,
175.487549340184));
#42430=CARTESIAN_POINT('Ctrl Pts',(-52.4727900597853,-91.3321155831465,
177.140258408853));
#42431=CARTESIAN_POINT('Ctrl Pts',(-53.4997649380853,-91.3169144285666,
178.454742197037));
#42432=CARTESIAN_POINT('Ctrl Pts',(-54.5267398163853,-91.3017132739867,
179.76922598522));
#42433=CARTESIAN_POINT('Ctrl Pts',(-56.1800747416305,-91.2197379537572,
179.975477717318));
#42434=CARTESIAN_POINT('Ctrl Pts',(-57.8334096668758,-91.1377626335277,
180.181729449417));
#42435=CARTESIAN_POINT('Ctrl Pts',(-59.1504250454758,-91.0916412238858,
179.158929658031));
#42436=CARTESIAN_POINT('Ctrl Pts',(-60.4674404240759,-91.045519814244,178.136129866644));
#42437=CARTESIAN_POINT('Ctrl Pts',(-60.6824680915738,-91.116877656869,176.483420797975));
#42438=CARTESIAN_POINT('Ctrl Pts',(-60.8974957590717,-91.1882354994941,
174.830711729305));
#42439=CARTESIAN_POINT('Ctrl Pts',(-59.8903970066058,-91.3898801833847,
173.516227941122));
#42440=CARTESIAN_POINT('Ctrl Pts',(-58.8832982541398,-91.5915248672754,
172.201744152939));
#42441=CARTESIAN_POINT('Ctrl Pts',(-57.2498394547286,-91.8599437168156,
171.99549242084));
#42442=CARTESIAN_POINT('Ctrl Pts',(-55.6163806553174,-92.1283625663558,
171.789240688742));
#42443=CARTESIAN_POINT('Ctrl Pts',(-54.3192414025514,-92.3609275053083,
172.812040480128));
#42444=CARTESIAN_POINT('Ctrl Pts',(-53.0221021497854,-92.5934924442608,
173.834840271514));
#42445=CARTESIAN_POINT('Ctrl Pts',(-52.8269506081215,-92.7085781309465,
175.487549340184));
#42446=CARTESIAN_POINT('Ctrl Pts',(-52.6317990664576,-92.8236638176322,
177.140258408853));
#42447=CARTESIAN_POINT('Ctrl Pts',(-53.6587739447575,-92.8084626630522,
178.454742197037));
#42448=CARTESIAN_POINT('Ctrl Pts',(-54.6857488230575,-92.7932615084723,
179.76922598522));
#42449=CARTESIAN_POINT('Ctrl Pts',(-56.3390837483028,-92.7112861882428,
179.975477717318));
#42450=CARTESIAN_POINT('Ctrl Pts',(-57.992418673548,-92.6293108680132,180.181729449417));
#42451=CARTESIAN_POINT('Ctrl Pts',(-59.3094340521481,-92.5831894583715,
179.158929658031));
#42452=CARTESIAN_POINT('Ctrl Pts',(-60.6264494307481,-92.5370680487296,
178.136129866644));
#42453=CARTESIAN_POINT('Ctrl Pts',(-60.841477098246,-92.6084258913547,176.483420797975));
#42454=CARTESIAN_POINT('Ctrl Pts',(-61.056504765744,-92.6797837339797,174.830711729305));
#42455=CARTESIAN_POINT('Ctrl Pts',(-60.049406013278,-92.8814284178703,173.516227941122));
#42456=CARTESIAN_POINT('Ctrl Pts',(-59.0423072608121,-93.083073101761,172.201744152939));
#42457=CARTESIAN_POINT('Ctrl Pts',(-57.4088484614008,-93.3514919513012,
171.99549242084));
#42458=CARTESIAN_POINT('Ctrl Pts',(-55.7753896619896,-93.6199108008414,
171.789240688742));
#42459=CARTESIAN_POINT('Ctrl Pts',(-54.4782504092236,-93.8524757397939,
172.812040480128));
#42460=CARTESIAN_POINT('Ctrl Pts',(-53.1811111564576,-94.0850406787465,
173.834840271514));
#42461=CARTESIAN_POINT('Ctrl Pts',(-52.9859596147937,-94.2001263654321,
175.487549340184));
#42462=CARTESIAN_POINT('Ctrl Pts',(-52.7908080731298,-94.3152120521177,
177.140258408853));
#42463=CARTESIAN_POINT('Ctrl Pts',(-53.8177829514298,-94.3000108975378,
178.454742197037));
#42464=CARTESIAN_POINT('Ctrl Pts',(-54.8447578297298,-94.2848097429579,
179.76922598522));
#42465=CARTESIAN_POINT('Ctrl Pts',(-56.498092754975,-94.2028344227284,179.975477717318));
#42466=CARTESIAN_POINT('Ctrl Pts',(-58.1514276802203,-94.1208591024989,
180.181729449417));
#42467=CARTESIAN_POINT('Ctrl Pts',(-59.4684430588203,-94.074737692857,179.158929658031));
#42468=CARTESIAN_POINT('Ctrl Pts',(-60.7854584374203,-94.0286162832152,
178.136129866644));
#42469=CARTESIAN_POINT('Ctrl Pts',(-61.0004861049183,-94.0999741258402,
176.483420797975));
#42470=CARTESIAN_POINT('Ctrl Pts',(-61.2155137724162,-94.1713319684653,
174.830711729305));
#42471=CARTESIAN_POINT('Ctrl Pts',(-60.2084150199502,-94.372976652356,173.516227941122));
#42472=CARTESIAN_POINT('Ctrl Pts',(-59.2013162674843,-94.5746213362466,
172.201744152939));
#42473=CARTESIAN_POINT('Ctrl Pts',(-57.5678574680731,-94.8430401857868,
171.99549242084));
#42474=CARTESIAN_POINT('Ctrl Pts',(-55.9343986686618,-95.111459035327,171.789240688742));
#42475=CARTESIAN_POINT('Ctrl Pts',(-54.6372594158958,-95.3440239742795,
172.812040480128));
#42476=CARTESIAN_POINT('Ctrl Pts',(-53.3401201631298,-95.5765889132321,
173.834840271514));
#42477=CARTESIAN_POINT('Ctrl Pts',(-53.1449686214659,-95.6916745999177,
175.487549340184));
#42478=CARTESIAN_POINT('Ctrl Pts',(-52.949817079802,-95.8067602866033,177.140258408853));
#42479=CARTESIAN_POINT('Ctrl Pts',(-53.976791958102,-95.7915591320234,178.454742197037));
#42480=CARTESIAN_POINT('Ctrl Pts',(-55.003766836402,-95.7763579774435,179.76922598522));
#42481=CARTESIAN_POINT('Ctrl Pts',(-56.6571017616472,-95.694382657214,179.975477717318));
#42482=CARTESIAN_POINT('Ctrl Pts',(-58.3104366868925,-95.6124073369845,
180.181729449417));
#42483=CARTESIAN_POINT('Ctrl Pts',(-59.6274520654925,-95.5662859273426,
179.158929658031));
#42484=CARTESIAN_POINT('Ctrl Pts',(-60.9444674440926,-95.5201645177008,
178.136129866644));
#42485=CARTESIAN_POINT('Ctrl Pts',(-61.1594951115905,-95.5915223603259,
176.483420797975));
#42486=CARTESIAN_POINT('Ctrl Pts',(-61.3745227790884,-95.6628802029509,
174.830711729305));
#42487=CARTESIAN_POINT('Ctrl Pts',(-60.3674240266225,-95.8645248868416,
173.516227941122));
#42488=CARTESIAN_POINT('Ctrl Pts',(-59.3603252741565,-96.0661695707322,
172.201744152939));
#42489=CARTESIAN_POINT('Ctrl Pts',(-57.7268664747453,-96.3345884202724,
171.99549242084));
#42490=CARTESIAN_POINT('Ctrl Pts',(-56.0934076753341,-96.6030072698126,
171.789240688742));
#42491=CARTESIAN_POINT('Ctrl Pts',(-54.7962684225681,-96.8355722087651,
172.812040480128));
#42492=CARTESIAN_POINT('Ctrl Pts',(-53.4991291698021,-97.0681371477177,
173.834840271514));
#42493=CARTESIAN_POINT('Ctrl Pts',(-53.3039776281381,-97.1832228344033,
175.487549340184));
#42494=CARTESIAN_POINT('Ctrl Pts',(-53.1088260864743,-97.298308521089,177.140258408853));
#42495=CARTESIAN_POINT('Ctrl Pts',(-54.1358009647742,-97.283107366509,178.454742197037));
#42496=CARTESIAN_POINT('Ctrl Pts',(-55.1627758430742,-97.2679062119291,
179.76922598522));
#42497=CARTESIAN_POINT('Ctrl Pts',(-56.8161107683195,-97.1859308916996,
179.975477717318));
#42498=CARTESIAN_POINT('Ctrl Pts',(-58.4694456935647,-97.1039555714701,
180.181729449417));
#42499=CARTESIAN_POINT('Ctrl Pts',(-59.7864610721647,-97.0578341618282,
179.158929658031));
#42500=CARTESIAN_POINT('Ctrl Pts',(-61.1034764507648,-97.0117127521864,
178.136129866644));
#42501=CARTESIAN_POINT('Ctrl Pts',(-61.3185041182627,-97.0830705948115,
176.483420797975));
#42502=CARTESIAN_POINT('Ctrl Pts',(-61.5335317857606,-97.1544284374365,
174.830711729305));
#42503=CARTESIAN_POINT('Ctrl Pts',(-60.5264330332947,-97.3560731213272,
173.516227941122));
#42504=CARTESIAN_POINT('Ctrl Pts',(-59.5193342808287,-97.5577178052177,
172.201744152939));
#42505=CARTESIAN_POINT('Ctrl Pts',(-57.8858754814175,-97.826136654758,171.99549242084));
#42506=CARTESIAN_POINT('Ctrl Pts',(-56.2524166820063,-98.0945555042982,
171.789240688742));
#42507=CARTESIAN_POINT('Ctrl Pts',(-54.9552774292403,-98.3271204432507,
172.812040480128));
#42508=CARTESIAN_POINT('Ctrl Pts',(-53.6581381764743,-98.5596853822032,
173.834840271514));
#42509=CARTESIAN_POINT('Ctrl Pts',(-53.4629866348104,-98.6747710688889,
175.487549340184));
#42510=CARTESIAN_POINT('Ctrl Pts',(-53.2678350931465,-98.7898567555745,
177.140258408853));
#42511=CARTESIAN_POINT('Ctrl Pts',(-54.2948099714464,-98.7746556009946,
178.454742197037));
#42512=CARTESIAN_POINT('Ctrl Pts',(-55.3217848497464,-98.7594544464147,
179.76922598522));
#42513=CARTESIAN_POINT('Ctrl Pts',(-56.9751197749917,-98.6774791261852,
179.975477717318));
#42514=CARTESIAN_POINT('Ctrl Pts',(-58.6284547002369,-98.5955038059557,
180.181729449417));
#42515=CARTESIAN_POINT('Ctrl Pts',(-59.945470078837,-98.5493823963139,179.158929658031));
#42516=CARTESIAN_POINT('Ctrl Pts',(-61.262485457437,-98.503260986672,178.136129866644));
#42517=CARTESIAN_POINT('Ctrl Pts',(-61.4775131249349,-98.5746188292971,
176.483420797975));
#42518=CARTESIAN_POINT('Ctrl Pts',(-61.6925407924329,-98.6459766719221,
174.830711729305));
#42519=CARTESIAN_POINT('Ctrl Pts',(-60.6854420399669,-98.8476213558127,
173.516227941122));
#42520=CARTESIAN_POINT('Ctrl Pts',(-59.678343287501,-99.0492660397034,172.201744152939));
#42521=CARTESIAN_POINT('Ctrl Pts',(-58.0448844880897,-99.3176848892436,
171.99549242084));
#42522=CARTESIAN_POINT('Ctrl Pts',(-56.4114256886785,-99.5861037387838,
171.789240688742));
#42523=CARTESIAN_POINT('Ctrl Pts',(-55.1142864359125,-99.8186686777363,
172.812040480128));
#42524=CARTESIAN_POINT('Ctrl Pts',(-53.8171471831465,-100.051233616689,
173.834840271514));
#42525=CARTESIAN_POINT('Ctrl Pts',(-53.6219956414826,-100.166319303375,
175.487549340184));
#42526=CARTESIAN_POINT('Ctrl Pts',(-53.4268440998187,-100.28140499006,177.140258408853));
#42527=CARTESIAN_POINT('Ctrl Pts',(-54.4538189781187,-100.26620383548,178.454742197037));
#42528=CARTESIAN_POINT('Ctrl Pts',(-55.4807938564187,-100.2510026809,179.76922598522));
#42529=CARTESIAN_POINT('Ctrl Pts',(-57.1341287816639,-100.169027360671,
179.975477717318));
#42530=CARTESIAN_POINT('Ctrl Pts',(-58.7874637069092,-100.087052040441,
180.181729449417));
#42531=CARTESIAN_POINT('Ctrl Pts',(-60.1044790855092,-100.040930630799,
179.158929658031));
#42532=CARTESIAN_POINT('Ctrl Pts',(-61.4214944641092,-99.9948092211576,
178.136129866644));
#42533=CARTESIAN_POINT('Ctrl Pts',(-61.6365221316072,-100.066167063783,
176.483420797975));
#42534=CARTESIAN_POINT('Ctrl Pts',(-61.8515497991051,-100.137524906408,
174.830711729305));
#42535=CARTESIAN_POINT('Ctrl Pts',(-60.8444510466391,-100.339169590298,
173.516227941122));
#42536=CARTESIAN_POINT('Ctrl Pts',(-59.8373522941732,-100.540814274189,
172.201744152939));
#42537=CARTESIAN_POINT('Ctrl Pts',(-58.203893494762,-100.809233123729,171.99549242084));
#42538=CARTESIAN_POINT('Ctrl Pts',(-56.5704346953508,-101.077651973269,
171.789240688742));
#42539=CARTESIAN_POINT('Ctrl Pts',(-55.2732954425847,-101.310216912222,
172.812040480128));
#42540=CARTESIAN_POINT('Ctrl Pts',(-53.9761561898187,-101.542781851174,
173.834840271514));
#42541=CARTESIAN_POINT('Ctrl Pts',(-53.7810046481548,-101.65786753786,175.487549340184));
#42542=CARTESIAN_POINT('Ctrl Pts',(-53.5858531064909,-101.772953224546,
177.140258408853));
#42543=CARTESIAN_POINT('Ctrl Pts',(-54.6128279847909,-101.757752069966,
178.454742197037));
#42544=CARTESIAN_POINT('Ctrl Pts',(-55.6398028630909,-101.742550915386,
179.76922598522));
#42545=CARTESIAN_POINT('Ctrl Pts',(-57.2931377883361,-101.660575595156,
179.975477717318));
#42546=CARTESIAN_POINT('Ctrl Pts',(-58.9464727135814,-101.578600274927,
180.181729449417));
#42547=CARTESIAN_POINT('Ctrl Pts',(-60.2634880921814,-101.532478865285,
179.158929658031));
#42548=CARTESIAN_POINT('Ctrl Pts',(-61.5805034707815,-101.486357455643,
178.136129866644));
#42549=CARTESIAN_POINT('Ctrl Pts',(-61.7955311382794,-101.557715298268,
176.483420797975));
#42550=CARTESIAN_POINT('Ctrl Pts',(-62.0105588057773,-101.629073140893,
174.830711729305));
#42551=CARTESIAN_POINT('Ctrl Pts',(-61.0034600533114,-101.830717824784,
173.516227941122));
#42552=CARTESIAN_POINT('Ctrl Pts',(-59.9963613008454,-102.032362508675,
172.201744152939));
#42553=CARTESIAN_POINT('Ctrl Pts',(-58.3629025014342,-102.300781358215,
171.99549242084));
#42554=CARTESIAN_POINT('Ctrl Pts',(-56.729443702023,-102.569200207755,171.789240688742));
#42555=CARTESIAN_POINT('Ctrl Pts',(-55.432304449257,-102.801765146708,172.812040480128));
#42556=CARTESIAN_POINT('Ctrl Pts',(-54.135165196491,-103.03433008566,173.834840271514));
#42557=CARTESIAN_POINT('Ctrl Pts',(-53.9400136548271,-103.149415772346,
175.487549340184));
#42558=CARTESIAN_POINT('Ctrl Pts',(-53.7448621131632,-103.264501459031,
177.140258408853));
#42559=CARTESIAN_POINT('Ctrl Pts',(-54.7718369914631,-103.249300304451,
178.454742197037));
#42560=CARTESIAN_POINT('Ctrl Pts',(-55.7988118697631,-103.234099149872,
179.76922598522));
#42561=CARTESIAN_POINT('Ctrl Pts',(-57.4521467950084,-103.152123829642,
179.975477717318));
#42562=CARTESIAN_POINT('Ctrl Pts',(-59.1054817202536,-103.070148509412,
180.181729449417));
#42563=CARTESIAN_POINT('Ctrl Pts',(-60.4224970988536,-103.024027099771,
179.158929658031));
#42564=CARTESIAN_POINT('Ctrl Pts',(-61.7395124774537,-102.977905690129,
178.136129866644));
#42565=CARTESIAN_POINT('Ctrl Pts',(-61.9545401449516,-103.049263532754,
176.483420797975));
#42566=CARTESIAN_POINT('Ctrl Pts',(-62.1695678124496,-103.120621375379,
174.830711729305));
#42567=CARTESIAN_POINT('Ctrl Pts',(-61.1624690599836,-103.32226605927,173.516227941122));
#42568=CARTESIAN_POINT('Ctrl Pts',(-60.1553703075177,-103.52391074316,172.201744152939));
#42569=CARTESIAN_POINT('Ctrl Pts',(-58.5219115081064,-103.7923295927,171.99549242084));
#42570=CARTESIAN_POINT('Ctrl Pts',(-56.8884527086952,-104.060748442241,
171.789240688742));
#42571=CARTESIAN_POINT('Ctrl Pts',(-55.5913134559292,-104.293313381193,
172.812040480128));
#42572=CARTESIAN_POINT('Ctrl Pts',(-54.2941742031632,-104.525878320146,
173.834840271514));
#42573=CARTESIAN_POINT('Ctrl Pts',(-54.0990226614993,-104.640964006831,
175.487549340184));
#42574=CARTESIAN_POINT('Ctrl Pts',(-53.9038711198354,-104.756049693517,
177.140258408853));
#42575=CARTESIAN_POINT('Ctrl Pts',(-54.9308459981354,-104.740848538937,
178.454742197037));
#42576=CARTESIAN_POINT('Ctrl Pts',(-55.9578208764353,-104.725647384357,
179.76922598522));
#42577=CARTESIAN_POINT('Ctrl Pts',(-57.6111558016806,-104.643672064128,
179.975477717318));
#42578=CARTESIAN_POINT('Ctrl Pts',(-59.2644907269258,-104.561696743898,
180.181729449417));
#42579=CARTESIAN_POINT('Ctrl Pts',(-60.5815061055259,-104.515575334256,
179.158929658031));
#42580=CARTESIAN_POINT('Ctrl Pts',(-61.8985214841259,-104.469453924614,
178.136129866644));
#42581=CARTESIAN_POINT('Ctrl Pts',(-62.1135491516238,-104.540811767239,
176.483420797975));
#42582=CARTESIAN_POINT('Ctrl Pts',(-62.3285768191218,-104.612169609865,
174.830711729305));
#42583=CARTESIAN_POINT('Ctrl Pts',(-61.3214780666558,-104.813814293755,
173.516227941122));
#42584=CARTESIAN_POINT('Ctrl Pts',(-60.3143793141899,-105.015458977646,
172.201744152939));
#42585=CARTESIAN_POINT('Ctrl Pts',(-58.6809205147787,-105.283877827186,
171.99549242084));
#42586=CARTESIAN_POINT('Ctrl Pts',(-57.0474617153674,-105.552296676726,
171.789240688742));
#42587=CARTESIAN_POINT('Ctrl Pts',(-55.7503224626014,-105.784861615679,
172.812040480128));
#42588=CARTESIAN_POINT('Ctrl Pts',(-54.4531832098354,-106.017426554631,
173.834840271514));
#42589=CARTESIAN_POINT('Ctrl Pts',(-54.2580316681715,-106.132512241317,
175.487549340184));
#42590=CARTESIAN_POINT('Ctrl Pts',(-54.0628801265076,-106.247597928003,
177.140258408853));
#42591=CARTESIAN_POINT('Ctrl Pts',(-55.0898550048076,-106.232396773423,
178.454742197037));
#42592=CARTESIAN_POINT('Ctrl Pts',(-56.1168298831076,-106.217195618843,
179.76922598522));
#42593=CARTESIAN_POINT('Ctrl Pts',(-57.7701648083528,-106.135220298613,
179.975477717318));
#42594=CARTESIAN_POINT('Ctrl Pts',(-59.4234997335981,-106.053244978384,
180.181729449417));
#42595=CARTESIAN_POINT('Ctrl Pts',(-60.7405151121981,-106.007123568742,
179.158929658031));
#42596=CARTESIAN_POINT('Ctrl Pts',(-62.0575304907981,-105.9610021591,178.136129866644));
#42597=CARTESIAN_POINT('Ctrl Pts',(-62.2725581582961,-106.032360001725,
176.483420797975));
#42598=CARTESIAN_POINT('Ctrl Pts',(-62.487585825794,-106.10371784435,174.830711729305));
#42599=CARTESIAN_POINT('Ctrl Pts',(-61.480487073328,-106.305362528241,173.516227941122));
#42600=CARTESIAN_POINT('Ctrl Pts',(-60.4733883208621,-106.507007212131,
172.201744152939));
#42601=CARTESIAN_POINT('Ctrl Pts',(-58.8399295214509,-106.775426061672,
171.99549242084));
#42602=CARTESIAN_POINT('Ctrl Pts',(-57.2064707220397,-107.043844911212,
171.789240688742));
#42603=CARTESIAN_POINT('Ctrl Pts',(-55.9093314692737,-107.276409850164,
172.812040480128));
#42604=CARTESIAN_POINT('Ctrl Pts',(-54.6121922165077,-107.508974789117,
173.834840271514));
#42605=CARTESIAN_POINT('Ctrl Pts',(-54.4170406748437,-107.624060475802,
175.487549340184));
#42606=CARTESIAN_POINT('Ctrl Pts',(-54.2218891331799,-107.739146162488,
177.140258408853));
#42607=CARTESIAN_POINT('Ctrl Pts',(-55.2488640114798,-107.723945007908,
178.454742197037));
#42608=CARTESIAN_POINT('Ctrl Pts',(-56.2758388897798,-107.708743853328,
179.76922598522));
#42609=CARTESIAN_POINT('Ctrl Pts',(-57.929173815025,-107.626768533099,179.975477717318));
#42610=CARTESIAN_POINT('Ctrl Pts',(-59.5825087402703,-107.544793212869,
180.181729449417));
#42611=CARTESIAN_POINT('Ctrl Pts',(-60.8995241188703,-107.498671803227,
179.158929658031));
#42612=CARTESIAN_POINT('Ctrl Pts',(-62.2165394974704,-107.452550393586,
178.136129866644));
#42613=CARTESIAN_POINT('Ctrl Pts',(-62.4315671649683,-107.523908236211,
176.483420797975));
#42614=CARTESIAN_POINT('Ctrl Pts',(-62.6465948324662,-107.595266078836,
174.830711729305));
#42615=CARTESIAN_POINT('Ctrl Pts',(-61.6394960800003,-107.796910762726,
173.516227941122));
#42616=CARTESIAN_POINT('Ctrl Pts',(-60.6323973275343,-107.998555446617,
172.201744152939));
#42617=CARTESIAN_POINT('Ctrl Pts',(-58.9989385281231,-108.266974296157,
171.99549242084));
#42618=CARTESIAN_POINT('Ctrl Pts',(-57.3654797287119,-108.535393145697,
171.789240688742));
#42619=CARTESIAN_POINT('Ctrl Pts',(-56.0683404759459,-108.76795808465,172.812040480128));
#42620=CARTESIAN_POINT('Ctrl Pts',(-54.7712012231799,-109.000523023602,
173.834840271514));
#42621=CARTESIAN_POINT('Ctrl Pts',(-54.576049681516,-109.115608710288,175.487549340184));
#42622=CARTESIAN_POINT('Ctrl Pts',(-54.3808981398521,-109.230694396974,
177.140258408853));
#42623=CARTESIAN_POINT('Ctrl Pts',(-55.407873018152,-109.215493242394,178.454742197037));
#42624=CARTESIAN_POINT('Ctrl Pts',(-56.434847896452,-109.200292087814,179.76922598522));
#42625=CARTESIAN_POINT('Ctrl Pts',(-58.0881828216973,-109.118316767584,
179.975477717318));
#42626=CARTESIAN_POINT('Ctrl Pts',(-59.7415177469425,-109.036341447355,
180.181729449417));
#42627=CARTESIAN_POINT('Ctrl Pts',(-61.0585331255426,-108.990220037713,
179.158929658031));
#42628=CARTESIAN_POINT('Ctrl Pts',(-62.3755485041426,-108.944098628071,
178.136129866644));
#42629=CARTESIAN_POINT('Ctrl Pts',(-62.5905761716405,-109.015456470696,
176.483420797975));
#42630=CARTESIAN_POINT('Ctrl Pts',(-62.8056038391385,-109.086814313321,
174.830711729305));
#42631=CARTESIAN_POINT('Ctrl Pts',(-61.7985050866725,-109.288458997212,
173.516227941122));
#42632=CARTESIAN_POINT('Ctrl Pts',(-60.7914063342066,-109.490103681103,
172.201744152939));
#42633=CARTESIAN_POINT('Ctrl Pts',(-59.1579475347953,-109.758522530643,
171.99549242084));
#42634=CARTESIAN_POINT('Ctrl Pts',(-57.5244887353841,-110.026941380183,
171.789240688742));
#42635=CARTESIAN_POINT('Ctrl Pts',(-56.2273494826181,-110.259506319136,
172.812040480128));
#42636=CARTESIAN_POINT('Ctrl Pts',(-54.9302102298521,-110.492071258088,
173.834840271514));
#42637=CARTESIAN_POINT('Ctrl Pts',(-54.7350586881882,-110.607156944774,
175.487549340184));
#42638=CARTESIAN_POINT('Ctrl Pts',(-54.5399071465243,-110.722242631459,
177.140258408853));
#42639=CARTESIAN_POINT('Ctrl Pts',(-55.5668820248243,-110.707041476879,
178.454742197037));
#42640=CARTESIAN_POINT('Ctrl Pts',(-56.5938569031242,-110.691840322299,
179.76922598522));
#42641=CARTESIAN_POINT('Ctrl Pts',(-58.2471918283695,-110.60986500207,179.975477717318));
#42642=CARTESIAN_POINT('Ctrl Pts',(-59.9005267536148,-110.52788968184,180.181729449417));
#42643=CARTESIAN_POINT('Ctrl Pts',(-61.2175421322148,-110.481768272199,
179.158929658031));
#42644=CARTESIAN_POINT('Ctrl Pts',(-62.5345575108148,-110.435646862557,
178.136129866644));
#42645=CARTESIAN_POINT('Ctrl Pts',(-62.7495851783128,-110.507004705182,
176.483420797975));
#42646=CARTESIAN_POINT('Ctrl Pts',(-62.9646128458107,-110.578362547807,
174.830711729305));
#42647=CARTESIAN_POINT('Ctrl Pts',(-61.9575140933447,-110.780007231698,
173.516227941122));
#42648=CARTESIAN_POINT('Ctrl Pts',(-60.9504153408788,-110.981651915588,
172.201744152939));
#42649=CARTESIAN_POINT('Ctrl Pts',(-59.3169565414675,-111.250070765128,
171.99549242084));
#42650=CARTESIAN_POINT('Ctrl Pts',(-57.6834977420563,-111.518489614669,
171.789240688742));
#42651=CARTESIAN_POINT('Ctrl Pts',(-56.3863584892903,-111.751054553621,
172.812040480128));
#42652=CARTESIAN_POINT('Ctrl Pts',(-55.0892192365243,-111.983619492574,
173.834840271514));
#42653=CARTESIAN_POINT('Ctrl Pts',(-54.8940676948604,-112.098705179259,
175.487549340184));
#42654=CARTESIAN_POINT('Ctrl Pts',(-54.6989161531965,-112.213790865945,
177.140258408853));
#42655=CARTESIAN_POINT('Ctrl Pts',(-55.7258910314965,-112.198589711365,
178.454742197037));
#42656=CARTESIAN_POINT('Ctrl Pts',(-56.7528659097965,-112.183388556785,
179.76922598522));
#42657=CARTESIAN_POINT('Ctrl Pts',(-58.4062008350417,-112.101413236556,
179.975477717318));
#42658=CARTESIAN_POINT('Ctrl Pts',(-60.059535760287,-112.019437916326,180.181729449417));
#42659=CARTESIAN_POINT('Ctrl Pts',(-61.376551138887,-111.973316506684,179.158929658031));
#42660=CARTESIAN_POINT('Ctrl Pts',(-62.6935665174871,-111.927195097042,
178.136129866644));
#42661=CARTESIAN_POINT('Ctrl Pts',(-62.908594184985,-111.998552939667,176.483420797975));
#42662=CARTESIAN_POINT('Ctrl Pts',(-63.1236218524829,-112.069910782293,
174.830711729305));
#42663=CARTESIAN_POINT('Ctrl Pts',(-62.116523100017,-112.271555466183,173.516227941122));
#42664=CARTESIAN_POINT('Ctrl Pts',(-61.109424347551,-112.473200150074,172.201744152939));
#42665=CARTESIAN_POINT('Ctrl Pts',(-59.4759655481398,-112.741618999614,
171.99549242084));
#42666=CARTESIAN_POINT('Ctrl Pts',(-57.8425067487286,-113.010037849154,
171.789240688742));
#42667=CARTESIAN_POINT('Ctrl Pts',(-56.5453674959626,-113.242602788107,
172.812040480128));
#42668=CARTESIAN_POINT('Ctrl Pts',(-55.2482282431966,-113.475167727059,
173.834840271514));
#42669=CARTESIAN_POINT('Ctrl Pts',(-55.0530767015326,-113.590253413745,
175.487549340184));
#42670=CARTESIAN_POINT('Ctrl Pts',(-54.8579251598688,-113.705339100431,
177.140258408853));
#42671=CARTESIAN_POINT('Ctrl Pts',(-55.8849000381687,-113.690137945851,
178.454742197037));
#42672=CARTESIAN_POINT('Ctrl Pts',(-56.9118749164687,-113.674936791271,
179.76922598522));
#42673=CARTESIAN_POINT('Ctrl Pts',(-58.565209841714,-113.592961471041,179.975477717318));
#42674=CARTESIAN_POINT('Ctrl Pts',(-60.2185447669592,-113.510986150812,
180.181729449417));
#42675=CARTESIAN_POINT('Ctrl Pts',(-61.5355601455592,-113.46486474117,179.158929658031));
#42676=CARTESIAN_POINT('Ctrl Pts',(-62.8525755241593,-113.418743331528,
178.136129866644));
#42677=CARTESIAN_POINT('Ctrl Pts',(-63.0676031916572,-113.490101174153,
176.483420797975));
#42678=CARTESIAN_POINT('Ctrl Pts',(-63.2826308591551,-113.561459016778,
174.830711729305));
#42679=CARTESIAN_POINT('Ctrl Pts',(-62.2755321066892,-113.763103700669,
173.516227941122));
#42680=CARTESIAN_POINT('Ctrl Pts',(-61.2684333542232,-113.964748384559,
172.201744152939));
#42681=CARTESIAN_POINT('Ctrl Pts',(-59.634974554812,-114.2331672341,171.99549242084));
#42682=CARTESIAN_POINT('Ctrl Pts',(-58.0015157554008,-114.50158608364,171.789240688742));
#42683=CARTESIAN_POINT('Ctrl Pts',(-56.7043765026348,-114.734151022592,
172.812040480128));
#42684=CARTESIAN_POINT('Ctrl Pts',(-55.4072372498688,-114.966715961545,
173.834840271514));
#42685=CARTESIAN_POINT('Ctrl Pts',(-55.2120857082049,-115.08180164823,175.487549340184));
#42686=CARTESIAN_POINT('Ctrl Pts',(-55.016934166541,-115.196887334916,177.140258408853));
#42687=CARTESIAN_POINT('Ctrl Pts',(-56.043909044841,-115.181686180336,178.454742197037));
#42688=CARTESIAN_POINT('Ctrl Pts',(-57.0708839231409,-115.166485025756,
179.76922598522));
#42689=CARTESIAN_POINT('Ctrl Pts',(-58.7242188483862,-115.084509705527,
179.975477717318));
#42690=CARTESIAN_POINT('Ctrl Pts',(-60.3775537736314,-115.002534385297,
180.181729449417));
#42691=CARTESIAN_POINT('Ctrl Pts',(-61.6945691522315,-114.956412975655,
179.158929658031));
#42692=CARTESIAN_POINT('Ctrl Pts',(-63.0115845308315,-114.910291566014,
178.136129866644));
#42693=CARTESIAN_POINT('Ctrl Pts',(-63.2266121983294,-114.981649408639,
176.483420797975));
#42694=CARTESIAN_POINT('Ctrl Pts',(-63.4416398658274,-115.053007251264,
174.830711729305));
#42695=CARTESIAN_POINT('Ctrl Pts',(-62.4345411133614,-115.254651935154,
173.516227941122));
#42696=CARTESIAN_POINT('Ctrl Pts',(-61.4274423608955,-115.456296619045,
172.201744152939));
#42697=CARTESIAN_POINT('Ctrl Pts',(-59.7939835614843,-115.724715468585,
171.99549242084));
#42698=CARTESIAN_POINT('Ctrl Pts',(-58.160524762073,-115.993134318125,171.789240688742));
#42699=CARTESIAN_POINT('Ctrl Pts',(-56.863385509307,-116.225699257078,172.812040480128));
#42700=CARTESIAN_POINT('Ctrl Pts',(-55.566246256541,-116.45826419603,173.834840271514));
#42701=CARTESIAN_POINT('Ctrl Pts',(-55.3710947148771,-116.573349882716,
175.487549340184));
#42702=CARTESIAN_POINT('Ctrl Pts',(-55.1759431732132,-116.688435569402,
177.140258408853));
#42703=CARTESIAN_POINT('Ctrl Pts',(-56.2029180515132,-116.673234414822,
178.454742197037));
#42704=CARTESIAN_POINT('Ctrl Pts',(-57.2298929298132,-116.658033260242,
179.76922598522));
#42705=CARTESIAN_POINT('Ctrl Pts',(-58.8832278550584,-116.576057940012,
179.975477717318));
#42706=CARTESIAN_POINT('Ctrl Pts',(-60.5365627803037,-116.494082619783,
180.181729449417));
#42707=CARTESIAN_POINT('Ctrl Pts',(-61.8535781589037,-116.447961210141,
179.158929658031));
#42708=CARTESIAN_POINT('Ctrl Pts',(-63.1705935375037,-116.401839800499,
178.136129866644));
#42709=CARTESIAN_POINT('Ctrl Pts',(-63.3856212050017,-116.473197643124,
176.483420797975));
#42710=CARTESIAN_POINT('Ctrl Pts',(-63.6006488724996,-116.544555485749,
174.830711729305));
#42711=CARTESIAN_POINT('Ctrl Pts',(-62.5935501200336,-116.74620016964,173.516227941122));
#42712=CARTESIAN_POINT('Ctrl Pts',(-61.5864513675677,-116.947844853531,
172.201744152939));
#42713=CARTESIAN_POINT('Ctrl Pts',(-59.9529925681565,-117.216263703071,
171.99549242084));
#42714=CARTESIAN_POINT('Ctrl Pts',(-58.3195337687452,-117.484682552611,
171.789240688742));
#42715=CARTESIAN_POINT('Ctrl Pts',(-57.0223945159792,-117.717247491564,
172.812040480128));
#42716=CARTESIAN_POINT('Ctrl Pts',(-55.7252552632132,-117.949812430516,
173.834840271514));
#42717=CARTESIAN_POINT('Ctrl Pts',(-55.5301037215493,-118.064898117202,
175.487549340184));
#42718=CARTESIAN_POINT('Ctrl Pts',(-55.3349521798854,-118.179983803887,
177.140258408853));
#42719=CARTESIAN_POINT('Ctrl Pts',(-56.3619270581854,-118.164782649307,
178.454742197037));
#42720=CARTESIAN_POINT('Ctrl Pts',(-57.3889019364854,-118.149581494728,
179.76922598522));
#42721=CARTESIAN_POINT('Ctrl Pts',(-59.0422368617306,-118.067606174498,
179.975477717318));
#42722=CARTESIAN_POINT('Ctrl Pts',(-60.6955717869759,-117.985630854268,
180.181729449417));
#42723=CARTESIAN_POINT('Ctrl Pts',(-62.0125871655759,-117.939509444627,
179.158929658031));
#42724=CARTESIAN_POINT('Ctrl Pts',(-63.329602544176,-117.893388034985,178.136129866644));
#42725=CARTESIAN_POINT('Ctrl Pts',(-63.5446302116739,-117.96474587761,176.483420797975));
#42726=CARTESIAN_POINT('Ctrl Pts',(-63.7596578791718,-118.036103720235,
174.830711729305));
#42727=CARTESIAN_POINT('Ctrl Pts',(-62.7525591267059,-118.237748404126,
173.516227941122));
#42728=CARTESIAN_POINT('Ctrl Pts',(-61.7454603742399,-118.439393088016,
172.201744152939));
#42729=CARTESIAN_POINT('Ctrl Pts',(-60.1120015748287,-118.707811937556,
171.99549242084));
#42730=CARTESIAN_POINT('Ctrl Pts',(-58.4785427754175,-118.976230787097,
171.789240688742));
#42731=CARTESIAN_POINT('Ctrl Pts',(-57.1814035226515,-119.208795726049,
172.812040480128));
#42732=CARTESIAN_POINT('Ctrl Pts',(-55.8842642698855,-119.441360665002,
173.834840271514));
#42733=CARTESIAN_POINT('Ctrl Pts',(-55.6891127282216,-119.556446351687,
175.487549340184));
#42734=CARTESIAN_POINT('Ctrl Pts',(-55.4939611865577,-119.671532038373,
177.140258408853));
#42735=CARTESIAN_POINT('Ctrl Pts',(-56.5209360648576,-119.656330883793,
178.454742197037));
#42736=CARTESIAN_POINT('Ctrl Pts',(-57.5479109431576,-119.641129729213,
179.76922598522));
#42737=CARTESIAN_POINT('Ctrl Pts',(-59.2012458684029,-119.559154408984,
179.975477717318));
#42738=CARTESIAN_POINT('Ctrl Pts',(-60.8545807936481,-119.477179088754,
180.181729449417));
#42739=CARTESIAN_POINT('Ctrl Pts',(-62.1715961722481,-119.431057679112,
179.158929658031));
#42740=CARTESIAN_POINT('Ctrl Pts',(-63.4886115508482,-119.38493626947,178.136129866644));
#42741=CARTESIAN_POINT('Ctrl Pts',(-63.7036392183461,-119.456294112095,
176.483420797975));
#42742=CARTESIAN_POINT('Ctrl Pts',(-63.918666885844,-119.527651954721,174.830711729305));
#42743=CARTESIAN_POINT('Ctrl Pts',(-62.9115681333781,-119.729296638611,
173.516227941122));
#42744=CARTESIAN_POINT('Ctrl Pts',(-61.9044693809121,-119.930941322502,
172.201744152939));
#42745=CARTESIAN_POINT('Ctrl Pts',(-60.2710105815009,-120.199360172042,
171.99549242084));
#42746=CARTESIAN_POINT('Ctrl Pts',(-58.6375517820897,-120.467779021582,
171.789240688742));
#42747=CARTESIAN_POINT('Ctrl Pts',(-57.3404125293237,-120.700343960535,
172.812040480128));
#42748=CARTESIAN_POINT('Ctrl Pts',(-56.0432732765577,-120.932908899487,
173.834840271514));
#42749=CARTESIAN_POINT('Ctrl Pts',(-55.8481217348938,-121.047994586173,
175.487549340184));
#42750=CARTESIAN_POINT('Ctrl Pts',(-55.6529701932299,-121.163080272859,
177.140258408853));
#42751=CARTESIAN_POINT('Ctrl Pts',(-56.6799450715299,-121.147879118279,
178.454742197037));
#42752=CARTESIAN_POINT('Ctrl Pts',(-57.7069199498298,-121.132677963699,
179.76922598522));
#42753=CARTESIAN_POINT('Ctrl Pts',(-59.3602548750751,-121.050702643469,
179.975477717318));
#42754=CARTESIAN_POINT('Ctrl Pts',(-61.0135898003203,-120.96872732324,180.181729449417));
#42755=CARTESIAN_POINT('Ctrl Pts',(-62.3306051789204,-120.922605913598,
179.158929658031));
#42756=CARTESIAN_POINT('Ctrl Pts',(-63.6476205575204,-120.876484503956,
178.136129866644));
#42757=CARTESIAN_POINT('Ctrl Pts',(-63.8626482250183,-120.947842346581,
176.483420797975));
#42758=CARTESIAN_POINT('Ctrl Pts',(-64.0776758925163,-121.019200189206,
174.830711729305));
#42759=CARTESIAN_POINT('Ctrl Pts',(-63.0705771400503,-121.220844873097,
173.516227941122));
#42760=CARTESIAN_POINT('Ctrl Pts',(-62.0634783875844,-121.422489556987,
172.201744152939));
#42761=CARTESIAN_POINT('Ctrl Pts',(-60.4300195881731,-121.690908406528,
171.99549242084));
#42762=CARTESIAN_POINT('Ctrl Pts',(-58.7965607887619,-121.959327256068,
171.789240688742));
#42763=CARTESIAN_POINT('Ctrl Pts',(-57.4994215359959,-122.19189219502,172.812040480128));
#42764=CARTESIAN_POINT('Ctrl Pts',(-56.2022822832299,-122.424457133973,
173.834840271514));
#42765=CARTESIAN_POINT('Ctrl Pts',(-56.007130741566,-122.539542820658,175.487549340184));
#42766=CARTESIAN_POINT('Ctrl Pts',(-55.8119791999021,-122.654628507344,
177.140258408853));
#42767=CARTESIAN_POINT('Ctrl Pts',(-56.8389540782021,-122.639427352764,
178.454742197037));
#42768=CARTESIAN_POINT('Ctrl Pts',(-57.8659289565021,-122.624226198184,
179.76922598522));
#42769=CARTESIAN_POINT('Ctrl Pts',(-59.5192638817473,-122.542250877955,
179.975477717318));
#42770=CARTESIAN_POINT('Ctrl Pts',(-61.1725988069926,-122.460275557725,
180.181729449417));
#42771=CARTESIAN_POINT('Ctrl Pts',(-62.4896141855926,-122.414154148083,
179.158929658031));
#42772=CARTESIAN_POINT('Ctrl Pts',(-63.8066295641926,-122.368032738442,
178.136129866644));
#42773=CARTESIAN_POINT('Ctrl Pts',(-64.0216572316905,-122.439390581067,
176.483420797975));
#42774=CARTESIAN_POINT('Ctrl Pts',(-64.2366848991885,-122.510748423692,
174.830711729305));
#42775=CARTESIAN_POINT('Ctrl Pts',(-63.2295861467226,-122.712393107582,
173.516227941122));
#42776=CARTESIAN_POINT('Ctrl Pts',(-62.2224873942566,-122.914037791473,
172.201744152939));
#42777=CARTESIAN_POINT('Ctrl Pts',(-60.5890285948454,-123.182456641013,
171.99549242084));
#42778=CARTESIAN_POINT('Ctrl Pts',(-58.9555697954342,-123.450875490553,
171.789240688742));
#42779=CARTESIAN_POINT('Ctrl Pts',(-57.6584305426681,-123.683440429506,
172.812040480128));
#42780=CARTESIAN_POINT('Ctrl Pts',(-56.3612912899021,-123.916005368458,
173.834840271514));
#42781=CARTESIAN_POINT('Ctrl Pts',(-56.1661397482382,-124.031091055144,
175.487549340184));
#42782=CARTESIAN_POINT('Ctrl Pts',(-55.9709882065743,-124.14617674183,177.140258408853));
#42783=CARTESIAN_POINT('Ctrl Pts',(-56.9979630848743,-124.13097558725,178.454742197037));
#42784=CARTESIAN_POINT('Ctrl Pts',(-58.0249379631743,-124.11577443267,179.76922598522));
#42785=CARTESIAN_POINT('Ctrl Pts',(-59.6782728884195,-124.03379911244,179.975477717318));
#42786=CARTESIAN_POINT('Ctrl Pts',(-61.3316078136648,-123.951823792211,
180.181729449417));
#42787=CARTESIAN_POINT('Ctrl Pts',(-62.6486231922648,-123.905702382569,
179.158929658031));
#42788=CARTESIAN_POINT('Ctrl Pts',(-63.9656385708649,-123.859580972927,
178.136129866644));
#42789=CARTESIAN_POINT('Ctrl Pts',(-64.1806662383628,-123.930938815552,
176.483420797975));
#42790=CARTESIAN_POINT('Ctrl Pts',(-64.3956939058607,-124.002296658177,
174.830711729305));
#42791=CARTESIAN_POINT('Ctrl Pts',(-63.3885951533948,-124.203941342068,
173.516227941122));
#42792=CARTESIAN_POINT('Ctrl Pts',(-62.3814964009288,-124.405586025959,
172.201744152939));
#42793=CARTESIAN_POINT('Ctrl Pts',(-60.7480376015176,-124.674004875499,
171.99549242084));
#42794=CARTESIAN_POINT('Ctrl Pts',(-59.1145788021064,-124.942423725039,
171.789240688742));
#42795=CARTESIAN_POINT('Ctrl Pts',(-57.8174395493404,-125.174988663992,
172.812040480128));
#42796=CARTESIAN_POINT('Ctrl Pts',(-56.5203002965744,-125.407553602944,
173.834840271514));
#42797=CARTESIAN_POINT('Ctrl Pts',(-56.3251487549105,-125.52263928963,175.487549340184));
#42798=CARTESIAN_POINT('Ctrl Pts',(-56.1299972132466,-125.637724976315,
177.140258408853));
#42799=CARTESIAN_POINT('Ctrl Pts',(-57.1569720915465,-125.622523821735,
178.454742197037));
#42800=CARTESIAN_POINT('Ctrl Pts',(-58.1839469698465,-125.607322667156,
179.76922598522));
#42801=CARTESIAN_POINT('Ctrl Pts',(-59.8372818950918,-125.525347346926,
179.975477717318));
#42802=CARTESIAN_POINT('Ctrl Pts',(-61.490616820337,-125.443372026696,180.181729449417));
#42803=CARTESIAN_POINT('Ctrl Pts',(-62.8076321989371,-125.397250617055,
179.158929658031));
#42804=CARTESIAN_POINT('Ctrl Pts',(-64.1246475775371,-125.351129207413,
178.136129866644));
#42805=CARTESIAN_POINT('Ctrl Pts',(-64.339675245035,-125.422487050038,176.483420797975));
#42806=CARTESIAN_POINT('Ctrl Pts',(-64.5547029125329,-125.493844892663,
174.830711729305));
#42807=CARTESIAN_POINT('Ctrl Pts',(-63.547604160067,-125.695489576554,173.516227941122));
#42808=CARTESIAN_POINT('Ctrl Pts',(-62.5405054076011,-125.897134260444,
172.201744152939));
#42809=CARTESIAN_POINT('Ctrl Pts',(-60.9070466081898,-126.165553109984,
171.99549242084));
#42810=CARTESIAN_POINT('Ctrl Pts',(-59.2735878087786,-126.433971959525,
171.789240688742));
#42811=CARTESIAN_POINT('Ctrl Pts',(-57.9764485560126,-126.666536898477,
172.812040480128));
#42812=CARTESIAN_POINT('Ctrl Pts',(-56.6793093032466,-126.89910183743,173.834840271514));
#42813=CARTESIAN_POINT('Ctrl Pts',(-56.4841577615827,-127.014187524115,
175.487549340184));
#42814=CARTESIAN_POINT('Ctrl Pts',(-56.2890062199188,-127.129273210801,
177.140258408853));
#42815=CARTESIAN_POINT('Ctrl Pts',(-57.3159810982188,-127.114072056221,
178.454742197037));
#42816=CARTESIAN_POINT('Ctrl Pts',(-58.3429559765187,-127.098870901641,
179.76922598522));
#42817=CARTESIAN_POINT('Ctrl Pts',(-59.996290901764,-127.016895581412,179.975477717318));
#42818=CARTESIAN_POINT('Ctrl Pts',(-61.6496258270093,-126.934920261182,
180.181729449417));
#42819=CARTESIAN_POINT('Ctrl Pts',(-62.9666412056093,-126.88879885154,179.158929658031));
#42820=CARTESIAN_POINT('Ctrl Pts',(-64.2836565842093,-126.842677441898,
178.136129866644));
#42821=CARTESIAN_POINT('Ctrl Pts',(-64.4986842517073,-126.914035284523,
176.483420797975));
#42822=CARTESIAN_POINT('Ctrl Pts',(-64.7137119192052,-126.985393127149,
174.830711729305));
#42823=CARTESIAN_POINT('Ctrl Pts',(-63.7066131667392,-127.187037811039,
173.516227941122));
#42824=CARTESIAN_POINT('Ctrl Pts',(-62.6995144142733,-127.38868249493,172.201744152939));
#42825=CARTESIAN_POINT('Ctrl Pts',(-61.0660556148621,-127.65710134447,171.99549242084));
#42826=CARTESIAN_POINT('Ctrl Pts',(-59.4325968154509,-127.92552019401,171.789240688742));
#42827=CARTESIAN_POINT('Ctrl Pts',(-58.1354575626848,-128.158085132963,
172.812040480128));
#42828=CARTESIAN_POINT('Ctrl Pts',(-56.8383183099188,-128.390650071915,
173.834840271514));
#42829=CARTESIAN_POINT('Ctrl Pts',(-56.6431667682549,-128.505735758601,
175.487549340184));
#42830=CARTESIAN_POINT('Ctrl Pts',(-56.448015226591,-128.620821445287,177.140258408853));
#42831=CARTESIAN_POINT('Ctrl Pts',(-57.474990104891,-128.605620290707,178.454742197037));
#42832=CARTESIAN_POINT('Ctrl Pts',(-58.501964983191,-128.590419136127,179.76922598522));
#42833=CARTESIAN_POINT('Ctrl Pts',(-60.1552999084362,-128.508443815897,
179.975477717318));
#42834=CARTESIAN_POINT('Ctrl Pts',(-61.8086348336815,-128.426468495668,
180.181729449417));
#42835=CARTESIAN_POINT('Ctrl Pts',(-63.1256502122815,-128.380347086026,
179.158929658031));
#42836=CARTESIAN_POINT('Ctrl Pts',(-64.4426655908815,-128.334225676384,
178.136129866644));
#42837=CARTESIAN_POINT('Ctrl Pts',(-64.6576932583795,-128.405583519009,
176.483420797975));
#42838=CARTESIAN_POINT('Ctrl Pts',(-64.8727209258774,-128.476941361634,
174.830711729305));
#42839=CARTESIAN_POINT('Ctrl Pts',(-63.8656221734115,-128.678586045525,
173.516227941122));
#42840=CARTESIAN_POINT('Ctrl Pts',(-62.8585234209455,-128.880230729415,
172.201744152939));
#42841=CARTESIAN_POINT('Ctrl Pts',(-61.2250646215343,-129.148649578956,
171.99549242084));
#42842=CARTESIAN_POINT('Ctrl Pts',(-59.5916058221231,-129.417068428496,
171.789240688742));
#42843=CARTESIAN_POINT('Ctrl Pts',(-58.2944665693571,-129.649633367448,
172.812040480128));
#42844=CARTESIAN_POINT('Ctrl Pts',(-56.997327316591,-129.882198306401,173.834840271514));
#42845=CARTESIAN_POINT('Ctrl Pts',(-56.8021757749272,-129.997283993086,
175.487549340184));
#42846=CARTESIAN_POINT('Ctrl Pts',(-56.6070242332633,-130.112369679772,
177.140258408853));
#42847=CARTESIAN_POINT('Ctrl Pts',(-57.6339991115632,-130.097168525192,
178.454742197037));
#42848=CARTESIAN_POINT('Ctrl Pts',(-58.6609739898632,-130.081967370612,
179.76922598522));
#42849=CARTESIAN_POINT('Ctrl Pts',(-60.3143089151084,-129.999992050383,
179.975477717318));
#42850=CARTESIAN_POINT('Ctrl Pts',(-61.9676438403537,-129.918016730153,
180.181729449417));
#42851=CARTESIAN_POINT('Ctrl Pts',(-63.2846592189537,-129.871895320511,
179.158929658031));
#42852=CARTESIAN_POINT('Ctrl Pts',(-64.6016745975538,-129.82577391087,178.136129866644));
#42853=CARTESIAN_POINT('Ctrl Pts',(-64.8167022650517,-129.897131753495,
176.483420797975));
#42854=CARTESIAN_POINT('Ctrl Pts',(-65.0317299325496,-129.96848959612,174.830711729305));
#42855=CARTESIAN_POINT('Ctrl Pts',(-64.0246311800837,-130.17013428001,173.516227941122));
#42856=CARTESIAN_POINT('Ctrl Pts',(-63.0175324276178,-130.371778963901,
172.201744152939));
#42857=CARTESIAN_POINT('Ctrl Pts',(-61.3840736282065,-130.640197813441,
171.99549242084));
#42858=CARTESIAN_POINT('Ctrl Pts',(-59.7506148287953,-130.908616662981,
171.789240688742));
#42859=CARTESIAN_POINT('Ctrl Pts',(-58.4534755760293,-131.141181601934,
172.812040480128));
#42860=CARTESIAN_POINT('Ctrl Pts',(-57.1563363232633,-131.373746540886,
173.834840271514));
#42861=CARTESIAN_POINT('Ctrl Pts',(-56.9611847815994,-131.488832227572,
175.487549340184));
#42862=CARTESIAN_POINT('Ctrl Pts',(-56.7660332399355,-131.603917914258,
177.140258408853));
#42863=CARTESIAN_POINT('Ctrl Pts',(-57.7930081182354,-131.588716759678,
178.454742197037));
#42864=CARTESIAN_POINT('Ctrl Pts',(-58.8199829965354,-131.573515605098,
179.76922598522));
#42865=CARTESIAN_POINT('Ctrl Pts',(-60.4733179217807,-131.491540284868,
179.975477717318));
#42866=CARTESIAN_POINT('Ctrl Pts',(-61.5428145880944,-131.438512715943,
180.108896262184));
#42867=CARTESIAN_POINT('Ctrl Pts',(-62.5366952746482,-131.398006590211,
179.689905107434));
#42868=CARTESIAN_POINT('Ctrl Pts',(-50.1415580290747,-67.5188568440608,
175.487549340184));
#42869=CARTESIAN_POINT('Ctrl Pts',(-49.9464064874108,-67.6339425307465,
177.140258408853));
#42870=CARTESIAN_POINT('Ctrl Pts',(-50.9733813657108,-67.6187413761666,
178.454742197037));
#42871=CARTESIAN_POINT('Ctrl Pts',(-52.0003562440107,-67.6035402215866,
179.76922598522));
#42872=CARTESIAN_POINT('Ctrl Pts',(-53.653691169256,-67.5215649013571,179.975477717318));
#42873=CARTESIAN_POINT('Ctrl Pts',(-55.3070260945012,-67.4395895811276,
180.181729449417));
#42874=CARTESIAN_POINT('Ctrl Pts',(-56.6240414731013,-67.3934681714858,
179.158929658031));
#42875=CARTESIAN_POINT('Ctrl Pts',(-57.9410568517013,-67.347346761844,178.136129866644));
#42876=CARTESIAN_POINT('Ctrl Pts',(-58.1560845191993,-67.418704604469,176.483420797975));
#42877=CARTESIAN_POINT('Ctrl Pts',(-58.3711121866972,-67.4900624470941,
174.830711729305));
#42878=CARTESIAN_POINT('Ctrl Pts',(-57.3640134342312,-67.6917071309847,
173.516227941122));
#42879=CARTESIAN_POINT('Ctrl Pts',(-56.3569146817653,-67.8933518148753,
172.201744152939));
#42880=CARTESIAN_POINT('Ctrl Pts',(-54.7234558823541,-68.1617706644155,
171.99549242084));
#42881=CARTESIAN_POINT('Ctrl Pts',(-53.0899970829429,-68.4301895139558,
171.789240688742));
#42882=CARTESIAN_POINT('Ctrl Pts',(-51.7928578301768,-68.6627544529083,
172.812040480128));
#42883=CARTESIAN_POINT('Ctrl Pts',(-50.4957185774108,-68.8953193918608,
173.834840271514));
#42884=CARTESIAN_POINT('Ctrl Pts',(-50.3005670357469,-69.0104050785464,
175.487549340184));
#42885=CARTESIAN_POINT('Ctrl Pts',(-50.105415494083,-69.1254907652321,177.140258408853));
#42886=CARTESIAN_POINT('Ctrl Pts',(-51.132390372383,-69.1102896106521,178.454742197037));
#42887=CARTESIAN_POINT('Ctrl Pts',(-52.159365250683,-69.0950884560723,179.76922598522));
#42888=CARTESIAN_POINT('Ctrl Pts',(-53.8127001759282,-69.0131131358427,
179.975477717318));
#42889=CARTESIAN_POINT('Ctrl Pts',(-55.4660351011735,-68.9311378156132,
180.181729449417));
#42890=CARTESIAN_POINT('Ctrl Pts',(-56.7830504797735,-68.8850164059714,
179.158929658031));
#42891=CARTESIAN_POINT('Ctrl Pts',(-58.1000658583736,-68.8388949963296,
178.136129866644));
#42892=CARTESIAN_POINT('Ctrl Pts',(-58.3150935258715,-68.9102528389546,
176.483420797975));
#42893=CARTESIAN_POINT('Ctrl Pts',(-58.5301211933694,-68.9816106815797,
174.830711729305));
#42894=CARTESIAN_POINT('Ctrl Pts',(-57.5230224409035,-69.1832553654703,
173.516227941122));
#42895=CARTESIAN_POINT('Ctrl Pts',(-56.5159236884375,-69.3849000493609,
172.201744152939));
#42896=CARTESIAN_POINT('Ctrl Pts',(-54.8824648890263,-69.6533188989011,
171.99549242084));
#42897=CARTESIAN_POINT('Ctrl Pts',(-53.2490060896151,-69.9217377484414,
171.789240688742));
#42898=CARTESIAN_POINT('Ctrl Pts',(-51.9518668368491,-70.1543026873939,
172.812040480128));
#42899=CARTESIAN_POINT('Ctrl Pts',(-50.654727584083,-70.3868676263464,173.834840271514));
#42900=CARTESIAN_POINT('Ctrl Pts',(-50.4595760424191,-70.501953313032,175.487549340184));
#42901=CARTESIAN_POINT('Ctrl Pts',(-50.2644245007553,-70.6170389997177,
177.140258408853));
#42902=CARTESIAN_POINT('Ctrl Pts',(-51.2913993790552,-70.6018378451378,
178.454742197037));
#42903=CARTESIAN_POINT('Ctrl Pts',(-52.3183742573552,-70.5866366905578,
179.76922598522));
#42904=CARTESIAN_POINT('Ctrl Pts',(-53.9717091826004,-70.5046613703283,
179.975477717318));
#42905=CARTESIAN_POINT('Ctrl Pts',(-55.6250441078457,-70.4226860500988,
180.181729449417));
#42906=CARTESIAN_POINT('Ctrl Pts',(-56.9420594864457,-70.376564640457,179.158929658031));
#42907=CARTESIAN_POINT('Ctrl Pts',(-58.2590748650458,-70.3304432308151,
178.136129866644));
#42908=CARTESIAN_POINT('Ctrl Pts',(-58.4741025325437,-70.4018010734402,
176.483420797975));
#42909=CARTESIAN_POINT('Ctrl Pts',(-58.6891302000416,-70.4731589160653,
174.830711729305));
#42910=CARTESIAN_POINT('Ctrl Pts',(-57.6820314475757,-70.6748035999559,
173.516227941122));
#42911=CARTESIAN_POINT('Ctrl Pts',(-56.6749326951098,-70.8764482838465,
172.201744152939));
#42912=CARTESIAN_POINT('Ctrl Pts',(-55.0414738956985,-71.1448671333867,
171.99549242084));
#42913=CARTESIAN_POINT('Ctrl Pts',(-53.4080150962873,-71.413285982927,171.789240688742));
#42914=CARTESIAN_POINT('Ctrl Pts',(-52.1108758435213,-71.6458509218795,
172.812040480128));
#42915=CARTESIAN_POINT('Ctrl Pts',(-50.8137365907553,-71.878415860832,173.834840271514));
#42916=CARTESIAN_POINT('Ctrl Pts',(-50.6185850490914,-71.9935015475176,
175.487549340184));
#42917=CARTESIAN_POINT('Ctrl Pts',(-50.4234335074275,-72.1085872342033,
177.140258408853));
#42918=CARTESIAN_POINT('Ctrl Pts',(-51.4504083857275,-72.0933860796234,
178.454742197037));
#42919=CARTESIAN_POINT('Ctrl Pts',(-52.4773832640274,-72.0781849250434,
179.76922598522));
#42920=CARTESIAN_POINT('Ctrl Pts',(-54.1307181892727,-71.9962096048139,
179.975477717318));
#42921=CARTESIAN_POINT('Ctrl Pts',(-55.7840531145179,-71.9142342845844,
180.181729449417));
#42922=CARTESIAN_POINT('Ctrl Pts',(-57.101068493118,-71.8681128749426,179.158929658031));
#42923=CARTESIAN_POINT('Ctrl Pts',(-58.418083871718,-71.8219914653008,178.136129866644));
#42924=CARTESIAN_POINT('Ctrl Pts',(-58.6331115392159,-71.8933493079258,
176.483420797975));
#42925=CARTESIAN_POINT('Ctrl Pts',(-58.8481392067139,-71.9647071505509,
174.830711729305));
#42926=CARTESIAN_POINT('Ctrl Pts',(-57.8410404542479,-72.1663518344415,
173.516227941122));
#42927=CARTESIAN_POINT('Ctrl Pts',(-56.833941701782,-72.3679965183321,172.201744152939));
#42928=CARTESIAN_POINT('Ctrl Pts',(-55.2004829023707,-72.6364153678723,
171.99549242084));
#42929=CARTESIAN_POINT('Ctrl Pts',(-53.5670241029595,-72.9048342174126,
171.789240688742));
#42930=CARTESIAN_POINT('Ctrl Pts',(-52.2698848501935,-73.1373991563651,
172.812040480128));
#42931=CARTESIAN_POINT('Ctrl Pts',(-50.9727455974275,-73.3699640953176,
173.834840271514));
#42932=CARTESIAN_POINT('Ctrl Pts',(-50.7775940557636,-73.4850497820032,
175.487549340184));
#42933=CARTESIAN_POINT('Ctrl Pts',(-50.5824425140997,-73.6001354686889,
177.140258408853));
#42934=CARTESIAN_POINT('Ctrl Pts',(-51.6094173923997,-73.5849343141089,
178.454742197037));
#42935=CARTESIAN_POINT('Ctrl Pts',(-52.6363922706997,-73.5697331595291,
179.76922598522));
#42936=CARTESIAN_POINT('Ctrl Pts',(-54.2897271959449,-73.4877578392995,
179.975477717318));
#42937=CARTESIAN_POINT('Ctrl Pts',(-55.9430621211902,-73.40578251907,180.181729449417));
#42938=CARTESIAN_POINT('Ctrl Pts',(-57.2600774997902,-73.3596611094282,
179.158929658031));
#42939=CARTESIAN_POINT('Ctrl Pts',(-58.5770928783902,-73.3135396997863,
178.136129866644));
#42940=CARTESIAN_POINT('Ctrl Pts',(-58.7921205458882,-73.3848975424114,
176.483420797975));
#42941=CARTESIAN_POINT('Ctrl Pts',(-59.0071482133861,-73.4562553850365,
174.830711729305));
#42942=CARTESIAN_POINT('Ctrl Pts',(-58.0000494609201,-73.6579000689271,
173.516227941122));
#42943=CARTESIAN_POINT('Ctrl Pts',(-56.9929507084542,-73.8595447528177,
172.201744152939));
#42944=CARTESIAN_POINT('Ctrl Pts',(-55.359491909043,-74.1279636023579,171.99549242084));
#42945=CARTESIAN_POINT('Ctrl Pts',(-53.7260331096318,-74.3963824518981,
171.789240688742));
#42946=CARTESIAN_POINT('Ctrl Pts',(-52.4288938568657,-74.6289473908507,
172.812040480128));
#42947=CARTESIAN_POINT('Ctrl Pts',(-51.1317546040997,-74.8615123298032,
173.834840271514));
#42948=CARTESIAN_POINT('Ctrl Pts',(-50.9366030624358,-74.9765980164889,
175.487549340184));
#42949=CARTESIAN_POINT('Ctrl Pts',(-50.7414515207719,-75.0916837031745,
177.140258408853));
#42950=CARTESIAN_POINT('Ctrl Pts',(-51.7684263990719,-75.0764825485946,
178.454742197037));
#42951=CARTESIAN_POINT('Ctrl Pts',(-52.7954012773719,-75.0612813940147,
179.76922598522));
#42952=CARTESIAN_POINT('Ctrl Pts',(-54.4487362026171,-74.9793060737851,
179.975477717318));
#42953=CARTESIAN_POINT('Ctrl Pts',(-56.1020711278624,-74.8973307535556,
180.181729449417));
#42954=CARTESIAN_POINT('Ctrl Pts',(-57.4190865064624,-74.8512093439138,
179.158929658031));
#42955=CARTESIAN_POINT('Ctrl Pts',(-58.7361018850625,-74.805087934272,178.136129866644));
#42956=CARTESIAN_POINT('Ctrl Pts',(-58.9511295525604,-74.876445776897,176.483420797975));
#42957=CARTESIAN_POINT('Ctrl Pts',(-59.1661572200583,-74.9478036195221,
174.830711729305));
#42958=CARTESIAN_POINT('Ctrl Pts',(-58.1590584675924,-75.1494483034127,
173.516227941122));
#42959=CARTESIAN_POINT('Ctrl Pts',(-57.1519597151264,-75.3510929873033,
172.201744152939));
#42960=CARTESIAN_POINT('Ctrl Pts',(-55.5185009157152,-75.6195118368435,
171.99549242084));
#42961=CARTESIAN_POINT('Ctrl Pts',(-53.885042116304,-75.8879306863838,171.789240688742));
#42962=CARTESIAN_POINT('Ctrl Pts',(-52.587902863538,-76.1204956253363,172.812040480128));
#42963=CARTESIAN_POINT('Ctrl Pts',(-51.290763610772,-76.3530605642888,173.834840271514));
#42964=CARTESIAN_POINT('Ctrl Pts',(-51.0956120691081,-76.4681462509745,
175.487549340184));
#42965=CARTESIAN_POINT('Ctrl Pts',(-50.9004605274442,-76.5832319376601,
177.140258408853));
#42966=CARTESIAN_POINT('Ctrl Pts',(-51.9274354057441,-76.5680307830801,
178.454742197037));
#42967=CARTESIAN_POINT('Ctrl Pts',(-52.9544102840441,-76.5528296285002,
179.76922598522));
#42968=CARTESIAN_POINT('Ctrl Pts',(-54.6077452092894,-76.4708543082707,
179.975477717318));
#42969=CARTESIAN_POINT('Ctrl Pts',(-56.2610801345346,-76.3888789880412,
180.181729449417));
#42970=CARTESIAN_POINT('Ctrl Pts',(-57.5780955131346,-76.3427575783994,
179.158929658031));
#42971=CARTESIAN_POINT('Ctrl Pts',(-58.8951108917347,-76.2966361687575,
178.136129866644));
#42972=CARTESIAN_POINT('Ctrl Pts',(-59.1101385592326,-76.3679940113826,
176.483420797975));
#42973=CARTESIAN_POINT('Ctrl Pts',(-59.3251662267305,-76.4393518540077,
174.830711729305));
#42974=CARTESIAN_POINT('Ctrl Pts',(-58.3180674742646,-76.6409965378983,
173.516227941122));
#42975=CARTESIAN_POINT('Ctrl Pts',(-57.3109687217987,-76.8426412217889,
172.201744152939));
#42976=CARTESIAN_POINT('Ctrl Pts',(-55.6775099223874,-77.1110600713291,
171.99549242084));
#42977=CARTESIAN_POINT('Ctrl Pts',(-54.0440511229762,-77.3794789208693,
171.789240688742));
#42978=CARTESIAN_POINT('Ctrl Pts',(-52.7469118702102,-77.6120438598219,
172.812040480128));
#42979=CARTESIAN_POINT('Ctrl Pts',(-51.4497726174442,-77.8446087987744,
173.834840271514));
#42980=CARTESIAN_POINT('Ctrl Pts',(-51.2546210757803,-77.95969448546,175.487549340184));
#42981=CARTESIAN_POINT('Ctrl Pts',(-51.0594695341164,-78.0747801721457,
177.140258408853));
#42982=CARTESIAN_POINT('Ctrl Pts',(-52.0864444124164,-78.0595790175658,
178.454742197037));
#42983=CARTESIAN_POINT('Ctrl Pts',(-53.1134192907163,-78.0443778629858,
179.76922598522));
#42984=CARTESIAN_POINT('Ctrl Pts',(-54.7667542159616,-77.9624025427563,
179.975477717318));
#42985=CARTESIAN_POINT('Ctrl Pts',(-56.4200891412068,-77.8804272225268,
180.181729449417));
#42986=CARTESIAN_POINT('Ctrl Pts',(-57.7371045198069,-77.834305812885,179.158929658031));
#42987=CARTESIAN_POINT('Ctrl Pts',(-59.0541198984069,-77.7881844032432,
178.136129866644));
#42988=CARTESIAN_POINT('Ctrl Pts',(-59.2691475659048,-77.8595422458682,
176.483420797975));
#42989=CARTESIAN_POINT('Ctrl Pts',(-59.4841752334028,-77.9309000884933,
174.830711729305));
#42990=CARTESIAN_POINT('Ctrl Pts',(-58.4770764809368,-78.1325447723839,
173.516227941122));
#42991=CARTESIAN_POINT('Ctrl Pts',(-57.4699777284709,-78.3341894562745,
172.201744152939));
#42992=CARTESIAN_POINT('Ctrl Pts',(-55.8365189290597,-78.6026083058147,
171.99549242084));
#42993=CARTESIAN_POINT('Ctrl Pts',(-54.2030601296484,-78.871027155355,171.789240688742));
#42994=CARTESIAN_POINT('Ctrl Pts',(-52.9059208768824,-79.1035920943075,
172.812040480128));
#42995=CARTESIAN_POINT('Ctrl Pts',(-51.6087816241164,-79.33615703326,173.834840271514));
#42996=CARTESIAN_POINT('Ctrl Pts',(-51.4136300824525,-79.4512427199456,
175.487549340184));
#42997=CARTESIAN_POINT('Ctrl Pts',(-51.2184785407886,-79.5663284066313,
177.140258408853));
#42998=CARTESIAN_POINT('Ctrl Pts',(-52.2454534190886,-79.5511272520514,
178.454742197037));
#42999=CARTESIAN_POINT('Ctrl Pts',(-53.2724282973886,-79.5359260974714,
179.76922598522));
#43000=CARTESIAN_POINT('Ctrl Pts',(-54.9257632226338,-79.4539507772419,
179.975477717318));
#43001=CARTESIAN_POINT('Ctrl Pts',(-56.5790981478791,-79.3719754570124,
180.181729449417));
#43002=CARTESIAN_POINT('Ctrl Pts',(-57.8961135264791,-79.3258540473706,
179.158929658031));
#43003=CARTESIAN_POINT('Ctrl Pts',(-59.2131289050791,-79.2797326377288,
178.136129866644));
#43004=CARTESIAN_POINT('Ctrl Pts',(-59.4281565725771,-79.3510904803538,
176.483420797975));
#43005=CARTESIAN_POINT('Ctrl Pts',(-59.643184240075,-79.4224483229789,174.830711729305));
#43006=CARTESIAN_POINT('Ctrl Pts',(-58.6360854876091,-79.6240930068695,
173.516227941122));
#43007=CARTESIAN_POINT('Ctrl Pts',(-57.6289867351431,-79.8257376907601,
172.201744152939));
#43008=CARTESIAN_POINT('Ctrl Pts',(-55.9955279357319,-80.0941565403003,
171.99549242084));
#43009=CARTESIAN_POINT('Ctrl Pts',(-54.3620691363207,-80.3625753898405,
171.789240688742));
#43010=CARTESIAN_POINT('Ctrl Pts',(-53.0649298835546,-80.5951403287931,
172.812040480128));
#43011=CARTESIAN_POINT('Ctrl Pts',(-51.7677906307886,-80.8277052677456,
173.834840271514));
#43012=CARTESIAN_POINT('Ctrl Pts',(-51.5726390891247,-80.9427909544312,
175.487549340184));
#43013=CARTESIAN_POINT('Ctrl Pts',(-51.3774875474608,-81.0578766411169,
177.140258408853));
#43014=CARTESIAN_POINT('Ctrl Pts',(-52.4044624257608,-81.042675486537,178.454742197037));
#43015=CARTESIAN_POINT('Ctrl Pts',(-53.4314373040608,-81.027474331957,179.76922598522));
#43016=CARTESIAN_POINT('Ctrl Pts',(-55.084772229306,-80.9454990117275,179.975477717318));
#43017=CARTESIAN_POINT('Ctrl Pts',(-56.7381071545513,-80.863523691498,180.181729449417));
#43018=CARTESIAN_POINT('Ctrl Pts',(-58.0551225331513,-80.8174022818562,
179.158929658031));
#43019=CARTESIAN_POINT('Ctrl Pts',(-59.3721379117514,-80.7712808722144,
178.136129866644));
#43020=CARTESIAN_POINT('Ctrl Pts',(-59.5871655792493,-80.8426387148394,
176.483420797975));
#43021=CARTESIAN_POINT('Ctrl Pts',(-59.8021932467472,-80.9139965574645,
174.830711729305));
#43022=CARTESIAN_POINT('Ctrl Pts',(-58.7950944942813,-81.1156412413551,
173.516227941122));
#43023=CARTESIAN_POINT('Ctrl Pts',(-57.7879957418153,-81.3172859252457,
172.201744152939));
#43024=CARTESIAN_POINT('Ctrl Pts',(-56.1545369424041,-81.5857047747859,
171.99549242084));
#43025=CARTESIAN_POINT('Ctrl Pts',(-54.5210781429929,-81.8541236243262,
171.789240688742));
#43026=CARTESIAN_POINT('Ctrl Pts',(-53.2239388902269,-82.0866885632787,
172.812040480128));
#43027=CARTESIAN_POINT('Ctrl Pts',(-51.9267996374609,-82.3192535022312,
173.834840271514));
#43028=CARTESIAN_POINT('Ctrl Pts',(-51.731648095797,-82.4343391889168,175.487549340184));
#43029=CARTESIAN_POINT('Ctrl Pts',(-51.5364965541331,-82.5494248756025,
177.140258408853));
#43030=CARTESIAN_POINT('Ctrl Pts',(-52.563471432433,-82.5342237210226,178.454742197037));
#43031=CARTESIAN_POINT('Ctrl Pts',(-53.590446310733,-82.5190225664426,179.76922598522));
#43032=CARTESIAN_POINT('Ctrl Pts',(-55.2437812359783,-82.4370472462131,
179.975477717318));
#43033=CARTESIAN_POINT('Ctrl Pts',(-56.8971161612235,-82.3550719259836,
180.181729449417));
#43034=CARTESIAN_POINT('Ctrl Pts',(-58.2141315398236,-82.3089505163418,
179.158929658031));
#43035=CARTESIAN_POINT('Ctrl Pts',(-59.5311469184236,-82.2628291066999,
178.136129866644));
#43036=CARTESIAN_POINT('Ctrl Pts',(-59.7461745859215,-82.334186949325,176.483420797975));
#43037=CARTESIAN_POINT('Ctrl Pts',(-59.9612022534195,-82.4055447919501,
174.830711729305));
#43038=CARTESIAN_POINT('Ctrl Pts',(-58.9541035009535,-82.6071894758407,
173.516227941122));
#43039=CARTESIAN_POINT('Ctrl Pts',(-57.9470047484876,-82.8088341597313,
172.201744152939));
#43040=CARTESIAN_POINT('Ctrl Pts',(-56.3135459490763,-83.0772530092715,
171.99549242084));
#43041=CARTESIAN_POINT('Ctrl Pts',(-54.6800871496651,-83.3456718588118,
171.789240688742));
#43042=CARTESIAN_POINT('Ctrl Pts',(-53.3829478968991,-83.5782367977643,
172.812040480128));
#43043=CARTESIAN_POINT('Ctrl Pts',(-52.0858086441331,-83.8108017367168,
173.834840271514));
#43044=CARTESIAN_POINT('Ctrl Pts',(-51.8906571024692,-83.9258874234024,
175.487549340184));
#43045=CARTESIAN_POINT('Ctrl Pts',(-51.6955055608053,-84.0409731100881,
177.140258408853));
#43046=CARTESIAN_POINT('Ctrl Pts',(-52.7224804391053,-84.0257719555082,
178.454742197037));
#43047=CARTESIAN_POINT('Ctrl Pts',(-53.7494553174052,-84.0105708009282,
179.76922598522));
#43048=CARTESIAN_POINT('Ctrl Pts',(-55.4027902426505,-83.9285954806987,
179.975477717318));
#43049=CARTESIAN_POINT('Ctrl Pts',(-57.0561251678958,-83.8466201604692,
180.181729449417));
#43050=CARTESIAN_POINT('Ctrl Pts',(-58.3731405464958,-83.8004987508274,
179.158929658031));
#43051=CARTESIAN_POINT('Ctrl Pts',(-59.6901559250958,-83.7543773411855,
178.136129866644));
#43052=CARTESIAN_POINT('Ctrl Pts',(-59.9051835925938,-83.8257351838106,
176.483420797975));
#43053=CARTESIAN_POINT('Ctrl Pts',(-60.1202112600917,-83.8970930264357,
174.830711729305));
#43054=CARTESIAN_POINT('Ctrl Pts',(-59.1131125076257,-84.0987377103263,
173.516227941122));
#43055=CARTESIAN_POINT('Ctrl Pts',(-58.1060137551598,-84.3003823942169,
172.201744152939));
#43056=CARTESIAN_POINT('Ctrl Pts',(-56.4725549557486,-84.5688012437571,
171.99549242084));
#43057=CARTESIAN_POINT('Ctrl Pts',(-54.8390961563373,-84.8372200932974,
171.789240688742));
#43058=CARTESIAN_POINT('Ctrl Pts',(-53.5419569035713,-85.0697850322499,
172.812040480128));
#43059=CARTESIAN_POINT('Ctrl Pts',(-52.2448176508053,-85.3023499712024,
173.834840271514));
#43060=CARTESIAN_POINT('Ctrl Pts',(-52.0496661091414,-85.417435657888,175.487549340184));
#43061=CARTESIAN_POINT('Ctrl Pts',(-51.8545145674775,-85.5325213445737,
177.140258408853));
#43062=CARTESIAN_POINT('Ctrl Pts',(-52.8814894457775,-85.5173201899938,
178.454742197037));
#43063=CARTESIAN_POINT('Ctrl Pts',(-53.9084643240775,-85.5021190354138,
179.76922598522));
#43064=CARTESIAN_POINT('Ctrl Pts',(-55.5617992493227,-85.4201437151843,
179.975477717318));
#43065=CARTESIAN_POINT('Ctrl Pts',(-57.215134174568,-85.3381683949548,180.181729449417));
#43066=CARTESIAN_POINT('Ctrl Pts',(-58.532149553168,-85.292046985313,179.158929658031));
#43067=CARTESIAN_POINT('Ctrl Pts',(-59.849164931768,-85.2459255756712,178.136129866644));
#43068=CARTESIAN_POINT('Ctrl Pts',(-60.064192599266,-85.3172834182962,176.483420797975));
#43069=CARTESIAN_POINT('Ctrl Pts',(-60.2792202667639,-85.3886412609213,
174.830711729305));
#43070=CARTESIAN_POINT('Ctrl Pts',(-59.272121514298,-85.5902859448119,173.516227941122));
#43071=CARTESIAN_POINT('Ctrl Pts',(-58.265022761832,-85.7919306287025,172.201744152939));
#43072=CARTESIAN_POINT('Ctrl Pts',(-56.6315639624208,-86.0603494782428,
171.99549242084));
#43073=CARTESIAN_POINT('Ctrl Pts',(-54.9981051630096,-86.328768327783,171.789240688742));
#43074=CARTESIAN_POINT('Ctrl Pts',(-53.7009659102436,-86.5613332667355,
172.812040480128));
#43075=CARTESIAN_POINT('Ctrl Pts',(-52.4038266574776,-86.793898205688,173.834840271514));
#43076=CARTESIAN_POINT('Ctrl Pts',(-52.2086751158136,-86.9089838923736,
175.487549340184));
#43077=CARTESIAN_POINT('Ctrl Pts',(-52.0135235741498,-87.0240695790593,
177.140258408853));
#43078=CARTESIAN_POINT('Ctrl Pts',(-53.0404984524497,-87.0088684244793,
178.454742197037));
#43079=CARTESIAN_POINT('Ctrl Pts',(-54.0674733307497,-86.9936672698994,
179.76922598522));
#43080=CARTESIAN_POINT('Ctrl Pts',(-55.720808255995,-86.9116919496699,179.975477717318));
#43081=CARTESIAN_POINT('Ctrl Pts',(-57.3741431812402,-86.8297166294404,
180.181729449417));
#43082=CARTESIAN_POINT('Ctrl Pts',(-58.6911585598402,-86.7835952197986,
179.158929658031));
#43083=CARTESIAN_POINT('Ctrl Pts',(-60.0081739384403,-86.7374738101568,
178.136129866644));
#43084=CARTESIAN_POINT('Ctrl Pts',(-60.2232016059382,-86.8088316527818,
176.483420797975));
#43085=CARTESIAN_POINT('Ctrl Pts',(-60.4382292734361,-86.8801894954069,
174.830711729305));
#43086=CARTESIAN_POINT('Ctrl Pts',(-59.4311305209702,-87.0818341792975,
173.516227941122));
#43087=CARTESIAN_POINT('Ctrl Pts',(-58.4240317685042,-87.2834788631881,
172.201744152939));
#43088=CARTESIAN_POINT('Ctrl Pts',(-56.790572969093,-87.5518977127283,171.99549242084));
#43089=CARTESIAN_POINT('Ctrl Pts',(-55.1571141696818,-87.8203165622686,
171.789240688742));
#43090=CARTESIAN_POINT('Ctrl Pts',(-53.8599749169158,-88.0528815012211,
172.812040480128));
#43091=CARTESIAN_POINT('Ctrl Pts',(-52.5628356641498,-88.2854464401736,
173.834840271514));
#43092=CARTESIAN_POINT('Ctrl Pts',(-52.3676841224859,-88.4005321268593,
175.487549340184));
#43093=CARTESIAN_POINT('Ctrl Pts',(-52.172532580822,-88.5156178135449,177.140258408853));
#43094=CARTESIAN_POINT('Ctrl Pts',(-53.199507459122,-88.500416658965,178.454742197037));
#43095=CARTESIAN_POINT('Ctrl Pts',(-54.2264823374219,-88.4852155043851,
179.76922598522));
#43096=CARTESIAN_POINT('Ctrl Pts',(-55.8798172626672,-88.4032401841555,
179.975477717318));
#43097=CARTESIAN_POINT('Ctrl Pts',(-57.5331521879124,-88.321264863926,180.181729449417));
#43098=CARTESIAN_POINT('Ctrl Pts',(-58.8501675665125,-88.2751434542842,
179.158929658031));
#43099=CARTESIAN_POINT('Ctrl Pts',(-60.1671829451125,-88.2290220446423,
178.136129866644));
#43100=CARTESIAN_POINT('Ctrl Pts',(-60.3822106126104,-88.3003798872674,
176.483420797975));
#43101=CARTESIAN_POINT('Ctrl Pts',(-60.5972382801084,-88.3717377298925,
174.830711729305));
#43102=CARTESIAN_POINT('Ctrl Pts',(-59.5901395276424,-88.5733824137831,
173.516227941122));
#43103=CARTESIAN_POINT('Ctrl Pts',(-58.5830407751765,-88.7750270976737,
172.201744152939));
#43104=CARTESIAN_POINT('Ctrl Pts',(-56.9495819757652,-89.0434459472139,
171.99549242084));
#43105=CARTESIAN_POINT('Ctrl Pts',(-55.316123176354,-89.3118647967542,171.789240688742));
#43106=CARTESIAN_POINT('Ctrl Pts',(-54.018983923588,-89.5444297357067,172.812040480128));
#43107=CARTESIAN_POINT('Ctrl Pts',(-52.721844670822,-89.7769946746592,173.834840271514));
#43108=CARTESIAN_POINT('Ctrl Pts',(-52.5266931291581,-89.8920803613448,
175.487549340184));
#43109=CARTESIAN_POINT('Ctrl Pts',(-52.3315415874942,-90.0071660480305,
177.140258408853));
#43110=CARTESIAN_POINT('Ctrl Pts',(-53.3585164657942,-89.9919648934506,
178.454742197037));
#43111=CARTESIAN_POINT('Ctrl Pts',(-54.3854913440941,-89.9767637388707,
179.76922598522));
#43112=CARTESIAN_POINT('Ctrl Pts',(-56.0388262693394,-89.8947884186411,
179.975477717318));
#43113=CARTESIAN_POINT('Ctrl Pts',(-57.6921611945847,-89.8128130984116,
180.181729449417));
#43114=CARTESIAN_POINT('Ctrl Pts',(-59.0091765731847,-89.7666916887698,
179.158929658031));
#43115=CARTESIAN_POINT('Ctrl Pts',(-60.3261919517847,-89.720570279128,178.136129866644));
#43116=CARTESIAN_POINT('Ctrl Pts',(-60.5412196192827,-89.791928121753,176.483420797975));
#43117=CARTESIAN_POINT('Ctrl Pts',(-60.7562472867806,-89.8632859643781,
174.830711729305));
#43118=CARTESIAN_POINT('Ctrl Pts',(-59.7491485343146,-90.0649306482687,
173.516227941122));
#43119=CARTESIAN_POINT('Ctrl Pts',(-58.7420497818487,-90.2665753321593,
172.201744152939));
#43120=CARTESIAN_POINT('Ctrl Pts',(-57.1085909824375,-90.5349941816995,
171.99549242084));
#43121=CARTESIAN_POINT('Ctrl Pts',(-55.4751321830263,-90.8034130312398,
171.789240688742));
#43122=CARTESIAN_POINT('Ctrl Pts',(-54.1779929302602,-91.0359779701923,
172.812040480128));
#43123=CARTESIAN_POINT('Ctrl Pts',(-52.8808536774942,-91.2685429091448,
173.834840271514));
#43124=CARTESIAN_POINT('Ctrl Pts',(-52.6857021358303,-91.3836285958304,
175.487549340184));
#43125=CARTESIAN_POINT('Ctrl Pts',(-52.4905505941664,-91.4987142825161,
177.140258408853));
#43126=CARTESIAN_POINT('Ctrl Pts',(-53.5175254724664,-91.4835131279361,
178.454742197037));
#43127=CARTESIAN_POINT('Ctrl Pts',(-54.5445003507664,-91.4683119733563,
179.76922598522));
#43128=CARTESIAN_POINT('Ctrl Pts',(-56.1978352760116,-91.3863366531267,
179.975477717318));
#43129=CARTESIAN_POINT('Ctrl Pts',(-57.8511702012569,-91.3043613328972,
180.181729449417));
#43130=CARTESIAN_POINT('Ctrl Pts',(-59.1681855798569,-91.2582399232554,
179.158929658031));
#43131=CARTESIAN_POINT('Ctrl Pts',(-60.485200958457,-91.2121185136135,178.136129866644));
#43132=CARTESIAN_POINT('Ctrl Pts',(-60.7002286259549,-91.2834763562386,
176.483420797975));
#43133=CARTESIAN_POINT('Ctrl Pts',(-60.9152562934528,-91.3548341988637,
174.830711729305));
#43134=CARTESIAN_POINT('Ctrl Pts',(-59.9081575409869,-91.5564788827543,
173.516227941122));
#43135=CARTESIAN_POINT('Ctrl Pts',(-58.9010587885209,-91.7581235666449,
172.201744152939));
#43136=CARTESIAN_POINT('Ctrl Pts',(-57.2675999891097,-92.0265424161851,
171.99549242084));
#43137=CARTESIAN_POINT('Ctrl Pts',(-55.6341411896985,-92.2949612657254,
171.789240688742));
#43138=CARTESIAN_POINT('Ctrl Pts',(-54.3370019369325,-92.5275262046779,
172.812040480128));
#43139=CARTESIAN_POINT('Ctrl Pts',(-53.0398626841665,-92.7600911436304,
173.834840271514));
#43140=CARTESIAN_POINT('Ctrl Pts',(-52.8447111425026,-92.875176830316,175.487549340184));
#43141=CARTESIAN_POINT('Ctrl Pts',(-52.6495596008387,-92.9902625170017,
177.140258408853));
#43142=CARTESIAN_POINT('Ctrl Pts',(-53.6765344791386,-92.9750613624218,
178.454742197037));
#43143=CARTESIAN_POINT('Ctrl Pts',(-54.7035093574386,-92.9598602078419,
179.76922598522));
#43144=CARTESIAN_POINT('Ctrl Pts',(-56.3568442826839,-92.8778848876123,
179.975477717318));
#43145=CARTESIAN_POINT('Ctrl Pts',(-58.0101792079291,-92.7959095673828,
180.181729449417));
#43146=CARTESIAN_POINT('Ctrl Pts',(-59.3271945865291,-92.749788157741,179.158929658031));
#43147=CARTESIAN_POINT('Ctrl Pts',(-60.6442099651292,-92.7036667480992,
178.136129866644));
#43148=CARTESIAN_POINT('Ctrl Pts',(-60.8592376326271,-92.7750245907242,
176.483420797975));
#43149=CARTESIAN_POINT('Ctrl Pts',(-61.074265300125,-92.8463824333493,174.830711729305));
#43150=CARTESIAN_POINT('Ctrl Pts',(-60.0671665476591,-93.0480271172399,
173.516227941122));
#43151=CARTESIAN_POINT('Ctrl Pts',(-59.0600677951932,-93.2496718011305,
172.201744152939));
#43152=CARTESIAN_POINT('Ctrl Pts',(-57.4266089957819,-93.5180906506707,
171.99549242084));
#43153=CARTESIAN_POINT('Ctrl Pts',(-55.7931501963707,-93.786509500211,171.789240688742));
#43154=CARTESIAN_POINT('Ctrl Pts',(-54.4960109436047,-94.0190744391634,
172.812040480128));
#43155=CARTESIAN_POINT('Ctrl Pts',(-53.1988716908387,-94.251639378116,173.834840271514));
#43156=CARTESIAN_POINT('Ctrl Pts',(-53.0037201491748,-94.3667250648016,
175.487549340184));
#43157=CARTESIAN_POINT('Ctrl Pts',(-52.8085686075109,-94.4818107514873,
177.140258408853));
#43158=CARTESIAN_POINT('Ctrl Pts',(-53.8355434858109,-94.4666095969074,
178.454742197037));
#43159=CARTESIAN_POINT('Ctrl Pts',(-54.8625183641108,-94.4514084423274,
179.76922598522));
#43160=CARTESIAN_POINT('Ctrl Pts',(-56.5158532893561,-94.3694331220979,
179.975477717318));
#43161=CARTESIAN_POINT('Ctrl Pts',(-58.1691882146013,-94.2874578018684,
180.181729449417));
#43162=CARTESIAN_POINT('Ctrl Pts',(-59.4862035932014,-94.2413363922266,
179.158929658031));
#43163=CARTESIAN_POINT('Ctrl Pts',(-60.8032189718014,-94.1952149825848,
178.136129866644));
#43164=CARTESIAN_POINT('Ctrl Pts',(-61.0182466392993,-94.2665728252098,
176.483420797975));
#43165=CARTESIAN_POINT('Ctrl Pts',(-61.2332743067973,-94.3379306678349,
174.830711729305));
#43166=CARTESIAN_POINT('Ctrl Pts',(-60.2261755543313,-94.5395753517255,
173.516227941122));
#43167=CARTESIAN_POINT('Ctrl Pts',(-59.2190768018654,-94.7412200356161,
172.201744152939));
#43168=CARTESIAN_POINT('Ctrl Pts',(-57.5856180024542,-95.0096388851563,
171.99549242084));
#43169=CARTESIAN_POINT('Ctrl Pts',(-55.9521592030429,-95.2780577346965,
171.789240688742));
#43170=CARTESIAN_POINT('Ctrl Pts',(-54.6550199502769,-95.5106226736491,
172.812040480128));
#43171=CARTESIAN_POINT('Ctrl Pts',(-53.3578806975109,-95.7431876126016,
173.834840271514));
#43172=CARTESIAN_POINT('Ctrl Pts',(-53.162729155847,-95.8582732992872,175.487549340184));
#43173=CARTESIAN_POINT('Ctrl Pts',(-52.9675776141831,-95.9733589859729,
177.140258408853));
#43174=CARTESIAN_POINT('Ctrl Pts',(-53.9945524924831,-95.958157831393,178.454742197037));
#43175=CARTESIAN_POINT('Ctrl Pts',(-55.0215273707831,-95.9429566768131,
179.76922598522));
#43176=CARTESIAN_POINT('Ctrl Pts',(-56.6748622960283,-95.8609813565835,
179.975477717318));
#43177=CARTESIAN_POINT('Ctrl Pts',(-58.3281972212736,-95.779006036354,180.181729449417));
#43178=CARTESIAN_POINT('Ctrl Pts',(-59.6452125998736,-95.7328846267122,
179.158929658031));
#43179=CARTESIAN_POINT('Ctrl Pts',(-60.9622279784736,-95.6867632170703,
178.136129866644));
#43180=CARTESIAN_POINT('Ctrl Pts',(-61.1772556459716,-95.7581210596954,
176.483420797975));
#43181=CARTESIAN_POINT('Ctrl Pts',(-61.3922833134695,-95.8294789023205,
174.830711729305));
#43182=CARTESIAN_POINT('Ctrl Pts',(-60.3851845610036,-96.0311235862111,
173.516227941122));
#43183=CARTESIAN_POINT('Ctrl Pts',(-59.3780858085376,-96.2327682701017,
172.201744152939));
#43184=CARTESIAN_POINT('Ctrl Pts',(-57.7446270091264,-96.5011871196419,
171.99549242084));
#43185=CARTESIAN_POINT('Ctrl Pts',(-56.1111682097152,-96.7696059691822,
171.789240688742));
#43186=CARTESIAN_POINT('Ctrl Pts',(-54.8140289569491,-97.0021709081347,
172.812040480128));
#43187=CARTESIAN_POINT('Ctrl Pts',(-53.5168897041831,-97.2347358470872,
173.834840271514));
#43188=CARTESIAN_POINT('Ctrl Pts',(-53.3217381625192,-97.3498215337729,
175.487549340184));
#43189=CARTESIAN_POINT('Ctrl Pts',(-53.1265866208553,-97.4649072204585,
177.140258408853));
#43190=CARTESIAN_POINT('Ctrl Pts',(-54.1535614991553,-97.4497060658786,
178.454742197037));
#43191=CARTESIAN_POINT('Ctrl Pts',(-55.1805363774553,-97.4345049112986,
179.76922598522));
#43192=CARTESIAN_POINT('Ctrl Pts',(-56.8338713027005,-97.3525295910691,
179.975477717318));
#43193=CARTESIAN_POINT('Ctrl Pts',(-58.4872062279458,-97.2705542708396,
180.181729449417));
#43194=CARTESIAN_POINT('Ctrl Pts',(-59.8042216065458,-97.2244328611978,
179.158929658031));
#43195=CARTESIAN_POINT('Ctrl Pts',(-61.1212369851459,-97.178311451556,178.136129866644));
#43196=CARTESIAN_POINT('Ctrl Pts',(-61.3362646526438,-97.249669294181,176.483420797975));
#43197=CARTESIAN_POINT('Ctrl Pts',(-61.5512923201417,-97.3210271368061,
174.830711729305));
#43198=CARTESIAN_POINT('Ctrl Pts',(-60.5441935676758,-97.5226718206967,
173.516227941122));
#43199=CARTESIAN_POINT('Ctrl Pts',(-59.5370948152098,-97.7243165045873,
172.201744152939));
#43200=CARTESIAN_POINT('Ctrl Pts',(-57.9036360157986,-97.9927353541275,
171.99549242084));
#43201=CARTESIAN_POINT('Ctrl Pts',(-56.2701772163874,-98.2611542036678,
171.789240688742));
#43202=CARTESIAN_POINT('Ctrl Pts',(-54.9730379636214,-98.4937191426203,
172.812040480128));
#43203=CARTESIAN_POINT('Ctrl Pts',(-53.6758987108554,-98.7262840815728,
173.834840271514));
#43204=CARTESIAN_POINT('Ctrl Pts',(-53.4807471691915,-98.8413697682584,
175.487549340184));
#43205=CARTESIAN_POINT('Ctrl Pts',(-53.2855956275276,-98.9564554549441,
177.140258408853));
#43206=CARTESIAN_POINT('Ctrl Pts',(-54.3125705058275,-98.9412543003642,
178.454742197037));
#43207=CARTESIAN_POINT('Ctrl Pts',(-55.3395453841275,-98.9260531457843,
179.76922598522));
#43208=CARTESIAN_POINT('Ctrl Pts',(-56.9928803093728,-98.8440778255547,
179.975477717318));
#43209=CARTESIAN_POINT('Ctrl Pts',(-58.646215234618,-98.7621025053252,180.181729449417));
#43210=CARTESIAN_POINT('Ctrl Pts',(-59.9632306132181,-98.7159810956834,
179.158929658031));
#43211=CARTESIAN_POINT('Ctrl Pts',(-61.2802459918181,-98.6698596860415,
178.136129866644));
#43212=CARTESIAN_POINT('Ctrl Pts',(-61.495273659316,-98.7412175286666,176.483420797975));
#43213=CARTESIAN_POINT('Ctrl Pts',(-61.710301326814,-98.8125753712917,174.830711729305));
#43214=CARTESIAN_POINT('Ctrl Pts',(-60.703202574348,-99.0142200551823,173.516227941122));
#43215=CARTESIAN_POINT('Ctrl Pts',(-59.6961038218821,-99.2158647390729,
172.201744152939));
#43216=CARTESIAN_POINT('Ctrl Pts',(-58.0626450224708,-99.4842835886131,
171.99549242084));
#43217=CARTESIAN_POINT('Ctrl Pts',(-56.4291862230596,-99.7527024381534,
171.789240688742));
#43218=CARTESIAN_POINT('Ctrl Pts',(-55.1320469702936,-99.9852673771059,
172.812040480128));
#43219=CARTESIAN_POINT('Ctrl Pts',(-53.8349077175276,-100.217832316058,
173.834840271514));
#43220=CARTESIAN_POINT('Ctrl Pts',(-53.6397561758637,-100.332918002744,
175.487549340184));
#43221=CARTESIAN_POINT('Ctrl Pts',(-53.4446046341998,-100.44800368943,177.140258408853));
#43222=CARTESIAN_POINT('Ctrl Pts',(-54.4715795124998,-100.43280253485,178.454742197037));
#43223=CARTESIAN_POINT('Ctrl Pts',(-55.4985543907998,-100.41760138027,179.76922598522));
#43224=CARTESIAN_POINT('Ctrl Pts',(-57.151889316045,-100.33562606004,179.975477717318));
#43225=CARTESIAN_POINT('Ctrl Pts',(-58.8052242412903,-100.253650739811,
180.181729449417));
#43226=CARTESIAN_POINT('Ctrl Pts',(-60.1222396198903,-100.207529330169,
179.158929658031));
#43227=CARTESIAN_POINT('Ctrl Pts',(-61.4392549984903,-100.161407920527,
178.136129866644));
#43228=CARTESIAN_POINT('Ctrl Pts',(-61.6542826659882,-100.232765763152,
176.483420797975));
#43229=CARTESIAN_POINT('Ctrl Pts',(-61.8693103334862,-100.304123605777,
174.830711729305));
#43230=CARTESIAN_POINT('Ctrl Pts',(-60.8622115810202,-100.505768289668,
173.516227941122));
#43231=CARTESIAN_POINT('Ctrl Pts',(-59.8551128285543,-100.707412973559,
172.201744152939));
#43232=CARTESIAN_POINT('Ctrl Pts',(-58.2216540291431,-100.975831823099,
171.99549242084));
#43233=CARTESIAN_POINT('Ctrl Pts',(-56.5881952297318,-101.244250672639,
171.789240688742));
#43234=CARTESIAN_POINT('Ctrl Pts',(-55.2910559769658,-101.476815611591,
172.812040480128));
#43235=CARTESIAN_POINT('Ctrl Pts',(-53.9939167241998,-101.709380550544,
173.834840271514));
#43236=CARTESIAN_POINT('Ctrl Pts',(-53.7987651825359,-101.82446623723,175.487549340184));
#43237=CARTESIAN_POINT('Ctrl Pts',(-53.603613640872,-101.939551923915,177.140258408853));
#43238=CARTESIAN_POINT('Ctrl Pts',(-54.630588519172,-101.924350769335,178.454742197037));
#43239=CARTESIAN_POINT('Ctrl Pts',(-55.657563397472,-101.909149614755,179.76922598522));
#43240=CARTESIAN_POINT('Ctrl Pts',(-57.3108983227172,-101.827174294526,
179.975477717318));
#43241=CARTESIAN_POINT('Ctrl Pts',(-58.9642332479625,-101.745198974296,
180.181729449417));
#43242=CARTESIAN_POINT('Ctrl Pts',(-60.2812486265625,-101.699077564655,
179.158929658031));
#43243=CARTESIAN_POINT('Ctrl Pts',(-61.5982640051626,-101.652956155013,
178.136129866644));
#43244=CARTESIAN_POINT('Ctrl Pts',(-61.8132916726605,-101.724313997638,
176.483420797975));
#43245=CARTESIAN_POINT('Ctrl Pts',(-62.0283193401584,-101.795671840263,
174.830711729305));
#43246=CARTESIAN_POINT('Ctrl Pts',(-61.0212205876925,-101.997316524153,
173.516227941122));
#43247=CARTESIAN_POINT('Ctrl Pts',(-60.0141218352265,-102.198961208044,
172.201744152939));
#43248=CARTESIAN_POINT('Ctrl Pts',(-58.3806630358153,-102.467380057584,
171.99549242084));
#43249=CARTESIAN_POINT('Ctrl Pts',(-56.7472042364041,-102.735798907125,
171.789240688742));
#43250=CARTESIAN_POINT('Ctrl Pts',(-55.4500649836381,-102.968363846077,
172.812040480128));
#43251=CARTESIAN_POINT('Ctrl Pts',(-54.1529257308721,-103.20092878503,173.834840271514));
#43252=CARTESIAN_POINT('Ctrl Pts',(-53.9577741892082,-103.316014471715,
175.487549340184));
#43253=CARTESIAN_POINT('Ctrl Pts',(-53.7626226475442,-103.431100158401,
177.140258408853));
#43254=CARTESIAN_POINT('Ctrl Pts',(-54.7895975258442,-103.415899003821,
178.454742197037));
#43255=CARTESIAN_POINT('Ctrl Pts',(-55.8165724041442,-103.400697849241,
179.76922598522));
#43256=CARTESIAN_POINT('Ctrl Pts',(-57.4699073293895,-103.318722529012,
179.975477717318));
#43257=CARTESIAN_POINT('Ctrl Pts',(-59.1232422546347,-103.236747208782,
180.181729449417));
#43258=CARTESIAN_POINT('Ctrl Pts',(-60.4402576332347,-103.19062579914,179.158929658031));
#43259=CARTESIAN_POINT('Ctrl Pts',(-61.7572730118348,-103.144504389498,
178.136129866644));
#43260=CARTESIAN_POINT('Ctrl Pts',(-61.9723006793327,-103.215862232123,
176.483420797975));
#43261=CARTESIAN_POINT('Ctrl Pts',(-62.1873283468306,-103.287220074748,
174.830711729305));
#43262=CARTESIAN_POINT('Ctrl Pts',(-61.1802295943647,-103.488864758639,
173.516227941122));
#43263=CARTESIAN_POINT('Ctrl Pts',(-60.1731308418988,-103.69050944253,172.201744152939));
#43264=CARTESIAN_POINT('Ctrl Pts',(-58.5396720424875,-103.95892829207,171.99549242084));
#43265=CARTESIAN_POINT('Ctrl Pts',(-56.9062132430763,-104.22734714161,171.789240688742));
#43266=CARTESIAN_POINT('Ctrl Pts',(-55.6090739903103,-104.459912080563,
172.812040480128));
#43267=CARTESIAN_POINT('Ctrl Pts',(-54.3119347375443,-104.692477019515,
173.834840271514));
#43268=CARTESIAN_POINT('Ctrl Pts',(-54.1167831958804,-104.807562706201,
175.487549340184));
#43269=CARTESIAN_POINT('Ctrl Pts',(-53.9216316542165,-104.922648392887,
177.140258408853));
#43270=CARTESIAN_POINT('Ctrl Pts',(-54.9486065325165,-104.907447238307,
178.454742197037));
#43271=CARTESIAN_POINT('Ctrl Pts',(-55.9755814108164,-104.892246083727,
179.76922598522));
#43272=CARTESIAN_POINT('Ctrl Pts',(-57.6289163360617,-104.810270763497,
179.975477717318));
#43273=CARTESIAN_POINT('Ctrl Pts',(-59.2822512613069,-104.728295443268,
180.181729449417));
#43274=CARTESIAN_POINT('Ctrl Pts',(-60.599266639907,-104.682174033626,179.158929658031));
#43275=CARTESIAN_POINT('Ctrl Pts',(-61.916282018507,-104.636052623984,178.136129866644));
#43276=CARTESIAN_POINT('Ctrl Pts',(-62.1313096860049,-104.707410466609,
176.483420797975));
#43277=CARTESIAN_POINT('Ctrl Pts',(-62.3463373535029,-104.778768309234,
174.830711729305));
#43278=CARTESIAN_POINT('Ctrl Pts',(-61.3392386010369,-104.980412993125,
173.516227941122));
#43279=CARTESIAN_POINT('Ctrl Pts',(-60.332139848571,-105.182057677015,172.201744152939));
#43280=CARTESIAN_POINT('Ctrl Pts',(-58.6986810491597,-105.450476526556,
171.99549242084));
#43281=CARTESIAN_POINT('Ctrl Pts',(-57.0652222497485,-105.718895376096,
171.789240688742));
#43282=CARTESIAN_POINT('Ctrl Pts',(-55.7680829969825,-105.951460315048,
172.812040480128));
#43283=CARTESIAN_POINT('Ctrl Pts',(-54.4709437442165,-106.184025254001,
173.834840271514));
#43284=CARTESIAN_POINT('Ctrl Pts',(-54.2757922025526,-106.299110940686,
175.487549340184));
#43285=CARTESIAN_POINT('Ctrl Pts',(-54.0806406608887,-106.414196627372,
177.140258408853));
#43286=CARTESIAN_POINT('Ctrl Pts',(-55.1076155391887,-106.398995472792,
178.454742197037));
#43287=CARTESIAN_POINT('Ctrl Pts',(-56.1345904174887,-106.383794318212,
179.76922598522));
#43288=CARTESIAN_POINT('Ctrl Pts',(-57.7879253427339,-106.301818997983,
179.975477717318));
#43289=CARTESIAN_POINT('Ctrl Pts',(-59.4412602679792,-106.219843677753,
180.181729449417));
#43290=CARTESIAN_POINT('Ctrl Pts',(-60.7582756465792,-106.173722268111,
179.158929658031));
#43291=CARTESIAN_POINT('Ctrl Pts',(-62.0752910251792,-106.12760085847,178.136129866644));
#43292=CARTESIAN_POINT('Ctrl Pts',(-62.2903186926772,-106.198958701095,
176.483420797975));
#43293=CARTESIAN_POINT('Ctrl Pts',(-62.5053463601751,-106.27031654372,174.830711729305));
#43294=CARTESIAN_POINT('Ctrl Pts',(-61.4982476077091,-106.47196122761,173.516227941122));
#43295=CARTESIAN_POINT('Ctrl Pts',(-60.4911488552432,-106.673605911501,
172.201744152939));
#43296=CARTESIAN_POINT('Ctrl Pts',(-58.857690055832,-106.942024761041,171.99549242084));
#43297=CARTESIAN_POINT('Ctrl Pts',(-57.2242312564208,-107.210443610581,
171.789240688742));
#43298=CARTESIAN_POINT('Ctrl Pts',(-55.9270920036547,-107.443008549534,
172.812040480128));
#43299=CARTESIAN_POINT('Ctrl Pts',(-54.6299527508887,-107.675573488486,
173.834840271514));
#43300=CARTESIAN_POINT('Ctrl Pts',(-54.4348012092248,-107.790659175172,
175.487549340184));
#43301=CARTESIAN_POINT('Ctrl Pts',(-54.2396496675609,-107.905744861858,
177.140258408853));
#43302=CARTESIAN_POINT('Ctrl Pts',(-55.2666245458609,-107.890543707278,
178.454742197037));
#43303=CARTESIAN_POINT('Ctrl Pts',(-56.2935994241609,-107.875342552698,
179.76922598522));
#43304=CARTESIAN_POINT('Ctrl Pts',(-57.9469343494061,-107.793367232468,
179.975477717318));
#43305=CARTESIAN_POINT('Ctrl Pts',(-59.6002692746514,-107.711391912239,
180.181729449417));
#43306=CARTESIAN_POINT('Ctrl Pts',(-60.9172846532514,-107.665270502597,
179.158929658031));
#43307=CARTESIAN_POINT('Ctrl Pts',(-62.2343000318515,-107.619149092955,
178.136129866644));
#43308=CARTESIAN_POINT('Ctrl Pts',(-62.4493276993494,-107.69050693558,176.483420797975));
#43309=CARTESIAN_POINT('Ctrl Pts',(-62.6643553668473,-107.761864778205,
174.830711729305));
#43310=CARTESIAN_POINT('Ctrl Pts',(-61.6572566143814,-107.963509462096,
173.516227941122));
#43311=CARTESIAN_POINT('Ctrl Pts',(-60.6501578619154,-108.165154145987,
172.201744152939));
#43312=CARTESIAN_POINT('Ctrl Pts',(-59.0166990625042,-108.433572995527,
171.99549242084));
#43313=CARTESIAN_POINT('Ctrl Pts',(-57.383240263093,-108.701991845067,171.789240688742));
#43314=CARTESIAN_POINT('Ctrl Pts',(-56.086101010327,-108.934556784019,172.812040480128));
#43315=CARTESIAN_POINT('Ctrl Pts',(-54.788961757561,-109.167121722972,173.834840271514));
#43316=CARTESIAN_POINT('Ctrl Pts',(-54.5938102158971,-109.282207409658,
175.487549340184));
#43317=CARTESIAN_POINT('Ctrl Pts',(-54.3986586742332,-109.397293096343,
177.140258408853));
#43318=CARTESIAN_POINT('Ctrl Pts',(-55.4256335525331,-109.382091941763,
178.454742197037));
#43319=CARTESIAN_POINT('Ctrl Pts',(-56.4526084308331,-109.366890787183,
179.76922598522));
#43320=CARTESIAN_POINT('Ctrl Pts',(-58.1059433560784,-109.284915466954,
179.975477717318));
#43321=CARTESIAN_POINT('Ctrl Pts',(-59.7592782813236,-109.202940146724,
180.181729449417));
#43322=CARTESIAN_POINT('Ctrl Pts',(-61.0762936599236,-109.156818737083,
179.158929658031));
#43323=CARTESIAN_POINT('Ctrl Pts',(-62.3933090385237,-109.110697327441,
178.136129866644));
#43324=CARTESIAN_POINT('Ctrl Pts',(-62.6083367060216,-109.182055170066,
176.483420797975));
#43325=CARTESIAN_POINT('Ctrl Pts',(-62.8233643735195,-109.253413012691,
174.830711729305));
#43326=CARTESIAN_POINT('Ctrl Pts',(-61.8162656210536,-109.455057696581,
173.516227941122));
#43327=CARTESIAN_POINT('Ctrl Pts',(-60.8091668685877,-109.656702380472,
172.201744152939));
#43328=CARTESIAN_POINT('Ctrl Pts',(-59.1757080691764,-109.925121230012,
171.99549242084));
#43329=CARTESIAN_POINT('Ctrl Pts',(-57.5422492697652,-110.193540079553,
171.789240688742));
#43330=CARTESIAN_POINT('Ctrl Pts',(-56.2451100169992,-110.426105018505,
172.812040480128));
#43331=CARTESIAN_POINT('Ctrl Pts',(-54.9479707642332,-110.658669957458,
173.834840271514));
#43332=CARTESIAN_POINT('Ctrl Pts',(-54.7528192225693,-110.773755644143,
175.487549340184));
#43333=CARTESIAN_POINT('Ctrl Pts',(-54.5576676809054,-110.888841330829,
177.140258408853));
#43334=CARTESIAN_POINT('Ctrl Pts',(-55.5846425592054,-110.873640176249,
178.454742197037));
#43335=CARTESIAN_POINT('Ctrl Pts',(-56.6116174375053,-110.858439021669,
179.76922598522));
#43336=CARTESIAN_POINT('Ctrl Pts',(-58.2649523627506,-110.77646370144,179.975477717318));
#43337=CARTESIAN_POINT('Ctrl Pts',(-59.9182872879959,-110.69448838121,180.181729449417));
#43338=CARTESIAN_POINT('Ctrl Pts',(-61.2353026665959,-110.648366971568,
179.158929658031));
#43339=CARTESIAN_POINT('Ctrl Pts',(-62.5523180451959,-110.602245561926,
178.136129866644));
#43340=CARTESIAN_POINT('Ctrl Pts',(-62.7673457126938,-110.673603404551,
176.483420797975));
#43341=CARTESIAN_POINT('Ctrl Pts',(-62.9823733801918,-110.744961247176,
174.830711729305));
#43342=CARTESIAN_POINT('Ctrl Pts',(-61.9752746277258,-110.946605931067,
173.516227941122));
#43343=CARTESIAN_POINT('Ctrl Pts',(-60.9681758752599,-111.148250614958,
172.201744152939));
#43344=CARTESIAN_POINT('Ctrl Pts',(-59.3347170758487,-111.416669464498,
171.99549242084));
#43345=CARTESIAN_POINT('Ctrl Pts',(-57.7012582764374,-111.685088314038,
171.789240688742));
#43346=CARTESIAN_POINT('Ctrl Pts',(-56.4041190236714,-111.917653252991,
172.812040480128));
#43347=CARTESIAN_POINT('Ctrl Pts',(-55.1069797709054,-112.150218191943,
173.834840271514));
#43348=CARTESIAN_POINT('Ctrl Pts',(-54.9118282292415,-112.265303878629,
175.487549340184));
#43349=CARTESIAN_POINT('Ctrl Pts',(-54.7166766875776,-112.380389565314,
177.140258408853));
#43350=CARTESIAN_POINT('Ctrl Pts',(-55.7436515658776,-112.365188410735,
178.454742197037));
#43351=CARTESIAN_POINT('Ctrl Pts',(-56.7706264441776,-112.349987256155,
179.76922598522));
#43352=CARTESIAN_POINT('Ctrl Pts',(-58.4239613694228,-112.268011935925,
179.975477717318));
#43353=CARTESIAN_POINT('Ctrl Pts',(-60.0772962946681,-112.186036615696,
180.181729449417));
#43354=CARTESIAN_POINT('Ctrl Pts',(-61.3943116732681,-112.139915206054,
179.158929658031));
#43355=CARTESIAN_POINT('Ctrl Pts',(-62.7113270518682,-112.093793796412,
178.136129866644));
#43356=CARTESIAN_POINT('Ctrl Pts',(-62.9263547193661,-112.165151639037,
176.483420797975));
#43357=CARTESIAN_POINT('Ctrl Pts',(-63.141382386864,-112.236509481662,174.830711729305));
#43358=CARTESIAN_POINT('Ctrl Pts',(-62.134283634398,-112.438154165553,173.516227941122));
#43359=CARTESIAN_POINT('Ctrl Pts',(-61.1271848819321,-112.639798849443,
172.201744152939));
#43360=CARTESIAN_POINT('Ctrl Pts',(-59.4937260825209,-112.908217698984,
171.99549242084));
#43361=CARTESIAN_POINT('Ctrl Pts',(-57.8602672831097,-113.176636548524,
171.789240688742));
#43362=CARTESIAN_POINT('Ctrl Pts',(-56.5631280303436,-113.409201487476,
172.812040480128));
#43363=CARTESIAN_POINT('Ctrl Pts',(-55.2659887775776,-113.641766426429,
173.834840271514));
#43364=CARTESIAN_POINT('Ctrl Pts',(-55.0708372359137,-113.756852113114,
175.487549340184));
#43365=CARTESIAN_POINT('Ctrl Pts',(-54.8756856942498,-113.8719377998,177.140258408853));
#43366=CARTESIAN_POINT('Ctrl Pts',(-55.9026605725498,-113.85673664522,178.454742197037));
#43367=CARTESIAN_POINT('Ctrl Pts',(-56.9296354508498,-113.84153549064,179.76922598522));
#43368=CARTESIAN_POINT('Ctrl Pts',(-58.582970376095,-113.759560170411,179.975477717318));
#43369=CARTESIAN_POINT('Ctrl Pts',(-60.2363053013403,-113.677584850181,
180.181729449417));
#43370=CARTESIAN_POINT('Ctrl Pts',(-61.5533206799403,-113.631463440539,
179.158929658031));
#43371=CARTESIAN_POINT('Ctrl Pts',(-62.8703360585404,-113.585342030898,
178.136129866644));
#43372=CARTESIAN_POINT('Ctrl Pts',(-63.0853637260383,-113.656699873523,
176.483420797975));
#43373=CARTESIAN_POINT('Ctrl Pts',(-63.3003913935362,-113.728057716148,
174.830711729305));
#43374=CARTESIAN_POINT('Ctrl Pts',(-62.2932926410703,-113.929702400038,
173.516227941122));
#43375=CARTESIAN_POINT('Ctrl Pts',(-61.2861938886043,-114.131347083929,
172.201744152939));
#43376=CARTESIAN_POINT('Ctrl Pts',(-59.6527350891931,-114.399765933469,
171.99549242084));
#43377=CARTESIAN_POINT('Ctrl Pts',(-58.0192762897819,-114.668184783009,
171.789240688742));
#43378=CARTESIAN_POINT('Ctrl Pts',(-56.7221370370159,-114.900749721962,
172.812040480128));
#43379=CARTESIAN_POINT('Ctrl Pts',(-55.4249977842499,-115.133314660914,
173.834840271514));
#43380=CARTESIAN_POINT('Ctrl Pts',(-55.229846242586,-115.2484003476,175.487549340184));
#43381=CARTESIAN_POINT('Ctrl Pts',(-55.0346947009221,-115.363486034286,
177.140258408853));
#43382=CARTESIAN_POINT('Ctrl Pts',(-56.061669579222,-115.348284879706,178.454742197037));
#43383=CARTESIAN_POINT('Ctrl Pts',(-57.088644457522,-115.333083725126,179.76922598522));
#43384=CARTESIAN_POINT('Ctrl Pts',(-58.7419793827673,-115.251108404896,
179.975477717318));
#43385=CARTESIAN_POINT('Ctrl Pts',(-60.3953143080125,-115.169133084667,
180.181729449417));
#43386=CARTESIAN_POINT('Ctrl Pts',(-61.7123296866126,-115.123011675025,
179.158929658031));
#43387=CARTESIAN_POINT('Ctrl Pts',(-63.0293450652126,-115.076890265383,
178.136129866644));
#43388=CARTESIAN_POINT('Ctrl Pts',(-63.2443727327105,-115.148248108008,
176.483420797975));
#43389=CARTESIAN_POINT('Ctrl Pts',(-63.4594004002085,-115.219605950633,
174.830711729305));
#43390=CARTESIAN_POINT('Ctrl Pts',(-62.4523016477425,-115.421250634524,
173.516227941122));
#43391=CARTESIAN_POINT('Ctrl Pts',(-61.4452028952766,-115.622895318415,
172.201744152939));
#43392=CARTESIAN_POINT('Ctrl Pts',(-59.8117440958653,-115.891314167955,
171.99549242084));
#43393=CARTESIAN_POINT('Ctrl Pts',(-58.1782852964541,-116.159733017495,
171.789240688742));
#43394=CARTESIAN_POINT('Ctrl Pts',(-56.8811460436881,-116.392297956447,
172.812040480128));
#43395=CARTESIAN_POINT('Ctrl Pts',(-55.5840067909221,-116.6248628954,173.834840271514));
#43396=CARTESIAN_POINT('Ctrl Pts',(-55.3888552492582,-116.739948582086,
175.487549340184));
#43397=CARTESIAN_POINT('Ctrl Pts',(-55.1937037075943,-116.855034268771,
177.140258408853));
#43398=CARTESIAN_POINT('Ctrl Pts',(-56.2206785858943,-116.839833114191,
178.454742197037));
#43399=CARTESIAN_POINT('Ctrl Pts',(-57.2476534641943,-116.824631959611,
179.76922598522));
#43400=CARTESIAN_POINT('Ctrl Pts',(-58.9009883894395,-116.742656639382,
179.975477717318));
#43401=CARTESIAN_POINT('Ctrl Pts',(-60.5543233146848,-116.660681319152,
180.181729449417));
#43402=CARTESIAN_POINT('Ctrl Pts',(-61.8713386932848,-116.614559909511,
179.158929658031));
#43403=CARTESIAN_POINT('Ctrl Pts',(-63.1883540718848,-116.568438499869,
178.136129866644));
#43404=CARTESIAN_POINT('Ctrl Pts',(-63.4033817393827,-116.639796342494,
176.483420797975));
#43405=CARTESIAN_POINT('Ctrl Pts',(-63.6184094068807,-116.711154185119,
174.830711729305));
#43406=CARTESIAN_POINT('Ctrl Pts',(-62.6113106544147,-116.91279886901,173.516227941122));
#43407=CARTESIAN_POINT('Ctrl Pts',(-61.6042119019488,-117.1144435529,172.201744152939));
#43408=CARTESIAN_POINT('Ctrl Pts',(-59.9707531025376,-117.38286240244,171.99549242084));
#43409=CARTESIAN_POINT('Ctrl Pts',(-58.3372943031263,-117.651281251981,
171.789240688742));
#43410=CARTESIAN_POINT('Ctrl Pts',(-57.0401550503603,-117.883846190933,
172.812040480128));
#43411=CARTESIAN_POINT('Ctrl Pts',(-55.7430157975943,-118.116411129886,
173.834840271514));
#43412=CARTESIAN_POINT('Ctrl Pts',(-55.5478642559304,-118.231496816571,
175.487549340184));
#43413=CARTESIAN_POINT('Ctrl Pts',(-55.3527127142665,-118.346582503257,
177.140258408853));
#43414=CARTESIAN_POINT('Ctrl Pts',(-56.3796875925665,-118.331381348677,
178.454742197037));
#43415=CARTESIAN_POINT('Ctrl Pts',(-57.4066624708665,-118.316180194097,
179.76922598522));
#43416=CARTESIAN_POINT('Ctrl Pts',(-59.0599973961117,-118.234204873868,
179.975477717318));
#43417=CARTESIAN_POINT('Ctrl Pts',(-60.713332321357,-118.152229553638,180.181729449417));
#43418=CARTESIAN_POINT('Ctrl Pts',(-62.030347699957,-118.106108143996,179.158929658031));
#43419=CARTESIAN_POINT('Ctrl Pts',(-63.3473630785571,-118.059986734354,
178.136129866644));
#43420=CARTESIAN_POINT('Ctrl Pts',(-63.562390746055,-118.131344576979,176.483420797975));
#43421=CARTESIAN_POINT('Ctrl Pts',(-63.7774184135529,-118.202702419604,
174.830711729305));
#43422=CARTESIAN_POINT('Ctrl Pts',(-62.770319661087,-118.404347103495,173.516227941122));
#43423=CARTESIAN_POINT('Ctrl Pts',(-61.763220908621,-118.605991787386,172.201744152939));
#43424=CARTESIAN_POINT('Ctrl Pts',(-60.1297621092098,-118.874410636926,
171.99549242084));
#43425=CARTESIAN_POINT('Ctrl Pts',(-58.4963033097986,-119.142829486466,
171.789240688742));
#43426=CARTESIAN_POINT('Ctrl Pts',(-57.1991640570326,-119.375394425419,
172.812040480128));
#43427=CARTESIAN_POINT('Ctrl Pts',(-55.9020248042666,-119.607959364371,
173.834840271514));
#43428=CARTESIAN_POINT('Ctrl Pts',(-55.7068732626027,-119.723045051057,
175.487549340184));
#43429=CARTESIAN_POINT('Ctrl Pts',(-55.5117217209387,-119.838130737742,
177.140258408853));
#43430=CARTESIAN_POINT('Ctrl Pts',(-56.5386965992387,-119.822929583163,
178.454742197037));
#43431=CARTESIAN_POINT('Ctrl Pts',(-57.5656714775387,-119.807728428583,
179.76922598522));
#43432=CARTESIAN_POINT('Ctrl Pts',(-59.219006402784,-119.725753108353,179.975477717318));
#43433=CARTESIAN_POINT('Ctrl Pts',(-60.8723413280292,-119.643777788124,
180.181729449417));
#43434=CARTESIAN_POINT('Ctrl Pts',(-62.1893567066292,-119.597656378482,
179.158929658031));
#43435=CARTESIAN_POINT('Ctrl Pts',(-63.5063720852293,-119.55153496884,178.136129866644));
#43436=CARTESIAN_POINT('Ctrl Pts',(-63.7213997527272,-119.622892811465,
176.483420797975));
#43437=CARTESIAN_POINT('Ctrl Pts',(-63.9364274202251,-119.69425065409,174.830711729305));
#43438=CARTESIAN_POINT('Ctrl Pts',(-62.9293286677592,-119.895895337981,
173.516227941122));
#43439=CARTESIAN_POINT('Ctrl Pts',(-61.9222299152932,-120.097540021871,
172.201744152939));
#43440=CARTESIAN_POINT('Ctrl Pts',(-60.288771115882,-120.365958871412,171.99549242084));
#43441=CARTESIAN_POINT('Ctrl Pts',(-58.6553123164708,-120.634377720952,
171.789240688742));
#43442=CARTESIAN_POINT('Ctrl Pts',(-57.3581730637048,-120.866942659904,
172.812040480128));
#43443=CARTESIAN_POINT('Ctrl Pts',(-56.0610338109388,-121.099507598857,
173.834840271514));
#43444=CARTESIAN_POINT('Ctrl Pts',(-55.8658822692749,-121.214593285542,
175.487549340184));
#43445=CARTESIAN_POINT('Ctrl Pts',(-55.670730727611,-121.329678972228,177.140258408853));
#43446=CARTESIAN_POINT('Ctrl Pts',(-56.697705605911,-121.314477817648,178.454742197037));
#43447=CARTESIAN_POINT('Ctrl Pts',(-57.7246804842109,-121.299276663068,
179.76922598522));
#43448=CARTESIAN_POINT('Ctrl Pts',(-59.3780154094562,-121.217301342839,
179.975477717318));
#43449=CARTESIAN_POINT('Ctrl Pts',(-61.0313503347014,-121.135326022609,
180.181729449417));
#43450=CARTESIAN_POINT('Ctrl Pts',(-62.3483657133015,-121.089204612967,
179.158929658031));
#43451=CARTESIAN_POINT('Ctrl Pts',(-63.6653810919015,-121.043083203326,
178.136129866644));
#43452=CARTESIAN_POINT('Ctrl Pts',(-63.8804087593994,-121.114441045951,
176.483420797975));
#43453=CARTESIAN_POINT('Ctrl Pts',(-64.0954364268974,-121.185798888576,
174.830711729305));
#43454=CARTESIAN_POINT('Ctrl Pts',(-63.0883376744314,-121.387443572466,
173.516227941122));
#43455=CARTESIAN_POINT('Ctrl Pts',(-62.0812389219655,-121.589088256357,
172.201744152939));
#43456=CARTESIAN_POINT('Ctrl Pts',(-60.4477801225542,-121.857507105897,
171.99549242084));
#43457=CARTESIAN_POINT('Ctrl Pts',(-58.814321323143,-122.125925955437,171.789240688742));
#43458=CARTESIAN_POINT('Ctrl Pts',(-57.517182070377,-122.35849089439,172.812040480128));
#43459=CARTESIAN_POINT('Ctrl Pts',(-56.220042817611,-122.591055833342,173.834840271514));
#43460=CARTESIAN_POINT('Ctrl Pts',(-56.0248912759471,-122.706141520028,
175.487549340184));
#43461=CARTESIAN_POINT('Ctrl Pts',(-55.8297397342832,-122.821227206714,
177.140258408853));
#43462=CARTESIAN_POINT('Ctrl Pts',(-56.8567146125832,-122.806026052134,
178.454742197037));
#43463=CARTESIAN_POINT('Ctrl Pts',(-57.8836894908832,-122.790824897554,
179.76922598522));
#43464=CARTESIAN_POINT('Ctrl Pts',(-59.5370244161284,-122.708849577324,
179.975477717318));
#43465=CARTESIAN_POINT('Ctrl Pts',(-61.1903593413737,-122.626874257095,
180.181729449417));
#43466=CARTESIAN_POINT('Ctrl Pts',(-62.5073747199737,-122.580752847453,
179.158929658031));
#43467=CARTESIAN_POINT('Ctrl Pts',(-63.8243900985737,-122.534631437811,
178.136129866644));
#43468=CARTESIAN_POINT('Ctrl Pts',(-64.0394177660717,-122.605989280436,
176.483420797975));
#43469=CARTESIAN_POINT('Ctrl Pts',(-64.2544454335696,-122.677347123061,
174.830711729305));
#43470=CARTESIAN_POINT('Ctrl Pts',(-63.2473466811036,-122.878991806952,
173.516227941122));
#43471=CARTESIAN_POINT('Ctrl Pts',(-62.2402479286377,-123.080636490843,
172.201744152939));
#43472=CARTESIAN_POINT('Ctrl Pts',(-60.6067891292265,-123.349055340383,
171.99549242084));
#43473=CARTESIAN_POINT('Ctrl Pts',(-58.9733303298152,-123.617474189923,
171.789240688742));
#43474=CARTESIAN_POINT('Ctrl Pts',(-57.6761910770492,-123.850039128875,
172.812040480128));
#43475=CARTESIAN_POINT('Ctrl Pts',(-56.3790518242832,-124.082604067828,
173.834840271514));
#43476=CARTESIAN_POINT('Ctrl Pts',(-56.1839002826193,-124.197689754514,
175.487549340184));
#43477=CARTESIAN_POINT('Ctrl Pts',(-55.9887487409554,-124.312775441199,
177.140258408853));
#43478=CARTESIAN_POINT('Ctrl Pts',(-57.0157236192554,-124.297574286619,
178.454742197037));
#43479=CARTESIAN_POINT('Ctrl Pts',(-58.0426984975554,-124.282373132039,
179.76922598522));
#43480=CARTESIAN_POINT('Ctrl Pts',(-59.6960334228006,-124.20039781181,179.975477717318));
#43481=CARTESIAN_POINT('Ctrl Pts',(-61.3493683480459,-124.11842249158,180.181729449417));
#43482=CARTESIAN_POINT('Ctrl Pts',(-62.6663837266459,-124.072301081939,
179.158929658031));
#43483=CARTESIAN_POINT('Ctrl Pts',(-63.983399105246,-124.026179672297,178.136129866644));
#43484=CARTESIAN_POINT('Ctrl Pts',(-64.1984267727439,-124.097537514922,
176.483420797975));
#43485=CARTESIAN_POINT('Ctrl Pts',(-64.4134544402418,-124.168895357547,
174.830711729305));
#43486=CARTESIAN_POINT('Ctrl Pts',(-63.4063556877759,-124.370540041437,
173.516227941122));
#43487=CARTESIAN_POINT('Ctrl Pts',(-62.3992569353099,-124.572184725328,
172.201744152939));
#43488=CARTESIAN_POINT('Ctrl Pts',(-60.7657981358987,-124.840603574868,
171.99549242084));
#43489=CARTESIAN_POINT('Ctrl Pts',(-59.1323393364875,-125.109022424409,
171.789240688742));
#43490=CARTESIAN_POINT('Ctrl Pts',(-57.8352000837215,-125.341587363361,
172.812040480128));
#43491=CARTESIAN_POINT('Ctrl Pts',(-56.5380608309555,-125.574152302314,
173.834840271514));
#43492=CARTESIAN_POINT('Ctrl Pts',(-56.3429092892916,-125.689237988999,
175.487549340184));
#43493=CARTESIAN_POINT('Ctrl Pts',(-56.1477577476277,-125.804323675685,
177.140258408853));
#43494=CARTESIAN_POINT('Ctrl Pts',(-57.1747326259276,-125.789122521105,
178.454742197037));
#43495=CARTESIAN_POINT('Ctrl Pts',(-58.2017075042276,-125.773921366525,
179.76922598522));
#43496=CARTESIAN_POINT('Ctrl Pts',(-59.8550424294729,-125.691946046296,
179.975477717318));
#43497=CARTESIAN_POINT('Ctrl Pts',(-61.5083773547181,-125.609970726066,
180.181729449417));
#43498=CARTESIAN_POINT('Ctrl Pts',(-62.8253927333181,-125.563849316424,
179.158929658031));
#43499=CARTESIAN_POINT('Ctrl Pts',(-64.1424081119182,-125.517727906782,
178.136129866644));
#43500=CARTESIAN_POINT('Ctrl Pts',(-64.3574357794161,-125.589085749407,
176.483420797975));
#43501=CARTESIAN_POINT('Ctrl Pts',(-64.572463446914,-125.660443592032,174.830711729305));
#43502=CARTESIAN_POINT('Ctrl Pts',(-63.5653646944481,-125.862088275923,
173.516227941122));
#43503=CARTESIAN_POINT('Ctrl Pts',(-62.5582659419822,-126.063732959814,
172.201744152939));
#43504=CARTESIAN_POINT('Ctrl Pts',(-60.9248071425709,-126.332151809354,
171.99549242084));
#43505=CARTESIAN_POINT('Ctrl Pts',(-59.2913483431597,-126.600570658894,
171.789240688742));
#43506=CARTESIAN_POINT('Ctrl Pts',(-57.9942090903937,-126.833135597847,
172.812040480128));
#43507=CARTESIAN_POINT('Ctrl Pts',(-56.6970698376277,-127.065700536799,
173.834840271514));
#43508=CARTESIAN_POINT('Ctrl Pts',(-56.5019182959638,-127.180786223485,
175.487549340184));
#43509=CARTESIAN_POINT('Ctrl Pts',(-56.3067667542999,-127.295871910171,
177.140258408853));
#43510=CARTESIAN_POINT('Ctrl Pts',(-57.3337416325999,-127.280670755591,
178.454742197037));
#43511=CARTESIAN_POINT('Ctrl Pts',(-58.3607165108998,-127.265469601011,
179.76922598522));
#43512=CARTESIAN_POINT('Ctrl Pts',(-60.0140514361451,-127.183494280781,
179.975477717318));
#43513=CARTESIAN_POINT('Ctrl Pts',(-61.6673863613903,-127.101518960552,
180.181729449417));
#43514=CARTESIAN_POINT('Ctrl Pts',(-62.9844017399904,-127.05539755091,179.158929658031));
#43515=CARTESIAN_POINT('Ctrl Pts',(-64.3014171185904,-127.009276141268,
178.136129866644));
#43516=CARTESIAN_POINT('Ctrl Pts',(-64.5164447860883,-127.080633983893,
176.483420797975));
#43517=CARTESIAN_POINT('Ctrl Pts',(-64.7314724535863,-127.151991826518,
174.830711729305));
#43518=CARTESIAN_POINT('Ctrl Pts',(-63.7243737011203,-127.353636510409,
173.516227941122));
#43519=CARTESIAN_POINT('Ctrl Pts',(-62.7172749486544,-127.555281194299,
172.201744152939));
#43520=CARTESIAN_POINT('Ctrl Pts',(-61.0838161492432,-127.82370004384,171.99549242084));
#43521=CARTESIAN_POINT('Ctrl Pts',(-59.4503573498319,-128.09211889338,171.789240688742));
#43522=CARTESIAN_POINT('Ctrl Pts',(-58.1532180970659,-128.324683832332,
172.812040480128));
#43523=CARTESIAN_POINT('Ctrl Pts',(-56.8560788442999,-128.557248771285,
173.834840271514));
#43524=CARTESIAN_POINT('Ctrl Pts',(-56.660927302636,-128.67233445797,175.487549340184));
#43525=CARTESIAN_POINT('Ctrl Pts',(-56.4657757609721,-128.787420144656,
177.140258408853));
#43526=CARTESIAN_POINT('Ctrl Pts',(-57.4927506392721,-128.772218990076,
178.454742197037));
#43527=CARTESIAN_POINT('Ctrl Pts',(-58.5197255175721,-128.757017835496,
179.76922598522));
#43528=CARTESIAN_POINT('Ctrl Pts',(-60.1730604428173,-128.675042515267,
179.975477717318));
#43529=CARTESIAN_POINT('Ctrl Pts',(-61.8263953680626,-128.593067195037,
180.181729449417));
#43530=CARTESIAN_POINT('Ctrl Pts',(-63.1434107466626,-128.546945785395,
179.158929658031));
#43531=CARTESIAN_POINT('Ctrl Pts',(-64.4604261252626,-128.500824375754,
178.136129866644));
#43532=CARTESIAN_POINT('Ctrl Pts',(-64.6754537927606,-128.572182218379,
176.483420797975));
#43533=CARTESIAN_POINT('Ctrl Pts',(-64.8904814602585,-128.643540061004,
174.830711729305));
#43534=CARTESIAN_POINT('Ctrl Pts',(-63.8833827077925,-128.845184744894,
173.516227941122));
#43535=CARTESIAN_POINT('Ctrl Pts',(-62.8762839553266,-129.046829428785,
172.201744152939));
#43536=CARTESIAN_POINT('Ctrl Pts',(-61.2428251559154,-129.315248278325,
171.99549242084));
#43537=CARTESIAN_POINT('Ctrl Pts',(-59.6093663565042,-129.583667127865,
171.789240688742));
#43538=CARTESIAN_POINT('Ctrl Pts',(-58.3122271037382,-129.816232066818,
172.812040480128));
#43539=CARTESIAN_POINT('Ctrl Pts',(-57.0150878509721,-130.04879700577,173.834840271514));
#43540=CARTESIAN_POINT('Ctrl Pts',(-56.8199363093082,-130.163882692456,
175.487549340184));
#43541=CARTESIAN_POINT('Ctrl Pts',(-56.6247847676443,-130.278968379142,
177.140258408853));
#43542=CARTESIAN_POINT('Ctrl Pts',(-57.6517596459443,-130.263767224562,
178.454742197037));
#43543=CARTESIAN_POINT('Ctrl Pts',(-58.6787345242443,-130.248566069982,
179.76922598522));
#43544=CARTESIAN_POINT('Ctrl Pts',(-60.3320694494895,-130.166590749752,
179.975477717318));
#43545=CARTESIAN_POINT('Ctrl Pts',(-61.9854043747348,-130.084615429523,
180.181729449417));
#43546=CARTESIAN_POINT('Ctrl Pts',(-63.3024197533348,-130.038494019881,
179.158929658031));
#43547=CARTESIAN_POINT('Ctrl Pts',(-64.6194351319349,-129.992372610239,
178.136129866644));
#43548=CARTESIAN_POINT('Ctrl Pts',(-64.8344627994328,-130.063730452864,
176.483420797975));
#43549=CARTESIAN_POINT('Ctrl Pts',(-65.0494904669307,-130.135088295489,
174.830711729305));
#43550=CARTESIAN_POINT('Ctrl Pts',(-64.0423917144648,-130.33673297938,173.516227941122));
#43551=CARTESIAN_POINT('Ctrl Pts',(-63.0352929619988,-130.538377663271,
172.201744152939));
#43552=CARTESIAN_POINT('Ctrl Pts',(-61.4018341625876,-130.806796512811,
171.99549242084));
#43553=CARTESIAN_POINT('Ctrl Pts',(-59.7683753631764,-131.075215362351,
171.789240688742));
#43554=CARTESIAN_POINT('Ctrl Pts',(-58.4712361104104,-131.307780301304,
172.812040480128));
#43555=CARTESIAN_POINT('Ctrl Pts',(-57.1740968576444,-131.540345240256,
173.834840271514));
#43556=CARTESIAN_POINT('Ctrl Pts',(-56.9789453159805,-131.655430926942,
175.487549340184));
#43557=CARTESIAN_POINT('Ctrl Pts',(-56.7837937743166,-131.770516613627,
177.140258408853));
#43558=CARTESIAN_POINT('Ctrl Pts',(-57.8107686526165,-131.755315459047,
178.454742197037));
#43559=CARTESIAN_POINT('Ctrl Pts',(-58.8377435309165,-131.740114304467,
179.76922598522));
#43560=CARTESIAN_POINT('Ctrl Pts',(-60.4910784561618,-131.658138984238,
179.975477717318));
#43561=CARTESIAN_POINT('Ctrl Pts',(-61.5605751224754,-131.605111415312,
180.108896262184));
#43562=CARTESIAN_POINT('Ctrl Pts',(-62.5544558090293,-131.564605289581,
179.689905107434));
#43563=CARTESIAN_POINT('Ctrl Pts',(-50.1798438064916,-67.6819458883961,
175.490142808619));
#43564=CARTESIAN_POINT('Ctrl Pts',(-49.9857604617556,-67.7969176981527,
177.134243841043));
#43565=CARTESIAN_POINT('Ctrl Pts',(-51.0074381646872,-67.7822812578569,
178.441881219107));
#43566=CARTESIAN_POINT('Ctrl Pts',(-52.0291158676188,-67.7676448175611,
179.74951859717));
#43567=CARTESIAN_POINT('Ctrl Pts',(-53.673891258688,-67.6865820008601,179.954696079469));
#43568=CARTESIAN_POINT('Ctrl Pts',(-55.3186666497572,-67.6055191841591,
180.159873561769));
#43569=CARTESIAN_POINT('Ctrl Pts',(-56.6288741944062,-67.5601235350989,
179.142400961866));
#43570=CARTESIAN_POINT('Ctrl Pts',(-57.9390817390552,-67.5147278860387,
178.124928361964));
#43571=CARTESIAN_POINT('Ctrl Pts',(-58.1530412096253,-67.5861996055927,
176.48082732954));
#43572=CARTESIAN_POINT('Ctrl Pts',(-58.3670006801954,-67.6576713251468,
174.836726297116));
#43573=CARTESIAN_POINT('Ctrl Pts',(-57.3651991030978,-67.8587512947533,
173.529088919052));
#43574=CARTESIAN_POINT('Ctrl Pts',(-56.3633975260002,-68.0598312643598,
172.221451540989));
#43575=CARTESIAN_POINT('Ctrl Pts',(-54.7384982607651,-68.3273376103715,
172.016274058689));
#43576=CARTESIAN_POINT('Ctrl Pts',(-53.1135989955299,-68.5948439563832,
171.81109657639));
#43577=CARTESIAN_POINT('Ctrl Pts',(-51.8232675767149,-68.8266831347541,
172.828569176292));
#43578=CARTESIAN_POINT('Ctrl Pts',(-50.5329361578999,-69.0585223131251,
173.846041776195));
#43579=CARTESIAN_POINT('Ctrl Pts',(-50.3388528131639,-69.1734941228817,
175.490142808619));
#43580=CARTESIAN_POINT('Ctrl Pts',(-50.1447694684278,-69.2884659326383,
177.134243841043));
#43581=CARTESIAN_POINT('Ctrl Pts',(-51.1664471713594,-69.2738294923425,
178.441881219107));
#43582=CARTESIAN_POINT('Ctrl Pts',(-52.188124874291,-69.2591930520467,179.74951859717));
#43583=CARTESIAN_POINT('Ctrl Pts',(-53.8329002653602,-69.1781302353457,
179.954696079469));
#43584=CARTESIAN_POINT('Ctrl Pts',(-55.4776756564294,-69.0970674186447,
180.159873561769));
#43585=CARTESIAN_POINT('Ctrl Pts',(-56.7878832010784,-69.0516717695845,
179.142400961866));
#43586=CARTESIAN_POINT('Ctrl Pts',(-58.0980907457274,-69.0062761205243,
178.124928361964));
#43587=CARTESIAN_POINT('Ctrl Pts',(-58.3120502162975,-69.0777478400783,
176.48082732954));
#43588=CARTESIAN_POINT('Ctrl Pts',(-58.5260096868676,-69.1492195596324,
174.836726297116));
#43589=CARTESIAN_POINT('Ctrl Pts',(-57.52420810977,-69.3502995292389,173.529088919052));
#43590=CARTESIAN_POINT('Ctrl Pts',(-56.5224065326725,-69.5513794988454,
172.221451540989));
#43591=CARTESIAN_POINT('Ctrl Pts',(-54.8975072674373,-69.8188858448571,
172.016274058689));
#43592=CARTESIAN_POINT('Ctrl Pts',(-53.2726080022022,-70.0863921908688,
171.81109657639));
#43593=CARTESIAN_POINT('Ctrl Pts',(-51.9822765833872,-70.3182313692397,
172.828569176292));
#43594=CARTESIAN_POINT('Ctrl Pts',(-50.6919451645722,-70.5500705476106,
173.846041776195));
#43595=CARTESIAN_POINT('Ctrl Pts',(-50.4978618198361,-70.6650423573673,
175.490142808619));
#43596=CARTESIAN_POINT('Ctrl Pts',(-50.3037784751,-70.7800141671239,177.134243841043));
#43597=CARTESIAN_POINT('Ctrl Pts',(-51.3254561780316,-70.7653777268281,
178.441881219107));
#43598=CARTESIAN_POINT('Ctrl Pts',(-52.3471338809632,-70.7507412865323,
179.74951859717));
#43599=CARTESIAN_POINT('Ctrl Pts',(-53.9919092720324,-70.6696784698313,
179.954696079469));
#43600=CARTESIAN_POINT('Ctrl Pts',(-55.6366846631016,-70.5886156531303,
180.159873561769));
#43601=CARTESIAN_POINT('Ctrl Pts',(-56.9468922077507,-70.5432200040701,
179.142400961866));
#43602=CARTESIAN_POINT('Ctrl Pts',(-58.2570997523997,-70.4978243550099,
178.124928361964));
#43603=CARTESIAN_POINT('Ctrl Pts',(-58.4710592229698,-70.5692960745639,
176.48082732954));
#43604=CARTESIAN_POINT('Ctrl Pts',(-58.6850186935399,-70.640767794118,174.836726297116));
#43605=CARTESIAN_POINT('Ctrl Pts',(-57.6832171164423,-70.8418477637245,
173.529088919052));
#43606=CARTESIAN_POINT('Ctrl Pts',(-56.6814155393447,-71.0429277333309,
172.221451540989));
#43607=CARTESIAN_POINT('Ctrl Pts',(-55.0565162741095,-71.3104340793427,
172.016274058689));
#43608=CARTESIAN_POINT('Ctrl Pts',(-53.4316170088744,-71.5779404253544,
171.81109657639));
#43609=CARTESIAN_POINT('Ctrl Pts',(-52.1412855900594,-71.8097796037253,
172.828569176292));
#43610=CARTESIAN_POINT('Ctrl Pts',(-50.8509541712444,-72.0416187820962,
173.846041776195));
#43611=CARTESIAN_POINT('Ctrl Pts',(-50.6568708265083,-72.1565905918529,
175.490142808619));
#43612=CARTESIAN_POINT('Ctrl Pts',(-50.4627874817723,-72.2715624016095,
177.134243841043));
#43613=CARTESIAN_POINT('Ctrl Pts',(-51.4844651847039,-72.2569259613137,
178.441881219107));
#43614=CARTESIAN_POINT('Ctrl Pts',(-52.5061428876355,-72.242289521018,179.74951859717));
#43615=CARTESIAN_POINT('Ctrl Pts',(-54.1509182787047,-72.1612267043169,
179.954696079469));
#43616=CARTESIAN_POINT('Ctrl Pts',(-55.7956936697739,-72.0801638876159,
180.159873561769));
#43617=CARTESIAN_POINT('Ctrl Pts',(-57.1059012144229,-72.0347682385557,
179.142400961866));
#43618=CARTESIAN_POINT('Ctrl Pts',(-58.4161087590719,-71.9893725894955,
178.124928361964));
#43619=CARTESIAN_POINT('Ctrl Pts',(-58.630068229642,-72.0608443090495,176.48082732954));
#43620=CARTESIAN_POINT('Ctrl Pts',(-58.8440277002121,-72.1323160286036,
174.836726297116));
#43621=CARTESIAN_POINT('Ctrl Pts',(-57.8422261231145,-72.3333959982101,
173.529088919052));
#43622=CARTESIAN_POINT('Ctrl Pts',(-56.8404245460169,-72.5344759678166,
172.221451540989));
#43623=CARTESIAN_POINT('Ctrl Pts',(-55.2155252807818,-72.8019823138283,
172.016274058689));
#43624=CARTESIAN_POINT('Ctrl Pts',(-53.5906260155466,-73.06948865984,171.81109657639));
#43625=CARTESIAN_POINT('Ctrl Pts',(-52.3002945967316,-73.3013278382109,
172.828569176292));
#43626=CARTESIAN_POINT('Ctrl Pts',(-51.0099631779166,-73.5331670165818,
173.846041776195));
#43627=CARTESIAN_POINT('Ctrl Pts',(-50.8158798331806,-73.6481388263385,
175.490142808619));
#43628=CARTESIAN_POINT('Ctrl Pts',(-50.6217964884445,-73.7631106360951,
177.134243841043));
#43629=CARTESIAN_POINT('Ctrl Pts',(-51.6434741913761,-73.7484741957993,
178.441881219107));
#43630=CARTESIAN_POINT('Ctrl Pts',(-52.6651518943077,-73.7338377555035,
179.74951859717));
#43631=CARTESIAN_POINT('Ctrl Pts',(-54.3099272853769,-73.6527749388025,
179.954696079469));
#43632=CARTESIAN_POINT('Ctrl Pts',(-55.9547026764461,-73.5717121221015,
180.159873561769));
#43633=CARTESIAN_POINT('Ctrl Pts',(-57.2649102210951,-73.5263164730413,
179.142400961866));
#43634=CARTESIAN_POINT('Ctrl Pts',(-58.5751177657441,-73.4809208239811,
178.124928361964));
#43635=CARTESIAN_POINT('Ctrl Pts',(-58.7890772363142,-73.5523925435351,
176.48082732954));
#43636=CARTESIAN_POINT('Ctrl Pts',(-59.0030367068843,-73.6238642630892,
174.836726297116));
#43637=CARTESIAN_POINT('Ctrl Pts',(-58.0012351297867,-73.8249442326957,
173.529088919052));
#43638=CARTESIAN_POINT('Ctrl Pts',(-56.9994335526892,-74.0260242023022,
172.221451540989));
#43639=CARTESIAN_POINT('Ctrl Pts',(-55.374534287454,-74.2935305483139,172.016274058689));
#43640=CARTESIAN_POINT('Ctrl Pts',(-53.7496350222188,-74.5610368943256,
171.81109657639));
#43641=CARTESIAN_POINT('Ctrl Pts',(-52.4593036034038,-74.7928760726965,
172.828569176292));
#43642=CARTESIAN_POINT('Ctrl Pts',(-51.1689721845888,-75.0247152510674,
173.846041776195));
#43643=CARTESIAN_POINT('Ctrl Pts',(-50.9748888398528,-75.1396870608241,
175.490142808619));
#43644=CARTESIAN_POINT('Ctrl Pts',(-50.7808054951167,-75.2546588705807,
177.134243841043));
#43645=CARTESIAN_POINT('Ctrl Pts',(-51.8024831980483,-75.2400224302849,
178.441881219107));
#43646=CARTESIAN_POINT('Ctrl Pts',(-52.8241609009799,-75.2253859899892,
179.74951859717));
#43647=CARTESIAN_POINT('Ctrl Pts',(-54.4689362920491,-75.1443231732881,
179.954696079469));
#43648=CARTESIAN_POINT('Ctrl Pts',(-56.1137116831183,-75.0632603565871,
180.159873561769));
#43649=CARTESIAN_POINT('Ctrl Pts',(-57.4239192277673,-75.0178647075269,
179.142400961866));
#43650=CARTESIAN_POINT('Ctrl Pts',(-58.7341267724164,-74.9724690584666,
178.124928361964));
#43651=CARTESIAN_POINT('Ctrl Pts',(-58.9480862429864,-75.0439407780207,
176.48082732954));
#43652=CARTESIAN_POINT('Ctrl Pts',(-59.1620457135565,-75.1154124975748,
174.836726297116));
#43653=CARTESIAN_POINT('Ctrl Pts',(-58.1602441364589,-75.3164924671813,
173.529088919052));
#43654=CARTESIAN_POINT('Ctrl Pts',(-57.1584425593614,-75.5175724367878,
172.221451540989));
#43655=CARTESIAN_POINT('Ctrl Pts',(-55.5335432941262,-75.7850787827995,
172.016274058689));
#43656=CARTESIAN_POINT('Ctrl Pts',(-53.9086440288911,-76.0525851288112,
171.81109657639));
#43657=CARTESIAN_POINT('Ctrl Pts',(-52.6183126100761,-76.2844243071821,
172.828569176292));
#43658=CARTESIAN_POINT('Ctrl Pts',(-51.3279811912611,-76.5162634855531,
173.846041776195));
#43659=CARTESIAN_POINT('Ctrl Pts',(-51.133897846525,-76.6312352953097,175.490142808619));
#43660=CARTESIAN_POINT('Ctrl Pts',(-50.939814501789,-76.7462071050663,177.134243841043));
#43661=CARTESIAN_POINT('Ctrl Pts',(-51.9614922047205,-76.7315706647705,
178.441881219107));
#43662=CARTESIAN_POINT('Ctrl Pts',(-52.9831699076522,-76.7169342244747,
179.74951859717));
#43663=CARTESIAN_POINT('Ctrl Pts',(-54.6279452987213,-76.6358714077737,
179.954696079469));
#43664=CARTESIAN_POINT('Ctrl Pts',(-56.2727206897905,-76.5548085910727,
180.159873561769));
#43665=CARTESIAN_POINT('Ctrl Pts',(-57.5829282344396,-76.5094129420125,
179.142400961866));
#43666=CARTESIAN_POINT('Ctrl Pts',(-58.8931357790886,-76.4640172929522,
178.124928361964));
#43667=CARTESIAN_POINT('Ctrl Pts',(-59.1070952496587,-76.5354890125063,
176.48082732954));
#43668=CARTESIAN_POINT('Ctrl Pts',(-59.3210547202288,-76.6069607320604,
174.836726297116));
#43669=CARTESIAN_POINT('Ctrl Pts',(-58.3192531431312,-76.8080407016669,
173.529088919052));
#43670=CARTESIAN_POINT('Ctrl Pts',(-57.3174515660336,-77.0091206712734,
172.221451540989));
#43671=CARTESIAN_POINT('Ctrl Pts',(-55.6925523007984,-77.2766270172851,
172.016274058689));
#43672=CARTESIAN_POINT('Ctrl Pts',(-54.0676530355633,-77.5441333632968,
171.81109657639));
#43673=CARTESIAN_POINT('Ctrl Pts',(-52.7773216167483,-77.7759725416677,
172.828569176292));
#43674=CARTESIAN_POINT('Ctrl Pts',(-51.4869901979333,-78.0078117200386,
173.846041776195));
#43675=CARTESIAN_POINT('Ctrl Pts',(-51.2929068531972,-78.1227835297953,
175.490142808619));
#43676=CARTESIAN_POINT('Ctrl Pts',(-51.0988235084612,-78.2377553395519,
177.134243841043));
#43677=CARTESIAN_POINT('Ctrl Pts',(-52.1205012113928,-78.2231188992561,
178.441881219107));
#43678=CARTESIAN_POINT('Ctrl Pts',(-53.1421789143244,-78.2084824589603,
179.74951859717));
#43679=CARTESIAN_POINT('Ctrl Pts',(-54.7869543053936,-78.1274196422593,
179.954696079469));
#43680=CARTESIAN_POINT('Ctrl Pts',(-56.4317296964628,-78.0463568255583,
180.159873561769));
#43681=CARTESIAN_POINT('Ctrl Pts',(-57.7419372411118,-78.0009611764981,
179.142400961866));
#43682=CARTESIAN_POINT('Ctrl Pts',(-59.0521447857608,-77.9555655274379,
178.124928361964));
#43683=CARTESIAN_POINT('Ctrl Pts',(-59.2661042563309,-78.0270372469919,
176.48082732954));
#43684=CARTESIAN_POINT('Ctrl Pts',(-59.480063726901,-78.098508966546,174.836726297116));
#43685=CARTESIAN_POINT('Ctrl Pts',(-58.4782621498034,-78.2995889361525,
173.529088919052));
#43686=CARTESIAN_POINT('Ctrl Pts',(-57.4764605727058,-78.500668905759,172.221451540989));
#43687=CARTESIAN_POINT('Ctrl Pts',(-55.8515613074707,-78.7681752517707,
172.016274058689));
#43688=CARTESIAN_POINT('Ctrl Pts',(-54.2266620422355,-79.0356815977824,
171.81109657639));
#43689=CARTESIAN_POINT('Ctrl Pts',(-52.9363306234205,-79.2675207761533,
172.828569176292));
#43690=CARTESIAN_POINT('Ctrl Pts',(-51.6459992046055,-79.4993599545243,
173.846041776195));
#43691=CARTESIAN_POINT('Ctrl Pts',(-51.4519158598695,-79.6143317642809,
175.490142808619));
#43692=CARTESIAN_POINT('Ctrl Pts',(-51.2578325151334,-79.7293035740375,
177.134243841043));
#43693=CARTESIAN_POINT('Ctrl Pts',(-52.279510218065,-79.7146671337417,178.441881219107));
#43694=CARTESIAN_POINT('Ctrl Pts',(-53.3011879209966,-79.7000306934459,
179.74951859717));
#43695=CARTESIAN_POINT('Ctrl Pts',(-54.9459633120658,-79.6189678767449,
179.954696079469));
#43696=CARTESIAN_POINT('Ctrl Pts',(-56.590738703135,-79.5379050600439,180.159873561769));
#43697=CARTESIAN_POINT('Ctrl Pts',(-57.900946247784,-79.4925094109837,179.142400961866));
#43698=CARTESIAN_POINT('Ctrl Pts',(-59.211153792433,-79.4471137619235,178.124928361964));
#43699=CARTESIAN_POINT('Ctrl Pts',(-59.4251132630031,-79.5185854814775,
176.48082732954));
#43700=CARTESIAN_POINT('Ctrl Pts',(-59.6390727335732,-79.5900572010316,
174.836726297116));
#43701=CARTESIAN_POINT('Ctrl Pts',(-58.6372711564756,-79.7911371706381,
173.529088919052));
#43702=CARTESIAN_POINT('Ctrl Pts',(-57.6354695793781,-79.9922171402446,
172.221451540989));
#43703=CARTESIAN_POINT('Ctrl Pts',(-56.0105703141429,-80.2597234862563,
172.016274058689));
#43704=CARTESIAN_POINT('Ctrl Pts',(-54.3856710489078,-80.527229832268,171.81109657639));
#43705=CARTESIAN_POINT('Ctrl Pts',(-53.0953396300927,-80.7590690106389,
172.828569176292));
#43706=CARTESIAN_POINT('Ctrl Pts',(-51.8050082112778,-80.9909081890099,
173.846041776195));
#43707=CARTESIAN_POINT('Ctrl Pts',(-51.6109248665417,-81.1058799987665,
175.490142808619));
#43708=CARTESIAN_POINT('Ctrl Pts',(-51.4168415218056,-81.2208518085231,
177.134243841043));
#43709=CARTESIAN_POINT('Ctrl Pts',(-52.4385192247372,-81.2062153682273,
178.441881219107));
#43710=CARTESIAN_POINT('Ctrl Pts',(-53.4601969276688,-81.1915789279315,
179.74951859717));
#43711=CARTESIAN_POINT('Ctrl Pts',(-55.104972318738,-81.1105161112305,179.954696079469));
#43712=CARTESIAN_POINT('Ctrl Pts',(-56.7497477098072,-81.0294532945295,
180.159873561769));
#43713=CARTESIAN_POINT('Ctrl Pts',(-58.0599552544562,-80.9840576454693,
179.142400961866));
#43714=CARTESIAN_POINT('Ctrl Pts',(-59.3701627991053,-80.9386619964091,
178.124928361964));
#43715=CARTESIAN_POINT('Ctrl Pts',(-59.5841222696753,-81.0101337159631,
176.48082732954));
#43716=CARTESIAN_POINT('Ctrl Pts',(-59.7980817402454,-81.0816054355172,
174.836726297116));
#43717=CARTESIAN_POINT('Ctrl Pts',(-58.7962801631479,-81.2826854051237,
173.529088919052));
#43718=CARTESIAN_POINT('Ctrl Pts',(-57.7944785860503,-81.4837653747302,
172.221451540989));
#43719=CARTESIAN_POINT('Ctrl Pts',(-56.1695793208151,-81.7512717207419,
172.016274058689));
#43720=CARTESIAN_POINT('Ctrl Pts',(-54.54468005558,-82.0187780667536,171.81109657639));
#43721=CARTESIAN_POINT('Ctrl Pts',(-53.254348636765,-82.2506172451245,172.828569176292));
#43722=CARTESIAN_POINT('Ctrl Pts',(-51.96401721795,-82.4824564234954,173.846041776195));
#43723=CARTESIAN_POINT('Ctrl Pts',(-51.7699338732139,-82.5974282332521,
175.490142808619));
#43724=CARTESIAN_POINT('Ctrl Pts',(-51.5758505284779,-82.7124000430087,
177.134243841043));
#43725=CARTESIAN_POINT('Ctrl Pts',(-52.5975282314095,-82.6977636027129,
178.441881219107));
#43726=CARTESIAN_POINT('Ctrl Pts',(-53.6192059343411,-82.6831271624172,
179.74951859717));
#43727=CARTESIAN_POINT('Ctrl Pts',(-55.2639813254103,-82.6020643457161,
179.954696079469));
#43728=CARTESIAN_POINT('Ctrl Pts',(-56.9087567164794,-82.5210015290151,
180.159873561769));
#43729=CARTESIAN_POINT('Ctrl Pts',(-58.2189642611285,-82.4756058799549,
179.142400961866));
#43730=CARTESIAN_POINT('Ctrl Pts',(-59.5291718057775,-82.4302102308947,
178.124928361964));
#43731=CARTESIAN_POINT('Ctrl Pts',(-59.7431312763476,-82.5016819504488,
176.48082732954));
#43732=CARTESIAN_POINT('Ctrl Pts',(-59.9570907469177,-82.5731536700028,
174.836726297116));
#43733=CARTESIAN_POINT('Ctrl Pts',(-58.9552891698201,-82.7742336396093,
173.529088919052));
#43734=CARTESIAN_POINT('Ctrl Pts',(-57.9534875927225,-82.9753136092158,
172.221451540989));
#43735=CARTESIAN_POINT('Ctrl Pts',(-56.3285883274873,-83.2428199552275,
172.016274058689));
#43736=CARTESIAN_POINT('Ctrl Pts',(-54.7036890622522,-83.5103263012392,
171.81109657639));
#43737=CARTESIAN_POINT('Ctrl Pts',(-53.4133576434372,-83.7421654796101,
172.828569176292));
#43738=CARTESIAN_POINT('Ctrl Pts',(-52.1230262246222,-83.9740046579811,
173.846041776195));
#43739=CARTESIAN_POINT('Ctrl Pts',(-51.9289428798862,-84.0889764677377,
175.490142808619));
#43740=CARTESIAN_POINT('Ctrl Pts',(-51.7348595351501,-84.2039482774943,
177.134243841043));
#43741=CARTESIAN_POINT('Ctrl Pts',(-52.7565372380817,-84.1893118371985,
178.441881219107));
#43742=CARTESIAN_POINT('Ctrl Pts',(-53.7782149410133,-84.1746753969028,
179.74951859717));
#43743=CARTESIAN_POINT('Ctrl Pts',(-55.4229903320825,-84.0936125802018,
179.954696079469));
#43744=CARTESIAN_POINT('Ctrl Pts',(-57.0677657231517,-84.0125497635007,
180.159873561769));
#43745=CARTESIAN_POINT('Ctrl Pts',(-58.3779732678007,-83.9671541144405,
179.142400961866));
#43746=CARTESIAN_POINT('Ctrl Pts',(-59.6881808124497,-83.9217584653803,
178.124928361964));
#43747=CARTESIAN_POINT('Ctrl Pts',(-59.9021402830198,-83.9932301849343,
176.48082732954));
#43748=CARTESIAN_POINT('Ctrl Pts',(-60.1160997535899,-84.0647019044884,
174.836726297116));
#43749=CARTESIAN_POINT('Ctrl Pts',(-59.1142981764923,-84.2657818740949,
173.529088919052));
#43750=CARTESIAN_POINT('Ctrl Pts',(-58.1124965993947,-84.4668618437014,
172.221451540989));
#43751=CARTESIAN_POINT('Ctrl Pts',(-56.4875973341596,-84.7343681897131,
172.016274058689));
#43752=CARTESIAN_POINT('Ctrl Pts',(-54.8626980689244,-85.0018745357248,
171.81109657639));
#43753=CARTESIAN_POINT('Ctrl Pts',(-53.5723666501094,-85.2337137140957,
172.828569176292));
#43754=CARTESIAN_POINT('Ctrl Pts',(-52.2820352312944,-85.4655528924667,
173.846041776195));
#43755=CARTESIAN_POINT('Ctrl Pts',(-52.0879518865584,-85.5805247022233,
175.490142808619));
#43756=CARTESIAN_POINT('Ctrl Pts',(-51.8938685418223,-85.6954965119799,
177.134243841043));
#43757=CARTESIAN_POINT('Ctrl Pts',(-52.9155462447539,-85.6808600716841,
178.441881219107));
#43758=CARTESIAN_POINT('Ctrl Pts',(-53.9372239476855,-85.6662236313883,
179.74951859717));
#43759=CARTESIAN_POINT('Ctrl Pts',(-55.5819993387547,-85.5851608146873,
179.954696079469));
#43760=CARTESIAN_POINT('Ctrl Pts',(-57.2267747298239,-85.5040979979863,
180.159873561769));
#43761=CARTESIAN_POINT('Ctrl Pts',(-58.5369822744729,-85.4587023489261,
179.142400961866));
#43762=CARTESIAN_POINT('Ctrl Pts',(-59.847189819122,-85.4133066998659,178.124928361964));
#43763=CARTESIAN_POINT('Ctrl Pts',(-60.061149289692,-85.4847784194199,176.48082732954));
#43764=CARTESIAN_POINT('Ctrl Pts',(-60.2751087602621,-85.556250138974,174.836726297116));
#43765=CARTESIAN_POINT('Ctrl Pts',(-59.2733071831645,-85.7573301085805,
173.529088919052));
#43766=CARTESIAN_POINT('Ctrl Pts',(-58.271505606067,-85.9584100781869,172.221451540989));
#43767=CARTESIAN_POINT('Ctrl Pts',(-56.6466063408318,-86.2259164241987,
172.016274058689));
#43768=CARTESIAN_POINT('Ctrl Pts',(-55.0217070755966,-86.4934227702104,
171.81109657639));
#43769=CARTESIAN_POINT('Ctrl Pts',(-53.7313756567816,-86.7252619485813,
172.828569176292));
#43770=CARTESIAN_POINT('Ctrl Pts',(-52.4410442379667,-86.9571011269522,
173.846041776195));
#43771=CARTESIAN_POINT('Ctrl Pts',(-52.2469608932306,-87.0720729367089,
175.490142808619));
#43772=CARTESIAN_POINT('Ctrl Pts',(-52.0528775484945,-87.1870447464655,
177.134243841043));
#43773=CARTESIAN_POINT('Ctrl Pts',(-53.0745552514261,-87.1724083061697,
178.441881219107));
#43774=CARTESIAN_POINT('Ctrl Pts',(-54.0962329543578,-87.1577718658739,
179.74951859717));
#43775=CARTESIAN_POINT('Ctrl Pts',(-55.7410083454269,-87.0767090491729,
179.954696079469));
#43776=CARTESIAN_POINT('Ctrl Pts',(-57.3857837364961,-86.9956462324719,
180.159873561769));
#43777=CARTESIAN_POINT('Ctrl Pts',(-58.6959912811452,-86.9502505834117,
179.142400961866));
#43778=CARTESIAN_POINT('Ctrl Pts',(-60.0061988257942,-86.9048549343515,
178.124928361964));
#43779=CARTESIAN_POINT('Ctrl Pts',(-60.2201582963643,-86.9763266539055,
176.48082732954));
#43780=CARTESIAN_POINT('Ctrl Pts',(-60.4341177669343,-87.0477983734596,
174.836726297116));
#43781=CARTESIAN_POINT('Ctrl Pts',(-59.4323161898368,-87.2488783430661,
173.529088919052));
#43782=CARTESIAN_POINT('Ctrl Pts',(-58.4305146127392,-87.4499583126726,
172.221451540989));
#43783=CARTESIAN_POINT('Ctrl Pts',(-56.805615347504,-87.7174646586843,172.016274058689));
#43784=CARTESIAN_POINT('Ctrl Pts',(-55.1807160822689,-87.984971004696,171.81109657639));
#43785=CARTESIAN_POINT('Ctrl Pts',(-53.8903846634539,-88.2168101830669,
172.828569176292));
#43786=CARTESIAN_POINT('Ctrl Pts',(-52.6000532446389,-88.4486493614378,
173.846041776195));
#43787=CARTESIAN_POINT('Ctrl Pts',(-52.4059698999028,-88.5636211711945,
175.490142808619));
#43788=CARTESIAN_POINT('Ctrl Pts',(-52.2118865551668,-88.6785929809511,
177.134243841043));
#43789=CARTESIAN_POINT('Ctrl Pts',(-53.2335642580984,-88.6639565406553,
178.441881219107));
#43790=CARTESIAN_POINT('Ctrl Pts',(-54.25524196103,-88.6493201003596,179.74951859717));
#43791=CARTESIAN_POINT('Ctrl Pts',(-55.9000173520992,-88.5682572836585,
179.954696079469));
#43792=CARTESIAN_POINT('Ctrl Pts',(-57.5447927431684,-88.4871944669575,
180.159873561769));
#43793=CARTESIAN_POINT('Ctrl Pts',(-58.8550002878174,-88.4417988178973,
179.142400961866));
#43794=CARTESIAN_POINT('Ctrl Pts',(-60.1652078324664,-88.3964031688371,
178.124928361964));
#43795=CARTESIAN_POINT('Ctrl Pts',(-60.3791673030365,-88.4678748883911,
176.48082732954));
#43796=CARTESIAN_POINT('Ctrl Pts',(-60.5931267736066,-88.5393466079452,
174.836726297116));
#43797=CARTESIAN_POINT('Ctrl Pts',(-59.591325196509,-88.7404265775517,173.529088919052));
#43798=CARTESIAN_POINT('Ctrl Pts',(-58.5895236194114,-88.9415065471582,
172.221451540989));
#43799=CARTESIAN_POINT('Ctrl Pts',(-56.9646243541763,-89.2090128931699,
172.016274058689));
#43800=CARTESIAN_POINT('Ctrl Pts',(-55.3397250889411,-89.4765192391816,
171.81109657639));
#43801=CARTESIAN_POINT('Ctrl Pts',(-54.0493936701261,-89.7083584175525,
172.828569176292));
#43802=CARTESIAN_POINT('Ctrl Pts',(-52.7590622513111,-89.9401975959235,
173.846041776195));
#43803=CARTESIAN_POINT('Ctrl Pts',(-52.5649789065751,-90.0551694056801,
175.490142808619));
#43804=CARTESIAN_POINT('Ctrl Pts',(-52.370895561839,-90.1701412154367,177.134243841043));
#43805=CARTESIAN_POINT('Ctrl Pts',(-53.3925732647706,-90.1555047751409,
178.441881219107));
#43806=CARTESIAN_POINT('Ctrl Pts',(-54.4142509677022,-90.1408683348452,
179.74951859717));
#43807=CARTESIAN_POINT('Ctrl Pts',(-56.0590263587714,-90.0598055181441,
179.954696079469));
#43808=CARTESIAN_POINT('Ctrl Pts',(-57.7038017498406,-89.9787427014431,
180.159873561769));
#43809=CARTESIAN_POINT('Ctrl Pts',(-59.0140092944896,-89.9333470523829,
179.142400961866));
#43810=CARTESIAN_POINT('Ctrl Pts',(-60.3242168391386,-89.8879514033226,
178.124928361964));
#43811=CARTESIAN_POINT('Ctrl Pts',(-60.5381763097087,-89.9594231228767,
176.48082732954));
#43812=CARTESIAN_POINT('Ctrl Pts',(-60.7521357802788,-90.0308948424308,
174.836726297116));
#43813=CARTESIAN_POINT('Ctrl Pts',(-59.7503342031812,-90.2319748120373,
173.529088919052));
#43814=CARTESIAN_POINT('Ctrl Pts',(-58.7485326260837,-90.4330547816438,
172.221451540989));
#43815=CARTESIAN_POINT('Ctrl Pts',(-57.1236333608485,-90.7005611276555,
172.016274058689));
#43816=CARTESIAN_POINT('Ctrl Pts',(-55.4987340956133,-90.9680674736672,
171.81109657639));
#43817=CARTESIAN_POINT('Ctrl Pts',(-54.2084026767983,-91.1999066520381,
172.828569176292));
#43818=CARTESIAN_POINT('Ctrl Pts',(-52.9180712579833,-91.431745830409,173.846041776195));
#43819=CARTESIAN_POINT('Ctrl Pts',(-52.7239879132473,-91.5467176401657,
175.490142808619));
#43820=CARTESIAN_POINT('Ctrl Pts',(-52.5299045685112,-91.6616894499223,
177.134243841043));
#43821=CARTESIAN_POINT('Ctrl Pts',(-53.5515822714428,-91.6470530096265,
178.441881219107));
#43822=CARTESIAN_POINT('Ctrl Pts',(-54.5732599743744,-91.6324165693307,
179.74951859717));
#43823=CARTESIAN_POINT('Ctrl Pts',(-56.2180353654436,-91.5513537526297,
179.954696079469));
#43824=CARTESIAN_POINT('Ctrl Pts',(-57.8628107565128,-91.4702909359287,
180.159873561769));
#43825=CARTESIAN_POINT('Ctrl Pts',(-59.1730183011618,-91.4248952868685,
179.142400961866));
#43826=CARTESIAN_POINT('Ctrl Pts',(-60.4832258458109,-91.3794996378083,
178.124928361964));
#43827=CARTESIAN_POINT('Ctrl Pts',(-60.6971853163809,-91.4509713573623,
176.48082732954));
#43828=CARTESIAN_POINT('Ctrl Pts',(-60.911144786951,-91.5224430769164,174.836726297116));
#43829=CARTESIAN_POINT('Ctrl Pts',(-59.9093432098535,-91.7235230465229,
173.529088919052));
#43830=CARTESIAN_POINT('Ctrl Pts',(-58.9075416327559,-91.9246030161294,
172.221451540989));
#43831=CARTESIAN_POINT('Ctrl Pts',(-57.2826423675207,-92.1921093621411,
172.016274058689));
#43832=CARTESIAN_POINT('Ctrl Pts',(-55.6577431022856,-92.4596157081528,
171.81109657639));
#43833=CARTESIAN_POINT('Ctrl Pts',(-54.3674116834706,-92.6914548865237,
172.828569176292));
#43834=CARTESIAN_POINT('Ctrl Pts',(-53.0770802646556,-92.9232940648947,
173.846041776195));
#43835=CARTESIAN_POINT('Ctrl Pts',(-52.8829969199195,-93.0382658746513,
175.490142808619));
#43836=CARTESIAN_POINT('Ctrl Pts',(-52.6889135751835,-93.1532376844079,
177.134243841043));
#43837=CARTESIAN_POINT('Ctrl Pts',(-53.7105912781151,-93.1386012441121,
178.441881219107));
#43838=CARTESIAN_POINT('Ctrl Pts',(-54.7322689810467,-93.1239648038163,
179.74951859717));
#43839=CARTESIAN_POINT('Ctrl Pts',(-56.3770443721158,-93.0429019871153,
179.954696079469));
#43840=CARTESIAN_POINT('Ctrl Pts',(-58.021819763185,-92.9618391704143,180.159873561769));
#43841=CARTESIAN_POINT('Ctrl Pts',(-59.3320273078341,-92.9164435213541,
179.142400961866));
#43842=CARTESIAN_POINT('Ctrl Pts',(-60.6422348524831,-92.8710478722939,
178.124928361964));
#43843=CARTESIAN_POINT('Ctrl Pts',(-60.8561943230532,-92.9425195918479,
176.48082732954));
#43844=CARTESIAN_POINT('Ctrl Pts',(-61.0701537936232,-93.013991311402,174.836726297116));
#43845=CARTESIAN_POINT('Ctrl Pts',(-60.0683522165257,-93.2150712810085,
173.529088919052));
#43846=CARTESIAN_POINT('Ctrl Pts',(-59.0665506394281,-93.416151250615,172.221451540989));
#43847=CARTESIAN_POINT('Ctrl Pts',(-57.4416513741929,-93.6836575966267,
172.016274058689));
#43848=CARTESIAN_POINT('Ctrl Pts',(-55.8167521089578,-93.9511639426384,
171.81109657639));
#43849=CARTESIAN_POINT('Ctrl Pts',(-54.5264206901428,-94.1830031210093,
172.828569176292));
#43850=CARTESIAN_POINT('Ctrl Pts',(-53.2360892713278,-94.4148422993803,
173.846041776195));
#43851=CARTESIAN_POINT('Ctrl Pts',(-53.0420059265917,-94.5298141091369,
175.490142808619));
#43852=CARTESIAN_POINT('Ctrl Pts',(-52.8479225818557,-94.6447859188935,
177.134243841043));
#43853=CARTESIAN_POINT('Ctrl Pts',(-53.8696002847873,-94.6301494785977,
178.441881219107));
#43854=CARTESIAN_POINT('Ctrl Pts',(-54.8912779877189,-94.615513038302,179.74951859717));
#43855=CARTESIAN_POINT('Ctrl Pts',(-56.5360533787881,-94.5344502216009,
179.954696079469));
#43856=CARTESIAN_POINT('Ctrl Pts',(-58.1808287698573,-94.4533874048999,
180.159873561769));
#43857=CARTESIAN_POINT('Ctrl Pts',(-59.4910363145063,-94.4079917558397,
179.142400961866));
#43858=CARTESIAN_POINT('Ctrl Pts',(-60.8012438591553,-94.3625961067795,
178.124928361964));
#43859=CARTESIAN_POINT('Ctrl Pts',(-61.0152033297254,-94.4340678263335,
176.48082732954));
#43860=CARTESIAN_POINT('Ctrl Pts',(-61.2291628002955,-94.5055395458876,
174.836726297116));
#43861=CARTESIAN_POINT('Ctrl Pts',(-60.2273612231979,-94.7066195154941,
173.529088919052));
#43862=CARTESIAN_POINT('Ctrl Pts',(-59.2255596461003,-94.9076994851006,
172.221451540989));
#43863=CARTESIAN_POINT('Ctrl Pts',(-57.6006603808652,-95.1752058311123,
172.016274058689));
#43864=CARTESIAN_POINT('Ctrl Pts',(-55.97576111563,-95.442712177124,171.81109657639));
#43865=CARTESIAN_POINT('Ctrl Pts',(-54.685429696815,-95.6745513554949,172.828569176292));
#43866=CARTESIAN_POINT('Ctrl Pts',(-53.395098278,-95.9063905338659,173.846041776195));
#43867=CARTESIAN_POINT('Ctrl Pts',(-53.201014933264,-96.0213623436225,175.490142808619));
#43868=CARTESIAN_POINT('Ctrl Pts',(-53.0069315885279,-96.1363341533791,
177.134243841043));
#43869=CARTESIAN_POINT('Ctrl Pts',(-54.0286092914595,-96.1216977130833,
178.441881219107));
#43870=CARTESIAN_POINT('Ctrl Pts',(-55.0502869943911,-96.1070612727875,
179.74951859717));
#43871=CARTESIAN_POINT('Ctrl Pts',(-56.6950623854603,-96.0259984560865,
179.954696079469));
#43872=CARTESIAN_POINT('Ctrl Pts',(-58.3398377765295,-95.9449356393855,
180.159873561769));
#43873=CARTESIAN_POINT('Ctrl Pts',(-59.6500453211785,-95.8995399903253,
179.142400961866));
#43874=CARTESIAN_POINT('Ctrl Pts',(-60.9602528658275,-95.8541443412651,
178.124928361964));
#43875=CARTESIAN_POINT('Ctrl Pts',(-61.1742123363976,-95.9256160608192,
176.48082732954));
#43876=CARTESIAN_POINT('Ctrl Pts',(-61.3881718069677,-95.9970877803732,
174.836726297116));
#43877=CARTESIAN_POINT('Ctrl Pts',(-60.3863702298701,-96.1981677499797,
173.529088919052));
#43878=CARTESIAN_POINT('Ctrl Pts',(-59.3845686527726,-96.3992477195862,
172.221451540989));
#43879=CARTESIAN_POINT('Ctrl Pts',(-57.7596693875374,-96.6667540655979,
172.016274058689));
#43880=CARTESIAN_POINT('Ctrl Pts',(-56.1347701223022,-96.9342604116096,
171.81109657639));
#43881=CARTESIAN_POINT('Ctrl Pts',(-54.8444387034872,-97.1660995899806,
172.828569176292));
#43882=CARTESIAN_POINT('Ctrl Pts',(-53.5541072846722,-97.3979387683514,
173.846041776195));
#43883=CARTESIAN_POINT('Ctrl Pts',(-53.3600239399362,-97.5129105781081,
175.490142808619));
#43884=CARTESIAN_POINT('Ctrl Pts',(-53.1659405952001,-97.6278823878647,
177.134243841043));
#43885=CARTESIAN_POINT('Ctrl Pts',(-54.1876182981317,-97.6132459475689,
178.441881219107));
#43886=CARTESIAN_POINT('Ctrl Pts',(-55.2092960010633,-97.5986095072732,
179.74951859717));
#43887=CARTESIAN_POINT('Ctrl Pts',(-56.8540713921325,-97.5175466905721,
179.954696079469));
#43888=CARTESIAN_POINT('Ctrl Pts',(-58.4988467832017,-97.4364838738711,
180.159873561769));
#43889=CARTESIAN_POINT('Ctrl Pts',(-59.8090543278507,-97.3910882248109,
179.142400961866));
#43890=CARTESIAN_POINT('Ctrl Pts',(-61.1192618724998,-97.3456925757507,
178.124928361964));
#43891=CARTESIAN_POINT('Ctrl Pts',(-61.3332213430699,-97.4171642953048,
176.48082732954));
#43892=CARTESIAN_POINT('Ctrl Pts',(-61.5471808136399,-97.4886360148588,
174.836726297116));
#43893=CARTESIAN_POINT('Ctrl Pts',(-60.5453792365424,-97.6897159844653,
173.529088919052));
#43894=CARTESIAN_POINT('Ctrl Pts',(-59.5435776594448,-97.8907959540718,
172.221451540989));
#43895=CARTESIAN_POINT('Ctrl Pts',(-57.9186783942096,-98.1583023000835,
172.016274058689));
#43896=CARTESIAN_POINT('Ctrl Pts',(-56.2937791289745,-98.4258086460952,
171.81109657639));
#43897=CARTESIAN_POINT('Ctrl Pts',(-55.0034477101595,-98.6576478244661,
172.828569176292));
#43898=CARTESIAN_POINT('Ctrl Pts',(-53.7131162913445,-98.8894870028371,
173.846041776195));
#43899=CARTESIAN_POINT('Ctrl Pts',(-53.5190329466084,-99.0044588125937,
175.490142808619));
#43900=CARTESIAN_POINT('Ctrl Pts',(-53.3249496018724,-99.1194306223503,
177.134243841043));
#43901=CARTESIAN_POINT('Ctrl Pts',(-54.346627304804,-99.1047941820545,178.441881219107));
#43902=CARTESIAN_POINT('Ctrl Pts',(-55.3683050077356,-99.0901577417588,
179.74951859717));
#43903=CARTESIAN_POINT('Ctrl Pts',(-57.0130803988047,-99.0090949250577,
179.954696079469));
#43904=CARTESIAN_POINT('Ctrl Pts',(-58.6578557898739,-98.9280321083567,
180.159873561769));
#43905=CARTESIAN_POINT('Ctrl Pts',(-59.968063334523,-98.8826364592965,179.142400961866));
#43906=CARTESIAN_POINT('Ctrl Pts',(-61.278270879172,-98.8372408102363,178.124928361964));
#43907=CARTESIAN_POINT('Ctrl Pts',(-61.4922303497421,-98.9087125297904,
176.48082732954));
#43908=CARTESIAN_POINT('Ctrl Pts',(-61.7061898203122,-98.9801842493444,
174.836726297116));
#43909=CARTESIAN_POINT('Ctrl Pts',(-60.7043882432146,-99.1812642189509,
173.529088919052));
#43910=CARTESIAN_POINT('Ctrl Pts',(-59.702586666117,-99.3823441885574,172.221451540989));
#43911=CARTESIAN_POINT('Ctrl Pts',(-58.0776874008818,-99.6498505345691,
172.016274058689));
#43912=CARTESIAN_POINT('Ctrl Pts',(-56.4527881356467,-99.9173568805808,
171.81109657639));
#43913=CARTESIAN_POINT('Ctrl Pts',(-55.1624567168317,-100.149196058952,
172.828569176292));
#43914=CARTESIAN_POINT('Ctrl Pts',(-53.8721252980167,-100.381035237323,
173.846041776195));
#43915=CARTESIAN_POINT('Ctrl Pts',(-53.6780419532806,-100.496007047079,
175.490142808619));
#43916=CARTESIAN_POINT('Ctrl Pts',(-53.4839586085446,-100.610978856836,
177.134243841043));
#43917=CARTESIAN_POINT('Ctrl Pts',(-54.5056363114762,-100.59634241654,178.441881219107));
#43918=CARTESIAN_POINT('Ctrl Pts',(-55.5273140144078,-100.581705976244,
179.74951859717));
#43919=CARTESIAN_POINT('Ctrl Pts',(-57.172089405477,-100.500643159543,179.954696079469));
#43920=CARTESIAN_POINT('Ctrl Pts',(-58.8168647965462,-100.419580342842,
180.159873561769));
#43921=CARTESIAN_POINT('Ctrl Pts',(-60.1270723411952,-100.374184693782,
179.142400961866));
#43922=CARTESIAN_POINT('Ctrl Pts',(-61.4372798858442,-100.328789044722,
178.124928361964));
#43923=CARTESIAN_POINT('Ctrl Pts',(-61.6512393564143,-100.400260764276,
176.48082732954));
#43924=CARTESIAN_POINT('Ctrl Pts',(-61.8651988269844,-100.47173248383,174.836726297116));
#43925=CARTESIAN_POINT('Ctrl Pts',(-60.8633972498868,-100.672812453437,
173.529088919052));
#43926=CARTESIAN_POINT('Ctrl Pts',(-59.8615956727892,-100.873892423043,
172.221451540989));
#43927=CARTESIAN_POINT('Ctrl Pts',(-58.2366964075541,-101.141398769055,
172.016274058689));
#43928=CARTESIAN_POINT('Ctrl Pts',(-56.6117971423189,-101.408905115066,
171.81109657639));
#43929=CARTESIAN_POINT('Ctrl Pts',(-55.3214657235039,-101.640744293437,
172.828569176292));
#43930=CARTESIAN_POINT('Ctrl Pts',(-54.0311343046889,-101.872583471808,
173.846041776195));
#43931=CARTESIAN_POINT('Ctrl Pts',(-53.8370509599529,-101.987555281565,
175.490142808619));
#43932=CARTESIAN_POINT('Ctrl Pts',(-53.6429676152168,-102.102527091321,
177.134243841043));
#43933=CARTESIAN_POINT('Ctrl Pts',(-54.6646453181484,-102.087890651026,
178.441881219107));
#43934=CARTESIAN_POINT('Ctrl Pts',(-55.68632302108,-102.07325421073,179.74951859717));
#43935=CARTESIAN_POINT('Ctrl Pts',(-57.3310984121492,-101.992191394029,
179.954696079469));
#43936=CARTESIAN_POINT('Ctrl Pts',(-58.9758738032184,-101.911128577328,
180.159873561769));
#43937=CARTESIAN_POINT('Ctrl Pts',(-60.2860813478674,-101.865732928268,
179.142400961866));
#43938=CARTESIAN_POINT('Ctrl Pts',(-61.5962888925164,-101.820337279207,
178.124928361964));
#43939=CARTESIAN_POINT('Ctrl Pts',(-61.8102483630865,-101.891808998762,
176.48082732954));
#43940=CARTESIAN_POINT('Ctrl Pts',(-62.0242078336566,-101.963280718316,
174.836726297116));
#43941=CARTESIAN_POINT('Ctrl Pts',(-61.022406256559,-102.164360687922,173.529088919052));
#43942=CARTESIAN_POINT('Ctrl Pts',(-60.0206046794615,-102.365440657529,
172.221451540989));
#43943=CARTESIAN_POINT('Ctrl Pts',(-58.3957054142263,-102.63294700354,172.016274058689));
#43944=CARTESIAN_POINT('Ctrl Pts',(-56.7708061489911,-102.900453349552,
171.81109657639));
#43945=CARTESIAN_POINT('Ctrl Pts',(-55.4804747301761,-103.132292527923,
172.828569176292));
#43946=CARTESIAN_POINT('Ctrl Pts',(-54.1901433113612,-103.364131706294,
173.846041776195));
#43947=CARTESIAN_POINT('Ctrl Pts',(-53.9960599666251,-103.479103516051,
175.490142808619));
#43948=CARTESIAN_POINT('Ctrl Pts',(-53.801976621889,-103.594075325807,177.134243841043));
#43949=CARTESIAN_POINT('Ctrl Pts',(-54.8236543248206,-103.579438885511,
178.441881219107));
#43950=CARTESIAN_POINT('Ctrl Pts',(-55.8453320277522,-103.564802445216,
179.74951859717));
#43951=CARTESIAN_POINT('Ctrl Pts',(-57.4901074188214,-103.483739628515,
179.954696079469));
#43952=CARTESIAN_POINT('Ctrl Pts',(-59.1348828098906,-103.402676811814,
180.159873561769));
#43953=CARTESIAN_POINT('Ctrl Pts',(-60.4450903545396,-103.357281162753,
179.142400961866));
#43954=CARTESIAN_POINT('Ctrl Pts',(-61.7552978991887,-103.311885513693,
178.124928361964));
#43955=CARTESIAN_POINT('Ctrl Pts',(-61.9692573697588,-103.383357233247,
176.48082732954));
#43956=CARTESIAN_POINT('Ctrl Pts',(-62.1832168403288,-103.454828952801,
174.836726297116));
#43957=CARTESIAN_POINT('Ctrl Pts',(-61.1814152632313,-103.655908922408,
173.529088919052));
#43958=CARTESIAN_POINT('Ctrl Pts',(-60.1796136861337,-103.856988892014,
172.221451540989));
#43959=CARTESIAN_POINT('Ctrl Pts',(-58.5547144208985,-104.124495238026,
172.016274058689));
#43960=CARTESIAN_POINT('Ctrl Pts',(-56.9298151556634,-104.392001584038,
171.81109657639));
#43961=CARTESIAN_POINT('Ctrl Pts',(-55.6394837368484,-104.623840762409,
172.828569176292));
#43962=CARTESIAN_POINT('Ctrl Pts',(-54.3491523180334,-104.855679940779,
173.846041776195));
#43963=CARTESIAN_POINT('Ctrl Pts',(-54.1550689732973,-104.970651750536,
175.490142808619));
#43964=CARTESIAN_POINT('Ctrl Pts',(-53.9609856285613,-105.085623560293,
177.134243841043));
#43965=CARTESIAN_POINT('Ctrl Pts',(-54.9826633314929,-105.070987119997,
178.441881219107));
#43966=CARTESIAN_POINT('Ctrl Pts',(-56.0043410344245,-105.056350679701,
179.74951859717));
#43967=CARTESIAN_POINT('Ctrl Pts',(-57.6491164254937,-104.975287863,179.954696079469));
#43968=CARTESIAN_POINT('Ctrl Pts',(-59.2938918165628,-104.894225046299,
180.159873561769));
#43969=CARTESIAN_POINT('Ctrl Pts',(-60.6040993612119,-104.848829397239,
179.142400961866));
#43970=CARTESIAN_POINT('Ctrl Pts',(-61.9143069058609,-104.803433748179,
178.124928361964));
#43971=CARTESIAN_POINT('Ctrl Pts',(-62.128266376431,-104.874905467733,176.48082732954));
#43972=CARTESIAN_POINT('Ctrl Pts',(-62.3422258470011,-104.946377187287,
174.836726297116));
#43973=CARTESIAN_POINT('Ctrl Pts',(-61.3404242699035,-105.147457156893,
173.529088919052));
#43974=CARTESIAN_POINT('Ctrl Pts',(-60.3386226928059,-105.3485371265,172.221451540989));
#43975=CARTESIAN_POINT('Ctrl Pts',(-58.7137234275708,-105.616043472511,
172.016274058689));
#43976=CARTESIAN_POINT('Ctrl Pts',(-57.0888241623356,-105.883549818523,
171.81109657639));
#43977=CARTESIAN_POINT('Ctrl Pts',(-55.7984927435206,-106.115388996894,
172.828569176292));
#43978=CARTESIAN_POINT('Ctrl Pts',(-54.5081613247056,-106.347228175265,
173.846041776195));
#43979=CARTESIAN_POINT('Ctrl Pts',(-54.3140779799695,-106.462199985022,
175.490142808619));
#43980=CARTESIAN_POINT('Ctrl Pts',(-54.1199946352335,-106.577171794778,
177.134243841043));
#43981=CARTESIAN_POINT('Ctrl Pts',(-55.1416723381651,-106.562535354483,
178.441881219107));
#43982=CARTESIAN_POINT('Ctrl Pts',(-56.1633500410967,-106.547898914187,
179.74951859717));
#43983=CARTESIAN_POINT('Ctrl Pts',(-57.8081254321659,-106.466836097486,
179.954696079469));
#43984=CARTESIAN_POINT('Ctrl Pts',(-59.4529008232351,-106.385773280785,
180.159873561769));
#43985=CARTESIAN_POINT('Ctrl Pts',(-60.7631083678841,-106.340377631725,
179.142400961866));
#43986=CARTESIAN_POINT('Ctrl Pts',(-62.0733159125331,-106.294981982664,
178.124928361964));
#43987=CARTESIAN_POINT('Ctrl Pts',(-62.2872753831032,-106.366453702218,
176.48082732954));
#43988=CARTESIAN_POINT('Ctrl Pts',(-62.5012348536733,-106.437925421772,
174.836726297116));
#43989=CARTESIAN_POINT('Ctrl Pts',(-61.4994332765757,-106.639005391379,
173.529088919052));
#43990=CARTESIAN_POINT('Ctrl Pts',(-60.4976316994782,-106.840085360985,
172.221451540989));
#43991=CARTESIAN_POINT('Ctrl Pts',(-58.872732434243,-107.107591706997,172.016274058689));
#43992=CARTESIAN_POINT('Ctrl Pts',(-57.2478331690078,-107.375098053009,
171.81109657639));
#43993=CARTESIAN_POINT('Ctrl Pts',(-55.9575017501928,-107.60693723138,172.828569176292));
#43994=CARTESIAN_POINT('Ctrl Pts',(-54.6671703313778,-107.838776409751,
173.846041776195));
#43995=CARTESIAN_POINT('Ctrl Pts',(-54.4730869866418,-107.953748219507,
175.490142808619));
#43996=CARTESIAN_POINT('Ctrl Pts',(-54.2790036419057,-108.068720029264,
177.134243841043));
#43997=CARTESIAN_POINT('Ctrl Pts',(-55.3006813448373,-108.054083588968,
178.441881219107));
#43998=CARTESIAN_POINT('Ctrl Pts',(-56.3223590477689,-108.039447148672,
179.74951859717));
#43999=CARTESIAN_POINT('Ctrl Pts',(-57.9671344388381,-107.958384331971,
179.954696079469));
#44000=CARTESIAN_POINT('Ctrl Pts',(-59.6119098299073,-107.87732151527,180.159873561769));
#44001=CARTESIAN_POINT('Ctrl Pts',(-60.9221173745563,-107.83192586621,179.142400961866));
#44002=CARTESIAN_POINT('Ctrl Pts',(-62.2323249192054,-107.78653021715,178.124928361964));
#44003=CARTESIAN_POINT('Ctrl Pts',(-62.4462843897754,-107.858001936704,
176.48082732954));
#44004=CARTESIAN_POINT('Ctrl Pts',(-62.6602438603455,-107.929473656258,
174.836726297116));
#44005=CARTESIAN_POINT('Ctrl Pts',(-61.6584422832479,-108.130553625865,
173.529088919052));
#44006=CARTESIAN_POINT('Ctrl Pts',(-60.6566407061504,-108.331633595471,
172.221451540989));
#44007=CARTESIAN_POINT('Ctrl Pts',(-59.0317414409152,-108.599139941483,
172.016274058689));
#44008=CARTESIAN_POINT('Ctrl Pts',(-57.4068421756801,-108.866646287494,
171.81109657639));
#44009=CARTESIAN_POINT('Ctrl Pts',(-56.1165107568651,-109.098485465865,
172.828569176292));
#44010=CARTESIAN_POINT('Ctrl Pts',(-54.8261793380501,-109.330324644236,
173.846041776195));
#44011=CARTESIAN_POINT('Ctrl Pts',(-54.632095993314,-109.445296453993,175.490142808619));
#44012=CARTESIAN_POINT('Ctrl Pts',(-54.438012648578,-109.56026826375,177.134243841043));
#44013=CARTESIAN_POINT('Ctrl Pts',(-55.4596903515096,-109.545631823454,
178.441881219107));
#44014=CARTESIAN_POINT('Ctrl Pts',(-56.4813680544411,-109.530995383158,
179.74951859717));
#44015=CARTESIAN_POINT('Ctrl Pts',(-58.1261434455103,-109.449932566457,
179.954696079469));
#44016=CARTESIAN_POINT('Ctrl Pts',(-59.7709188365795,-109.368869749756,
180.159873561769));
#44017=CARTESIAN_POINT('Ctrl Pts',(-61.0811263812286,-109.323474100696,
179.142400961866));
#44018=CARTESIAN_POINT('Ctrl Pts',(-62.3913339258776,-109.278078451635,
178.124928361964));
#44019=CARTESIAN_POINT('Ctrl Pts',(-62.6052933964477,-109.34955017119,176.48082732954));
#44020=CARTESIAN_POINT('Ctrl Pts',(-62.8192528670178,-109.421021890744,
174.836726297116));
#44021=CARTESIAN_POINT('Ctrl Pts',(-61.8174512899202,-109.62210186035,173.529088919052));
#44022=CARTESIAN_POINT('Ctrl Pts',(-60.8156497128226,-109.823181829957,
172.221451540989));
#44023=CARTESIAN_POINT('Ctrl Pts',(-59.1907504475874,-110.090688175968,
172.016274058689));
#44024=CARTESIAN_POINT('Ctrl Pts',(-57.5658511823523,-110.35819452198,171.81109657639));
#44025=CARTESIAN_POINT('Ctrl Pts',(-56.2755197635373,-110.590033700351,
172.828569176292));
#44026=CARTESIAN_POINT('Ctrl Pts',(-54.9851883447223,-110.821872878722,
173.846041776195));
#44027=CARTESIAN_POINT('Ctrl Pts',(-54.7911049999862,-110.936844688478,
175.490142808619));
#44028=CARTESIAN_POINT('Ctrl Pts',(-54.5970216552502,-111.051816498235,
177.134243841043));
#44029=CARTESIAN_POINT('Ctrl Pts',(-55.6186993581818,-111.037180057939,
178.441881219107));
#44030=CARTESIAN_POINT('Ctrl Pts',(-56.6403770611134,-111.022543617644,
179.74951859717));
#44031=CARTESIAN_POINT('Ctrl Pts',(-58.2851524521826,-110.941480800943,
179.954696079469));
#44032=CARTESIAN_POINT('Ctrl Pts',(-59.9299278432518,-110.860417984242,
180.159873561769));
#44033=CARTESIAN_POINT('Ctrl Pts',(-61.2401353879008,-110.815022335181,
179.142400961866));
#44034=CARTESIAN_POINT('Ctrl Pts',(-62.5503429325498,-110.769626686121,
178.124928361964));
#44035=CARTESIAN_POINT('Ctrl Pts',(-62.7643024031199,-110.841098405675,
176.48082732954));
#44036=CARTESIAN_POINT('Ctrl Pts',(-62.97826187369,-110.912570125229,174.836726297116));
#44037=CARTESIAN_POINT('Ctrl Pts',(-61.9764602965924,-111.113650094836,
173.529088919052));
#44038=CARTESIAN_POINT('Ctrl Pts',(-60.9746587194948,-111.314730064442,
172.221451540989));
#44039=CARTESIAN_POINT('Ctrl Pts',(-59.3497594542597,-111.582236410454,
172.016274058689));
#44040=CARTESIAN_POINT('Ctrl Pts',(-57.7248601890245,-111.849742756466,
171.81109657639));
#44041=CARTESIAN_POINT('Ctrl Pts',(-56.4345287702095,-112.081581934837,
172.828569176292));
#44042=CARTESIAN_POINT('Ctrl Pts',(-55.1441973513945,-112.313421113207,
173.846041776195));
#44043=CARTESIAN_POINT('Ctrl Pts',(-54.9501140066585,-112.428392922964,
175.490142808619));
#44044=CARTESIAN_POINT('Ctrl Pts',(-54.7560306619224,-112.543364732721,
177.134243841043));
#44045=CARTESIAN_POINT('Ctrl Pts',(-55.777708364854,-112.528728292425,178.441881219107));
#44046=CARTESIAN_POINT('Ctrl Pts',(-56.7993860677856,-112.514091852129,
179.74951859717));
#44047=CARTESIAN_POINT('Ctrl Pts',(-58.4441614588548,-112.433029035428,
179.954696079469));
#44048=CARTESIAN_POINT('Ctrl Pts',(-60.088936849924,-112.351966218727,180.159873561769));
#44049=CARTESIAN_POINT('Ctrl Pts',(-61.399144394573,-112.306570569667,179.142400961866));
#44050=CARTESIAN_POINT('Ctrl Pts',(-62.709351939222,-112.261174920607,178.124928361964));
#44051=CARTESIAN_POINT('Ctrl Pts',(-62.9233114097921,-112.332646640161,
176.48082732954));
#44052=CARTESIAN_POINT('Ctrl Pts',(-63.1372708803622,-112.404118359715,
174.836726297116));
#44053=CARTESIAN_POINT('Ctrl Pts',(-62.1354693032646,-112.605198329321,
173.529088919052));
#44054=CARTESIAN_POINT('Ctrl Pts',(-61.1336677261671,-112.806278298928,
172.221451540989));
#44055=CARTESIAN_POINT('Ctrl Pts',(-59.5087684609319,-113.07378464494,172.016274058689));
#44056=CARTESIAN_POINT('Ctrl Pts',(-57.8838691956967,-113.341290990951,
171.81109657639));
#44057=CARTESIAN_POINT('Ctrl Pts',(-56.5935377768817,-113.573130169322,
172.828569176292));
#44058=CARTESIAN_POINT('Ctrl Pts',(-55.3032063580667,-113.804969347693,
173.846041776195));
#44059=CARTESIAN_POINT('Ctrl Pts',(-55.1091230133307,-113.91994115745,175.490142808619));
#44060=CARTESIAN_POINT('Ctrl Pts',(-54.9150396685946,-114.034912967206,
177.134243841043));
#44061=CARTESIAN_POINT('Ctrl Pts',(-55.9367173715262,-114.020276526911,
178.441881219107));
#44062=CARTESIAN_POINT('Ctrl Pts',(-56.9583950744578,-114.005640086615,
179.74951859717));
#44063=CARTESIAN_POINT('Ctrl Pts',(-58.603170465527,-113.924577269914,179.954696079469));
#44064=CARTESIAN_POINT('Ctrl Pts',(-60.2479458565962,-113.843514453213,
180.159873561769));
#44065=CARTESIAN_POINT('Ctrl Pts',(-61.5581534012452,-113.798118804152,
179.142400961866));
#44066=CARTESIAN_POINT('Ctrl Pts',(-62.8683609458943,-113.752723155092,
178.124928361964));
#44067=CARTESIAN_POINT('Ctrl Pts',(-63.0823204164643,-113.824194874646,
176.48082732954));
#44068=CARTESIAN_POINT('Ctrl Pts',(-63.2962798870344,-113.8956665942,174.836726297116));
#44069=CARTESIAN_POINT('Ctrl Pts',(-62.2944783099369,-114.096746563807,
173.529088919052));
#44070=CARTESIAN_POINT('Ctrl Pts',(-61.2926767328393,-114.297826533413,
172.221451540989));
#44071=CARTESIAN_POINT('Ctrl Pts',(-59.6677774676041,-114.565332879425,
172.016274058689));
#44072=CARTESIAN_POINT('Ctrl Pts',(-58.042878202369,-114.832839225437,171.81109657639));
#44073=CARTESIAN_POINT('Ctrl Pts',(-56.752546783554,-115.064678403808,172.828569176292));
#44074=CARTESIAN_POINT('Ctrl Pts',(-55.462215364739,-115.296517582179,173.846041776195));
#44075=CARTESIAN_POINT('Ctrl Pts',(-55.2681320200029,-115.411489391935,
175.490142808619));
#44076=CARTESIAN_POINT('Ctrl Pts',(-55.0740486752669,-115.526461201692,
177.134243841043));
#44077=CARTESIAN_POINT('Ctrl Pts',(-56.0957263781985,-115.511824761396,
178.441881219107));
#44078=CARTESIAN_POINT('Ctrl Pts',(-57.1174040811301,-115.4971883211,179.74951859717));
#44079=CARTESIAN_POINT('Ctrl Pts',(-58.7621794721992,-115.416125504399,
179.954696079469));
#44080=CARTESIAN_POINT('Ctrl Pts',(-60.4069548632684,-115.335062687698,
180.159873561769));
#44081=CARTESIAN_POINT('Ctrl Pts',(-61.7171624079175,-115.289667038638,
179.142400961866));
#44082=CARTESIAN_POINT('Ctrl Pts',(-63.0273699525665,-115.244271389578,
178.124928361964));
#44083=CARTESIAN_POINT('Ctrl Pts',(-63.2413294231366,-115.315743109132,
176.48082732954));
#44084=CARTESIAN_POINT('Ctrl Pts',(-63.4552888937067,-115.387214828686,
174.836726297116));
#44085=CARTESIAN_POINT('Ctrl Pts',(-62.4534873166091,-115.588294798292,
173.529088919052));
#44086=CARTESIAN_POINT('Ctrl Pts',(-61.4516857395115,-115.789374767899,
172.221451540989));
#44087=CARTESIAN_POINT('Ctrl Pts',(-59.8267864742763,-116.056881113911,
172.016274058689));
#44088=CARTESIAN_POINT('Ctrl Pts',(-58.2018872090412,-116.324387459922,
171.81109657639));
#44089=CARTESIAN_POINT('Ctrl Pts',(-56.9115557902262,-116.556226638293,
172.828569176292));
#44090=CARTESIAN_POINT('Ctrl Pts',(-55.6212243714112,-116.788065816664,
173.846041776195));
#44091=CARTESIAN_POINT('Ctrl Pts',(-55.4271410266751,-116.903037626421,
175.490142808619));
#44092=CARTESIAN_POINT('Ctrl Pts',(-55.2330576819391,-117.018009436177,
177.134243841043));
#44093=CARTESIAN_POINT('Ctrl Pts',(-56.2547353848707,-117.003372995882,
178.441881219107));
#44094=CARTESIAN_POINT('Ctrl Pts',(-57.2764130878023,-116.988736555586,
179.74951859717));
#44095=CARTESIAN_POINT('Ctrl Pts',(-58.9211884788715,-116.907673738885,
179.954696079469));
#44096=CARTESIAN_POINT('Ctrl Pts',(-60.5659638699407,-116.826610922184,
180.159873561769));
#44097=CARTESIAN_POINT('Ctrl Pts',(-61.8761714145897,-116.781215273124,
179.142400961866));
#44098=CARTESIAN_POINT('Ctrl Pts',(-63.1863789592387,-116.735819624063,
178.124928361964));
#44099=CARTESIAN_POINT('Ctrl Pts',(-63.4003384298088,-116.807291343618,
176.48082732954));
#44100=CARTESIAN_POINT('Ctrl Pts',(-63.6142979003789,-116.878763063172,
174.836726297116));
#44101=CARTESIAN_POINT('Ctrl Pts',(-62.6124963232813,-117.079843032778,
173.529088919052));
#44102=CARTESIAN_POINT('Ctrl Pts',(-61.6106947461837,-117.280923002385,
172.221451540989));
#44103=CARTESIAN_POINT('Ctrl Pts',(-59.9857954809486,-117.548429348396,
172.016274058689));
#44104=CARTESIAN_POINT('Ctrl Pts',(-58.3608962157134,-117.815935694408,
171.81109657639));
#44105=CARTESIAN_POINT('Ctrl Pts',(-57.0705647968984,-118.047774872779,
172.828569176292));
#44106=CARTESIAN_POINT('Ctrl Pts',(-55.7802333780834,-118.27961405115,173.846041776195));
#44107=CARTESIAN_POINT('Ctrl Pts',(-55.5861500333474,-118.394585860907,
175.490142808619));
#44108=CARTESIAN_POINT('Ctrl Pts',(-55.3920666886113,-118.509557670663,
177.134243841043));
#44109=CARTESIAN_POINT('Ctrl Pts',(-56.4137443915429,-118.494921230367,
178.441881219107));
#44110=CARTESIAN_POINT('Ctrl Pts',(-57.4354220944745,-118.480284790072,
179.74951859717));
#44111=CARTESIAN_POINT('Ctrl Pts',(-59.0801974855437,-118.399221973371,
179.954696079469));
#44112=CARTESIAN_POINT('Ctrl Pts',(-60.7249728766129,-118.31815915667,180.159873561769));
#44113=CARTESIAN_POINT('Ctrl Pts',(-62.0351804212619,-118.272763507609,
179.142400961866));
#44114=CARTESIAN_POINT('Ctrl Pts',(-63.345387965911,-118.227367858549,178.124928361964));
#44115=CARTESIAN_POINT('Ctrl Pts',(-63.559347436481,-118.298839578103,176.48082732954));
#44116=CARTESIAN_POINT('Ctrl Pts',(-63.7733069070511,-118.370311297657,
174.836726297116));
#44117=CARTESIAN_POINT('Ctrl Pts',(-62.7715053299535,-118.571391267264,
173.529088919052));
#44118=CARTESIAN_POINT('Ctrl Pts',(-61.769703752856,-118.77247123687,172.221451540989));
#44119=CARTESIAN_POINT('Ctrl Pts',(-60.1448044876208,-119.039977582882,
172.016274058689));
#44120=CARTESIAN_POINT('Ctrl Pts',(-58.5199052223856,-119.307483928894,
171.81109657639));
#44121=CARTESIAN_POINT('Ctrl Pts',(-57.2295738035707,-119.539323107265,
172.828569176292));
#44122=CARTESIAN_POINT('Ctrl Pts',(-55.9392423847557,-119.771162285635,
173.846041776195));
#44123=CARTESIAN_POINT('Ctrl Pts',(-55.7451590400196,-119.886134095392,
175.490142808619));
#44124=CARTESIAN_POINT('Ctrl Pts',(-55.5510756952835,-120.001105905149,
177.134243841043));
#44125=CARTESIAN_POINT('Ctrl Pts',(-56.5727533982151,-119.986469464853,
178.441881219107));
#44126=CARTESIAN_POINT('Ctrl Pts',(-57.5944311011467,-119.971833024557,
179.74951859717));
#44127=CARTESIAN_POINT('Ctrl Pts',(-59.2392064922159,-119.890770207856,
179.954696079469));
#44128=CARTESIAN_POINT('Ctrl Pts',(-60.8839818832851,-119.809707391155,
180.159873561769));
#44129=CARTESIAN_POINT('Ctrl Pts',(-62.1941894279341,-119.764311742095,
179.142400961866));
#44130=CARTESIAN_POINT('Ctrl Pts',(-63.5043969725832,-119.718916093035,
178.124928361964));
#44131=CARTESIAN_POINT('Ctrl Pts',(-63.7183564431533,-119.790387812589,
176.48082732954));
#44132=CARTESIAN_POINT('Ctrl Pts',(-63.9323159137233,-119.861859532143,
174.836726297116));
#44133=CARTESIAN_POINT('Ctrl Pts',(-62.9305143366258,-120.062939501749,
173.529088919052));
#44134=CARTESIAN_POINT('Ctrl Pts',(-61.9287127595282,-120.264019471356,
172.221451540989));
#44135=CARTESIAN_POINT('Ctrl Pts',(-60.303813494293,-120.531525817368,172.016274058689));
#44136=CARTESIAN_POINT('Ctrl Pts',(-58.6789142290579,-120.799032163379,
171.81109657639));
#44137=CARTESIAN_POINT('Ctrl Pts',(-57.3885828102429,-121.03087134175,172.828569176292));
#44138=CARTESIAN_POINT('Ctrl Pts',(-56.0982513914279,-121.262710520121,
173.846041776195));
#44139=CARTESIAN_POINT('Ctrl Pts',(-55.9041680466918,-121.377682329878,
175.490142808619));
#44140=CARTESIAN_POINT('Ctrl Pts',(-55.7100847019558,-121.492654139634,
177.134243841043));
#44141=CARTESIAN_POINT('Ctrl Pts',(-56.7317624048874,-121.478017699339,
178.441881219107));
#44142=CARTESIAN_POINT('Ctrl Pts',(-57.753440107819,-121.463381259043,179.74951859717));
#44143=CARTESIAN_POINT('Ctrl Pts',(-59.3982154988882,-121.382318442342,
179.954696079469));
#44144=CARTESIAN_POINT('Ctrl Pts',(-61.0429908899573,-121.301255625641,
180.159873561769));
#44145=CARTESIAN_POINT('Ctrl Pts',(-62.3531984346064,-121.25585997658,179.142400961866));
#44146=CARTESIAN_POINT('Ctrl Pts',(-63.6634059792554,-121.21046432752,178.124928361964));
#44147=CARTESIAN_POINT('Ctrl Pts',(-63.8773654498255,-121.281936047074,
176.48082732954));
#44148=CARTESIAN_POINT('Ctrl Pts',(-64.0913249203956,-121.353407766628,
174.836726297116));
#44149=CARTESIAN_POINT('Ctrl Pts',(-63.089523343298,-121.554487736235,173.529088919052));
#44150=CARTESIAN_POINT('Ctrl Pts',(-62.0877217662004,-121.755567705841,
172.221451540989));
#44151=CARTESIAN_POINT('Ctrl Pts',(-60.4628225009653,-122.023074051853,
172.016274058689));
#44152=CARTESIAN_POINT('Ctrl Pts',(-58.8379232357301,-122.290580397865,
171.81109657639));
#44153=CARTESIAN_POINT('Ctrl Pts',(-57.5475918169151,-122.522419576236,
172.828569176292));
#44154=CARTESIAN_POINT('Ctrl Pts',(-56.2572603981001,-122.754258754607,
173.846041776195));
#44155=CARTESIAN_POINT('Ctrl Pts',(-56.0631770533641,-122.869230564363,
175.490142808619));
#44156=CARTESIAN_POINT('Ctrl Pts',(-55.869093708628,-122.98420237412,177.134243841043));
#44157=CARTESIAN_POINT('Ctrl Pts',(-56.8907714115596,-122.969565933824,
178.441881219107));
#44158=CARTESIAN_POINT('Ctrl Pts',(-57.9124491144912,-122.954929493528,
179.74951859717));
#44159=CARTESIAN_POINT('Ctrl Pts',(-59.5572245055604,-122.873866676827,
179.954696079469));
#44160=CARTESIAN_POINT('Ctrl Pts',(-61.2019998966296,-122.792803860126,
180.159873561769));
#44161=CARTESIAN_POINT('Ctrl Pts',(-62.5122074412786,-122.747408211066,
179.142400961866));
#44162=CARTESIAN_POINT('Ctrl Pts',(-63.8224149859276,-122.702012562006,
178.124928361964));
#44163=CARTESIAN_POINT('Ctrl Pts',(-64.0363744564977,-122.77348428156,176.48082732954));
#44164=CARTESIAN_POINT('Ctrl Pts',(-64.2503339270678,-122.844956001114,
174.836726297116));
#44165=CARTESIAN_POINT('Ctrl Pts',(-63.2485323499702,-123.046035970721,
173.529088919052));
#44166=CARTESIAN_POINT('Ctrl Pts',(-62.2467307728726,-123.247115940327,
172.221451540989));
#44167=CARTESIAN_POINT('Ctrl Pts',(-60.6218315076375,-123.514622286339,
172.016274058689));
#44168=CARTESIAN_POINT('Ctrl Pts',(-58.9969322424023,-123.78212863235,171.81109657639));
#44169=CARTESIAN_POINT('Ctrl Pts',(-57.7066008235873,-124.013967810721,
172.828569176292));
#44170=CARTESIAN_POINT('Ctrl Pts',(-56.4162694047723,-124.245806989092,
173.846041776195));
#44171=CARTESIAN_POINT('Ctrl Pts',(-56.2221860600363,-124.360778798849,
175.490142808619));
#44172=CARTESIAN_POINT('Ctrl Pts',(-56.0281027153002,-124.475750608606,
177.134243841043));
#44173=CARTESIAN_POINT('Ctrl Pts',(-57.0497804182318,-124.46111416831,178.441881219107));
#44174=CARTESIAN_POINT('Ctrl Pts',(-58.0714581211634,-124.446477728014,
179.74951859717));
#44175=CARTESIAN_POINT('Ctrl Pts',(-59.7162335122326,-124.365414911313,
179.954696079469));
#44176=CARTESIAN_POINT('Ctrl Pts',(-61.3610089033018,-124.284352094612,
180.159873561769));
#44177=CARTESIAN_POINT('Ctrl Pts',(-62.6712164479508,-124.238956445552,
179.142400961866));
#44178=CARTESIAN_POINT('Ctrl Pts',(-63.9814239925999,-124.193560796491,
178.124928361964));
#44179=CARTESIAN_POINT('Ctrl Pts',(-64.1953834631699,-124.265032516046,
176.48082732954));
#44180=CARTESIAN_POINT('Ctrl Pts',(-64.40934293374,-124.3365042356,174.836726297116));
#44181=CARTESIAN_POINT('Ctrl Pts',(-63.4075413566424,-124.537584205206,
173.529088919052));
#44182=CARTESIAN_POINT('Ctrl Pts',(-62.4057397795449,-124.738664174813,
172.221451540989));
#44183=CARTESIAN_POINT('Ctrl Pts',(-60.7808405143097,-125.006170520824,
172.016274058689));
#44184=CARTESIAN_POINT('Ctrl Pts',(-59.1559412490746,-125.273676866836,
171.81109657639));
#44185=CARTESIAN_POINT('Ctrl Pts',(-57.8656098302596,-125.505516045207,
172.828569176292));
#44186=CARTESIAN_POINT('Ctrl Pts',(-56.5752784114446,-125.737355223578,
173.846041776195));
#44187=CARTESIAN_POINT('Ctrl Pts',(-56.3811950667085,-125.852327033334,
175.490142808619));
#44188=CARTESIAN_POINT('Ctrl Pts',(-56.1871117219724,-125.967298843091,
177.134243841043));
#44189=CARTESIAN_POINT('Ctrl Pts',(-57.208789424904,-125.952662402795,178.441881219107));
#44190=CARTESIAN_POINT('Ctrl Pts',(-58.2304671278357,-125.9380259625,179.74951859717));
#44191=CARTESIAN_POINT('Ctrl Pts',(-59.8752425189048,-125.856963145799,
179.954696079469));
#44192=CARTESIAN_POINT('Ctrl Pts',(-61.520017909974,-125.775900329098,180.159873561769));
#44193=CARTESIAN_POINT('Ctrl Pts',(-62.8302254546231,-125.730504680037,
179.142400961866));
#44194=CARTESIAN_POINT('Ctrl Pts',(-64.1404329992721,-125.685109030977,
178.124928361964));
#44195=CARTESIAN_POINT('Ctrl Pts',(-64.3543924698422,-125.756580750531,
176.48082732954));
#44196=CARTESIAN_POINT('Ctrl Pts',(-64.5683519404122,-125.828052470085,
174.836726297116));
#44197=CARTESIAN_POINT('Ctrl Pts',(-63.5665503633147,-126.029132439692,
173.529088919052));
#44198=CARTESIAN_POINT('Ctrl Pts',(-62.5647487862171,-126.230212409298,
172.221451540989));
#44199=CARTESIAN_POINT('Ctrl Pts',(-60.9398495209819,-126.49771875531,172.016274058689));
#44200=CARTESIAN_POINT('Ctrl Pts',(-59.3149502557468,-126.765225101322,
171.81109657639));
#44201=CARTESIAN_POINT('Ctrl Pts',(-58.0246188369318,-126.997064279693,
172.828569176292));
#44202=CARTESIAN_POINT('Ctrl Pts',(-56.7342874181168,-127.228903458063,
173.846041776195));
#44203=CARTESIAN_POINT('Ctrl Pts',(-56.5402040733807,-127.34387526782,175.490142808619));
#44204=CARTESIAN_POINT('Ctrl Pts',(-56.3461207286447,-127.458847077577,
177.134243841043));
#44205=CARTESIAN_POINT('Ctrl Pts',(-57.3677984315763,-127.444210637281,
178.441881219107));
#44206=CARTESIAN_POINT('Ctrl Pts',(-58.3894761345079,-127.429574196985,
179.74951859717));
#44207=CARTESIAN_POINT('Ctrl Pts',(-60.0342515255771,-127.348511380284,
179.954696079469));
#44208=CARTESIAN_POINT('Ctrl Pts',(-61.6790269166463,-127.267448563583,
180.159873561769));
#44209=CARTESIAN_POINT('Ctrl Pts',(-62.9892344612953,-127.222052914523,
179.142400961866));
#44210=CARTESIAN_POINT('Ctrl Pts',(-64.2994420059443,-127.176657265463,
178.124928361964));
#44211=CARTESIAN_POINT('Ctrl Pts',(-64.5134014765144,-127.248128985017,
176.48082732954));
#44212=CARTESIAN_POINT('Ctrl Pts',(-64.7273609470845,-127.319600704571,
174.836726297116));
#44213=CARTESIAN_POINT('Ctrl Pts',(-63.7255593699869,-127.520680674177,
173.529088919052));
#44214=CARTESIAN_POINT('Ctrl Pts',(-62.7237577928893,-127.721760643784,
172.221451540989));
#44215=CARTESIAN_POINT('Ctrl Pts',(-61.0988585276542,-127.989266989795,
172.016274058689));
#44216=CARTESIAN_POINT('Ctrl Pts',(-59.473959262419,-128.256773335807,171.81109657639));
#44217=CARTESIAN_POINT('Ctrl Pts',(-58.183627843604,-128.488612514178,172.828569176292));
#44218=CARTESIAN_POINT('Ctrl Pts',(-56.893296424789,-128.720451692549,173.846041776195));
#44219=CARTESIAN_POINT('Ctrl Pts',(-56.699213080053,-128.835423502306,175.490142808619));
#44220=CARTESIAN_POINT('Ctrl Pts',(-56.5051297353169,-128.950395312062,
177.134243841043));
#44221=CARTESIAN_POINT('Ctrl Pts',(-57.5268074382485,-128.935758871767,
178.441881219107));
#44222=CARTESIAN_POINT('Ctrl Pts',(-58.5484851411801,-128.921122431471,
179.74951859717));
#44223=CARTESIAN_POINT('Ctrl Pts',(-60.1932605322493,-128.84005961477,179.954696079469));
#44224=CARTESIAN_POINT('Ctrl Pts',(-61.8380359233185,-128.758996798069,
180.159873561769));
#44225=CARTESIAN_POINT('Ctrl Pts',(-63.1482434679675,-128.713601149008,
179.142400961866));
#44226=CARTESIAN_POINT('Ctrl Pts',(-64.4584510126165,-128.668205499948,
178.124928361964));
#44227=CARTESIAN_POINT('Ctrl Pts',(-64.6724104831866,-128.739677219502,
176.48082732954));
#44228=CARTESIAN_POINT('Ctrl Pts',(-64.8863699537567,-128.811148939056,
174.836726297116));
#44229=CARTESIAN_POINT('Ctrl Pts',(-63.8845683766591,-129.012228908663,
173.529088919052));
#44230=CARTESIAN_POINT('Ctrl Pts',(-62.8827667995616,-129.213308878269,
172.221451540989));
#44231=CARTESIAN_POINT('Ctrl Pts',(-61.2578675343264,-129.480815224281,
172.016274058689));
#44232=CARTESIAN_POINT('Ctrl Pts',(-59.6329682690912,-129.748321570293,
171.81109657639));
#44233=CARTESIAN_POINT('Ctrl Pts',(-58.3426368502762,-129.980160748664,
172.828569176292));
#44234=CARTESIAN_POINT('Ctrl Pts',(-57.0523054314612,-130.211999927035,
173.846041776195));
#44235=CARTESIAN_POINT('Ctrl Pts',(-56.8582220867252,-130.326971736791,
175.490142808619));
#44236=CARTESIAN_POINT('Ctrl Pts',(-56.6641387419891,-130.441943546548,
177.134243841043));
#44237=CARTESIAN_POINT('Ctrl Pts',(-57.6858164449207,-130.427307106252,
178.441881219107));
#44238=CARTESIAN_POINT('Ctrl Pts',(-58.7074941478523,-130.412670665956,
179.74951859717));
#44239=CARTESIAN_POINT('Ctrl Pts',(-60.3522695389215,-130.331607849255,
179.954696079469));
#44240=CARTESIAN_POINT('Ctrl Pts',(-61.9970449299907,-130.250545032554,
180.159873561769));
#44241=CARTESIAN_POINT('Ctrl Pts',(-63.3072524746397,-130.205149383494,
179.142400961866));
#44242=CARTESIAN_POINT('Ctrl Pts',(-64.6174600192888,-130.159753734434,
178.124928361964));
#44243=CARTESIAN_POINT('Ctrl Pts',(-64.8314194898588,-130.231225453988,
176.48082732954));
#44244=CARTESIAN_POINT('Ctrl Pts',(-65.0453789604289,-130.302697173542,
174.836726297116));
#44245=CARTESIAN_POINT('Ctrl Pts',(-64.0435773833314,-130.503777143149,
173.529088919052));
#44246=CARTESIAN_POINT('Ctrl Pts',(-63.0417758062338,-130.704857112755,
172.221451540989));
#44247=CARTESIAN_POINT('Ctrl Pts',(-61.4168765409986,-130.972363458767,
172.016274058689));
#44248=CARTESIAN_POINT('Ctrl Pts',(-59.7919772757635,-131.239869804778,
171.81109657639));
#44249=CARTESIAN_POINT('Ctrl Pts',(-58.5016458569485,-131.471708983149,
172.828569176292));
#44250=CARTESIAN_POINT('Ctrl Pts',(-57.2113144381335,-131.70354816152,173.846041776195));
#44251=CARTESIAN_POINT('Ctrl Pts',(-57.0172310933974,-131.818519971277,
175.490142808619));
#44252=CARTESIAN_POINT('Ctrl Pts',(-56.8231477486614,-131.933491781033,
177.134243841043));
#44253=CARTESIAN_POINT('Ctrl Pts',(-57.844825451593,-131.918855340738,178.441881219107));
#44254=CARTESIAN_POINT('Ctrl Pts',(-58.8665031545246,-131.904218900442,
179.74951859717));
#44255=CARTESIAN_POINT('Ctrl Pts',(-60.5112785455938,-131.823156083741,
179.954696079469));
#44256=CARTESIAN_POINT('Ctrl Pts',(-61.5752382858275,-131.770718788127,
180.087419721831));
#44257=CARTESIAN_POINT('Ctrl Pts',(-62.5639783363627,-131.730760688539,
179.670610857428));
#44258=CARTESIAN_POINT('Origin',(-65.8133517206249,-123.652567188025,171.594677789993));
#44259=CARTESIAN_POINT('Origin',(-64.6054323897224,-123.781339458681,170.37181129294));
#44260=CARTESIAN_POINT('Origin',(-63.1416108368898,-123.937392615849,169.475191110882));
#44261=CARTESIAN_POINT('Origin',(-61.5069590500029,-124.111657417267,168.956925549718));
#44262=CARTESIAN_POINT('Origin',(-59.7964770491983,-124.294006226103,168.847134320046));
#44263=CARTESIAN_POINT('Origin',(-58.1095718310134,-124.473841592396,169.152198089058));
#44264=CARTESIAN_POINT('Origin',(-56.5442801950783,-124.640712138335,169.854387659362));
#44265=CARTESIAN_POINT('Origin',(-55.1915712016699,-124.784919954338,170.912894325486));
#44266=CARTESIAN_POINT('Origin',(-54.1300593805879,-124.898084206314,172.26620152751));
#44267=CARTESIAN_POINT('Origin',(-53.4214359404352,-124.973628199272,173.835659969925));
#44268=CARTESIAN_POINT('Origin',(-53.1068834998121,-125.007161590934,175.530058432807));
#44269=CARTESIAN_POINT('Origin',(-53.2046827032159,-124.996735542465,177.25092463638));
#44270=CARTESIAN_POINT('Origin',(-53.7091498164305,-124.942955977905,178.898248091987));
#44271=CARTESIAN_POINT('Origin',(-54.5909670444992,-124.848948370066,180.376292348166));
#44272=CARTESIAN_POINT('Origin',(-55.7988863754018,-124.72017609941,181.599158845219));
#44273=CARTESIAN_POINT('Origin',(-66.6951689486936,-123.558559580185,173.072722046172));
#44274=CARTESIAN_POINT('Origin',(-54.0803126256813,-66.8261507513496,175.985485069079));
#47695=UNCERTAINTY_MEASURE_WITH_UNIT(LENGTH_MEASURE(0.01),#47718,
'DISTANCE_ACCURACY_VALUE',
'Maximum model space distance between geometric entities at asserted c
onnectivities');
#47703=UNCERTAINTY_MEASURE_WITH_UNIT(LENGTH_MEASURE(0.01),#47718,
'DISTANCE_ACCURACY_VALUE',
'Maximum model space distance between geometric entities at asserted c
onnectivities');
#47709=(
GEOMETRIC_REPRESENTATION_CONTEXT(3)
GLOBAL_UNCERTAINTY_ASSIGNED_CONTEXT((#47695))
GLOBAL_UNIT_ASSIGNED_CONTEXT((#47718,#47720,#47721))
REPRESENTATION_CONTEXT('','3D')
);
#47717=(
GEOMETRIC_REPRESENTATION_CONTEXT(3)
GLOBAL_UNCERTAINTY_ASSIGNED_CONTEXT((#47703))
GLOBAL_UNIT_ASSIGNED_CONTEXT((#47718,#47720,#47721))
REPRESENTATION_CONTEXT('','3D')
);
#47718=(
LENGTH_UNIT()
NAMED_UNIT(*)
SI_UNIT(.MILLI.,.METRE.)
);
#47720=(
NAMED_UNIT(*)
PLANE_ANGLE_UNIT()
SI_UNIT($,.RADIAN.)
);
#47721=(
NAMED_UNIT(*)
SI_UNIT($,.STERADIAN.)
SOLID_ANGLE_UNIT()
);
#47727=SHAPE_DEFINITION_REPRESENTATION(#47740,#47765);
#47740=PRODUCT_DEFINITION_SHAPE('',$,#47779);
#47765=SHAPE_REPRESENTATION('',(#9345),#47709);
#47773=PRODUCT_DEFINITION_CONTEXT('part definition',#47814,'design');
#47779=PRODUCT_DEFINITION('Adjustment Screw','Adjustment Screw',#47792,
#47773);
#47792=PRODUCT_DEFINITION_FORMATION('',$,#47821);
#47814=APPLICATION_CONTEXT(
'Core Data for Automotive Mechanical Design Process');
#47815=PRODUCT_CONTEXT('part definition',#47814,'mechanical');
#47821=PRODUCT('Adjustment Screw','Adjustment Screw',$,(#47815));
#47830=PRESENTATION_STYLE_ASSIGNMENT((#47832));
#47832=SURFACE_STYLE_USAGE(.BOTH.,#47834);
#47834=SURFACE_SIDE_STYLE('',(#47836));
#47836=SURFACE_STYLE_FILL_AREA(#47838);
#47838=FILL_AREA_STYLE('Opaque(202,209,238)',(#47840));
#47840=FILL_AREA_STYLE_COLOUR('Opaque(202,209,238)',#47842);
#47842=COLOUR_RGB('Opaque(202,209,238)', 0.66274510, 0.83137255, 0.94901961);
ENDSEC;
END-ISO-10303-21;
